ISO-10303-21;
HEADER;
FILE_DESCRIPTION (('STEP AP214'),
    '1' );
FILE_NAME ('4. Adjustment Screw.step',
    '2026-10-09T08:13:37',
    ( '' ),
    ( '' ),
    'SwSTEP 2.0',
    'SolidWorks 2021',
    '' );
FILE_SCHEMA (( 'AUTOMOTIVE_DESIGN' ));
ENDSEC;

DATA;
#13=CARTESIAN_POINT ( 'NONE',  ( -99.50499999999996703, -6.826472737025115478, -4.959722759717899443 ) ) ;
#17=CARTESIAN_POINT ( 'NONE',  ( -133.7070736234661865, -3.094860106618431139, -9.524999999999991473 ) ) ;
#19=CARTESIAN_POINT ( 'NONE',  ( -65.45707362346617231, -9.058813317711329915, 2.943386871421371787 ) ) ;
#27=CARTESIAN_POINT ( 'NONE',  ( -109.2549999999999955, -4.716976649647092401, 6.492361379858946790 ) ) ;
#29=CARTESIAN_POINT ( 'NONE',  ( -119.3949999999999676, -6.826472737025115478, -4.959722759717899443 ) ) ;
#36=CARTESIAN_POINT ( 'NONE',  ( -167.2429263765338305, 5.598654528085804216, 7.705886871421366635 ) ) ;
#37=( LENGTH_UNIT ( ) NAMED_UNIT ( * ) SI_UNIT ( .MILLI., .METRE. ) );
#38=CARTESIAN_POINT ( 'NONE',  ( -176.3949999999999818, -6.826472737025115478, -4.959722759717899443 ) ) ;
#45=CARTESIAN_POINT ( 'NONE',  ( -72.14292637653379359, 5.598654528085800663, -7.705886871421367523 ) ) ;
#53=CARTESIAN_POINT ( 'NONE',  ( -181.7050000000000125, 2.607480562269072433, 8.024999999999991473 ) ) ;
#65=CARTESIAN_POINT ( 'NONE',  ( -91.85499999999998977, 4.716976649647094177, 6.492361379858945902 ) ) ;
#76=CARTESIAN_POINT ( 'NONE',  ( -65.54499999999998749, -7.632228543268600340, -2.479861379858950166 ) ) ;
#88=CARTESIAN_POINT ( 'NONE',  ( -127.2550000000000097, -4.716976649647092401, 6.492361379858946790 ) ) ;
#95=CARTESIAN_POINT ( 'NONE',  ( -162.5070736234661979, 8.102448949553176405, 5.886773742842740909 ) ) ;
#98=( BOUNDED_CURVE ( )  B_SPLINE_CURVE ( 2, ( #68533, #63250, #15098, #47110, #57988, #9804, #31215, #52708, #25942 ),
 .UNSPECIFIED., .F., .F. ) 
 B_SPLINE_CURVE_WITH_KNOTS ( ( 3, 2, 2, 2, 3 ),
 ( 0.01408042836260392332, 0.01521739130434775211, 0.01739130434782587206, 0.01956521739130399548, 0.02173913043478211196 ),
 .UNSPECIFIED. ) 
 CURVE ( )  GEOMETRIC_REPRESENTATION_ITEM ( )  RATIONAL_B_SPLINE_CURVE ( ( 0.9755800536518706156, 0.9744024134823617844, 1.000000000000000000, 0.9510565162951535312, 1.000000000000000000, 0.9510565162951535312, 1.000000000000000000, 0.9510565162951647444, 0.9999999999999887867 ) ) 
 REPRESENTATION_ITEM ( '' )  );
#99=CARTESIAN_POINT ( 'NONE',  ( -92.45707362346617231, -9.058813317711329915, 2.943386871421371787 ) ) ;
#109=CARTESIAN_POINT ( 'NONE',  ( -139.8550000000000182, 4.716976649647094177, 6.492361379858945902 ) ) ;
#110=CARTESIAN_POINT ( 'NONE',  ( -86.15707362346617515, -9.058813317711329915, -2.943386871421370898 ) ) ;
#112=CARTESIAN_POINT ( 'NONE',  ( -141.5950000000000273, 2.607480562269073321, 8.024999999999991473 ) ) ;
#113=CARTESIAN_POINT ( 'NONE',  ( -142.0449999999999875, 7.632228543268600340, 2.479861379858949277 ) ) ;
#121=CARTESIAN_POINT ( 'NONE',  ( -52.85499999999998266, 4.716976649647094177, 6.492361379858945902 ) ) ;
#124=CARTESIAN_POINT ( 'NONE',  ( -56.24499999999999034, -4.716976649647093289, -6.492361379858945902 ) ) ;
#131=CARTESIAN_POINT ( 'NONE',  ( -108.1429263765338078, 5.598654528085800663, -7.705886871421367523 ) ) ;
#135=CARTESIAN_POINT ( 'NONE',  ( -89.30707362346616662, -10.01517768586948698, 6.132527647946031529E-16 ) ) ;
#149=VERTEX_POINT ( 'NONE', #38256 ) ;
#157=EDGE_CURVE ( 'NONE', #21970, #6242, #4359, .T. ) ;
#160=CARTESIAN_POINT ( 'NONE',  ( -103.0449999999999875, 7.632228543268600340, 2.479861379858949277 ) ) ;
#177=EDGE_CURVE ( 'NONE', #27373, #65754, #48012, .T. ) ;
#179=CARTESIAN_POINT ( 'NONE',  ( -165.8070736234661808, 10.01517768586948698, -1.839758294383808966E-15 ) ) ;
#183=DIRECTION ( 'NONE',  ( -1.000000000000000000, -0.000000000000000000, -0.000000000000000000 ) ) ;
#193=CARTESIAN_POINT ( 'NONE',  ( -49.55707362346617373, -1.166476076187852838E-15, -9.524999999999991473 ) ) ;
#199=CARTESIAN_POINT ( 'NONE',  ( -166.1049999999999898, -6.826472737025115478, 4.959722759717900331 ) ) ;
#201=CARTESIAN_POINT ( 'NONE',  ( -147.5070736234661695, 8.102448949553176405, 5.886773742842740909 ) ) ;
#202=CARTESIAN_POINT ( 'NONE',  ( -176.6949999999999363, -8.437984349512085203, 5.166775262442717831E-16 ) ) ;
#203=CARTESIAN_POINT ( 'NONE',  ( -162.8949999999999534, 6.826472737025115478, 4.959722759717899443 ) ) ;
#206=CARTESIAN_POINT ( 'NONE',  ( -83.60499999999998977, 6.826472737025113702, -4.959722759717902107 ) ) ;
#211=CARTESIAN_POINT ( 'NONE',  ( -76.94499999999997897, -9.827790563157499189E-16, -8.024999999999991473 ) ) ;
#218=EDGE_CURVE ( 'NONE', #1575, #11319, #54033, .T. ) ;
#239=CARTESIAN_POINT ( 'NONE',  ( -116.0049999999999955, 6.826472737025115478, 4.959722759717899443 ) ) ;
#244=ORIENTED_EDGE ( 'NONE', *, *, #29335, .T. ) ;
#246=VERTEX_POINT ( 'NONE', #61384 ) ;
#260=CARTESIAN_POINT ( 'NONE',  ( -47.75707362346617657, -5.598654528085801552, 7.705886871421367523 ) ) ;
#271=CARTESIAN_POINT ( 'NONE',  ( -141.6550000000000011, -7.632228543268600340, -2.479861379858950166 ) ) ;
#277=CARTESIAN_POINT ( 'NONE',  ( -106.6429263765338078, -5.598654528085801552, 7.705886871421367523 ) ) ;
#287=CARTESIAN_POINT ( 'NONE',  ( -55.55499999999999261, 0.000000000000000000, 8.024999999999991473 ) ) ;
#297=CARTESIAN_POINT ( 'NONE',  ( -195.0000000000000000, 0.000000000000000000, 9.524999999999991473 ) ) ;
#300=CARTESIAN_POINT ( 'NONE',  ( -111.1449999999999960, -4.716976649647092401, 6.492361379858946790 ) ) ;
#302=CARTESIAN_POINT ( 'NONE',  ( -91.79500000000000171, 2.607480562269068880, -8.024999999999993250 ) ) ;
#313=CARTESIAN_POINT ( 'NONE',  ( -124.3429263765337964, -9.058813317711329915, 2.943386871421371787 ) ) ;
#314=CARTESIAN_POINT ( 'NONE',  ( -149.0949999999999704, -2.607480562269071545, -8.024999999999991473 ) ) ;
#317=FACE_OUTER_BOUND ( 'NONE', #34215, .T. ) ;
#327=CARTESIAN_POINT ( 'NONE',  ( -129.6570736234661751, 9.058813317711329915, 2.943386871421369566 ) ) ;
#328=AXIS2_PLACEMENT_3D ( 'NONE', #15577, #26444, #22218 ) ;
#331=CARTESIAN_POINT ( 'NONE',  ( -138.2049999999999557, -2.607480562269071545, -8.024999999999991473 ) ) ;
#346=CARTESIAN_POINT ( 'NONE',  ( -60.65499999999998693, -7.632228543268600340, -2.479861379858950166 ) ) ;
#347=CARTESIAN_POINT ( 'NONE',  ( -124.4949999999999761, 6.826472737025113702, -4.959722759717902107 ) ) ;
#365=CARTESIAN_POINT ( 'NONE',  ( -170.4549999999999841, 7.632228543268599452, -2.479861379858951942 ) ) ;
#374=DIRECTION ( 'NONE',  ( -1.000000000000000000, -0.000000000000000000, -0.000000000000000000 ) ) ;
#375=CARTESIAN_POINT ( 'NONE',  ( -88.85499999999998977, 4.716976649647094177, 6.492361379858945902 ) ) ;
#378=CARTESIAN_POINT ( 'NONE',  ( -46.25707362346617657, 5.598654528085800663, -7.705886871421367523 ) ) ;
#383=CARTESIAN_POINT ( 'NONE',  ( -63.50707362346616947, 8.102448949553176405, 5.886773742842740909 ) ) ;
#392=CARTESIAN_POINT ( 'NONE',  ( -102.5049999999999955, -6.826472737025115478, -4.959722759717899443 ) ) ;
#394=CARTESIAN_POINT ( 'NONE',  ( -115.0449999999999875, 7.632228543268600340, 2.479861379858949277 ) ) ;
#398=CARTESIAN_POINT ( 'NONE',  ( -153.6570736234661751, 9.058813317711329915, 2.943386871421369566 ) ) ;
#400=CARTESIAN_POINT ( 'NONE',  ( -161.3929263765337794, 8.102448949553176405, 5.886773742842740909 ) ) ;
#401=CARTESIAN_POINT ( 'NONE',  ( -174.2949999999999591, -2.607480562269069768, 8.024999999999991473 ) ) ;
#409=CARTESIAN_POINT ( 'NONE',  ( -74.39292637653380780, 8.102448949553176405, 5.886773742842740909 ) ) ;
#418=CARTESIAN_POINT ( 'NONE',  ( -177.2050000000000125, -2.607480562269071545, -8.024999999999991473 ) ) ;
#423=DIRECTION ( 'NONE',  ( -1.000000000000000000, -0.000000000000000000, -0.000000000000000000 ) ) ;
#430=CARTESIAN_POINT ( 'NONE',  ( -96.80499999999999261, -8.437984349512086979, 5.166775262442717831E-16 ) ) ;
#435=CARTESIAN_POINT ( 'NONE',  ( -92.00707362346615525, -8.102448949553174629, -5.886773742842741797 ) ) ;
#438=CARTESIAN_POINT ( 'NONE',  ( -126.8929263765338220, -8.102448949553174629, -5.886773742842741797 ) ) ;
#442=CARTESIAN_POINT ( 'NONE',  ( -59.24499999999999034, -4.716976649647093289, -6.492361379858945902 ) ) ;
#447=CARTESIAN_POINT ( 'NONE',  ( -139.2570736234661695, 5.598654528085800663, -7.705886871421367523 ) ) ;
#450=CARTESIAN_POINT ( 'NONE',  ( -195.0000000000000000, 0.000000000000000000, 0.000000000000000000 ) ) ;
#453=CARTESIAN_POINT ( 'NONE',  ( -117.8050000000000068, -8.437984349512085203, 5.166775262442717831E-16 ) ) ;
#461=CARTESIAN_POINT ( 'NONE',  ( -159.5070736234661979, 8.102448949553176405, 5.886773742842740909 ) ) ;
#464=CARTESIAN_POINT ( 'NONE',  ( -99.05707362346618083, 0.000000000000000000, 9.524999999999991473 ) ) ;
#471=CARTESIAN_POINT ( 'NONE',  ( -144.9550000000000125, -7.632228543268599452, 2.479861379858951054 ) ) ;
#474=CARTESIAN_POINT ( 'NONE',  ( -144.4449999999999932, 0.000000000000000000, 8.024999999999991473 ) ) ;
#476=CARTESIAN_POINT ( 'NONE',  ( -136.6449999999999818, 4.716976649647091513, -6.492361379858946790 ) ) ;
#477=EDGE_LOOP ( 'NONE', ( #1632, #5095, #61496, #50075 ) ) ;
#481=CARTESIAN_POINT ( 'NONE',  ( -50.45499999999996987, 7.632228543268599452, -2.479861379858951942 ) ) ;
#482=CARTESIAN_POINT ( 'NONE',  ( -57.59499999999998465, 2.607480562269073321, 8.024999999999991473 ) ) ;
#486=CARTESIAN_POINT ( 'NONE',  ( -103.1929263765338192, -10.01517768586948698, 6.132527647946031529E-16 ) ) ;
#507=ORIENTED_EDGE ( 'NONE', *, *, #36909, .F. ) ;
#517=CARTESIAN_POINT ( 'NONE',  ( -90.44499999999997897, 0.000000000000000000, 8.024999999999991473 ) ) ;
#523=CARTESIAN_POINT ( 'NONE',  ( -175.4929263765337737, -8.102448949553174629, 5.886773742842742685 ) ) ;
#539=CARTESIAN_POINT ( 'NONE',  ( -115.4929263765338021, -8.102448949553174629, 5.886773742842742685 ) ) ;
#541=CARTESIAN_POINT ( 'NONE',  ( -161.5429263765338135, 9.058813317711329915, 2.943386871421369566 ) ) ;
#547=CARTESIAN_POINT ( 'NONE',  ( -171.0549999999999784, -9.827790563157499189E-16, -8.024999999999991473 ) ) ;
#550=CARTESIAN_POINT ( 'NONE',  ( -171.1449999999999818, -4.716976649647092401, 6.492361379858946790 ) ) ;
#553=CARTESIAN_POINT ( 'NONE',  ( -166.7949999999999875, 2.607480562269069324, -8.024999999999993250 ) ) ;
#559=CARTESIAN_POINT ( 'NONE',  ( -79.85499999999997556, 4.716976649647094177, 6.492361379858945902 ) ) ;
#560=CARTESIAN_POINT ( 'NONE',  ( -195.0000000000000000, 0.000000000000000000, 0.000000000000000000 ) ) ;
#564=CARTESIAN_POINT ( 'NONE',  ( -85.49499999999999034, 6.826472737025113702, -4.959722759717902107 ) ) ;
#588=CARTESIAN_POINT ( 'NONE',  ( -195.0000000000000000, 0.000000000000000000, 0.000000000000000000 ) ) ;
#591=CARTESIAN_POINT ( 'NONE',  ( -112.2549999999999955, -4.716976649647092401, 6.492361379858946790 ) ) ;
#595=LINE ( 'NONE', #31625, #55701 ) ;
#606=CARTESIAN_POINT ( 'NONE',  ( -118.4070736234669710, 3.094860106605118233, -9.525000000009663736 ) ) ;
#608=DIRECTION ( 'NONE',  ( -1.000000000000000000, -0.000000000000000000, -0.000000000000000000 ) ) ;
#618=VERTEX_POINT ( 'NONE', #65903 ) ;
#619=CARTESIAN_POINT ( 'NONE',  ( -50.24292637653379501, 5.598654528085804216, 7.705886871421366635 ) ) ;
#624=CARTESIAN_POINT ( 'NONE',  ( -140.4549999999999841, 7.632228543268599452, -2.479861379858951942 ) ) ;
#634=CARTESIAN_POINT ( 'NONE',  ( -58.10499999999999687, -6.826472737025115478, 4.959722759717900331 ) ) ;
#641=CARTESIAN_POINT ( 'NONE',  ( -96.44292637653380496, -1.166476076187852838E-15, -9.524999999999991473 ) ) ;
#647=CARTESIAN_POINT ( 'NONE',  ( -106.3449999999999989, 7.632228543268599452, -2.479861379858951942 ) ) ;
#649=CARTESIAN_POINT ( 'NONE',  ( -87.59499999999999886, 2.607480562269073321, 8.024999999999991473 ) ) ;
#652=AXIS2_PLACEMENT_3D ( 'NONE', #67205, #12333, #13740 ) ;
#658=CARTESIAN_POINT ( 'NONE',  ( -125.9929263765338021, 8.102448949553171076, -5.886773742842744461 ) ) ;
#659=CARTESIAN_POINT ( 'NONE',  ( -143.9950000000000045, -6.826472737025115478, 4.959722759717900331 ) ) ;
#669=CARTESIAN_POINT ( 'NONE',  ( -60.14292637653380069, 5.598654528085800663, -7.705886871421367523 ) ) ;
#673=CARTESIAN_POINT ( 'NONE',  ( -136.5549999999999784, 0.000000000000000000, 8.024999999999991473 ) ) ;
#682=CARTESIAN_POINT ( 'NONE',  ( -94.70707362346726654, -3.094860106636581509, -9.524999999986803800 ) ) ;
#684=CARTESIAN_POINT ( 'NONE',  ( -55.25499999999999545, -4.716976649647092401, 6.492361379858946790 ) ) ;
#685=CARTESIAN_POINT ( 'NONE',  ( -119.5449999999999875, -7.632228543268600340, -2.479861379858950166 ) ) ;
#694=CYLINDRICAL_SURFACE ( 'NONE', #40795, 9.524999999999991473 ) ;
#696=ORIENTED_EDGE ( 'NONE', *, *, #23588, .F. ) ;
#699=CARTESIAN_POINT ( 'NONE',  ( -174.5049999999999955, -6.826472737025115478, -4.959722759717899443 ) ) ;
#709=FACE_OUTER_BOUND ( 'NONE', #7778, .T. ) ;
#710=CARTESIAN_POINT ( 'NONE',  ( -84.50499999999999545, -6.826472737025115478, -4.959722759717899443 ) ) ;
#715=CARTESIAN_POINT ( 'NONE',  ( -64.55707362346618083, -1.166476076187852838E-15, -9.524999999999991473 ) ) ;
#721=CARTESIAN_POINT ( 'NONE',  ( -100.5549999999999926, 0.000000000000000000, 8.024999999999991473 ) ) ;
#724=CARTESIAN_POINT ( 'NONE',  ( -120.1449999999999818, -4.716976649647092401, 6.492361379858946790 ) ) ;
#728=EDGE_CURVE ( 'NONE', #56584, #51279, #30456, .T. ) ;
#729=CARTESIAN_POINT ( 'NONE',  ( -151.1929263765337907, -10.01517768586948698, 6.132527647946031529E-16 ) ) ;
#731=CARTESIAN_POINT ( 'NONE',  ( -172.1949999999999648, 8.437984349512085203, -1.550032578732815448E-15 ) ) ;
#735=EDGE_CURVE ( 'NONE', #36722, #13211, #28412, .T. ) ;
#739=CARTESIAN_POINT ( 'NONE',  ( -68.24292637653380211, 5.598654528085804216, 7.705886871421366635 ) ) ;
#747=CARTESIAN_POINT ( 'NONE',  ( -165.5049999999999955, -6.826472737025113702, -4.959722759717900331 ) ) ;
#755=CARTESIAN_POINT ( 'NONE',  ( -81.80499999999996419, -8.437984349512086979, 5.166775262442717831E-16 ) ) ;
#762=ORIENTED_EDGE ( 'NONE', *, *, #11363, .F. ) ;
#763=CARTESIAN_POINT ( 'NONE',  ( -62.24499999999998323, -4.716976649647093289, -6.492361379858945902 ) ) ;
#769=ORIENTED_EDGE ( 'NONE', *, *, #2609, .T. ) ;
#776=CARTESIAN_POINT ( 'NONE',  ( -117.3549999999999898, -4.716976649647093289, -6.492361379858945902 ) ) ;
#780=CARTESIAN_POINT ( 'NONE',  ( -147.2070736234661865, 3.094860106618433360, 9.524999999999991473 ) ) ;
#782=CARTESIAN_POINT ( 'NONE',  ( -94.10707362346613536, 8.102448949553171076, -5.886773742842744461 ) ) ;
#792=CARTESIAN_POINT ( 'NONE',  ( -128.1550000000000011, 7.632228543268600340, 2.479861379858949277 ) ) ;
#793=CARTESIAN_POINT ( 'NONE',  ( -163.9429263765338192, 0.000000000000000000, 9.524999999999991473 ) ) ;
#794=ADVANCED_FACE ( 'NONE', ( #22135 ), #59760, .T. ) ;
#795=CARTESIAN_POINT ( 'NONE',  ( -147.2929263765342682, 3.094860106610630712, -9.525000000005659828 ) ) ;
#797=CARTESIAN_POINT ( 'NONE',  ( -147.1450000000000102, -4.716976649647092401, 6.492361379858946790 ) ) ;
#798=CARTESIAN_POINT ( 'NONE',  ( -128.9950000000000045, -6.826472737025113702, 4.959722759717902107 ) ) ;
#804=CARTESIAN_POINT ( 'NONE',  ( -180.7429263765338021, -5.598654528085803328, -7.705886871421366635 ) ) ;
#806=CARTESIAN_POINT ( 'NONE',  ( -59.84499999999998465, -7.632228543268599452, 2.479861379858951054 ) ) ;
#811=CARTESIAN_POINT ( 'NONE',  ( -76.40707362346616094, 3.094860106618428031, -9.524999999999993250 ) ) ;
#812=CARTESIAN_POINT ( 'NONE',  ( -104.3929263765338078, 8.102448949553176405, 5.886773742842740909 ) ) ;
#841=CARTESIAN_POINT ( 'NONE',  ( -86.99499999999997613, -6.826472737025115478, 4.959722759717900331 ) ) ;
#857=CARTESIAN_POINT ( 'NONE',  ( -179.7570736234661979, -5.598654528085801552, 7.705886871421367523 ) ) ;
#860=ADVANCED_FACE ( 'NONE', ( #67456 ), #46041, .T. ) ;
#862=CARTESIAN_POINT ( 'NONE',  ( -115.0429263765338135, -9.058813317711329915, -2.943386871421370898 ) ) ;
#863=ORIENTED_EDGE ( 'NONE', *, *, #33369, .F. ) ;
#865=CARTESIAN_POINT ( 'NONE',  ( -162.2929263765340977, 3.094860106613655404, -9.525000000003460698 ) ) ;
#872=CARTESIAN_POINT ( 'NONE',  ( -158.6050000000000182, 6.826472737025113702, -4.959722759717902107 ) ) ;
#873=DIRECTION ( 'NONE',  ( -1.000000000000000000, -0.000000000000000000, -0.000000000000000000 ) ) ;
#874=CARTESIAN_POINT ( 'NONE',  ( -183.9431579317532055, -8.604615092590435665, -0.1013726718049147574 ) ) ;
#875=CARTESIAN_POINT ( 'NONE',  ( -172.6449999999999818, 4.716976649647091513, -6.492361379858946790 ) ) ;
#877=CARTESIAN_POINT ( 'NONE',  ( -170.9950000000000045, -6.826472737025113702, 4.959722759717902107 ) ) ;
#880=CARTESIAN_POINT ( 'NONE',  ( -90.29292637653378506, 3.094860106618428031, -9.524999999999993250 ) ) ;
#882=CARTESIAN_POINT ( 'NONE',  ( -86.15499999999998693, 7.632228543268600340, 2.479861379858949277 ) ) ;
#887=CARTESIAN_POINT ( 'NONE',  ( -85.19499999999999318, 8.437984349512086979, -1.550032578732815448E-15 ) ) ;
#889=CARTESIAN_POINT ( 'NONE',  ( -134.1570736234661751, -9.058813317711329915, -2.943386871421370898 ) ) ;
#895=CARTESIAN_POINT ( 'NONE',  ( -51.44292637653380496, -1.166476076187852838E-15, -9.524999999999991473 ) ) ;
#909=CARTESIAN_POINT ( 'NONE',  ( -115.5549999999999926, 0.000000000000000000, 8.024999999999991473 ) ) ;
#914=CARTESIAN_POINT ( 'NONE',  ( -57.14292637653378648, 5.598654528085800663, -7.705886871421367523 ) ) ;
#916=EDGE_LOOP ( 'NONE', ( #4799, #6621, #31272, #29643 ) ) ;
#935=CARTESIAN_POINT ( 'NONE',  ( -53.39292637653380069, 8.102448949553176405, 5.886773742842740909 ) ) ;
#937=DIRECTION ( 'NONE',  ( -1.000000000000000000, -0.000000000000000000, -0.000000000000000000 ) ) ;
#938=CARTESIAN_POINT ( 'NONE',  ( -158.9070736234665162, -3.094860106613422257, 9.525000000003631229 ) ) ;
#939=CARTESIAN_POINT ( 'NONE',  ( -138.6550000000000011, -7.632228543268600340, -2.479861379858950166 ) ) ;
#949=CARTESIAN_POINT ( 'NONE',  ( -51.50707362346618368, 8.102448949553176405, 5.886773742842740909 ) ) ;
#950=CARTESIAN_POINT ( 'NONE',  ( -52.85499999999998266, 4.716976649647094177, 6.492361379858945902 ) ) ;
#958=AXIS2_PLACEMENT_3D ( 'NONE', #57886, #42783, #47358 ) ;
#965=EDGE_CURVE ( 'NONE', #65527, #64066, #10468, .T. ) ;
#968=CARTESIAN_POINT ( 'NONE',  ( -79.55707362346616662, -1.166476076187852838E-15, -9.524999999999991473 ) ) ;
#972=CARTESIAN_POINT ( 'NONE',  ( -113.2449999999999903, -4.716976649647093289, -6.492361379858945902 ) ) ;
#974=CARTESIAN_POINT ( 'NONE',  ( -81.29499999999998749, -2.607480562269069768, 8.024999999999991473 ) ) ;
#982=CARTESIAN_POINT ( 'NONE',  ( -125.8429263765337964, 9.058813317711329915, -2.943386871421373119 ) ) ;
#984=CARTESIAN_POINT ( 'NONE',  ( -148.7950000000000159, 2.607480562269068880, -8.024999999999993250 ) ) ;
#987=CARTESIAN_POINT ( 'NONE',  ( -195.0000000000000000, 0.000000000000000000, 0.000000000000000000 ) ) ;
#994=CIRCLE ( 'NONE', #49400, 9.524999999999991473 ) ;
#997=CARTESIAN_POINT ( 'NONE',  ( -50.30707362346617373, -10.01517768586948698, 6.132527647946031529E-16 ) ) ;
#1000=EDGE_LOOP ( 'NONE', ( #21761, #35276, #54792, #50255 ) ) ;
#1001=CARTESIAN_POINT ( 'NONE',  ( -145.7050000000000125, 2.607480562269072433, 8.024999999999991473 ) ) ;
#1015=CARTESIAN_POINT ( 'NONE',  ( -55.55499999999999261, 0.000000000000000000, 8.024999999999991473 ) ) ;
#1016=CARTESIAN_POINT ( 'NONE',  ( -118.0450000000000017, 7.632228543268600340, 2.479861379858949277 ) ) ;
#1033=CARTESIAN_POINT ( 'NONE',  ( -172.8550000000000182, 4.716976649647094177, 6.492361379858945902 ) ) ;
#1048=CARTESIAN_POINT ( 'NONE',  ( -82.55499999999999261, 0.000000000000000000, 8.024999999999991473 ) ) ;
#1056=CARTESIAN_POINT ( 'NONE',  ( -57.05707362346618083, 0.000000000000000000, 9.524999999999991473 ) ) ;
#1062=CARTESIAN_POINT ( 'NONE',  ( -100.7049999999999841, 2.607480562269073321, 8.024999999999991473 ) ) ;
#1064=CARTESIAN_POINT ( 'NONE',  ( -115.1949999999999932, 8.437984349512085203, -1.550032578732815448E-15 ) ) ;
#1069=CARTESIAN_POINT ( 'NONE',  ( -18.30291578181160972, 11.39569540983528206, -3.767653220740891484 ) ) ;
#1070=CARTESIAN_POINT ( 'NONE',  ( -152.8429263765337964, 9.058813317711329915, -2.943386871421373119 ) ) ;
#1072=CARTESIAN_POINT ( 'NONE',  ( -172.4950000000000045, 6.826472737025113702, -4.959722759717902107 ) ) ;
#1081=CARTESIAN_POINT ( 'NONE',  ( -70.64292637653379359, -5.598654528085801552, 7.705886871421367523 ) ) ;
#1084=CARTESIAN_POINT ( 'NONE',  ( -195.0000000000000000, 0.000000000000000000, 0.000000000000000000 ) ) ;
#1093=CARTESIAN_POINT ( 'NONE',  ( -171.3550000000000182, -4.716976649647093289, -6.492361379858945902 ) ) ;
#1105=CARTESIAN_POINT ( 'NONE',  ( -84.80499999999999261, -8.437984349512086979, 5.166775262442717831E-16 ) ) ;
#1110=CARTESIAN_POINT ( 'NONE',  ( -169.9429263765337907, 0.000000000000000000, 9.524999999999991473 ) ) ;
#1118=CARTESIAN_POINT ( 'NONE',  ( -64.94499999999999318, -9.827790563157499189E-16, -8.024999999999991473 ) ) ;
#1132=CARTESIAN_POINT ( 'NONE',  ( -117.0549999999999926, -9.827790563157499189E-16, -8.024999999999991473 ) ) ;
#1135=CARTESIAN_POINT ( 'NONE',  ( -72.59292637653379643, -3.094860106618431139, -9.524999999999991473 ) ) ;
#1140=CARTESIAN_POINT ( 'NONE',  ( -149.9070736234661183, -3.094860106618429807, 9.524999999999991473 ) ) ;
#1143=CARTESIAN_POINT ( 'NONE',  ( -97.85707362346616378, -5.598654528085803328, -7.705886871421366635 ) ) ;
#1147=VERTEX_POINT ( 'NONE', #23771 ) ;
#1150=CARTESIAN_POINT ( 'NONE',  ( -130.1049999999999898, -6.826472737025115478, 4.959722759717900331 ) ) ;
#1151=CARTESIAN_POINT ( 'NONE',  ( -164.3929263765337794, 8.102448949553176405, 5.886773742842740909 ) ) ;
#1152=CARTESIAN_POINT ( 'NONE',  ( -146.9929263765338021, 8.102448949553172852, -5.886773742842744461 ) ) ;
#1154=CARTESIAN_POINT ( 'NONE',  ( -143.0949999999999704, -2.607480562269071545, -8.024999999999991473 ) ) ;
#1155=CARTESIAN_POINT ( 'NONE',  ( -133.3449999999999989, 7.632228543268599452, -2.479861379858951942 ) ) ;
#1164=CARTESIAN_POINT ( 'NONE',  ( -48.50499999999998835, -6.826472737025115478, -4.959722759717899443 ) ) ;
#1165=CARTESIAN_POINT ( 'NONE',  ( -54.44499999999999318, 0.000000000000000000, 8.024999999999991473 ) ) ;
#1168=LINE ( 'NONE', #22705, #15247 ) ;
#1173=CARTESIAN_POINT ( 'NONE',  ( -95.69292637653379074, 10.01517768586948698, -1.839758294383808571E-15 ) ) ;
#1180=CARTESIAN_POINT ( 'NONE',  ( -100.2570736234661695, 5.598654528085800663, -7.705886871421367523 ) ) ;
#1193=ADVANCED_FACE ( 'NONE', ( #3310, #15668 ), #63497, .T. ) ;
#1205=CARTESIAN_POINT ( 'NONE',  ( -94.55707362346616662, -1.166476076187852838E-15, -9.524999999999991473 ) ) ;
#1208=CARTESIAN_POINT ( 'NONE',  ( -94.34499999999998465, 7.632228543268599452, -2.479861379858951942 ) ) ;
#1210=CARTESIAN_POINT ( 'NONE',  ( -195.0000000000000000, 0.000000000000000000, 0.000000000000000000 ) ) ;
#1225=DIRECTION ( 'NONE',  ( -1.000000000000000000, -0.000000000000000000, -0.000000000000000000 ) ) ;
#1236=CARTESIAN_POINT ( 'NONE',  ( -148.8570736234661638, -5.598654528085803328, -7.705886871421366635 ) ) ;
#1239=CARTESIAN_POINT ( 'NONE',  ( -157.7049999999999557, 2.607480562269073321, 8.024999999999991473 ) ) ;
#1243=CARTESIAN_POINT ( 'NONE',  ( -169.6449999999999818, 4.716976649647091513, -6.492361379858946790 ) ) ;
#1244=CARTESIAN_POINT ( 'NONE',  ( -156.4449999999999932, 0.000000000000000000, 8.024999999999991473 ) ) ;
#1246=( BOUNDED_CURVE ( )  B_SPLINE_CURVE ( 2, ( #14281, #8668, #68114, #46334, #52297, #62798, #40698, #62111, #14641, #9015, #35747 ),
 .UNSPECIFIED., .F., .F. ) 
 B_SPLINE_CURVE_WITH_KNOTS ( ( 3, 2, 2, 2, 2, 3 ),
 ( 0.7391304347826086474, 0.7413043478260870067, 0.7434782608695652550, 0.7456521739130435034, 0.7478260869565217517, 0.7500000000000000000 ),
 .UNSPECIFIED. ) 
 CURVE ( )  GEOMETRIC_REPRESENTATION_ITEM ( )  RATIONAL_B_SPLINE_CURVE ( ( 1.000000000000000000, 0.9510565162951535312, 1.000000000000000000, 0.9510565162951535312, 1.000000000000000000, 0.9510565162951535312, 1.000000000000000000, 0.9510565162951535312, 1.000000000000000000, 0.9510565162951535312, 1.000000000000000000 ) ) 
 REPRESENTATION_ITEM ( '' )  );
#1250=LINE ( 'NONE', #60055, #46266 ) ;
#1251=CARTESIAN_POINT ( 'NONE',  ( -68.90499999999997272, 2.607480562269068880, -8.024999999999993250 ) ) ;
#1255=CARTESIAN_POINT ( 'NONE',  ( -74.69499999999995055, -8.437984349512086979, 5.166775262442717831E-16 ) ) ;
#1269=ORIENTED_EDGE ( 'NONE', *, *, #12536, .F. ) ;
#1270=VERTEX_POINT ( 'NONE', #47359 ) ;
#1279=CARTESIAN_POINT ( 'NONE',  ( -113.0049999999999812, 6.826472737025115478, 4.959722759717899443 ) ) ;
#1285=CARTESIAN_POINT ( 'NONE',  ( -68.90707362346616094, -3.094860106618429807, 9.524999999999991473 ) ) ;
#1304=CARTESIAN_POINT ( 'NONE',  ( -104.0929263765348054, 3.094860106635372698, 9.524999999987684873 ) ) ;
#1312=CARTESIAN_POINT ( 'NONE',  ( -195.0000000000000000, 0.000000000000000000, 0.000000000000000000 ) ) ;
#1314=CARTESIAN_POINT ( 'NONE',  ( -133.1050000000000182, -6.826472737025115478, 4.959722759717900331 ) ) ;
#1327=CARTESIAN_POINT ( 'NONE',  ( -57.95499999999997698, -7.632228543268599452, 2.479861379858951054 ) ) ;
#1332=CIRCLE ( 'NONE', #28318, 8.524999999999977263 ) ;
#1335=CARTESIAN_POINT ( 'NONE',  ( -129.2929263765344956, 3.094860106606730721, -9.525000000008491341 ) ) ;
#1343=CARTESIAN_POINT ( 'NONE',  ( -105.8949999999999818, 6.826472737025115478, 4.959722759717899443 ) ) ;
#1345=CARTESIAN_POINT ( 'NONE',  ( -79.94499999999999318, -9.827790563157499189E-16, -8.024999999999991473 ) ) ;
#1351=( BOUNDED_CURVE ( )  B_SPLINE_CURVE ( 2, ( #31554, #16113, #4825, #37593, #63906, #32255, #25576, #47091, #26277, #68515, #20312 ),
 .UNSPECIFIED., .F., .F. ) 
 B_SPLINE_CURVE_WITH_KNOTS ( ( 3, 2, 2, 2, 2, 3 ),
 ( 0.8695652173913043237, 0.8717391304347825720, 0.8739130434782608203, 0.8760869565217391797, 0.8782608695652174280, 0.8804347826086956763 ),
 .UNSPECIFIED. ) 
 CURVE ( )  GEOMETRIC_REPRESENTATION_ITEM ( )  RATIONAL_B_SPLINE_CURVE ( ( 1.000000000000000000, 0.9510565162951535312, 1.000000000000000000, 0.9510565162951535312, 1.000000000000000000, 0.9510565162951535312, 1.000000000000000000, 0.9510565162951535312, 1.000000000000000000, 0.9510565162951535312, 1.000000000000000000 ) ) 
 REPRESENTATION_ITEM ( '' )  );
#1356=CARTESIAN_POINT ( 'NONE',  ( -120.1429263765338078, 5.598654528085800663, -7.705886871421367523 ) ) ;
#1358=CARTESIAN_POINT ( 'NONE',  ( -135.4449999999999932, 0.000000000000000000, 8.024999999999991473 ) ) ;
#1361=ADVANCED_FACE ( 'NONE', ( #17064 ), #27566, .T. ) ;
#1362=CARTESIAN_POINT ( 'NONE',  ( -48.14499999999999602, -4.716976649647092401, 6.492361379858946790 ) ) ;
#1375=CARTESIAN_POINT ( 'NONE',  ( -140.0049999999999670, 6.826472737025115478, 4.959722759717899443 ) ) ;
#1394=CARTESIAN_POINT ( 'NONE',  ( -53.45499999999997698, 7.632228543268599452, -2.479861379858951942 ) ) ;
#1396=ORIENTED_EDGE ( 'NONE', *, *, #47139, .F. ) ;
#1411=CARTESIAN_POINT ( 'NONE',  ( -174.8050000000000068, -8.437984349512085203, 5.166775262442717831E-16 ) ) ;
#1414=CARTESIAN_POINT ( 'NONE',  ( -183.9999999999998863, -8.156250775944638320, 1.871348862729520279 ) ) ;
#1419=CARTESIAN_POINT ( 'NONE',  ( -81.80499999999996419, -8.437984349512085203, 5.166775262442717831E-16 ) ) ;
#1429=CARTESIAN_POINT ( 'NONE',  ( -110.6949999999999932, -8.437984349512085203, 5.166775262442717831E-16 ) ) ;
#1433=CARTESIAN_POINT ( 'NONE',  ( -18.76049541207539306, 11.53663499276287752, -3.311062927408552792 ) ) ;
#1434=CARTESIAN_POINT ( 'NONE',  ( -150.7429263765338021, -5.598654528085803328, -7.705886871421366635 ) ) ;
#1436=CARTESIAN_POINT ( 'NONE',  ( -175.0450000000000159, 7.632228543268600340, 2.479861379858949277 ) ) ;
#1439=CARTESIAN_POINT ( 'NONE',  ( -136.9429263765338192, 0.000000000000000000, 9.524999999999991473 ) ) ;
#1445=CARTESIAN_POINT ( 'NONE',  ( -68.69292637653381917, 10.01517768586948698, -1.839758294383808571E-15 ) ) ;
#1455=CARTESIAN_POINT ( 'NONE',  ( -166.2549999999999955, -4.716976649647092401, 6.492361379858946790 ) ) ;
#1462=FACE_OUTER_BOUND ( 'NONE', #20819, .T. ) ;
#1470=CARTESIAN_POINT ( 'NONE',  ( -195.0000000000000000, 0.000000000000000000, 9.524999999999991473 ) ) ;
#1471=EDGE_CURVE ( 'NONE', #62435, #36781, #56877, .T. ) ;
#1472=CARTESIAN_POINT ( 'NONE',  ( -81.95499999999998408, -7.632228543268599452, 2.479861379858951054 ) ) ;
#1479=CARTESIAN_POINT ( 'NONE',  ( -60.89499999999999602, 6.826472737025116366, 4.959722759717898555 ) ) ;
#1481=DIRECTION ( 'NONE',  ( 0.000000000000000000, 0.000000000000000000, 1.000000000000000000 ) ) ;
#1487=CARTESIAN_POINT ( 'NONE',  ( -55.79499999999998039, 2.607480562269069324, -8.024999999999993250 ) ) ;
#1493=CARTESIAN_POINT ( 'NONE',  ( -110.0049999999999955, 6.826472737025116366, 4.959722759717898555 ) ) ;
#1498=CARTESIAN_POINT ( 'NONE',  ( -153.9570736234661581, 9.058813317711329915, -2.943386871421373119 ) ) ;
#1503=CARTESIAN_POINT ( 'NONE',  ( -81.20707362346617231, 3.094860106618433360, 9.524999999999991473 ) ) ;
#1506=CARTESIAN_POINT ( 'NONE',  ( -96.44292637653380496, -1.166476076187852838E-15, -9.524999999999991473 ) ) ;
#1512=CARTESIAN_POINT ( 'NONE',  ( -128.4549999999999841, 7.632228543268599452, -2.479861379858951942 ) ) ;
#1516=CARTESIAN_POINT ( 'NONE',  ( -139.1950000000000216, 8.437984349512085203, -1.550032578732815448E-15 ) ) ;
#1519=CARTESIAN_POINT ( 'NONE',  ( -130.4950000000000045, 6.826472737025113702, -4.959722759717902107 ) ) ;
#1524=CARTESIAN_POINT ( 'NONE',  ( -48.65499999999997272, -7.632228543268600340, -2.479861379858950166 ) ) ;
#1525=CARTESIAN_POINT ( 'NONE',  ( -58.04499999999998749, 7.632228543268600340, 2.479861379858949277 ) ) ;
#1534=CARTESIAN_POINT ( 'NONE',  ( -99.59292637653381064, -3.094860106618431139, -9.524999999999991473 ) ) ;
#1535=PRODUCT_CONTEXT ( 'NONE', #25304, 'mechanical' ) ;
#1545=VERTEX_POINT ( 'NONE', #47649 ) ;
#1559=CARTESIAN_POINT ( 'NONE',  ( -115.8570736234661780, -5.598654528085803328, -7.705886871421366635 ) ) ;
#1563=CARTESIAN_POINT ( 'NONE',  ( -93.35707362346617799, 5.598654528085804216, 7.705886871421366635 ) ) ;
#1566=CARTESIAN_POINT ( 'NONE',  ( -93.44499999999999318, 0.000000000000000000, 8.024999999999991473 ) ) ;
#1575=VERTEX_POINT ( 'NONE', #63749 ) ;
#1578=CARTESIAN_POINT ( 'NONE',  ( -137.0929263765344217, 3.094860106628584351, 9.524999999992617816 ) ) ;
#1582=CARTESIAN_POINT ( 'NONE',  ( -176.7570736234661695, -5.598654528085801552, 7.705886871421367523 ) ) ;
#1586=CARTESIAN_POINT ( 'NONE',  ( -113.3070736234661666, -10.01517768586948698, 6.132527647946031529E-16 ) ) ;
#1596=CARTESIAN_POINT ( 'NONE',  ( -160.4049999999999727, -2.607480562269069768, 8.024999999999991473 ) ) ;
#1598=CARTESIAN_POINT ( 'NONE',  ( -183.9007312495837425, -8.565707761958867295, -1.052177752376815212 ) ) ;
#1599=CARTESIAN_POINT ( 'NONE',  ( -176.8449999999999989, -7.632228543268599452, 2.479861379858951054 ) ) ;
#1600=CARTESIAN_POINT ( 'NONE',  ( -156.5949999999999704, 2.607480562269072433, 8.024999999999991473 ) ) ;
#1603=DIRECTION ( 'NONE',  ( -1.000000000000000000, -0.000000000000000000, -0.000000000000000000 ) ) ;
#1607=CARTESIAN_POINT ( 'NONE',  ( -77.60499999999996135, 6.826472737025113702, -4.959722759717902107 ) ) ;
#1609=EDGE_CURVE ( 'NONE', #36722, #59012, #4024, .T. ) ;
#1611=CARTESIAN_POINT ( 'NONE',  ( -74.54499999999998749, -7.632228543268600340, -2.479861379858950166 ) ) ;
#1612=EDGE_CURVE ( 'NONE', #51275, #57245, #37073, .T. ) ;
#1630=CARTESIAN_POINT ( 'NONE',  ( -119.2429263765338021, 5.598654528085804216, 7.705886871421366635 ) ) ;
#1632=ORIENTED_EDGE ( 'NONE', *, *, #18041, .F. ) ;
#1636=CARTESIAN_POINT ( 'NONE',  ( -133.2570736234661695, 5.598654528085800663, -7.705886871421367523 ) ) ;
#1645=CARTESIAN_POINT ( 'NONE',  ( -113.3049999999999784, 8.437984349512086979, -1.550032578732815448E-15 ) ) ;
#1658=DIRECTION ( 'NONE',  ( -0.2503800040544290062, 0.000000000000000000, -0.9681476403781109630 ) ) ;
#1671=CARTESIAN_POINT ( 'NONE',  ( -129.8050000000000068, -8.437984349512085203, 5.166775262442717831E-16 ) ) ;
#1677=CARTESIAN_POINT ( 'NONE',  ( -157.7929263765340977, -3.094860106612715711, 9.525000000004141043 ) ) ;
#1683=CARTESIAN_POINT ( 'NONE',  ( -50.45499999999996987, 7.632228543268599452, -2.479861379858951942 ) ) ;
#1688=DIRECTION ( 'NONE',  ( 0.000000000000000000, 0.000000000000000000, 1.000000000000000000 ) ) ;
#1700=CARTESIAN_POINT ( 'NONE',  ( -97.49499999999999034, 6.826472737025113702, -4.959722759717902107 ) ) ;
#1701=EDGE_CURVE ( 'NONE', #44158, #54061, #62331, .T. ) ;
#1703=CARTESIAN_POINT ( 'NONE',  ( -80.99499999999999034, -6.826472737025115478, 4.959722759717900331 ) ) ;
#1711=CARTESIAN_POINT ( 'NONE',  ( -125.2429263765338021, 5.598654528085804216, 7.705886871421366635 ) ) ;
#1713=CARTESIAN_POINT ( 'NONE',  ( -140.9949999999999193, -6.826472737025115478, 4.959722759717900331 ) ) ;
#1730=CARTESIAN_POINT ( 'NONE',  ( -143.4550000000000125, 7.632228543268599452, -2.479861379858951942 ) ) ;
#1737=ORIENTED_EDGE ( 'NONE', *, *, #52562, .F. ) ;
#1746=CARTESIAN_POINT ( 'NONE',  ( -58.10499999999998977, -6.826472737025113702, 4.959722759717902107 ) ) ;
#1748=VERTEX_POINT ( 'NONE', #50030 ) ;
#1760=CARTESIAN_POINT ( 'NONE',  ( -164.7549999999999955, 4.716976649647091513, -6.492361379858946790 ) ) ;
#1769=CYLINDRICAL_SURFACE ( 'NONE', #53748, 9.524999999999991473 ) ;
#1770=CARTESIAN_POINT ( 'NONE',  ( -82.25499999999998124, -4.716976649647092401, 6.492361379858946790 ) ) ;
#1774=CARTESIAN_POINT ( 'NONE',  ( -150.0570736234661808, 0.000000000000000000, 9.524999999999991473 ) ) ;
#1778=ORIENTED_EDGE ( 'NONE', *, *, #49397, .T. ) ;
#1780=CARTESIAN_POINT ( 'NONE',  ( -52.55707362346618083, -1.166476076187852838E-15, -9.524999999999991473 ) ) ;
#1785=CARTESIAN_POINT ( 'NONE',  ( -107.2449999999999903, -4.716976649647093289, -6.492361379858945902 ) ) ;
#1788=CARTESIAN_POINT ( 'NONE',  ( -19.48793012548083325, 11.79525974137268562, 2.228109774474827276 ) ) ;
#1789=CARTESIAN_POINT ( 'NONE',  ( -152.2429263765338021, 5.598654528085804216, 7.705886871421366635 ) ) ;
#1790=CARTESIAN_POINT ( 'NONE',  ( -165.1449999999999818, -4.716976649647092401, 6.492361379858946790 ) ) ;
#1797=CARTESIAN_POINT ( 'NONE',  ( -64.64292637653379359, -5.598654528085801552, 7.705886871421367523 ) ) ;
#1804=CARTESIAN_POINT ( 'NONE',  ( -169.8550000000000182, 4.716976649647094177, 6.492361379858945902 ) ) ;
#1813=CARTESIAN_POINT ( 'NONE',  ( -82.55499999999999261, 0.000000000000000000, 8.024999999999991473 ) ) ;
#1820=CARTESIAN_POINT ( 'NONE',  ( -127.0429263765337993, -9.058813317711329915, -2.943386871421370898 ) ) ;
#1821=CARTESIAN_POINT ( 'NONE',  ( -112.9429263765338050, 0.000000000000000000, 9.524999999999991473 ) ) ;
#1823=CARTESIAN_POINT ( 'NONE',  ( -112.5570736234661808, -1.166476076187852838E-15, -9.524999999999991473 ) ) ;
#1827=CARTESIAN_POINT ( 'NONE',  ( -53.84499999999997755, -7.632228543268599452, 2.479861379858951054 ) ) ;
#1835=CARTESIAN_POINT ( 'NONE',  ( -49.04499999999998039, 7.632228543268600340, 2.479861379858949277 ) ) ;
#1839=CARTESIAN_POINT ( 'NONE',  ( -114.6549999999999869, -7.632228543268600340, -2.479861379858950166 ) ) ;
#1840=ORIENTED_EDGE ( 'NONE', *, *, #16931, .T. ) ;
#1844=FACE_OUTER_BOUND ( 'NONE', #6899, .T. ) ;
#1845=CARTESIAN_POINT ( 'NONE',  ( -154.1070736234661922, 8.102448949553171076, -5.886773742842744461 ) ) ;
#1848=CARTESIAN_POINT ( 'NONE',  ( -87.20707362346618652, 3.094860106618433360, 9.524999999999991473 ) ) ;
#1854=CARTESIAN_POINT ( 'NONE',  ( -126.5049999999999528, -6.826472737025115478, -4.959722759717899443 ) ) ;
#1859=CARTESIAN_POINT ( 'NONE',  ( -132.5949999999999989, 2.607480562269073321, 8.024999999999991473 ) ) ;
#1861=AXIS2_PLACEMENT_3D ( 'NONE', #1210, #22048, #4910 ) ;
#1862=CARTESIAN_POINT ( 'NONE',  ( -127.7949999999999875, 2.607480562269069324, -8.024999999999993250 ) ) ;
#1869=CARTESIAN_POINT ( 'NONE',  ( -183.0000000000000000, 0.000000000000000000, 9.524999999999991473 ) ) ;
#1870=CARTESIAN_POINT ( 'NONE',  ( -183.4429263765338192, -1.166476076187852838E-15, -9.524999999999991473 ) ) ;
#1871=CARTESIAN_POINT ( 'NONE',  ( -47.24499999999998323, -4.716976649647093289, -6.492361379858945902 ) ) ;
#1873=CARTESIAN_POINT ( 'NONE',  ( -102.3570736234661780, 5.598654528085804216, 7.705886871421366635 ) ) ;
#1876=CARTESIAN_POINT ( 'NONE',  ( -76.25707362346616947, 5.598654528085800663, -7.705886871421367523 ) ) ;
#1877=CARTESIAN_POINT ( 'NONE',  ( -92.84292637653379643, 9.058813317711329915, -2.943386871421373119 ) ) ;
#1879=CARTESIAN_POINT ( 'NONE',  ( -163.4070736234664309, 3.094860106614563122, -9.525000000002803446 ) ) ;
#1883=ORIENTED_EDGE ( 'NONE', *, *, #45933, .F. ) ;
#1898=CARTESIAN_POINT ( 'NONE',  ( -91.04499999999998749, 7.632228543268600340, 2.479861379858949277 ) ) ;
#1910=CYLINDRICAL_SURFACE ( 'NONE', #12487, 5.000000000000000000 ) ;
#1913=CARTESIAN_POINT ( 'NONE',  ( -176.9070736234661751, -3.094860106618429807, 9.524999999999991473 ) ) ;
#1917=CARTESIAN_POINT ( 'NONE',  ( -117.2070736234661723, 3.094860106618433360, 9.524999999999991473 ) ) ;
#1923=ORIENTED_EDGE ( 'NONE', *, *, #7630, .F. ) ;
#1924=CARTESIAN_POINT ( 'NONE',  ( -159.0550000000000068, -9.827790563157499189E-16, -8.024999999999991473 ) ) ;
#1926=CARTESIAN_POINT ( 'NONE',  ( -162.2949999999999875, -2.607480562269069768, 8.024999999999991473 ) ) ;
#1928=CARTESIAN_POINT ( 'NONE',  ( -162.4449999999999932, 0.000000000000000000, 8.024999999999991473 ) ) ;
#1935=CARTESIAN_POINT ( 'NONE',  ( -74.75499999999998124, 4.716976649647091513, -6.492361379858946790 ) ) ;
#1939=CARTESIAN_POINT ( 'NONE',  ( -74.09499999999998465, -2.607480562269071545, -8.024999999999991473 ) ) ;
#1952=CARTESIAN_POINT ( 'NONE',  ( -60.65707362346617515, 9.058813317711329915, 2.943386871421369566 ) ) ;
#1956=LINE ( 'NONE', #44982, #13535 ) ;
#1960=CARTESIAN_POINT ( 'NONE',  ( -100.4050000000000011, -2.607480562269069768, 8.024999999999991473 ) ) ;
#1972=CARTESIAN_POINT ( 'NONE',  ( -10.67562708368618551, -11.73435252745061774, -2.515260829213044058 ) ) ;
#1973=CARTESIAN_POINT ( 'NONE',  ( -150.4429263765338192, -1.166476076187852838E-15, -9.524999999999991473 ) ) ;
#1976=DIRECTION ( 'NONE',  ( 0.000000000000000000, 0.000000000000000000, 1.000000000000000000 ) ) ;
#1985=ORIENTED_EDGE ( 'NONE', *, *, #53832, .T. ) ;
#1989=CARTESIAN_POINT ( 'NONE',  ( -135.0549999999999784, -9.827790563157499189E-16, -8.024999999999991473 ) ) ;
#2002=CARTESIAN_POINT ( 'NONE',  ( -50.00499999999998835, 6.826472737025116366, 4.959722759717898555 ) ) ;
#2005=FACE_OUTER_BOUND ( 'NONE', #25769, .T. ) ;
#2009=CARTESIAN_POINT ( 'NONE',  ( -182.0949999999999989, -2.607480562269071545, -8.024999999999991473 ) ) ;
#2017=CARTESIAN_POINT ( 'NONE',  ( -98.39499999999999602, -6.826472737025113702, -4.959722759717900331 ) ) ;
#2019=CARTESIAN_POINT ( 'NONE',  ( -79.64499999999999602, 4.716976649647091513, -6.492361379858946790 ) ) ;
#2022=DIRECTION ( 'NONE',  ( -0.7071067811865426878, 0.000000000000000000, 0.7071067811865524577 ) ) ;
#2023=DIRECTION ( 'NONE',  ( -1.000000000000000000, -0.000000000000000000, -0.000000000000000000 ) ) ;
#2027=CARTESIAN_POINT ( 'NONE',  ( -113.0929263765338106, 3.094860106618433360, 9.524999999999991473 ) ) ;
#2028=( BOUNDED_CURVE ( )  B_SPLINE_CURVE ( 2, ( #895, #32636, #47235, #55123, #65351, #44297, #33003, #16846, #48526, #64672, #11535 ),
 .UNSPECIFIED., .F., .F. ) 
 B_SPLINE_CURVE_WITH_KNOTS ( ( 3, 2, 2, 2, 2, 3 ),
 ( 0.9673913043478260532, 0.9695652173913043015, 0.9717391304347826608, 0.9739130434782609091, 0.9760869565217391575, 0.9782608695652174058 ),
 .UNSPECIFIED. ) 
 CURVE ( )  GEOMETRIC_REPRESENTATION_ITEM ( )  RATIONAL_B_SPLINE_CURVE ( ( 1.000000000000000000, 0.9510565162951535312, 1.000000000000000000, 0.9510565162951535312, 1.000000000000000000, 0.9510565162951535312, 1.000000000000000000, 0.9510565162951535312, 1.000000000000000000, 0.9510565162951535312, 1.000000000000000000 ) ) 
 REPRESENTATION_ITEM ( '' )  );
#2029=CARTESIAN_POINT ( 'NONE',  ( -139.7950000000000159, 2.607480562269068880, -8.024999999999993250 ) ) ;
#2035=CARTESIAN_POINT ( 'NONE',  ( -173.0929263765339670, 3.094860106620836326, 9.524999999998247091 ) ) ;
#2047=CARTESIAN_POINT ( 'NONE',  ( -135.9549999999999841, -7.632228543268599452, 2.479861379858951054 ) ) ;
#2062=CARTESIAN_POINT ( 'NONE',  ( -58.55499999999999261, 0.000000000000000000, 8.024999999999991473 ) ) ;
#2066=LINE ( 'NONE', #55253, #51346 ) ;
#2068=ADVANCED_FACE ( 'NONE', ( #44939 ), #69638, .T. ) ;
#2080=CARTESIAN_POINT ( 'NONE',  ( -164.1550000000000011, 7.632228543268600340, 2.479861379858949277 ) ) ;
#2093=CARTESIAN_POINT ( 'NONE',  ( -74.60500000000000398, 6.826472737025113702, -4.959722759717902107 ) ) ;
#2106=CARTESIAN_POINT ( 'NONE',  ( -106.9449999999999790, -9.827790563157499189E-16, -8.024999999999991473 ) ) ;
#2110=CARTESIAN_POINT ( 'NONE',  ( -151.6429263765338078, -5.598654528085801552, 7.705886871421367523 ) ) ;
#2112=CARTESIAN_POINT ( 'NONE',  ( -163.7950000000000159, 2.607480562269068880, -8.024999999999993250 ) ) ;
#2117=EDGE_LOOP ( 'NONE', ( #67842, #36360, #14328 ) ) ;
#2118=CARTESIAN_POINT ( 'NONE',  ( -67.04292637653381348, -9.058813317711329915, -2.943386871421370898 ) ) ;
#2122=CARTESIAN_POINT ( 'NONE',  ( -142.9429263765337907, 0.000000000000000000, 9.524999999999991473 ) ) ;
#2126=CARTESIAN_POINT ( 'NONE',  ( -167.9050000000000011, 2.607480562269069324, -8.024999999999993250 ) ) ;
#2127=ORIENTED_EDGE ( 'NONE', *, *, #52281, .T. ) ;
#2139=CARTESIAN_POINT ( 'NONE',  ( -84.35499999999998977, -4.716976649647093289, -6.492361379858945902 ) ) ;
#2148=CARTESIAN_POINT ( 'NONE',  ( -112.7070736234670392, -3.094860106632951524, -9.524999999989441690 ) ) ;
#2152=CARTESIAN_POINT ( 'NONE',  ( -50.09499999999996334, -2.607480562269071545, -8.024999999999991473 ) ) ;
#2155=( BOUNDED_CURVE ( )  B_SPLINE_CURVE ( 2, ( #60281, #50426, #37227, #18067, #55347, #38871, #58639, #10464, #7170, #39552, #6804 ),
 .UNSPECIFIED., .F., .F. ) 
 B_SPLINE_CURVE_WITH_KNOTS ( ( 3, 2, 2, 2, 2, 3 ),
 ( 0.3043478260869494356, 0.3065217391304276284, 0.3086956521739058212, 0.3108695652173840696, 0.3130434782608623179, 0.3152173913043405107 ),
 .UNSPECIFIED. ) 
 CURVE ( )  GEOMETRIC_REPRESENTATION_ITEM ( )  RATIONAL_B_SPLINE_CURVE ( ( 1.000000000000159872, 0.9510565162949935480, 1.000000000000000000, 0.9510565162951535312, 1.000000000000000000, 0.9510565162951535312, 1.000000000000000000, 0.9510565162951535312, 1.000000000000000000, 0.9510565162953185103, 0.9999999999998350209 ) ) 
 REPRESENTATION_ITEM ( '' )  );
#2162=CARTESIAN_POINT ( 'NONE',  ( -56.09499999999997044, -2.607480562269071545, -8.024999999999991473 ) ) ;
#2166=CARTESIAN_POINT ( 'NONE',  ( -104.1549999999999869, 7.632228543268600340, 2.479861379858949277 ) ) ;
#2173=CARTESIAN_POINT ( 'NONE',  ( -154.7070736234661297, -3.094860106618431139, -9.524999999999991473 ) ) ;
#2177=CARTESIAN_POINT ( 'NONE',  ( -82.85707362346616378, -5.598654528085803328, -7.705886871421366635 ) ) ;
#2185=CARTESIAN_POINT ( 'NONE',  ( -134.0049999999999955, 6.826472737025116366, 4.959722759717898555 ) ) ;
#2186=CARTESIAN_POINT ( 'NONE',  ( -164.0929263765340806, 3.094860106622937312, 9.524999999996721201 ) ) ;
#2189=CARTESIAN_POINT ( 'NONE',  ( -134.5449999999999875, -7.632228543268600340, -2.479861379858950166 ) ) ;
#2191=CARTESIAN_POINT ( 'NONE',  ( -128.8449999999999989, -7.632228543268599452, 2.479861379858951054 ) ) ;
#2194=VERTEX_POINT ( 'NONE', #29399 ) ;
#2195=DIRECTION ( 'NONE',  ( -1.000000000000000000, -0.000000000000000000, -0.000000000000000000 ) ) ;
#2199=CARTESIAN_POINT ( 'NONE',  ( -177.1429263765338078, 5.598654528085800663, -7.705886871421367523 ) ) ;
#2201=CARTESIAN_POINT ( 'NONE',  ( -49.04499999999998039, 7.632228543268600340, 2.479861379858949277 ) ) ;
#2207=CARTESIAN_POINT ( 'NONE',  ( -99.14292637653380780, 5.598654528085800663, -7.705886871421367523 ) ) ;
#2236=CARTESIAN_POINT ( 'NONE',  ( -85.49499999999999034, 6.826472737025113702, -4.959722759717902107 ) ) ;
#2254=CARTESIAN_POINT ( 'NONE',  ( -175.2570736234661695, 5.598654528085800663, -7.705886871421367523 ) ) ;
#2258=CARTESIAN_POINT ( 'NONE',  ( -115.7070736234661865, -3.094860106618431139, -9.524999999999991473 ) ) ;
#2260=CARTESIAN_POINT ( 'NONE',  ( -195.0000000000000000, 1.166476076187852838E-15, -9.524999999999991473 ) ) ;
#2267=CARTESIAN_POINT ( 'NONE',  ( -161.0050000000000239, 6.826472737025116366, 4.959722759717898555 ) ) ;
#2268=DIRECTION ( 'NONE',  ( 0.000000000000000000, 0.000000000000000000, -1.000000000000000000 ) ) ;
#2269=CARTESIAN_POINT ( 'NONE',  ( -183.6553645613615231, -6.378555885439770812, -6.171192800300671522 ) ) ;
#2271=CARTESIAN_POINT ( 'NONE',  ( -160.9449999999999932, -9.827790563157499189E-16, -8.024999999999991473 ) ) ;
#2272=CARTESIAN_POINT ( 'NONE',  ( -160.9449999999999932, -9.827790563157499189E-16, -8.024999999999991473 ) ) ;
#2279=CARTESIAN_POINT ( 'NONE',  ( -76.40499999999995850, -2.607480562269069768, 8.024999999999991473 ) ) ;
#2282=CARTESIAN_POINT ( 'NONE',  ( -74.39499999999998181, -6.826472737025113702, -4.959722759717900331 ) ) ;
#2288=CARTESIAN_POINT ( 'NONE',  ( -195.0000000000000000, 0.000000000000000000, 9.524999999999991473 ) ) ;
#2294=DIRECTION ( 'NONE',  ( 0.000000000000000000, 0.000000000000000000, 1.000000000000000000 ) ) ;
#2300=ADVANCED_FACE ( 'NONE', ( #56014 ), #33198, .T. ) ;
#2315=CARTESIAN_POINT ( 'NONE',  ( -144.5929263765343080, -3.094860106626901253, -9.524999999993836397 ) ) ;
#2322=CARTESIAN_POINT ( 'NONE',  ( -109.3449999999999847, 7.632228543268599452, -2.479861379858951942 ) ) ;
#2327=CARTESIAN_POINT ( 'NONE',  ( -10.16375755832578776, -11.93254622256288577, 1.312058623809986502 ) ) ;
#2343=CARTESIAN_POINT ( 'NONE',  ( -130.8549999999999898, 4.716976649647094177, 6.492361379858945902 ) ) ;
#2358=CARTESIAN_POINT ( 'NONE',  ( -49.70499999999996987, 2.607480562269073321, 8.024999999999991473 ) ) ;
#2361=CARTESIAN_POINT ( 'NONE',  ( -183.9550000000000125, -7.632228543268599452, 2.479861379858951054 ) ) ;
#2362=CYLINDRICAL_SURFACE ( 'NONE', #40303, 9.524999999999991473 ) ;
#2363=CARTESIAN_POINT ( 'NONE',  ( -60.05707362346616662, 0.000000000000000000, 9.524999999999991473 ) ) ;
#2366=ORIENTED_EDGE ( 'NONE', *, *, #2755, .F. ) ;
#2367=( BOUNDED_CURVE ( )  B_SPLINE_CURVE ( 2, ( #19020, #13070, #23971, #7110, #34874, #34524, #8158, #19384, #46161, #51069, #1774 ),
 .UNSPECIFIED., .F., .F. ) 
 B_SPLINE_CURVE_WITH_KNOTS ( ( 3, 2, 2, 2, 2, 3 ),
 ( 0.2282608695652120212, 0.2304347826086902418, 0.2326086956521684346, 0.2347826086956466551, 0.2369565217391248479, 0.2391304347826030685 ),
 .UNSPECIFIED. ) 
 CURVE ( )  GEOMETRIC_REPRESENTATION_ITEM ( )  RATIONAL_B_SPLINE_CURVE ( ( 1.000000000000120570, 0.9510565162950328499, 1.000000000000000000, 0.9510565162951535312, 1.000000000000000000, 0.9510565162951535312, 1.000000000000000000, 0.9510565162951535312, 1.000000000000000000, 0.9510565162952804297, 0.9999999999998731015 ) ) 
 REPRESENTATION_ITEM ( '' )  );
#2369=CARTESIAN_POINT ( 'NONE',  ( -162.0570736234661808, 0.000000000000000000, 9.524999999999991473 ) ) ;
#2371=CARTESIAN_POINT ( 'NONE',  ( -98.45499999999998408, 7.632228543268599452, -2.479861379858951942 ) ) ;
#2376=CARTESIAN_POINT ( 'NONE',  ( -102.7449999999999903, 4.716976649647094177, 6.492361379858945902 ) ) ;
#2378=CARTESIAN_POINT ( 'NONE',  ( -76.64499999999999602, 4.716976649647091513, -6.492361379858946790 ) ) ;
#2388=CARTESIAN_POINT ( 'NONE',  ( -115.3429263765337964, -9.058813317711329915, 2.943386871421371787 ) ) ;
#2390=CARTESIAN_POINT ( 'NONE',  ( -137.5449999999999875, -7.632228543268600340, -2.479861379858950166 ) ) ;
#2409=CARTESIAN_POINT ( 'NONE',  ( -135.3549999999999898, -4.716976649647093289, -6.492361379858945902 ) ) ;
#2412=CARTESIAN_POINT ( 'NONE',  ( -171.7429263765338305, -5.598654528085803328, -7.705886871421366635 ) ) ;
#2413=CARTESIAN_POINT ( 'NONE',  ( -83.84292637653379643, 9.058813317711329915, -2.943386871421373119 ) ) ;
#2417=CARTESIAN_POINT ( 'NONE',  ( -102.2929263765348367, 3.094860106601218241, -9.525000000012498802 ) ) ;
#2434=CARTESIAN_POINT ( 'NONE',  ( -88.19292637653379074, -10.01517768586948698, 6.132527647946031529E-16 ) ) ;
#2444=CARTESIAN_POINT ( 'NONE',  ( -165.5049999999999955, -6.826472737025115478, -4.959722759717899443 ) ) ;
#2454=ORIENTED_EDGE ( 'NONE', *, *, #47966, .F. ) ;
#2458=CARTESIAN_POINT ( 'NONE',  ( -75.65499999999998693, -7.632228543268600340, -2.479861379858950166 ) ) ;
#2471=CARTESIAN_POINT ( 'NONE',  ( -104.6949999999999790, -8.437984349512085203, 5.166775262442717831E-16 ) ) ;
#2478=CARTESIAN_POINT ( 'NONE',  ( -19.83697256712734713, 11.93284552246408659, -1.308412769435526091 ) ) ;
#2481=CARTESIAN_POINT ( 'NONE',  ( -139.1929263765337907, -10.01517768586948698, 6.132527647946031529E-16 ) ) ;
#2482=CARTESIAN_POINT ( 'NONE',  ( -164.8449999999999989, -7.632228543268599452, 2.479861379858951054 ) ) ;
#2487=DIRECTION ( 'NONE',  ( 0.000000000000000000, 0.000000000000000000, 1.000000000000000000 ) ) ;
#2500=VERTEX_POINT ( 'NONE', #20111 ) ;
#2501=CARTESIAN_POINT ( 'NONE',  ( -159.9549999999999841, -7.632228543268599452, 2.479861379858951054 ) ) ;
#2507=EDGE_CURVE ( 'NONE', #56670, #18337, #32738, .T. ) ;
#2515=CARTESIAN_POINT ( 'NONE',  ( -75.05499999999997840, -9.827790563157499189E-16, -8.024999999999991473 ) ) ;
#2520=DIRECTION ( 'NONE',  ( 0.000000000000000000, 0.000000000000000000, 1.000000000000000000 ) ) ;
#2527=CARTESIAN_POINT ( 'NONE',  ( -55.19499999999998607, 8.437984349512085203, -1.550032578732815448E-15 ) ) ;
#2531=CARTESIAN_POINT ( 'NONE',  ( -86.99292637653378790, 8.102448949553172852, -5.886773742842744461 ) ) ;
#2535=CARTESIAN_POINT ( 'NONE',  ( -53.09499999999997755, -2.607480562269071545, -8.024999999999991473 ) ) ;
#2539=CARTESIAN_POINT ( 'NONE',  ( -104.7549999999999812, 4.716976649647091513, -6.492361379858946790 ) ) ;
#2544=CARTESIAN_POINT ( 'NONE',  ( -144.0570736234661808, 0.000000000000000000, 9.524999999999991473 ) ) ;
#2548=CARTESIAN_POINT ( 'NONE',  ( -83.30707362346619504, -10.01517768586948698, 6.132527647946031529E-16 ) ) ;
#2557=CARTESIAN_POINT ( 'NONE',  ( -125.0049999999999812, 6.826472737025116366, 4.959722759717898555 ) ) ;
#2561=CARTESIAN_POINT ( 'NONE',  ( -131.5449999999999875, -7.632228543268600340, -2.479861379858950166 ) ) ;
#2562=CARTESIAN_POINT ( 'NONE',  ( -117.2950000000000017, -2.607480562269069768, 8.024999999999991473 ) ) ;
#2564=VERTEX_POINT ( 'NONE', #30310 ) ;
#2569=CARTESIAN_POINT ( 'NONE',  ( -171.4429263765337907, -1.166476076187852838E-15, -9.524999999999991473 ) ) ;
#2581=CARTESIAN_POINT ( 'NONE',  ( -94.19292637653380496, -10.01517768586948698, 6.132527647946031529E-16 ) ) ;
#2588=CARTESIAN_POINT ( 'NONE',  ( -79.10707362346616378, 8.102448949553172852, -5.886773742842744461 ) ) ;
#2609=EDGE_CURVE ( 'NONE', #18673, #27373, #69510, .T. ) ;
#2612=CARTESIAN_POINT ( 'NONE',  ( -71.45707362346617231, -9.058813317711329915, 2.943386871421371787 ) ) ;
#2614=CARTESIAN_POINT ( 'NONE',  ( -77.99499999999997613, -6.826472737025115478, 4.959722759717900331 ) ) ;
#2622=VECTOR ( 'NONE', #32591, 1000.000000000000000 ) ;
#2624=ORIENTED_EDGE ( 'NONE', *, *, #68364, .F. ) ;
#2632=CARTESIAN_POINT ( 'NONE',  ( -170.3070736234661524, -10.01517768586948698, 6.132527647946031529E-16 ) ) ;
#2635=CARTESIAN_POINT ( 'NONE',  ( -111.9570736234661723, 9.058813317711329915, -2.943386871421373119 ) ) ;
#2636=CARTESIAN_POINT ( 'NONE',  ( -183.2030253043162702, 3.561627562078368392, -8.644815131452912027 ) ) ;
#2644=CARTESIAN_POINT ( 'NONE',  ( -153.2049999999999272, -2.607480562269071545, -8.024999999999991473 ) ) ;
#2648=CARTESIAN_POINT ( 'NONE',  ( -167.5449999999999875, -7.632228543268600340, -2.479861379858950166 ) ) ;
#2649=VECTOR ( 'NONE', #36470, 1000.000000000000000 ) ;
#2650=CARTESIAN_POINT ( 'NONE',  ( -152.6949999999999932, -8.437984349512086979, 5.166775262442717831E-16 ) ) ;
#2655=CARTESIAN_POINT ( 'NONE',  ( -122.2429263765338021, 5.598654528085804216, 7.705886871421366635 ) ) ;
#2656=CARTESIAN_POINT ( 'NONE',  ( -72.80499999999997840, -8.437984349512085203, 5.166775262442717831E-16 ) ) ;
#2661=CARTESIAN_POINT ( 'NONE',  ( -73.04499999999998749, 7.632228543268600340, 2.479861379858949277 ) ) ;
#2670=CARTESIAN_POINT ( 'NONE',  ( -195.0000000000000000, 0.000000000000000000, 9.524999999999991473 ) ) ;
#2680=CARTESIAN_POINT ( 'NONE',  ( -132.5070736234661410, 8.102448949553176405, 5.886773742842740909 ) ) ;
#2694=CARTESIAN_POINT ( 'NONE',  ( -112.1949999999999932, 8.437984349512085203, -1.550032578732815448E-15 ) ) ;
#2699=CARTESIAN_POINT ( 'NONE',  ( -10.00805068894159788, -11.99663851293724548, -0.3286071531843878235 ) ) ;
#2700=CARTESIAN_POINT ( 'NONE',  ( -180.0570736234661808, 0.000000000000000000, 9.524999999999991473 ) ) ;
#2709=CARTESIAN_POINT ( 'NONE',  ( -123.0570736234661808, 0.000000000000000000, 9.524999999999991473 ) ) ;
#2715=CARTESIAN_POINT ( 'NONE',  ( -135.2050000000000125, -2.607480562269071545, -8.024999999999991473 ) ) ;
#2718=AXIS2_PLACEMENT_3D ( 'NONE', #10242, #30983, #56065 ) ;
#2728=CARTESIAN_POINT ( 'NONE',  ( -48.05499999999998550, -9.827790563157499189E-16, -8.024999999999991473 ) ) ;
#2731=CARTESIAN_POINT ( 'NONE',  ( -180.8050000000000068, -8.437984349512085203, 5.166775262442717831E-16 ) ) ;
#2732=CARTESIAN_POINT ( 'NONE',  ( -91.49292637653378790, -8.102448949553174629, 5.886773742842742685 ) ) ;
#2734=CARTESIAN_POINT ( 'NONE',  ( -54.05707362346618083, 0.000000000000000000, 9.524999999999991473 ) ) ;
#2742=CARTESIAN_POINT ( 'NONE',  ( -104.1549999999999869, 7.632228543268600340, 2.479861379858949277 ) ) ;
#2746=EDGE_CURVE ( 'NONE', #65704, #55073, #10961, .T. ) ;
#2749=CARTESIAN_POINT ( 'NONE',  ( -103.7949999999999733, 2.607480562269069324, -8.024999999999993250 ) ) ;
#2751=CARTESIAN_POINT ( 'NONE',  ( -66.89499999999996760, 6.826472737025116366, 4.959722759717898555 ) ) ;
#2755=EDGE_CURVE ( 'NONE', #48114, #618, #45393, .T. ) ;
#2761=CARTESIAN_POINT ( 'NONE',  ( -118.6429263765337936, -5.598654528085801552, 7.705886871421367523 ) ) ;
#2763=CARTESIAN_POINT ( 'NONE',  ( -133.6449999999999818, 4.716976649647091513, -6.492361379858946790 ) ) ;
#2765=CARTESIAN_POINT ( 'NONE',  ( -195.0000000000000000, 0.000000000000000000, 0.000000000000000000 ) ) ;
#2771=CARTESIAN_POINT ( 'NONE',  ( -63.29292637653380638, 3.094860106618428031, -9.524999999999993250 ) ) ;
#2774=CARTESIAN_POINT ( 'NONE',  ( -97.70707362346722391, -3.094860106636044605, -9.524999999987192822 ) ) ;
#2775=DIRECTION ( 'NONE',  ( 0.000000000000000000, 0.000000000000000000, 1.000000000000000000 ) ) ;
#2777=CARTESIAN_POINT ( 'NONE',  ( -128.3050000000000068, 8.437984349512086979, -1.550032578732815448E-15 ) ) ;
#2781=CARTESIAN_POINT ( 'NONE',  ( -121.2570736234661695, 5.598654528085800663, -7.705886871421367523 ) ) ;
#2783=CARTESIAN_POINT ( 'NONE',  ( -172.6429263765338078, -5.598654528085801552, 7.705886871421367523 ) ) ;
#2809=CARTESIAN_POINT ( 'NONE',  ( -162.2049999999999557, -2.607480562269071545, -8.024999999999991473 ) ) ;
#2812=( BOUNDED_CURVE ( )  B_SPLINE_CURVE ( 2, ( #56066, #50808, #39939, #45893, #8251, #8595, #62396, #3249, #29693, #24737, #24399 ),
 .UNSPECIFIED., .F., .F. ) 
 B_SPLINE_CURVE_WITH_KNOTS ( ( 3, 2, 2, 2, 2, 3 ),
 ( 0.1847826086956477487, 0.1869565217391259693, 0.1891304347826041621, 0.1913043478260823549, 0.1934782608695605477, 0.1956521739130387683 ),
 .UNSPECIFIED. ) 
 CURVE ( )  GEOMETRIC_REPRESENTATION_ITEM ( )  RATIONAL_B_SPLINE_CURVE ( ( 1.000000000000099254, 0.9510565162950540552, 1.000000000000000000, 0.9510565162951535312, 1.000000000000000000, 0.9510565162951535312, 1.000000000000000000, 0.9510565162951535312, 1.000000000000000000, 0.9510565162952597795, 0.9999999999998937517 ) ) 
 REPRESENTATION_ITEM ( '' )  );
#2818=CARTESIAN_POINT ( 'NONE',  ( -72.65499999999998693, -7.632228543268600340, -2.479861379858950166 ) ) ;
#2831=AXIS2_PLACEMENT_3D ( 'NONE', #35817, #51649, #8735 ) ;
#2833=CARTESIAN_POINT ( 'NONE',  ( -107.8449999999999989, -7.632228543268599452, 2.479861379858951054 ) ) ;
#2840=CARTESIAN_POINT ( 'NONE',  ( -139.6429263765338078, -5.598654528085801552, 7.705886871421367523 ) ) ;
#2842=CARTESIAN_POINT ( 'NONE',  ( -171.1449999999999818, -4.716976649647092401, 6.492361379858946790 ) ) ;
#2853=CARTESIAN_POINT ( 'NONE',  ( -156.3549999999999898, -4.716976649647093289, -6.492361379858945902 ) ) ;
#2854=ORIENTED_EDGE ( 'NONE', *, *, #44010, .T. ) ;
#2859=CARTESIAN_POINT ( 'NONE',  ( -57.35707362346617799, 5.598654528085804216, 7.705886871421366635 ) ) ;
#2867=CARTESIAN_POINT ( 'NONE',  ( -70.40499999999998693, -2.607480562269069768, 8.024999999999991473 ) ) ;
#2876=ORIENTED_EDGE ( 'NONE', *, *, #7350, .T. ) ;
#2879=CARTESIAN_POINT ( 'NONE',  ( -51.74499999999998323, 4.716976649647094177, 6.492361379858945902 ) ) ;
#2880=ORIENTED_EDGE ( 'NONE', *, *, #2609, .F. ) ;
#2882=CARTESIAN_POINT ( 'NONE',  ( -86.39292637653379359, 8.102448949553176405, 5.886773742842740909 ) ) ;
#2885=CARTESIAN_POINT ( 'NONE',  ( -48.89499999999999602, 6.826472737025115478, 4.959722759717899443 ) ) ;
#2891=CARTESIAN_POINT ( 'NONE',  ( -108.3549999999999898, -4.716976649647093289, -6.492361379858945902 ) ) ;
#2893=EDGE_CURVE ( 'NONE', #47886, #63234, #31635, .T. ) ;
#2897=CARTESIAN_POINT ( 'NONE',  ( -139.1070736234661354, 8.102448949553171076, -5.886773742842744461 ) ) ;
#2901=CARTESIAN_POINT ( 'NONE',  ( -88.70707362346615810, -3.094860106618431139, -9.524999999999991473 ) ) ;
#2907=CARTESIAN_POINT ( 'NONE',  ( -120.9549999999999983, -7.632228543268599452, 2.479861379858951054 ) ) ;
#2909=CARTESIAN_POINT ( 'NONE',  ( -135.4449999999999932, 0.000000000000000000, 8.024999999999991473 ) ) ;
#2911=CARTESIAN_POINT ( 'NONE',  ( -119.5449999999999875, -7.632228543268600340, -2.479861379858950166 ) ) ;
#2917=EDGE_CURVE ( 'NONE', #66309, #53684, #21443, .T. ) ;
#2918=CARTESIAN_POINT ( 'NONE',  ( -170.8429263765337964, 9.058813317711329915, -2.943386871421373119 ) ) ;
#2919=CARTESIAN_POINT ( 'NONE',  ( -46.79499999999996618, 2.607480562269068880, -8.024999999999993250 ) ) ;
#2926=CARTESIAN_POINT ( 'NONE',  ( -89.09292637653379643, 3.094860106618433360, 9.524999999999991473 ) ) ;
#2951=CARTESIAN_POINT ( 'NONE',  ( -79.49499999999999034, 6.826472737025113702, -4.959722759717902107 ) ) ;
#2952=ORIENTED_EDGE ( 'NONE', *, *, #15800, .F. ) ;
#2962=CARTESIAN_POINT ( 'NONE',  ( -48.14292637653380780, 5.598654528085800663, -7.705886871421367523 ) ) ;
#2969=CARTESIAN_POINT ( 'NONE',  ( -170.1570736234661751, -9.058813317711329915, -2.943386871421370898 ) ) ;
#2972=CARTESIAN_POINT ( 'NONE',  ( -117.9570736234661723, 9.058813317711329915, -2.943386871421373119 ) ) ;
#2976=EDGE_LOOP ( 'NONE', ( #50392, #12873, #60251, #31713 ) ) ;
#2979=ADVANCED_FACE ( 'NONE', ( #11218 ), #43971, .T. ) ;
#2981=CARTESIAN_POINT ( 'NONE',  ( -114.3570736234661780, 5.598654528085804216, 7.705886871421366635 ) ) ;
#2982=CARTESIAN_POINT ( 'NONE',  ( -145.7050000000000125, 2.607480562269073321, 8.024999999999991473 ) ) ;
#2984=CARTESIAN_POINT ( 'NONE',  ( -163.6449999999999818, 4.716976649647091513, -6.492361379858946790 ) ) ;
#2985=CARTESIAN_POINT ( 'NONE',  ( -144.5949999999999989, 2.607480562269072433, 8.024999999999991473 ) ) ;
#2987=CARTESIAN_POINT ( 'NONE',  ( -195.0000000000000000, 0.000000000000000000, 0.000000000000000000 ) ) ;
#2990=CARTESIAN_POINT ( 'NONE',  ( -63.80499999999998550, -8.437984349512085203, 5.166775262442717831E-16 ) ) ;
#2992=CARTESIAN_POINT ( 'NONE',  ( -63.44499999999998607, 0.000000000000000000, 8.024999999999991473 ) ) ;
#2994=EDGE_CURVE ( 'NONE', #48545, #1748, #42584, .T. ) ;
#2997=EDGE_CURVE ( 'NONE', #6242, #36469, #28621, .T. ) ;
#2999=CARTESIAN_POINT ( 'NONE',  ( -159.0570736234661808, 0.000000000000000000, 9.524999999999991473 ) ) ;
#3024=CARTESIAN_POINT ( 'NONE',  ( -115.1949999999999932, 8.437984349512085203, -1.550032578732815448E-15 ) ) ;
#3027=CARTESIAN_POINT ( 'NONE',  ( -12.76760319936551724, -11.13076769754811757, 4.486084945087644549 ) ) ;
#3030=ORIENTED_EDGE ( 'NONE', *, *, #16573, .T. ) ;
#3042=CARTESIAN_POINT ( 'NONE',  ( -126.3549999999999898, -4.716976649647093289, -6.492361379858945902 ) ) ;
#3055=DIRECTION ( 'NONE',  ( -1.000000000000000000, -0.000000000000000000, -0.000000000000000000 ) ) ;
#3061=CARTESIAN_POINT ( 'NONE',  ( -180.9550000000000125, -7.632228543268599452, 2.479861379858951054 ) ) ;
#3064=CARTESIAN_POINT ( 'NONE',  ( -59.75707362346617657, -5.598654528085801552, 7.705886871421367523 ) ) ;
#3066=CARTESIAN_POINT ( 'NONE',  ( -176.8449999999999989, -7.632228543268599452, 2.479861379858951054 ) ) ;
#3072=CARTESIAN_POINT ( 'NONE',  ( -96.05499999999999261, -9.827790563157499189E-16, -8.024999999999991473 ) ) ;
#3077=CARTESIAN_POINT ( 'NONE',  ( -97.19499999999997897, 8.437984349512086979, -1.550032578732815448E-15 ) ) ;
#3079=CARTESIAN_POINT ( 'NONE',  ( -67.19499999999999318, 8.437984349512085203, -1.550032578732815448E-15 ) ) ;
#3086=CARTESIAN_POINT ( 'NONE',  ( -114.8929263765337936, -8.102448949553172852, -5.886773742842741797 ) ) ;
#3087=CARTESIAN_POINT ( 'NONE',  ( -131.6949999999999932, -8.437984349512085203, 5.166775262442717831E-16 ) ) ;
#3101=CARTESIAN_POINT ( 'NONE',  ( -128.7549999999999955, 4.716976649647091513, -6.492361379858946790 ) ) ;
#3104=CARTESIAN_POINT ( 'NONE',  ( -126.8070736234661666, 10.01517768586948698, -1.839758294383808571E-15 ) ) ;
#3108=ORIENTED_EDGE ( 'NONE', *, *, #10238, .T. ) ;
#3122=CARTESIAN_POINT ( 'NONE',  ( -88.34292637653381064, -9.058813317711329915, 2.943386871421371787 ) ) ;
#3133=CARTESIAN_POINT ( 'NONE',  ( -161.9050000000000011, 2.607480562269068880, -8.024999999999993250 ) ) ;
#3134=ADVANCED_FACE ( 'NONE', ( #9777 ), #19611, .T. ) ;
#3149=CARTESIAN_POINT ( 'NONE',  ( -71.60499999999997556, 6.826472737025113702, -4.959722759717902107 ) ) ;
#3153=CARTESIAN_POINT ( 'NONE',  ( -91.55707362346616662, -1.166476076187852838E-15, -9.524999999999991473 ) ) ;
#3160=CARTESIAN_POINT ( 'NONE',  ( -53.00707362346619078, -8.102448949553174629, -5.886773742842741797 ) ) ;
#3162=CARTESIAN_POINT ( 'NONE',  ( -97.49499999999999034, 6.826472737025113702, -4.959722759717902107 ) ) ;
#3167=CARTESIAN_POINT ( 'NONE',  ( -97.40707362346722675, 3.094860106600815453, -9.525000000012790125 ) ) ;
#3168=CARTESIAN_POINT ( 'NONE',  ( -71.24292637653380211, 5.598654528085804216, 7.705886871421366635 ) ) ;
#3169=CARTESIAN_POINT ( 'NONE',  ( -146.8429263765338249, 9.058813317711329915, -2.943386871421373119 ) ) ;
#3172=CARTESIAN_POINT ( 'NONE',  ( -155.9949999999999761, -6.826472737025115478, 4.959722759717900331 ) ) ;
#3186=CARTESIAN_POINT ( 'NONE',  ( -161.4549999999999841, 7.632228543268599452, -2.479861379858951942 ) ) ;
#3195=CARTESIAN_POINT ( 'NONE',  ( -57.20707362346615810, 3.094860106618433360, 9.524999999999991473 ) ) ;
#3199=VERTEX_POINT ( 'NONE', #36172 ) ;
#3202=CARTESIAN_POINT ( 'NONE',  ( -71.90499999999997272, 2.607480562269069324, -8.024999999999993250 ) ) ;
#3219=CARTESIAN_POINT ( 'NONE',  ( -56.39499999999997470, -6.826472737025115478, -4.959722759717899443 ) ) ;
#3232=CARTESIAN_POINT ( 'NONE',  ( -105.2049999999999841, -2.607480562269071545, -8.024999999999991473 ) ) ;
#3237=CARTESIAN_POINT ( 'NONE',  ( -142.5570736234661808, -1.166476076187852838E-15, -9.524999999999991473 ) ) ;
#3240=CARTESIAN_POINT ( 'NONE',  ( -76.10707362346617799, 8.102448949553171076, -5.886773742842744461 ) ) ;
#3248=CARTESIAN_POINT ( 'NONE',  ( -119.3049999999999926, 8.437984349512085203, -1.550032578732815448E-15 ) ) ;
#3249=CARTESIAN_POINT ( 'NONE',  ( -158.3929263765338078, 8.102448949553176405, 5.886773742842740909 ) ) ;
#3251=CARTESIAN_POINT ( 'NONE',  ( -124.9450000000000074, -9.827790563157499189E-16, -8.024999999999991473 ) ) ;
#3254=CARTESIAN_POINT ( 'NONE',  ( -117.4449999999999932, 0.000000000000000000, 8.024999999999991473 ) ) ;
#3261=CARTESIAN_POINT ( 'NONE',  ( -169.6429263765338078, -5.598654528085801552, 7.705886871421367523 ) ) ;
#3262=CARTESIAN_POINT ( 'NONE',  ( -53.24499999999999034, -4.716976649647093289, -6.492361379858945902 ) ) ;
#3268=CARTESIAN_POINT ( 'NONE',  ( -84.89292637653377938, -8.102448949553172852, -5.886773742842741797 ) ) ;
#3291=CARTESIAN_POINT ( 'NONE',  ( -105.6549999999999869, -7.632228543268600340, -2.479861379858950166 ) ) ;
#3297=CARTESIAN_POINT ( 'NONE',  ( -105.0570736234661666, 0.000000000000000000, 9.524999999999991473 ) ) ;
#3303=CARTESIAN_POINT ( 'NONE',  ( -83.54499999999998749, -7.632228543268600340, -2.479861379858950166 ) ) ;
#3310=FACE_BOUND ( 'NONE', #59746, .T. ) ;
#3317=CARTESIAN_POINT ( 'NONE',  ( -149.3929263765338078, 8.102448949553176405, 5.886773742842740909 ) ) ;
#3319=CARTESIAN_POINT ( 'NONE',  ( -169.5570736234661808, -1.166476076187852838E-15, -9.524999999999991473 ) ) ;
#3323=CARTESIAN_POINT ( 'NONE',  ( -100.7070736234661581, -3.094860106618431139, -9.524999999999991473 ) ) ;
#3324=LINE ( 'NONE', #2260, #56540 ) ;
#3325=CARTESIAN_POINT ( 'NONE',  ( -65.75707362346616947, -5.598654528085801552, 7.705886871421367523 ) ) ;
#3332=CARTESIAN_POINT ( 'NONE',  ( -148.2549999999999955, -4.716976649647092401, 6.492361379858946790 ) ) ;
#3334=CARTESIAN_POINT ( 'NONE',  ( -166.3449999999999989, 7.632228543268599452, -2.479861379858951942 ) ) ;
#3335=CARTESIAN_POINT ( 'NONE',  ( -145.3449999999999989, 7.632228543268599452, -2.479861379858951942 ) ) ;
#3342=CARTESIAN_POINT ( 'NONE',  ( -64.70499999999998408, 2.607480562269073321, 8.024999999999991473 ) ) ;
#3345=CARTESIAN_POINT ( 'NONE',  ( -61.49499999999998323, 6.826472737025113702, -4.959722759717902107 ) ) ;
#3358=CARTESIAN_POINT ( 'NONE',  ( -195.0000000000000000, 0.000000000000000000, 9.524999999999991473 ) ) ;
#3364=CARTESIAN_POINT ( 'NONE',  ( -60.35707362346616378, 5.598654528085804216, 7.705886871421366635 ) ) ;
#3381=CARTESIAN_POINT ( 'NONE',  ( -107.6949999999999932, -8.437984349512085203, 5.166775262442717831E-16 ) ) ;
#3401=CARTESIAN_POINT ( 'NONE',  ( -123.0549999999999926, -9.827790563157499189E-16, -8.024999999999991473 ) ) ;
#3416=CARTESIAN_POINT ( 'NONE',  ( -123.6570736234661751, 9.058813317711329915, 2.943386871421369566 ) ) ;
#3417=CARTESIAN_POINT ( 'NONE',  ( -178.7050000000000125, 2.607480562269073321, 8.024999999999991473 ) ) ;
#3419=CARTESIAN_POINT ( 'NONE',  ( -54.20707362346615810, 3.094860106618433360, 9.524999999999991473 ) ) ;
#3420=CARTESIAN_POINT ( 'NONE',  ( -172.3449999999999989, 7.632228543268599452, -2.479861379858951942 ) ) ;
#3422=ORIENTED_EDGE ( 'NONE', *, *, #42909, .F. ) ;
#3426=CARTESIAN_POINT ( 'NONE',  ( -90.05499999999997840, -9.827790563157499189E-16, -8.024999999999991473 ) ) ;
#3427=CARTESIAN_POINT ( 'NONE',  ( -88.64499999999998181, 4.716976649647091513, -6.492361379858946790 ) ) ;
#3429=CARTESIAN_POINT ( 'NONE',  ( -69.89499999999999602, 6.826472737025116366, 4.959722759717898555 ) ) ;
#3439=CARTESIAN_POINT ( 'NONE',  ( -109.9429263765338050, 0.000000000000000000, 9.524999999999991473 ) ) ;
#3441=CARTESIAN_POINT ( 'NONE',  ( -125.6950000000000074, -8.437984349512085203, 5.166775262442717831E-16 ) ) ;
#3462=CARTESIAN_POINT ( 'NONE',  ( -134.6050000000000182, 6.826472737025113702, -4.959722759717902107 ) ) ;
#3465=CARTESIAN_POINT ( 'NONE',  ( -122.4570736234661723, -9.058813317711329915, 2.943386871421371787 ) ) ;
#3469=CARTESIAN_POINT ( 'NONE',  ( -69.44292637653380496, -1.166476076187852838E-15, -9.524999999999991473 ) ) ;
#3482=LINE ( 'NONE', #9865, #44640 ) ;
#3489=CARTESIAN_POINT ( 'NONE',  ( -56.99292637653380211, 8.102448949553171076, -5.886773742842744461 ) ) ;
#3492=CARTESIAN_POINT ( 'NONE',  ( -157.4050000000000011, -2.607480562269069768, 8.024999999999991473 ) ) ;
#3505=CARTESIAN_POINT ( 'NONE',  ( -69.05499999999999261, -9.827790563157499189E-16, -8.024999999999991473 ) ) ;
#3515=DIRECTION ( 'NONE',  ( 0.000000000000000000, -0.000000000000000000, 1.000000000000000000 ) ) ;
#3519=CARTESIAN_POINT ( 'NONE',  ( -98.99499999999997613, -6.826472737025115478, 4.959722759717900331 ) ) ;
#3528=CARTESIAN_POINT ( 'NONE',  ( -139.4929263765338021, -8.102448949553172852, 5.886773742842742685 ) ) ;
#3530=CARTESIAN_POINT ( 'NONE',  ( -152.3950000000000102, -6.826472737025115478, -4.959722759717899443 ) ) ;
#3544=DIRECTION ( 'NONE',  ( 0.000000000000000000, 0.000000000000000000, 1.000000000000000000 ) ) ;
#3550=CARTESIAN_POINT ( 'NONE',  ( -162.8050000000000068, -8.437984349512086979, 5.166775262442717831E-16 ) ) ;
#3556=CARTESIAN_POINT ( 'NONE',  ( -195.0000000000000000, 0.000000000000000000, 0.000000000000000000 ) ) ;
#3562=CARTESIAN_POINT ( 'NONE',  ( -57.89292637653377938, -8.102448949553174629, -5.886773742842741797 ) ) ;
#3564=CARTESIAN_POINT ( 'NONE',  ( -71.45499999999998408, 7.632228543268599452, -2.479861379858951942 ) ) ;
#3565=CARTESIAN_POINT ( 'NONE',  ( -80.75707362346616947, -5.598654528085801552, 7.705886871421367523 ) ) ;
#3575=CARTESIAN_POINT ( 'NONE',  ( -179.6049999999999898, 6.826472737025113702, -4.959722759717902107 ) ) ;
#3587=CARTESIAN_POINT ( 'NONE',  ( -100.4050000000000011, -2.607480562269069768, 8.024999999999991473 ) ) ;
#3592=CARTESIAN_POINT ( 'NONE',  ( -137.1570736234661751, -9.058813317711329915, -2.943386871421370898 ) ) ;
#3595=CARTESIAN_POINT ( 'NONE',  ( -76.55707362346616662, -1.166476076187852838E-15, -9.524999999999991473 ) ) ;
#3603=CARTESIAN_POINT ( 'NONE',  ( -122.6049999999999898, 6.826472737025113702, -4.959722759717902107 ) ) ;
#3606=CARTESIAN_POINT ( 'NONE',  ( -128.2450000000000045, -4.716976649647093289, -6.492361379858945902 ) ) ;
#3616=CARTESIAN_POINT ( 'NONE',  ( -173.6929263765338192, 10.01517768586948698, -1.839758294383808571E-15 ) ) ;
#3621=EDGE_CURVE ( 'NONE', #55506, #27751, #11165, .T. ) ;
#3622=AXIS2_PLACEMENT_3D ( 'NONE', #41390, #30793, #19552 ) ;
#3628=CARTESIAN_POINT ( 'NONE',  ( -88.64292637653380780, -5.598654528085801552, 7.705886871421367523 ) ) ;
#3630=( BOUNDED_CURVE ( )  B_SPLINE_CURVE ( 2, ( #39130, #13047, #12687, #17660, #3122, #2434, #45457, #34500, #34160, #44427, #66876 ),
 .UNSPECIFIED., .F., .F. ) 
 B_SPLINE_CURVE_WITH_KNOTS ( ( 3, 2, 2, 2, 2, 3 ),
 ( 0.6956521739130434590, 0.6978260869565217073, 0.6999999999999999556, 0.7021739130434783149, 0.7043478260869565633, 0.7065217391304348116 ),
 .UNSPECIFIED. ) 
 CURVE ( )  GEOMETRIC_REPRESENTATION_ITEM ( )  RATIONAL_B_SPLINE_CURVE ( ( 1.000000000000000000, 0.9510565162951535312, 1.000000000000000000, 0.9510565162951535312, 1.000000000000000000, 0.9510565162951535312, 1.000000000000000000, 0.9510565162951535312, 1.000000000000000000, 0.9510565162951535312, 1.000000000000000000 ) ) 
 REPRESENTATION_ITEM ( '' )  );
#3635=CARTESIAN_POINT ( 'NONE',  ( -179.3929263765337794, 8.102448949553176405, 5.886773742842740909 ) ) ;
#3639=EDGE_LOOP ( 'NONE', ( #67182, #7617, #33295, #46023 ) ) ;
#3642=ORIENTED_EDGE ( 'NONE', *, *, #13104, .F. ) ;
#3651=CARTESIAN_POINT ( 'NONE',  ( -102.0549999999999926, -9.827790563157499189E-16, -8.024999999999991473 ) ) ;
#3661=CARTESIAN_POINT ( 'NONE',  ( -82.94499999999999318, -9.827790563157499189E-16, -8.024999999999991473 ) ) ;
#3678=CARTESIAN_POINT ( 'NONE',  ( -168.5070736234661979, 8.102448949553176405, 5.886773742842740909 ) ) ;
#3680=CARTESIAN_POINT ( 'NONE',  ( -103.2570736234661695, 5.598654528085800663, -7.705886871421367523 ) ) ;
#3683=CARTESIAN_POINT ( 'NONE',  ( -195.0000000000000000, 0.000000000000000000, 9.524999999999991473 ) ) ;
#3684=VERTEX_POINT ( 'NONE', #67562 ) ;
#3688=CARTESIAN_POINT ( 'NONE',  ( -60.74292637653380922, -5.598654528085803328, -7.705886871421366635 ) ) ;
#3690=CARTESIAN_POINT ( 'NONE',  ( -151.5550000000000068, 0.000000000000000000, 8.024999999999991473 ) ) ;
#3694=CARTESIAN_POINT ( 'NONE',  ( -151.0449999999999875, 7.632228543268600340, 2.479861379858949277 ) ) ;
#3696=CARTESIAN_POINT ( 'NONE',  ( -145.1949999999999648, 8.437984349512086979, -1.550032578732815448E-15 ) ) ;
#3699=CARTESIAN_POINT ( 'NONE',  ( -180.6570736234661751, 9.058813317711329915, 2.943386871421369566 ) ) ;
#3702=DIRECTION ( 'NONE',  ( -1.000000000000000000, -0.000000000000000000, -0.000000000000000000 ) ) ;
#3704=CARTESIAN_POINT ( 'NONE',  ( -64.40499999999998693, -2.607480562269069768, 8.024999999999991473 ) ) ;
#3707=CARTESIAN_POINT ( 'NONE',  ( -62.69499999999998607, -8.437984349512086979, 5.166775262442717831E-16 ) ) ;
#3708=AXIS2_PLACEMENT_3D ( 'NONE', #37478, #68752, #42056 ) ;
#3731=ORIENTED_EDGE ( 'NONE', *, *, #35594, .T. ) ;
#3733=LINE ( 'NONE', #19234, #23072 ) ;
#3740=CARTESIAN_POINT ( 'NONE',  ( -106.3449999999999989, 7.632228543268599452, -2.479861379858951942 ) ) ;
#3743=ADVANCED_FACE ( 'NONE', ( #51385, #24624 ), #46140, .F. ) ;
#3759=CARTESIAN_POINT ( 'NONE',  ( -140.5429263765338135, 9.058813317711329915, 2.943386871421369566 ) ) ;
#3761=CARTESIAN_POINT ( 'NONE',  ( -121.5549999999999926, 0.000000000000000000, 8.024999999999991473 ) ) ;
#3762=CARTESIAN_POINT ( 'NONE',  ( -183.9999999999999432, -1.549738613431724588, 7.912546321907711899 ) ) ;
#3769=EDGE_LOOP ( 'NONE', ( #45352, #61690, #34935, #20153 ) ) ;
#3778=CARTESIAN_POINT ( 'NONE',  ( -154.1929263765338192, -10.01517768586948698, 6.132527647946031529E-16 ) ) ;
#3779=CARTESIAN_POINT ( 'NONE',  ( -177.9550000000000125, -7.632228543268599452, 2.479861379858951054 ) ) ;
#3783=CARTESIAN_POINT ( 'NONE',  ( -181.4950000000000045, 6.826472737025113702, -4.959722759717902107 ) ) ;
#3785=CARTESIAN_POINT ( 'NONE',  ( -176.9949999999999761, -6.826472737025113702, 4.959722759717902107 ) ) ;
#3787=VERTEX_POINT ( 'NONE', #3858 ) ;
#3791=CARTESIAN_POINT ( 'NONE',  ( -93.20499999999998408, -2.607480562269071545, -8.024999999999991473 ) ) ;
#3797=CARTESIAN_POINT ( 'NONE',  ( -91.19499999999997897, 8.437984349512086979, -1.550032578732815448E-15 ) ) ;
#3799=CARTESIAN_POINT ( 'NONE',  ( -64.64499999999998181, 4.716976649647091513, -6.492361379858946790 ) ) ;
#3802=AXIS2_PLACEMENT_3D ( 'NONE', #55411, #44902, #66310 ) ;
#3808=CARTESIAN_POINT ( 'NONE',  ( -100.6429263765337936, -5.598654528085801552, 7.705886871421367523 ) ) ;
#3810=CARTESIAN_POINT ( 'NONE',  ( -132.2949999999999875, -2.607480562269069768, 8.024999999999991473 ) ) ;
#3816=ORIENTED_EDGE ( 'NONE', *, *, #10582, .F. ) ;
#3826=CARTESIAN_POINT ( 'NONE',  ( -122.6049999999999898, 6.826472737025113702, -4.959722759717902107 ) ) ;
#3827=ORIENTED_EDGE ( 'NONE', *, *, #54329, .F. ) ;
#3830=CARTESIAN_POINT ( 'NONE',  ( -127.5570736234661950, -1.166476076187852838E-15, -9.524999999999991473 ) ) ;
#3835=DIRECTION ( 'NONE',  ( -1.000000000000000000, -0.000000000000000000, -0.000000000000000000 ) ) ;
#3842=CARTESIAN_POINT ( 'NONE',  ( -48.05499999999998550, -9.827790563157499189E-16, -8.024999999999991473 ) ) ;
#3852=ORIENTED_EDGE ( 'NONE', *, *, #18178, .T. ) ;
#3855=CARTESIAN_POINT ( 'NONE',  ( -57.89292637653377938, -8.102448949553172852, -5.886773742842741797 ) ) ;
#3858=CARTESIAN_POINT ( 'NONE',  ( -165.4429263765337907, -1.166476076187852838E-15, -9.524999999999991473 ) ) ;
#3860=CARTESIAN_POINT ( 'NONE',  ( -150.6549999999999727, -7.632228543268600340, -2.479861379858950166 ) ) ;
#3866=CARTESIAN_POINT ( 'NONE',  ( -70.04292637653379927, -9.058813317711329915, -2.943386871421370898 ) ) ;
#3875=CARTESIAN_POINT ( 'NONE',  ( -62.45499999999998408, 7.632228543268599452, -2.479861379858951942 ) ) ;
#3881=CARTESIAN_POINT ( 'NONE',  ( -123.5929263765345638, -3.094860106631271091, -9.524999999990667376 ) ) ;
#3892=CARTESIAN_POINT ( 'NONE',  ( -94.34499999999998465, 7.632228543268599452, -2.479861379858951942 ) ) ;
#3897=CARTESIAN_POINT ( 'NONE',  ( -71.39292637653377938, 8.102448949553176405, 5.886773742842740909 ) ) ;
#3900=CARTESIAN_POINT ( 'NONE',  ( -147.4429263765338192, -1.166476076187852838E-15, -9.524999999999991473 ) ) ;
#3902=CARTESIAN_POINT ( 'NONE',  ( -155.0949999999999989, -2.607480562269071545, -8.024999999999991473 ) ) ;
#3903=CARTESIAN_POINT ( 'NONE',  ( -46.55707362346617373, -1.166476076187852838E-15, -9.524999999999991473 ) ) ;
#3916=CARTESIAN_POINT ( 'NONE',  ( -143.8429263765338249, 9.058813317711329915, -2.943386871421373119 ) ) ;
#3921=CARTESIAN_POINT ( 'NONE',  ( -155.7549999999999955, 4.716976649647091513, -6.492361379858946790 ) ) ;
#3935=CARTESIAN_POINT ( 'NONE',  ( -70.10499999999998977, -6.826472737025113702, 4.959722759717902107 ) ) ;
#3938=( BOUNDED_CURVE ( )  B_SPLINE_CURVE ( 2, ( #17337, #43048, #27484, #26461, #6388, #11672, #22230, #32095, #53219, #5339, #27817 ),
 .UNSPECIFIED., .F., .F. ) 
 B_SPLINE_CURVE_WITH_KNOTS ( ( 3, 2, 2, 2, 2, 3 ),
 ( 0.6847826086956522174, 0.6869565217391304657, 0.6891304347826087140, 0.6913043478260869623, 0.6934782608695652106, 0.6956521739130434590 ),
 .UNSPECIFIED. ) 
 CURVE ( )  GEOMETRIC_REPRESENTATION_ITEM ( )  RATIONAL_B_SPLINE_CURVE ( ( 1.000000000000000000, 0.9510565162951535312, 1.000000000000000000, 0.9510565162951535312, 1.000000000000000000, 0.9510565162951535312, 1.000000000000000000, 0.9510565162951535312, 1.000000000000000000, 0.9510565162951535312, 1.000000000000000000 ) ) 
 REPRESENTATION_ITEM ( '' )  );
#3949=CARTESIAN_POINT ( 'NONE',  ( -177.9550000000000125, -7.632228543268599452, 2.479861379858951054 ) ) ;
#3961=CARTESIAN_POINT ( 'NONE',  ( -92.00499999999998124, 6.826472737025116366, 4.959722759717898555 ) ) ;
#3967=CARTESIAN_POINT ( 'NONE',  ( -144.8070736234661808, 10.01517768586948698, -1.839758294383808571E-15 ) ) ;
#3971=CARTESIAN_POINT ( 'NONE',  ( -73.55707362346616662, -1.166476076187852838E-15, -9.524999999999991473 ) ) ;
#3972=CARTESIAN_POINT ( 'NONE',  ( -92.09292637653497593, 3.094860106637794317, 9.524999999985924504 ) ) ;
#3973=ORIENTED_EDGE ( 'NONE', *, *, #33153, .T. ) ;
#3974=CARTESIAN_POINT ( 'NONE',  ( -16.61951246926111381, -11.02716856853298033, 4.733319217996198702 ) ) ;
#3977=CARTESIAN_POINT ( 'NONE',  ( -107.9050000000000011, 2.607480562269068880, -8.024999999999993250 ) ) ;
#3980=CARTESIAN_POINT ( 'NONE',  ( -129.8949999999999818, 6.826472737025116366, 4.959722759717898555 ) ) ;
#3987=CARTESIAN_POINT ( 'NONE',  ( -166.7070736234663570, -3.094860106621724949, -9.524999999997598721 ) ) ;
#3989=CARTESIAN_POINT ( 'NONE',  ( -173.9929263765338021, 8.102448949553171076, -5.886773742842744461 ) ) ;
#3990=CARTESIAN_POINT ( 'NONE',  ( -182.2450000000000045, -4.716976649647093289, -6.492361379858945902 ) ) ;
#3995=CARTESIAN_POINT ( 'NONE',  ( -81.74292637653380211, -5.598654528085803328, -7.705886871421366635 ) ) ;
#4013=ORIENTED_EDGE ( 'NONE', *, *, #34615, .F. ) ;
#4014=CARTESIAN_POINT ( 'NONE',  ( -100.5570736234661808, -1.166476076187852838E-15, -9.524999999999991473 ) ) ;
#4015=CARTESIAN_POINT ( 'NONE',  ( -100.2549999999999812, -4.716976649647092401, 6.492361379858946790 ) ) ;
#4020=VECTOR ( 'NONE', #8010, 1000.000000000000000 ) ;
#4021=CARTESIAN_POINT ( 'NONE',  ( -104.3070736234661666, -10.01517768586948698, 6.132527647946031529E-16 ) ) ;
#4024=CIRCLE ( 'NONE', #59080, 5.499999999999985789 ) ;
#4027=CARTESIAN_POINT ( 'NONE',  ( -67.64499999999998181, 4.716976649647091513, -6.492361379858946790 ) ) ;
#4032=ORIENTED_EDGE ( 'NONE', *, *, #33524, .T. ) ;
#4042=CARTESIAN_POINT ( 'NONE',  ( -133.9429263765338192, 0.000000000000000000, 9.524999999999991473 ) ) ;
#4044=CARTESIAN_POINT ( 'NONE',  ( -167.0070736234661695, -8.102448949553172852, -5.886773742842741797 ) ) ;
#4047=CARTESIAN_POINT ( 'NONE',  ( -100.4070736234661894, 3.094860106618428031, -9.524999999999993250 ) ) ;
#4049=CARTESIAN_POINT ( 'NONE',  ( -65.90707362346617515, -3.094860106618429807, 9.524999999999991473 ) ) ;
#4051=ORIENTED_EDGE ( 'NONE', *, *, #8132, .F. ) ;
#4052=CARTESIAN_POINT ( 'NONE',  ( -107.3929263765338078, 8.102448949553176405, 5.886773742842740909 ) ) ;
#4057=CARTESIAN_POINT ( 'NONE',  ( -153.5049999999999670, -6.826472737025115478, -4.959722759717899443 ) ) ;
#4059=CARTESIAN_POINT ( 'NONE',  ( -155.6949999999999932, -8.437984349512085203, 5.166775262442717831E-16 ) ) ;
#4060=CARTESIAN_POINT ( 'NONE',  ( -152.5449999999999875, -7.632228543268600340, -2.479861379858950166 ) ) ;
#4062=( BOUNDED_CURVE ( )  B_SPLINE_CURVE ( 2, ( #6305, #54822, #277, #44687, #65408, #21810, #17592, #33059, #27734, #60126, #5957 ),
 .UNSPECIFIED., .F., .F. ) 
 B_SPLINE_CURVE_WITH_KNOTS ( ( 3, 2, 2, 2, 2, 3 ),
 ( 0.5652173913043344600, 0.5673913043478127083, 0.5695652173912908456, 0.5717391304347690939, 0.5739130434782472312, 0.5760869565217253685 ),
 .UNSPECIFIED. ) 
 CURVE ( )  GEOMETRIC_REPRESENTATION_ITEM ( )  RATIONAL_B_SPLINE_CURVE ( ( 1.000000000000299982, 0.9510565162948535489, 1.000000000000000000, 0.9510565162951535312, 1.000000000000000000, 0.9510565162951535312, 1.000000000000000000, 0.9510565162951535312, 1.000000000000000000, 0.9510565162954635055, 0.9999999999996900257 ) ) 
 REPRESENTATION_ITEM ( '' )  );
#4065=CARTESIAN_POINT ( 'NONE',  ( -59.30499999999999972, 8.437984349512085203, -1.550032578732815448E-15 ) ) ;
#4068=CARTESIAN_POINT ( 'NONE',  ( -64.34499999999998465, 7.632228543268599452, -2.479861379858951942 ) ) ;
#4070=CARTESIAN_POINT ( 'NONE',  ( -51.74292637653380211, -5.598654528085803328, -7.705886871421366635 ) ) ;
#4088=CARTESIAN_POINT ( 'NONE',  ( -109.5570736234661666, -1.166476076187852838E-15, -9.524999999999991473 ) ) ;
#4092=CARTESIAN_POINT ( 'NONE',  ( -84.74292637653380211, -5.598654528085803328, -7.705886871421366635 ) ) ;
#4096=CARTESIAN_POINT ( 'NONE',  ( -98.09499999999997044, -2.607480562269071545, -8.024999999999991473 ) ) ;
#4098=ADVANCED_FACE ( 'NONE', ( #58301 ), #56917, .T. ) ;
#4113=CARTESIAN_POINT ( 'NONE',  ( -140.0929263765343649, 3.094860106627776997, 9.524999999993202238 ) ) ;
#4114=CARTESIAN_POINT ( 'NONE',  ( -128.6049999999999898, 6.826472737025113702, -4.959722759717902107 ) ) ;
#4118=CARTESIAN_POINT ( 'NONE',  ( -126.4429263765338192, -1.166476076187852838E-15, -9.524999999999991473 ) ) ;
#4129=EDGE_LOOP ( 'NONE', ( #6995, #20071, #13810, #26628 ) ) ;
#4131=CARTESIAN_POINT ( 'NONE',  ( -174.2050000000000125, -2.607480562269071545, -8.024999999999991473 ) ) ;
#4134=CARTESIAN_POINT ( 'NONE',  ( -47.00707362346617657, -8.102448949553172852, -5.886773742842741797 ) ) ;
#4135=CARTESIAN_POINT ( 'NONE',  ( -179.9949999999999761, -6.826472737025113702, 4.959722759717902107 ) ) ;
#4139=CARTESIAN_POINT ( 'NONE',  ( -12.48350263443806618, 11.19219915118087982, 4.332593345627109294 ) ) ;
#4140=CARTESIAN_POINT ( 'NONE',  ( -93.80499999999999261, -8.437984349512085203, 5.166775262442717831E-16 ) ) ;
#4143=CARTESIAN_POINT ( 'NONE',  ( -94.19499999999999318, 8.437984349512086979, -1.550032578732815448E-15 ) ) ;
#4146=CARTESIAN_POINT ( 'NONE',  ( -70.79499999999998749, 2.607480562269068880, -8.024999999999993250 ) ) ;
#4153=CARTESIAN_POINT ( 'NONE',  ( -100.7929263765338135, -3.094860106618429807, 9.524999999999991473 ) ) ;
#4154=CARTESIAN_POINT ( 'NONE',  ( -126.2950000000000017, -2.607480562269069768, 8.024999999999991473 ) ) ;
#4163=CARTESIAN_POINT ( 'NONE',  ( -133.9429263765338192, 0.000000000000000000, 9.524999999999991473 ) ) ;
#4165=CYLINDRICAL_SURFACE ( 'NONE', #23633, 9.524999999999991473 ) ;
#4169=CARTESIAN_POINT ( 'NONE',  ( -121.8549999999999898, 4.716976649647094177, 6.492361379858945902 ) ) ;
#4170=EDGE_LOOP ( 'NONE', ( #24539, #10384, #12025, #61731 ) ) ;
#4173=CARTESIAN_POINT ( 'NONE',  ( -120.5070736234661695, 8.102448949553176405, 5.886773742842740909 ) ) ;
#4194=ORIENTED_EDGE ( 'NONE', *, *, #35521, .T. ) ;
#4198=CARTESIAN_POINT ( 'NONE',  ( -61.79292637653379217, -3.094860106618429807, 9.524999999999991473 ) ) ;
#4201=CARTESIAN_POINT ( 'NONE',  ( -151.7049999999999841, 2.607480562269073321, 8.024999999999991473 ) ) ;
#4213=CARTESIAN_POINT ( 'NONE',  ( -68.60499999999996135, 6.826472737025113702, -4.959722759717902107 ) ) ;
#4225=CARTESIAN_POINT ( 'NONE',  ( -101.9949999999999903, -6.826472737025115478, 4.959722759717900331 ) ) ;
#4232=CARTESIAN_POINT ( 'NONE',  ( -129.7429263765338021, -5.598654528085803328, -7.705886871421366635 ) ) ;
#4234=CARTESIAN_POINT ( 'NONE',  ( -159.8950000000000102, 6.826472737025116366, 4.959722759717898555 ) ) ;
#4244=ADVANCED_FACE ( 'NONE', ( #38279 ), #16474, .T. ) ;
#4247=CARTESIAN_POINT ( 'NONE',  ( -173.1570736234662036, -9.058813317711329915, -2.943386871421370898 ) ) ;
#4251=CARTESIAN_POINT ( 'NONE',  ( -148.4050000000000011, -2.607480562269069768, 8.024999999999991473 ) ) ;
#4259=CARTESIAN_POINT ( 'NONE',  ( -57.65707362346616804, 9.058813317711329915, 2.943386871421369566 ) ) ;
#4265=CARTESIAN_POINT ( 'NONE',  ( -68.15499999999997272, 7.632228543268600340, 2.479861379858949277 ) ) ;
#4274=EDGE_LOOP ( 'NONE', ( #14342, #55492, #61794, #62503 ) ) ;
#4279=CARTESIAN_POINT ( 'NONE',  ( -180.8050000000000068, -8.437984349512085203, 5.166775262442717831E-16 ) ) ;
#4290=CARTESIAN_POINT ( 'NONE',  ( -95.15499999999998693, 7.632228543268600340, 2.479861379858949277 ) ) ;
#4294=CARTESIAN_POINT ( 'NONE',  ( -128.9070736234661751, -3.094860106618429807, 9.524999999999991473 ) ) ;
#4298=CARTESIAN_POINT ( 'NONE',  ( -75.35707362346617799, 5.598654528085804216, 7.705886871421366635 ) ) ;
#4306=CARTESIAN_POINT ( 'NONE',  ( -110.0049999999999955, 6.826472737025116366, 4.959722759717898555 ) ) ;
#4309=CARTESIAN_POINT ( 'NONE',  ( -123.1449999999999960, -4.716976649647092401, 6.492361379858946790 ) ) ;
#4311=CARTESIAN_POINT ( 'NONE',  ( -117.5929263765346633, -3.094860106632549179, -9.524999999989734789 ) ) ;
#4314=CARTESIAN_POINT ( 'NONE',  ( -166.4929263765338021, -8.102448949553172852, 5.886773742842742685 ) ) ;
#4315=FILL_AREA_STYLE_COLOUR ( '', #58561 ) ;
#4325=CARTESIAN_POINT ( 'NONE',  ( -84.74292637653380211, -5.598654528085803328, -7.705886871421366635 ) ) ;
#4334=CARTESIAN_POINT ( 'NONE',  ( -175.7049999999999841, 2.607480562269072433, 8.024999999999991473 ) ) ;
#4346=CARTESIAN_POINT ( 'NONE',  ( -100.5549999999999926, 0.000000000000000000, 8.024999999999991473 ) ) ;
#4357=CARTESIAN_POINT ( 'NONE',  ( -71.39499999999998181, -6.826472737025115478, -4.959722759717899443 ) ) ;
#4359=( BOUNDED_CURVE ( )  B_SPLINE_CURVE ( 2, ( #22041, #49142, #39283, #33290, #48816, #6522, #43546, #60686, #32947, #54377, #6199 ),
 .UNSPECIFIED., .F., .F. ) 
 B_SPLINE_CURVE_WITH_KNOTS ( ( 3, 2, 2, 2, 2, 3 ),
 ( 0.4565217391304240424, 0.4586956521739022907, 0.4608695652173804835, 0.4630434782608586763, 0.4652173913043368692, 0.4673913043478151175 ),
 .UNSPECIFIED. ) 
 CURVE ( )  GEOMETRIC_REPRESENTATION_ITEM ( )  RATIONAL_B_SPLINE_CURVE ( ( 1.000000000000241140, 0.9510565162949122797, 1.000000000000000000, 0.9510565162951535312, 1.000000000000000000, 0.9510565162951535312, 1.000000000000000000, 0.9510565162951535312, 1.000000000000000000, 0.9510565162954009999, 0.9999999999997525313 ) ) 
 REPRESENTATION_ITEM ( '' )  );
#4366=DIRECTION ( 'NONE',  ( 0.000000000000000000, 0.000000000000000000, 1.000000000000000000 ) ) ;
#4378=CARTESIAN_POINT ( 'NONE',  ( -157.8570736234661922, -5.598654528085803328, -7.705886871421366635 ) ) ;
#4383=CARTESIAN_POINT ( 'NONE',  ( -100.1070736234661780, 8.102448949553171076, -5.886773742842744461 ) ) ;
#4388=CARTESIAN_POINT ( 'NONE',  ( -107.0929263765347628, 3.094860106634567565, 9.524999999988271071 ) ) ;
#4392=CARTESIAN_POINT ( 'NONE',  ( -140.4549999999999841, 7.632228543268599452, -2.479861379858951942 ) ) ;
#4395=CARTESIAN_POINT ( 'NONE',  ( -151.3449999999999989, 7.632228543268599452, -2.479861379858951942 ) ) ;
#4397=CARTESIAN_POINT ( 'NONE',  ( -139.9449999999999932, -9.827790563157499189E-16, -8.024999999999991473 ) ) ;
#4404=CARTESIAN_POINT ( 'NONE',  ( -66.20499999999996987, -2.607480562269071545, -8.024999999999991473 ) ) ;
#4414=CARTESIAN_POINT ( 'NONE',  ( -81.95707362346617231, 9.058813317711329915, -2.943386871421373119 ) ) ;
#4432=ORIENTED_EDGE ( 'NONE', *, *, #18194, .F. ) ;
#4434=CARTESIAN_POINT ( 'NONE',  ( -108.3570736234661780, 5.598654528085804216, 7.705886871421366635 ) ) ;
#4440=CARTESIAN_POINT ( 'NONE',  ( -85.79292637653378506, -3.094860106618429807, 9.524999999999991473 ) ) ;
#4444=CARTESIAN_POINT ( 'NONE',  ( -101.9949999999999903, -6.826472737025115478, 4.959722759717900331 ) ) ;
#4462=CARTESIAN_POINT ( 'NONE',  ( -184.0000000000000568, -3.034060806962692425, 7.439417636962661007 ) ) ;
#4465=( BOUNDED_CURVE ( )  B_SPLINE_CURVE ( 2, ( #15910, #38426, #669, #5645, #6010, #64417, #5300, #58447, #26423, #37741, #27446 ),
 .UNSPECIFIED., .F., .F. ) 
 B_SPLINE_CURVE_WITH_KNOTS ( ( 3, 2, 2, 2, 2, 3 ),
 ( 0.9021739130434782705, 0.9043478260869565188, 0.9065217391304347672, 0.9086956521739130155, 0.9108695652173912638, 0.9130434782608695121 ),
 .UNSPECIFIED. ) 
 CURVE ( )  GEOMETRIC_REPRESENTATION_ITEM ( )  RATIONAL_B_SPLINE_CURVE ( ( 1.000000000000000000, 0.9510565162951535312, 1.000000000000000000, 0.9510565162951535312, 1.000000000000000000, 0.9510565162951535312, 1.000000000000000000, 0.9510565162951535312, 1.000000000000000000, 0.9510565162951535312, 1.000000000000000000 ) ) 
 REPRESENTATION_ITEM ( '' )  );
#4472=VERTEX_POINT ( 'NONE', #19882 ) ;
#4478=CARTESIAN_POINT ( 'NONE',  ( -154.4929263765338021, -8.102448949553174629, 5.886773742842742685 ) ) ;
#4479=CARTESIAN_POINT ( 'NONE',  ( -173.1550000000000011, 7.632228543268600340, 2.479861379858949277 ) ) ;
#4483=CARTESIAN_POINT ( 'NONE',  ( -49.55707362346617373, -1.166476076187852838E-15, -9.524999999999991473 ) ) ;
#4485=CARTESIAN_POINT ( 'NONE',  ( -176.2449999999999761, -4.716976649647093289, -6.492361379858945902 ) ) ;
#4487=EDGE_LOOP ( 'NONE', ( #10166, #6476, #41292, #11420 ) ) ;
#4490=CARTESIAN_POINT ( 'NONE',  ( -14.66572272744468641, 10.90871211463571377, 5.000000000000001776 ) ) ;
#4491=CARTESIAN_POINT ( 'NONE',  ( -93.65499999999998693, -7.632228543268600340, -2.479861379858950166 ) ) ;
#4495=CARTESIAN_POINT ( 'NONE',  ( -88.04499999999998749, 7.632228543268600340, 2.479861379858949277 ) ) ;
#4497=CARTESIAN_POINT ( 'NONE',  ( -58.49499999999998323, 6.826472737025113702, -4.959722759717902107 ) ) ;
#4503=CYLINDRICAL_SURFACE ( 'NONE', #40582, 9.524999999999991473 ) ;
#4514=ADVANCED_FACE ( 'NONE', ( #40683, #25855 ), #62097, .F. ) ;
#4532=CARTESIAN_POINT ( 'NONE',  ( -117.8049999999999926, -8.437984349512086979, 5.166775262442717831E-16 ) ) ;
#4546=CARTESIAN_POINT ( 'NONE',  ( -55.40707362346616094, 3.094860106618428031, -9.524999999999993250 ) ) ;
#4548=CARTESIAN_POINT ( 'NONE',  ( -135.2070736234667550, 3.094860106628449792, 9.524999999992715516 ) ) ;
#4563=CARTESIAN_POINT ( 'NONE',  ( -54.44292637653380496, -1.166476076187852838E-15, -9.524999999999991473 ) ) ;
#4565=CARTESIAN_POINT ( 'NONE',  ( -155.1550000000000011, 7.632228543268600340, 2.479861379858949277 ) ) ;
#4566=ORIENTED_EDGE ( 'NONE', *, *, #32640, .T. ) ;
#4571=CARTESIAN_POINT ( 'NONE',  ( -69.59292637653379643, -3.094860106618431139, -9.524999999999991473 ) ) ;
#4578=CARTESIAN_POINT ( 'NONE',  ( -64.70499999999998408, 2.607480562269073321, 8.024999999999991473 ) ) ;
#4594=CARTESIAN_POINT ( 'NONE',  ( -118.6449999999999818, 4.716976649647091513, -6.492361379858946790 ) ) ;
#4596=CARTESIAN_POINT ( 'NONE',  ( -101.6949999999999790, -8.437984349512085203, 5.166775262442717831E-16 ) ) ;
#4606=CARTESIAN_POINT ( 'NONE',  ( -134.6929263765337907, 10.01517768586948698, -1.839758294383808571E-15 ) ) ;
#4608=CARTESIAN_POINT ( 'NONE',  ( -158.3949999999999818, -6.826472737025115478, -4.959722759717899443 ) ) ;
#4613=CARTESIAN_POINT ( 'NONE',  ( -133.1929263765337623, -10.01517768586948698, 6.132527647946031529E-16 ) ) ;
#4618=EDGE_CURVE ( 'NONE', #42104, #23846, #64599, .T. ) ;
#4619=CARTESIAN_POINT ( 'NONE',  ( -143.3929263765338078, 8.102448949553176405, 5.886773742842740909 ) ) ;
#4621=( GEOMETRIC_REPRESENTATION_CONTEXT ( 3 ) GLOBAL_UNCERTAINTY_ASSIGNED_CONTEXT ( ( #40360 ) ) GLOBAL_UNIT_ASSIGNED_CONTEXT ( ( #37, #69421, #64824 ) ) REPRESENTATION_CONTEXT ( 'NONE', 'WORKASPACE' ) );
#4625=CARTESIAN_POINT ( 'NONE',  ( -150.8050000000000068, -8.437984349512086979, 5.166775262442717831E-16 ) ) ;
#4639=CARTESIAN_POINT ( 'NONE',  ( -59.75499999999998835, 4.716976649647091513, -6.492361379858946790 ) ) ;
#4644=CARTESIAN_POINT ( 'NONE',  ( -183.0259559770162809, -0.7697107438453818506, 9.475620892396962702 ) ) ;
#4652=CARTESIAN_POINT ( 'NONE',  ( -179.3049999999999784, 8.437984349512085203, -1.550032578732815448E-15 ) ) ;
#4665=CARTESIAN_POINT ( 'NONE',  ( -92.75499999999999545, 4.716976649647091513, -6.492361379858946790 ) ) ;
#4668=VECTOR ( 'NONE', #50869, 1000.000000000000000 ) ;
#4670=CARTESIAN_POINT ( 'NONE',  ( -132.3570736234661922, 5.598654528085804216, 7.705886871421366635 ) ) ;
#4673=CARTESIAN_POINT ( 'NONE',  ( -77.75707362346618368, -5.598654528085801552, 7.705886871421367523 ) ) ;
#4681=CARTESIAN_POINT ( 'NONE',  ( -111.6549999999999869, -7.632228543268600340, -2.479861379858950166 ) ) ;
#4684=CARTESIAN_POINT ( 'NONE',  ( -130.0449999999999875, 7.632228543268600340, 2.479861379858949277 ) ) ;
#4685=CARTESIAN_POINT ( 'NONE',  ( -112.4070736234670989, 3.094860106603908090, -9.525000000010546586 ) ) ;
#4687=CARTESIAN_POINT ( 'NONE',  ( -118.7929263765346377, -3.094860106604648831, 9.525000000010006573 ) ) ;
#4692=CARTESIAN_POINT ( 'NONE',  ( -160.9429263765338192, 0.000000000000000000, 9.524999999999991473 ) ) ;
#4695=VECTOR ( 'NONE', #52480, 1000.000000000000000 ) ;
#4704=CARTESIAN_POINT ( 'NONE',  ( -72.29292637653379927, 3.094860106618428031, -9.524999999999993250 ) ) ;
#4712=CARTESIAN_POINT ( 'NONE',  ( -177.0549999999999784, -9.827790563157499189E-16, -8.024999999999991473 ) ) ;
#4714=ORIENTED_EDGE ( 'NONE', *, *, #13741, .T. ) ;
#4724=CARTESIAN_POINT ( 'NONE',  ( -96.20499999999996987, -2.607480562269071545, -8.024999999999991473 ) ) ;
#4732=CARTESIAN_POINT ( 'NONE',  ( -74.84499999999998465, -7.632228543268599452, 2.479861379858951054 ) ) ;
#4750=CARTESIAN_POINT ( 'NONE',  ( -156.8070736234661524, 10.01517768586948698, -1.839758294383808571E-15 ) ) ;
#4752=CARTESIAN_POINT ( 'NONE',  ( -99.35707362346617799, 5.598654528085804216, 7.705886871421366635 ) ) ;
#4764=CARTESIAN_POINT ( 'NONE',  ( -141.3550000000000182, -4.716976649647093289, -6.492361379858945902 ) ) ;
#4765=CARTESIAN_POINT ( 'NONE',  ( -87.05707362346618083, 0.000000000000000000, 9.524999999999991473 ) ) ;
#4769=CARTESIAN_POINT ( 'NONE',  ( -151.7949999999999591, 2.607480562269068880, -8.024999999999993250 ) ) ;
#4770=CARTESIAN_POINT ( 'NONE',  ( -134.3949999999999250, -6.826472737025113702, -4.959722759717900331 ) ) ;
#4772=CARTESIAN_POINT ( 'NONE',  ( -181.1070736234661354, 8.102448949553172852, -5.886773742842744461 ) ) ;
#4776=CARTESIAN_POINT ( 'NONE',  ( -51.65499999999997982, -7.632228543268600340, -2.479861379858950166 ) ) ;
#4799=ORIENTED_EDGE ( 'NONE', *, *, #20500, .F. ) ;
#4815=CARTESIAN_POINT ( 'NONE',  ( -99.44499999999999318, 0.000000000000000000, 8.024999999999991473 ) ) ;
#4818=CARTESIAN_POINT ( 'NONE',  ( -163.8570736234661922, -5.598654528085803328, -7.705886871421366635 ) ) ;
#4825=CARTESIAN_POINT ( 'NONE',  ( -62.75707362346616236, -5.598654528085801552, 7.705886871421367523 ) ) ;
#4837=CARTESIAN_POINT ( 'NONE',  ( -195.0000000000000000, 0.000000000000000000, 9.524999999999991473 ) ) ;
#4839=DIRECTION ( 'NONE',  ( -1.000000000000000000, -0.000000000000000000, -0.000000000000000000 ) ) ;
#4845=CARTESIAN_POINT ( 'NONE',  ( -169.8570736234661922, -5.598654528085803328, -7.705886871421366635 ) ) ;
#4850=CARTESIAN_POINT ( 'NONE',  ( -168.8049999999999500, -8.437984349512085203, 5.166775262442717831E-16 ) ) ;
#4852=CARTESIAN_POINT ( 'NONE',  ( -181.9449999999999932, -9.827790563157499189E-16, -8.024999999999991473 ) ) ;
#4854=CARTESIAN_POINT ( 'NONE',  ( -168.4449999999999932, 0.000000000000000000, 8.024999999999991473 ) ) ;
#4858=CARTESIAN_POINT ( 'NONE',  ( -12.92299149854152063, 11.10368424694205203, -4.551139136257919660 ) ) ;
#4860=CARTESIAN_POINT ( 'NONE',  ( -81.65499999999998693, -7.632228543268600340, -2.479861379858950166 ) ) ;
#4862=CARTESIAN_POINT ( 'NONE',  ( -168.2070736234663570, 3.094860106621407869, 9.524999999997831424 ) ) ;
#4866=CARTESIAN_POINT ( 'NONE',  ( -85.04499999999998749, 7.632228543268600340, 2.479861379858949277 ) ) ;
#4870=CARTESIAN_POINT ( 'NONE',  ( -172.1070736234661069, 8.102448949553172852, -5.886773742842744461 ) ) ;
#4884=CARTESIAN_POINT ( 'NONE',  ( -174.6570736234662036, 9.058813317711329915, 2.943386871421369566 ) ) ;
#4890=CARTESIAN_POINT ( 'NONE',  ( -120.9549999999999983, -7.632228543268599452, 2.479861379858951054 ) ) ;
#4892=CARTESIAN_POINT ( 'NONE',  ( -136.5570736234661808, -1.166476076187852838E-15, -9.524999999999991473 ) ) ;
#4902=CARTESIAN_POINT ( 'NONE',  ( -118.5570736234661808, -1.166476076187852838E-15, -9.524999999999991473 ) ) ;
#4910=DIRECTION ( 'NONE',  ( 0.000000000000000000, 0.000000000000000000, 1.000000000000000000 ) ) ;
#4916=CARTESIAN_POINT ( 'NONE',  ( -61.19292637653379074, -10.01517768586948698, 6.132527647946031529E-16 ) ) ;
#4920=CARTESIAN_POINT ( 'NONE',  ( -149.4550000000000125, 7.632228543268599452, -2.479861379858951942 ) ) ;
#4935=CARTESIAN_POINT ( 'NONE',  ( -65.60499999999997556, 6.826472737025113702, -4.959722759717902107 ) ) ;
#4953=CARTESIAN_POINT ( 'NONE',  ( -122.9949999999999903, -6.826472737025113702, 4.959722759717902107 ) ) ;
#4955=CARTESIAN_POINT ( 'NONE',  ( -83.99499999999999034, -6.826472737025115478, 4.959722759717900331 ) ) ;
#4961=CARTESIAN_POINT ( 'NONE',  ( -132.7429263765338021, -5.598654528085803328, -7.705886871421366635 ) ) ;
#4962=VECTOR ( 'NONE', #15210, 1000.000000000000000 ) ;
#4964=CARTESIAN_POINT ( 'NONE',  ( -149.2449999999999761, -4.716976649647093289, -6.492361379858945902 ) ) ;
#4977=CARTESIAN_POINT ( 'NONE',  ( -154.4049999999999727, -2.607480562269069768, 8.024999999999991473 ) ) ;
#4990=CARTESIAN_POINT ( 'NONE',  ( -63.35499999999998266, -4.716976649647093289, -6.492361379858945902 ) ) ;
#4999=CARTESIAN_POINT ( 'NONE',  ( -195.0000000000000000, 0.000000000000000000, 0.000000000000000000 ) ) ;
#5004=CARTESIAN_POINT ( 'NONE',  ( -178.8549999999999898, 4.716976649647094177, 6.492361379858945902 ) ) ;
#5011=ORIENTED_EDGE ( 'NONE', *, *, #157, .T. ) ;
#5016=CARTESIAN_POINT ( 'NONE',  ( -91.10500000000000398, -6.826472737025115478, 4.959722759717900331 ) ) ;
#5021=CARTESIAN_POINT ( 'NONE',  ( -133.2570736234661695, 5.598654528085800663, -7.705886871421367523 ) ) ;
#5024=CARTESIAN_POINT ( 'NONE',  ( -62.60707362346617089, -8.102448949553172852, 5.886773742842742685 ) ) ;
#5027=CARTESIAN_POINT ( 'NONE',  ( -80.24292637653380211, 5.598654528085804216, 7.705886871421366635 ) ) ;
#5034=CARTESIAN_POINT ( 'NONE',  ( -111.9549999999999841, -7.632228543268599452, 2.479861379858951054 ) ) ;
#5036=CARTESIAN_POINT ( 'NONE',  ( -112.3449999999999847, 7.632228543268599452, -2.479861379858951942 ) ) ;
#5043=CARTESIAN_POINT ( 'NONE',  ( -163.6429263765338078, -5.598654528085801552, 7.705886871421367523 ) ) ;
#5044=SURFACE_STYLE_USAGE ( .BOTH. , #58176 ) ;
#5045=CARTESIAN_POINT ( 'NONE',  ( -183.2949999999999307, -2.607480562269069768, 8.024999999999991473 ) ) ;
#5049=DIRECTION ( 'NONE',  ( -1.000000000000000000, -0.000000000000000000, -0.000000000000000000 ) ) ;
#5052=CARTESIAN_POINT ( 'NONE',  ( -78.59292637653381064, -3.094860106618431139, -9.524999999999991473 ) ) ;
#5060=CARTESIAN_POINT ( 'NONE',  ( -179.9049999999999727, 2.607480562269069324, -8.024999999999993250 ) ) ;
#5068=CARTESIAN_POINT ( 'NONE',  ( -101.6070736234661780, -8.102448949553174629, 5.886773742842742685 ) ) ;
#5069=CARTESIAN_POINT ( 'NONE',  ( -98.00499999999999545, 6.826472737025115478, 4.959722759717899443 ) ) ;
#5075=EDGE_CURVE ( 'NONE', #24108, #33812, #46062, .T. ) ;
#5083=CARTESIAN_POINT ( 'NONE',  ( -75.74499999999999034, 4.716976649647094177, 6.492361379858945902 ) ) ;
#5095=ORIENTED_EDGE ( 'NONE', *, *, #48628, .F. ) ;
#5097=CARTESIAN_POINT ( 'NONE',  ( -160.4929263765338021, -8.102448949553174629, 5.886773742842742685 ) ) ;
#5100=CARTESIAN_POINT ( 'NONE',  ( -158.3070736234662093, -10.01517768586948698, 6.132527647946031529E-16 ) ) ;
#5103=CARTESIAN_POINT ( 'NONE',  ( -90.35707362346617799, 5.598654528085804216, 7.705886871421366635 ) ) ;
#5110=CARTESIAN_POINT ( 'NONE',  ( -137.4549999999999841, 7.632228543268599452, -2.479861379858951942 ) ) ;
#5112=CARTESIAN_POINT ( 'NONE',  ( -157.1950000000000216, 8.437984349512085203, -1.550032578732815448E-15 ) ) ;
#5113=CARTESIAN_POINT ( 'NONE',  ( -142.4949999999999761, 6.826472737025113702, -4.959722759717902107 ) ) ;
#5117=CARTESIAN_POINT ( 'NONE',  ( -63.44292637653379785, -1.166476076187852838E-15, -9.524999999999991473 ) ) ;
#5119=CARTESIAN_POINT ( 'NONE',  ( -52.40499999999998693, -2.607480562269069768, 8.024999999999991473 ) ) ;
#5121=CARTESIAN_POINT ( 'NONE',  ( -52.94292637653380496, 0.000000000000000000, 9.524999999999991473 ) ) ;
#5126=CARTESIAN_POINT ( 'NONE',  ( -153.4429263765338192, -1.166476076187852838E-15, -9.524999999999991473 ) ) ;
#5144=ORIENTED_EDGE ( 'NONE', *, *, #42385, .F. ) ;
#5146=CARTESIAN_POINT ( 'NONE',  ( -108.9570736234661723, 9.058813317711329915, -2.943386871421373119 ) ) ;
#5148=CARTESIAN_POINT ( 'NONE',  ( -101.9929263765338021, 8.102448949553172852, -5.886773742842744461 ) ) ;
#5154=CARTESIAN_POINT ( 'NONE',  ( -104.2449999999999903, -4.716976649647093289, -6.492361379858945902 ) ) ;
#5167=VECTOR ( 'NONE', #6991, 1000.000000000000000 ) ;
#5172=CARTESIAN_POINT ( 'NONE',  ( -125.6929263765338192, 10.01517768586948698, -1.839758294383808966E-15 ) ) ;
#5176=EDGE_LOOP ( 'NONE', ( #22307, #19176 ) ) ;
#5180=DIRECTION ( 'NONE',  ( 0.000000000000000000, 0.000000000000000000, 1.000000000000000000 ) ) ;
#5185=CARTESIAN_POINT ( 'NONE',  ( -167.0049999999999670, 6.826472737025116366, 4.959722759717898555 ) ) ;
#5189=CARTESIAN_POINT ( 'NONE',  ( -49.40707362346615383, 3.094860106618428031, -9.524999999999993250 ) ) ;
#5191=CARTESIAN_POINT ( 'NONE',  ( -166.9450000000000216, -9.827790563157499189E-16, -8.024999999999991473 ) ) ;
#5196=CARTESIAN_POINT ( 'NONE',  ( -12.48648248363261004, 11.19366133502252048, -4.325373782235834241 ) ) ;
#5197=CARTESIAN_POINT ( 'NONE',  ( -84.95499999999998408, -7.632228543268599452, 2.479861379858951054 ) ) ;
#5200=CARTESIAN_POINT ( 'NONE',  ( -78.29499999999994486, -2.607480562269069768, 8.024999999999991473 ) ) ;
#5206=CARTESIAN_POINT ( 'NONE',  ( -108.0570736234661666, 0.000000000000000000, 9.524999999999991473 ) ) ;
#5218=CARTESIAN_POINT ( 'NONE',  ( -135.1429263765338078, 5.598654528085800663, -7.705886871421367523 ) ) ;
#5225=CARTESIAN_POINT ( 'NONE',  ( -119.9049999999999869, 2.607480562269069324, -8.024999999999993250 ) ) ;
#5233=ORIENTED_EDGE ( 'NONE', *, *, #37871, .T. ) ;
#5254=CARTESIAN_POINT ( 'NONE',  ( -145.4050000000000296, -2.607480562269069768, 8.024999999999991473 ) ) ;
#5265=CARTESIAN_POINT ( 'NONE',  ( -60.80499999999998550, -8.437984349512085203, 5.166775262442717831E-16 ) ) ;
#5280=CARTESIAN_POINT ( 'NONE',  ( -112.6449999999999960, 4.716976649647091513, -6.492361379858946790 ) ) ;
#5282=CARTESIAN_POINT ( 'NONE',  ( -88.49500000000000455, 6.826472737025113702, -4.959722759717902107 ) ) ;
#5289=CARTESIAN_POINT ( 'NONE',  ( -129.1429263765338078, 5.598654528085800663, -7.705886871421367523 ) ) ;
#5290=CARTESIAN_POINT ( 'NONE',  ( -150.2949999999999875, -2.607480562269069768, 8.024999999999991473 ) ) ;
#5293=CYLINDRICAL_SURFACE ( 'NONE', #45329, 9.524999999999991473 ) ;
#5300=CARTESIAN_POINT ( 'NONE',  ( -59.54292637653379927, 9.058813317711329915, 2.943386871421369566 ) ) ;
#5306=CARTESIAN_POINT ( 'NONE',  ( -150.5049999999999955, -6.826472737025113702, -4.959722759717900331 ) ) ;
#5311=CARTESIAN_POINT ( 'NONE',  ( -142.5570736234661808, -1.166476076187852838E-15, -9.524999999999991473 ) ) ;
#5322=CARTESIAN_POINT ( 'NONE',  ( -68.75499999999998124, 4.716976649647091513, -6.492361379858946790 ) ) ;
#5323=CARTESIAN_POINT ( 'NONE',  ( -123.7449999999999903, 4.716976649647094177, 6.492361379858945902 ) ) ;
#5330=VECTOR ( 'NONE', #53120, 1000.000000000000000 ) ;
#5337=CARTESIAN_POINT ( 'NONE',  ( -170.3049999999999784, 8.437984349512085203, -1.550032578732815448E-15 ) ) ;
#5339=CARTESIAN_POINT ( 'NONE',  ( -87.20707362346618652, 3.094860106618433360, 9.524999999999991473 ) ) ;
#5344=CARTESIAN_POINT ( 'NONE',  ( -128.7570736234661695, -5.598654528085801552, 7.705886871421367523 ) ) ;
#5346=CARTESIAN_POINT ( 'NONE',  ( -95.30499999999997840, 8.437984349512085203, -1.550032578732815448E-15 ) ) ;
#5350=CARTESIAN_POINT ( 'NONE',  ( -129.5070736234661695, 8.102448949553176405, 5.886773742842740909 ) ) ;
#5352=CARTESIAN_POINT ( 'NONE',  ( -69.20707362346617231, 3.094860106618433360, 9.524999999999991473 ) ) ;
#5360=CARTESIAN_POINT ( 'NONE',  ( -108.3549999999999898, -4.716976649647093289, -6.492361379858945902 ) ) ;
#5362=CARTESIAN_POINT ( 'NONE',  ( -113.5449999999999875, -7.632228543268600340, -2.479861379858950166 ) ) ;
#5367=CARTESIAN_POINT ( 'NONE',  ( -164.2429263765338021, 5.598654528085804216, 7.705886871421366635 ) ) ;
#5369=CARTESIAN_POINT ( 'NONE',  ( -180.4449999999999932, 0.000000000000000000, 8.024999999999991473 ) ) ;
#5375=CARTESIAN_POINT ( 'NONE',  ( -75.29292637653381348, 3.094860106618428031, -9.524999999999993250 ) ) ;
#5384=CARTESIAN_POINT ( 'NONE',  ( -183.2050000000000125, -2.607480562269071545, -8.024999999999991473 ) ) ;
#5391=( BOUNDED_CURVE ( )  B_SPLINE_CURVE ( 2, ( #16464, #59303, #11131, #523, #60019, #32580, #54043, #11486, #5847, #6213, #11831 ),
 .UNSPECIFIED., .F., .F. ) 
 B_SPLINE_CURVE_WITH_KNOTS ( ( 3, 2, 2, 2, 2, 3 ),
 ( 0.06521739130434632548, 0.06739130434782453216, 0.06956521739130275273, 0.07173913043478095941, 0.07391304347825917997, 0.07608695652173738666 ),
 .UNSPECIFIED. ) 
 CURVE ( )  GEOMETRIC_REPRESENTATION_ITEM ( )  RATIONAL_B_SPLINE_CURVE ( ( 1.000000000000033751, 0.9510565162951197804, 1.000000000000000000, 0.9510565162951535312, 1.000000000000000000, 0.9510565162951535312, 1.000000000000000000, 0.9510565162951535312, 1.000000000000000000, 0.9510565162951929441, 0.9999999999999605871 ) ) 
 REPRESENTATION_ITEM ( '' )  );
#5397=CARTESIAN_POINT ( 'NONE',  ( -97.40499999999997272, -2.607480562269069768, 8.024999999999991473 ) ) ;
#5405=ORIENTED_EDGE ( 'NONE', *, *, #34309, .T. ) ;
#5408=CARTESIAN_POINT ( 'NONE',  ( -74.54499999999998749, -7.632228543268600340, -2.479861379858950166 ) ) ;
#5415=CARTESIAN_POINT ( 'NONE',  ( -124.1049999999999756, -6.826472737025115478, 4.959722759717900331 ) ) ;
#5419=CARTESIAN_POINT ( 'NONE',  ( -160.7929263765341261, -3.094860106613354755, 9.525000000003679190 ) ) ;
#5422=CARTESIAN_POINT ( 'NONE',  ( -162.6570736234661751, 9.058813317711329915, 2.943386871421369566 ) ) ;
#5424=CARTESIAN_POINT ( 'NONE',  ( -98.90707362346618936, -3.094860106618429807, 9.524999999999991473 ) ) ;
#5432=CARTESIAN_POINT ( 'NONE',  ( -137.3049999999999784, 8.437984349512085203, -1.550032578732815448E-15 ) ) ;
#5433=CARTESIAN_POINT ( 'NONE',  ( -86.30707362346616662, -10.01517768586948698, 6.132527647946031529E-16 ) ) ;
#5436=CARTESIAN_POINT ( 'NONE',  ( -142.4949999999999761, 6.826472737025113702, -4.959722759717902107 ) ) ;
#5438=CARTESIAN_POINT ( 'NONE',  ( -138.5949999999999420, 2.607480562269072433, 8.024999999999991473 ) ) ;
#5442=CARTESIAN_POINT ( 'NONE',  ( -57.35499999999998977, -4.716976649647093289, -6.492361379858945902 ) ) ;
#5451=CARTESIAN_POINT ( 'NONE',  ( -102.5929263765337822, -3.094860106618431139, -9.524999999999991473 ) ) ;
#5454=CARTESIAN_POINT ( 'NONE',  ( -89.75707362346616947, -5.598654528085801552, 7.705886871421367523 ) ) ;
#5455=CARTESIAN_POINT ( 'NONE',  ( -99.95707362346617231, 9.058813317711329915, -2.943386871421373119 ) ) ;
#5479=CARTESIAN_POINT ( 'NONE',  ( -97.19499999999997897, 8.437984349512085203, -1.550032578732815448E-15 ) ) ;
#5488=CYLINDRICAL_SURFACE ( 'NONE', #12782, 9.524999999999991473 ) ;
#5493=CYLINDRICAL_SURFACE ( 'NONE', #41170, 9.524999999999991473 ) ;
#5502=CARTESIAN_POINT ( 'NONE',  ( -114.7429263765338021, -5.598654528085803328, -7.705886871421366635 ) ) ;
#5509=CARTESIAN_POINT ( 'NONE',  ( -43.99999999999998579, 1.469576158976823356E-15, -11.99999999999999467 ) ) ;
#5512=CARTESIAN_POINT ( 'NONE',  ( -164.9049999999999443, 2.607480562269068880, -8.024999999999993250 ) ) ;
#5515=CARTESIAN_POINT ( 'NONE',  ( -178.4949999999999477, 6.826472737025113702, -4.959722759717902107 ) ) ;
#5516=CARTESIAN_POINT ( 'NONE',  ( -163.6449999999999818, 4.716976649647091513, -6.492361379858946790 ) ) ;
#5523=CARTESIAN_POINT ( 'NONE',  ( -10.25964396124710021, 11.89359207642228533, -1.623549840978965930 ) ) ;
#5525=CARTESIAN_POINT ( 'NONE',  ( -83.30500000000000682, 8.437984349512085203, -1.550032578732815448E-15 ) ) ;
#5529=EDGE_CURVE ( 'NONE', #47886, #45514, #1246, .T. ) ;
#5530=CARTESIAN_POINT ( 'NONE',  ( -77.84499999999998465, -7.632228543268599452, 2.479861379858951054 ) ) ;
#5531=EDGE_CURVE ( 'NONE', #41269, #55073, #53895, .T. ) ;
#5536=CARTESIAN_POINT ( 'NONE',  ( -171.0570736234661808, 0.000000000000000000, 9.524999999999991473 ) ) ;
#5539=CARTESIAN_POINT ( 'NONE',  ( -74.54292637653379927, 9.058813317711329915, 2.943386871421369566 ) ) ;
#5543=ADVANCED_FACE ( 'NONE', ( #21075, #63643 ), #64689, .T. ) ;
#5549=DIRECTION ( 'NONE',  ( 0.000000000000000000, 0.000000000000000000, 1.000000000000000000 ) ) ;
#5561=CARTESIAN_POINT ( 'NONE',  ( -109.1049999999999898, -6.826472737025113702, 4.959722759717902107 ) ) ;
#5566=CARTESIAN_POINT ( 'NONE',  ( -55.94292637653380496, 0.000000000000000000, 9.524999999999991473 ) ) ;
#5567=CARTESIAN_POINT ( 'NONE',  ( -138.0570736234661808, 0.000000000000000000, 9.524999999999991473 ) ) ;
#5570=EDGE_CURVE ( 'NONE', #12708, #32796, #595, .T. ) ;
#5586=ORIENTED_EDGE ( 'NONE', *, *, #52985, .F. ) ;
#5590=CARTESIAN_POINT ( 'NONE',  ( -49.49292637653378790, -8.102448949553172852, 5.886773742842742685 ) ) ;
#5594=CARTESIAN_POINT ( 'NONE',  ( -140.0049999999999386, 6.826472737025116366, 4.959722759717898555 ) ) ;
#5599=PRESENTATION_STYLE_ASSIGNMENT (( #32343 ) ) ;
#5605=CARTESIAN_POINT ( 'NONE',  ( -56.45499999999997698, 7.632228543268599452, -2.479861379858951942 ) ) ;
#5620=CARTESIAN_POINT ( 'NONE',  ( -114.2949999999999875, -2.607480562269069768, 8.024999999999991473 ) ) ;
#5622=CARTESIAN_POINT ( 'NONE',  ( -83.54499999999998749, -7.632228543268600340, -2.479861379858950166 ) ) ;
#5630=CARTESIAN_POINT ( 'NONE',  ( -131.5429263765338135, 9.058813317711329915, 2.943386871421369566 ) ) ;
#5631=CARTESIAN_POINT ( 'NONE',  ( -144.2950000000000159, -2.607480562269069768, 8.024999999999991473 ) ) ;
#5634=CARTESIAN_POINT ( 'NONE',  ( -47.99499999999998323, -6.826472737025113702, 4.959722759717902107 ) ) ;
#5637=ORIENTED_EDGE ( 'NONE', *, *, #34773, .T. ) ;
#5645=CARTESIAN_POINT ( 'NONE',  ( -59.99292637653380211, 8.102448949553172852, -5.886773742842744461 ) ) ;
#5649=CARTESIAN_POINT ( 'NONE',  ( -155.1550000000000011, 7.632228543268600340, 2.479861379858949277 ) ) ;
#5665=CARTESIAN_POINT ( 'NONE',  ( -61.10499999999996845, -6.826472737025113702, 4.959722759717902107 ) ) ;
#5666=CARTESIAN_POINT ( 'NONE',  ( -123.4449999999999932, 0.000000000000000000, 8.024999999999991473 ) ) ;
#5679=CARTESIAN_POINT ( 'NONE',  ( -171.8050000000000068, -8.437984349512085203, 5.166775262442717831E-16 ) ) ;
#5690=CARTESIAN_POINT ( 'NONE',  ( -83.90500000000000114, 2.607480562269068880, -8.024999999999993250 ) ) ;
#5698=CARTESIAN_POINT ( 'NONE',  ( -62.90707362346616804, -3.094860106618429807, 9.524999999999991473 ) ) ;
#5706=CARTESIAN_POINT ( 'NONE',  ( -105.2049999999999841, -2.607480562269071545, -8.024999999999991473 ) ) ;
#5709=CARTESIAN_POINT ( 'NONE',  ( -115.9449999999999932, -9.827790563157499189E-16, -8.024999999999991473 ) ) ;
#5714=CARTESIAN_POINT ( 'NONE',  ( -153.9570736234661581, 9.058813317711329915, -2.943386871421373119 ) ) ;
#5715=CARTESIAN_POINT ( 'NONE',  ( -163.1929263765338192, -10.01517768586948698, 6.132527647946031529E-16 ) ) ;
#5717=CARTESIAN_POINT ( 'NONE',  ( -176.6949999999999363, -8.437984349512085203, 5.166775262442717831E-16 ) ) ;
#5724=VECTOR ( 'NONE', #60067, 1000.000000000000000 ) ;
#5725=CARTESIAN_POINT ( 'NONE',  ( -73.79292637653378506, -3.094860106618429807, 9.524999999999991473 ) ) ;
#5728=DIRECTION ( 'NONE',  ( 0.000000000000000000, 0.000000000000000000, 1.000000000000000000 ) ) ;
#5731=CARTESIAN_POINT ( 'NONE',  ( -195.0000000000000000, 0.000000000000000000, 0.000000000000000000 ) ) ;
#5733=CARTESIAN_POINT ( 'NONE',  ( -181.8549999999999898, 4.716976649647094177, 6.492361379858945902 ) ) ;
#5738=CARTESIAN_POINT ( 'NONE',  ( -75.05707362346616662, 0.000000000000000000, 9.524999999999991473 ) ) ;
#5745=CARTESIAN_POINT ( 'NONE',  ( -93.20499999999998408, -2.607480562269071545, -8.024999999999991473 ) ) ;
#5747=CARTESIAN_POINT ( 'NONE',  ( -92.45707362346617231, -9.058813317711329915, 2.943386871421371787 ) ) ;
#5752=CARTESIAN_POINT ( 'NONE',  ( -59.99499999999996902, -6.826472737025115478, 4.959722759717900331 ) ) ;
#5762=MECHANICAL_DESIGN_GEOMETRIC_PRESENTATION_REPRESENTATION('',(#47411),#50737);
#5763=CARTESIAN_POINT ( 'NONE',  ( -108.4429263765338050, -1.166476076187852838E-15, -9.524999999999991473 ) ) ;
#5765=CARTESIAN_POINT ( 'NONE',  ( -118.8549999999999898, 4.716976649647094177, 6.492361379858945902 ) ) ;
#5766=ORIENTED_EDGE ( 'NONE', *, *, #41495, .T. ) ;
#5772=DIRECTION ( 'NONE',  ( 0.000000000000000000, 0.000000000000000000, 1.000000000000000000 ) ) ;
#5773=CARTESIAN_POINT ( 'NONE',  ( -159.9570736234661865, 9.058813317711329915, -2.943386871421373119 ) ) ;
#5777=CARTESIAN_POINT ( 'NONE',  ( -98.60707362346616378, -8.102448949553172852, 5.886773742842742685 ) ) ;
#5786=CARTESIAN_POINT ( 'NONE',  ( -141.5049999999999955, -6.826472737025115478, -4.959722759717899443 ) ) ;
#5789=CARTESIAN_POINT ( 'NONE',  ( -171.0570736234661808, 0.000000000000000000, 9.524999999999991473 ) ) ;
#5791=CARTESIAN_POINT ( 'NONE',  ( -142.3449999999999989, 7.632228543268599452, -2.479861379858951942 ) ) ;
#5793=CARTESIAN_POINT ( 'NONE',  ( -136.1949999999999932, 8.437984349512086979, -1.550032578732815448E-15 ) ) ;
#5795=EDGE_CURVE ( 'NONE', #62473, #21970, #19598, .T. ) ;
#5802=CARTESIAN_POINT ( 'NONE',  ( -51.80499999999998550, -8.437984349512085203, 5.166775262442717831E-16 ) ) ;
#5804=CARTESIAN_POINT ( 'NONE',  ( -61.79499999999998039, 2.607480562269068880, -8.024999999999993250 ) ) ;
#5810=CARTESIAN_POINT ( 'NONE',  ( -103.3429263765338106, -9.058813317711329915, 2.943386871421371787 ) ) ;
#5811=( BOUNDED_CURVE ( )  B_SPLINE_CURVE ( 2, ( #13602, #56161, #67418, #18867, #40724, #51257, #19581, #45322, #62135, #8353, #2999 ),
 .UNSPECIFIED., .F., .F. ) 
 B_SPLINE_CURVE_WITH_KNOTS ( ( 3, 2, 2, 2, 2, 3 ),
 ( 0.1630434782608656819, 0.1652173913043438747, 0.1673913043478220952, 0.1695652173913003158, 0.1717391304347785363, 0.1739130434782567292 ),
 .UNSPECIFIED. ) 
 CURVE ( )  GEOMETRIC_REPRESENTATION_ITEM ( )  RATIONAL_B_SPLINE_CURVE ( ( 1.000000000000087486, 0.9510565162950660456, 1.000000000000000000, 0.9510565162951535312, 1.000000000000000000, 0.9510565162951535312, 1.000000000000000000, 0.9510565162951535312, 1.000000000000000000, 0.9510565162952466789, 0.9999999999999068523 ) ) 
 REPRESENTATION_ITEM ( '' )  );
#5815=CARTESIAN_POINT ( 'NONE',  ( -88.55707362346616662, -1.166476076187852838E-15, -9.524999999999991473 ) ) ;
#5835=ORIENTED_EDGE ( 'NONE', *, *, #61863, .T. ) ;
#5838=CARTESIAN_POINT ( 'NONE',  ( -195.0000000000000000, 1.166476076187852838E-15, -9.524999999999991473 ) ) ;
#5842=CARTESIAN_POINT ( 'NONE',  ( -92.24499999999999034, -4.716976649647093289, -6.492361379858945902 ) ) ;
#5846=EDGE_LOOP ( 'NONE', ( #62894, #14954, #68417, #1778 ) ) ;
#5847=CARTESIAN_POINT ( 'NONE',  ( -174.7429263765338305, -5.598654528085803328, -7.705886871421366635 ) ) ;
#5861=CARTESIAN_POINT ( 'NONE',  ( -126.4429263765338192, -1.166476076187852838E-15, -9.524999999999991473 ) ) ;
#5868=CARTESIAN_POINT ( 'NONE',  ( -162.4429263765338192, -1.166476076187852838E-15, -9.524999999999991473 ) ) ;
#5874=CARTESIAN_POINT ( 'NONE',  ( -172.5549999999999784, 0.000000000000000000, 8.024999999999991473 ) ) ;
#5877=CARTESIAN_POINT ( 'NONE',  ( -172.7950000000000159, 2.607480562269068880, -8.024999999999993250 ) ) ;
#5881=CARTESIAN_POINT ( 'NONE',  ( -170.2450000000000045, -4.716976649647093289, -6.492361379858945902 ) ) ;
#5888=CARTESIAN_POINT ( 'NONE',  ( -87.20499999999999829, -2.607480562269071545, -8.024999999999991473 ) ) ;
#5892=CARTESIAN_POINT ( 'NONE',  ( -78.59499999999998465, 2.607480562269072433, 8.024999999999991473 ) ) ;
#5894=CARTESIAN_POINT ( 'NONE',  ( -134.9070736234667720, -3.094860106608412931, 9.525000000007270984 ) ) ;
#5896=CARTESIAN_POINT ( 'NONE',  ( -176.9929263765337737, 8.102448949553172852, -5.886773742842744461 ) ) ;
#5910=( BOUNDED_CURVE ( )  B_SPLINE_CURVE ( 2, ( #58259, #57935, #31159, #42142, #4414, #25889, #20631, #10083, #31511, #50484, #12134 ),
 .UNSPECIFIED., .F., .F. ) 
 B_SPLINE_CURVE_WITH_KNOTS ( ( 3, 2, 2, 2, 2, 3 ),
 ( 0.7282608695652174058, 0.7304347826086956541, 0.7326086956521739024, 0.7347826086956521507, 0.7369565217391303991, 0.7391304347826086474 ),
 .UNSPECIFIED. ) 
 CURVE ( )  GEOMETRIC_REPRESENTATION_ITEM ( )  RATIONAL_B_SPLINE_CURVE ( ( 1.000000000000000000, 0.9510565162951535312, 1.000000000000000000, 0.9510565162951535312, 1.000000000000000000, 0.9510565162951535312, 1.000000000000000000, 0.9510565162951535312, 1.000000000000000000, 0.9510565162951535312, 1.000000000000000000 ) ) 
 REPRESENTATION_ITEM ( '' )  );
#5913=ADVANCED_FACE ( 'NONE', ( #63215 ), #11117, .T. ) ;
#5917=CARTESIAN_POINT ( 'NONE',  ( -114.3549999999999898, -4.716976649647093289, -6.492361379858945902 ) ) ;
#5918=ORIENTED_EDGE ( 'NONE', *, *, #45922, .T. ) ;
#5922=CARTESIAN_POINT ( 'NONE',  ( -68.15707362346616094, -9.058813317711329915, -2.943386871421370898 ) ) ;
#5932=CARTESIAN_POINT ( 'NONE',  ( -195.0000000000000000, 0.000000000000000000, 9.524999999999991473 ) ) ;
#5934=CARTESIAN_POINT ( 'NONE',  ( -13.37557077883746004, -11.02493375743656223, 4.740230301942971458 ) ) ;
#5936=ORIENTED_EDGE ( 'NONE', *, *, #26378, .T. ) ;
#5942=ADVANCED_FACE ( 'NONE', ( #26593 ), #41796, .T. ) ;
#5947=CARTESIAN_POINT ( 'NONE',  ( -50.69292637653379785, 10.01517768586948698, -1.839758294383808571E-15 ) ) ;
#5950=CARTESIAN_POINT ( 'NONE',  ( -145.8549999999999898, 4.716976649647094177, 6.492361379858945902 ) ) ;
#5957=CARTESIAN_POINT ( 'NONE',  ( -105.4429263765338050, -1.166476076187852838E-15, -9.524999999999991473 ) ) ;
#5958=AXIS2_PLACEMENT_3D ( 'NONE', #19329, #50323, #2775 ) ;
#5960=ORIENTED_EDGE ( 'NONE', *, *, #36909, .T. ) ;
#5966=CARTESIAN_POINT ( 'NONE',  ( -53.60499999999998977, 6.826472737025113702, -4.959722759717902107 ) ) ;
#5982=CARTESIAN_POINT ( 'NONE',  ( -107.9949999999999761, -6.826472737025113702, 4.959722759717902107 ) ) ;
#5984=CARTESIAN_POINT ( 'NONE',  ( -83.24499999999999034, -4.716976649647093289, -6.492361379858945902 ) ) ;
#5988=CARTESIAN_POINT ( 'NONE',  ( -166.8570736234661922, -5.598654528085803328, -7.705886871421366635 ) ) ;
#5994=CARTESIAN_POINT ( 'NONE',  ( -126.7429263765338163, -5.598654528085803328, -7.705886871421366635 ) ) ;
#5995=CARTESIAN_POINT ( 'NONE',  ( -147.2949999999999591, -2.607480562269069768, 8.024999999999991473 ) ) ;
#5998=CARTESIAN_POINT ( 'NONE',  ( -66.65707362346616094, 9.058813317711329915, 2.943386871421369566 ) ) ;
#5999=LINE ( 'NONE', #27438, #55239 ) ;
#6010=CARTESIAN_POINT ( 'NONE',  ( -59.84292637653379643, 9.058813317711329915, -2.943386871421373119 ) ) ;
#6011=CARTESIAN_POINT ( 'NONE',  ( -49.70707362346615810, -3.094860106618431139, -9.524999999999991473 ) ) ;
#6015=CARTESIAN_POINT ( 'NONE',  ( -137.0049999999999670, 6.826472737025115478, 4.959722759717899443 ) ) ;
#6031=CARTESIAN_POINT ( 'NONE',  ( -51.20499999999996277, -2.607480562269071545, -8.024999999999991473 ) ) ;
#6032=CARTESIAN_POINT ( 'NONE',  ( -116.2449999999999903, -4.716976649647093289, -6.492361379858945902 ) ) ;
#6039=EDGE_CURVE ( 'NONE', #1147, #12752, #38253, .T. ) ;
#6046=CARTESIAN_POINT ( 'NONE',  ( -173.4549999999999841, 7.632228543268599452, -2.479861379858951942 ) ) ;
#6054=CARTESIAN_POINT ( 'NONE',  ( -77.24292637653380211, 5.598654528085804216, 7.705886871421366635 ) ) ;
#6058=CARTESIAN_POINT ( 'NONE',  ( -88.70499999999998408, 2.607480562269073321, 8.024999999999991473 ) ) ;
#6063=CARTESIAN_POINT ( 'NONE',  ( -60.80707362346617373, 10.01517768586948698, -1.839758294383808571E-15 ) ) ;
#6071=CARTESIAN_POINT ( 'NONE',  ( -101.4549999999999841, 7.632228543268599452, -2.479861379858951942 ) ) ;
#6074=CARTESIAN_POINT ( 'NONE',  ( -114.4449999999999932, 0.000000000000000000, 8.024999999999991473 ) ) ;
#6081=CARTESIAN_POINT ( 'NONE',  ( -155.0929263765337964, 3.094860106618433360, 9.524999999999991473 ) ) ;
#6082=CARTESIAN_POINT ( 'NONE',  ( -178.0450000000000159, 7.632228543268600340, 2.479861379858949277 ) ) ;
#6090=CARTESIAN_POINT ( 'NONE',  ( 0.000000000000000000, 0.000000000000000000, 0.000000000000000000 ) ) ;
#6092=CARTESIAN_POINT ( 'NONE',  ( -73.34292637653381064, -9.058813317711329915, 2.943386871421371787 ) ) ;
#6098=CARTESIAN_POINT ( 'NONE',  ( -168.5049999999999955, -6.826472737025113702, -4.959722759717900331 ) ) ;
#6101=ADVANCED_BREP_SHAPE_REPRESENTATION ( '', ( #28116, #42840 ), #4621 ) ;
#6107=CARTESIAN_POINT ( 'NONE',  ( -181.5570736234661808, -1.166476076187852838E-15, -9.524999999999991473 ) ) ;
#6113=CARTESIAN_POINT ( 'NONE',  ( -91.10499999999998977, -6.826472737025113702, 4.959722759717902107 ) ) ;
#6118=CARTESIAN_POINT ( 'NONE',  ( -91.55707362346616662, -1.166476076187852838E-15, -9.524999999999991473 ) ) ;
#6120=EDGE_CURVE ( 'NONE', #31091, #69107, #24709, .T. ) ;
#6126=CARTESIAN_POINT ( 'NONE',  ( -60.74499999999997613, 4.716976649647094177, 6.492361379858945902 ) ) ;
#6139=CARTESIAN_POINT ( 'NONE',  ( -118.7049999999999699, 2.607480562269073321, 8.024999999999991473 ) ) ;
#6146=AXIS2_PLACEMENT_3D ( 'NONE', #8465, #24961, #41187 ) ;
#6147=CARTESIAN_POINT ( 'NONE',  ( -148.8570736234661638, -5.598654528085803328, -7.705886871421366635 ) ) ;
#6149=CARTESIAN_POINT ( 'NONE',  ( -97.40707362346614673, 3.094860106618428031, -9.524999999999993250 ) ) ;
#6155=CARTESIAN_POINT ( 'NONE',  ( -129.3549999999999898, -4.716976649647093289, -6.492361379858945902 ) ) ;
#6158=CARTESIAN_POINT ( 'NONE',  ( -144.1449999999999818, -4.716976649647092401, 6.492361379858946790 ) ) ;
#6160=CARTESIAN_POINT ( 'NONE',  ( -126.8949999999999818, 6.826472737025115478, 4.959722759717899443 ) ) ;
#6162=CIRCLE ( 'NONE', #64616, 10.99999999999995381 ) ;
#6166=CARTESIAN_POINT ( 'NONE',  ( -184.7929263765338135, -3.094860106618429807, 9.524999999999991473 ) ) ;
#6168=CARTESIAN_POINT ( 'NONE',  ( -63.44499999999998607, 0.000000000000000000, 8.024999999999991473 ) ) ;
#6169=CARTESIAN_POINT ( 'NONE',  ( -139.1929263765337907, -10.01517768586948698, 6.132527647946031529E-16 ) ) ;
#6174=CARTESIAN_POINT ( 'NONE',  ( -104.8429263765338106, 9.058813317711329915, -2.943386871421373119 ) ) ;
#6179=CARTESIAN_POINT ( 'NONE',  ( -99.20707362346720970, 3.094860106635777264, 9.524999999987391774 ) ) ;
#6186=EDGE_LOOP ( 'NONE', ( #35211, #42911, #21981, #23585 ) ) ;
#6192=VERTEX_POINT ( 'NONE', #20845 ) ;
#6194=CARTESIAN_POINT ( 'NONE',  ( -195.0000000000000000, 0.000000000000000000, 0.000000000000000000 ) ) ;
#6199=CARTESIAN_POINT ( 'NONE',  ( -118.5570736234661808, -1.166476076187852838E-15, -9.524999999999991473 ) ) ;
#6205=CARTESIAN_POINT ( 'NONE',  ( -87.44499999999999318, 0.000000000000000000, 8.024999999999991473 ) ) ;
#6212=ORIENTED_EDGE ( 'NONE', *, *, #42310, .T. ) ;
#6213=CARTESIAN_POINT ( 'NONE',  ( -174.5929263765339385, -3.094860106620549001, -9.524999999998453148 ) ) ;
#6214=( BOUNDED_CURVE ( )  B_SPLINE_CURVE ( 2, ( #38396, #29143, #54839, #50631, #66097, #11953, #39763, #12635, #23535, #28808, #49958 ),
 .UNSPECIFIED., .F., .F. ) 
 B_SPLINE_CURVE_WITH_KNOTS ( ( 3, 2, 2, 2, 2, 3 ),
 ( 0.2717391304347762659, 0.2739130434782544588, 0.2760869565217327071, 0.2782608695652109554, 0.2804347826086891482, 0.2826086956521673410 ),
 .UNSPECIFIED. ) 
 CURVE ( )  GEOMETRIC_REPRESENTATION_ITEM ( )  RATIONAL_B_SPLINE_CURVE ( ( 1.000000000000142553, 0.9510565162950110896, 1.000000000000000000, 0.9510565162951535312, 1.000000000000000000, 0.9510565162951535312, 1.000000000000000000, 0.9510565162951535312, 1.000000000000000000, 0.9510565162953009688, 0.9999999999998525624 ) ) 
 REPRESENTATION_ITEM ( '' )  );
#6220=CARTESIAN_POINT ( 'NONE',  ( -166.4070736234663741, 3.094860106615134221, -9.525000000002387779 ) ) ;
#6235=CARTESIAN_POINT ( 'NONE',  ( -159.8049999999999784, -8.437984349512085203, 5.166775262442717831E-16 ) ) ;
#6237=CARTESIAN_POINT ( 'NONE',  ( -183.6149733308552641, -5.710802470748983062, -6.846503224029541812 ) ) ;
#6238=CARTESIAN_POINT ( 'NONE',  ( -170.5450000000000159, -7.632228543268600340, -2.479861379858950166 ) ) ;
#6240=CARTESIAN_POINT ( 'NONE',  ( -167.2450000000000045, -4.716976649647093289, -6.492361379858945902 ) ) ;
#6241=( BOUNDED_CURVE ( )  B_SPLINE_CURVE ( 2, ( #29339, #39601, #24078, #56791, #19124, #35335, #34616, #61005, #55744, #18792, #7550 ),
 .UNSPECIFIED., .F., .F. ) 
 B_SPLINE_CURVE_WITH_KNOTS ( ( 3, 2, 2, 2, 2, 3 ),
 ( 0.4565217391304239314, 0.4586956521739021797, 0.4608695652173803725, 0.4630434782608585098, 0.4652173913043367026, 0.4673913043478149509 ),
 .UNSPECIFIED. ) 
 CURVE ( )  GEOMETRIC_REPRESENTATION_ITEM ( )  RATIONAL_B_SPLINE_CURVE ( ( 1.000000000000243805, 0.9510565162949098372, 1.000000000000000000, 0.9510565162951535312, 1.000000000000000000, 0.9510565162951535312, 1.000000000000000000, 0.9510565162951535312, 1.000000000000000000, 0.9510565162954047747, 0.9999999999997487565 ) ) 
 REPRESENTATION_ITEM ( '' )  );
#6242=VERTEX_POINT ( 'NONE', #54217 ) ;
#6245=CARTESIAN_POINT ( 'NONE',  ( -84.20499999999995566, -2.607480562269071545, -8.024999999999991473 ) ) ;
#6247=DIRECTION ( 'NONE',  ( 0.000000000000000000, 0.000000000000000000, 1.000000000000000000 ) ) ;
#6249=CARTESIAN_POINT ( 'NONE',  ( -79.64499999999999602, 4.716976649647091513, -6.492361379858946790 ) ) ;
#6264=ORIENTED_EDGE ( 'NONE', *, *, #19914, .F. ) ;
#6272=CARTESIAN_POINT ( 'NONE',  ( -117.2049999999999699, -2.607480562269071545, -8.024999999999991473 ) ) ;
#6276=CARTESIAN_POINT ( 'NONE',  ( -56.39292637653378648, 8.102448949553176405, 5.886773742842740909 ) ) ;
#6277=CARTESIAN_POINT ( 'NONE',  ( -68.30707362346618083, -10.01517768586948698, 6.132527647946031529E-16 ) ) ;
#6300=CARTESIAN_POINT ( 'NONE',  ( -146.9049999999999727, 2.607480562269068880, -8.024999999999993250 ) ) ;
#6305=CARTESIAN_POINT ( 'NONE',  ( -106.9429263765337907, 0.000000000000000000, 9.524999999999991473 ) ) ;
#6309=DIRECTION ( 'NONE',  ( 0.000000000000000000, 0.000000000000000000, 1.000000000000000000 ) ) ;
#6311=CARTESIAN_POINT ( 'NONE',  ( -57.20499999999996987, -2.607480562269071545, -8.024999999999991473 ) ) ;
#6312=ORIENTED_EDGE ( 'NONE', *, *, #22393, .F. ) ;
#6321=EDGE_CURVE ( 'NONE', #65527, #61162, #66635, .T. ) ;
#6328=CARTESIAN_POINT ( 'NONE',  ( -110.9949999999999903, -6.826472737025113702, 4.959722759717902107 ) ) ;
#6330=AXIS2_PLACEMENT_3D ( 'NONE', #54122, #54472, #65385 ) ;
#6331=CARTESIAN_POINT ( 'NONE',  ( -89.99499999999999034, -6.826472737025115478, 4.959722759717900331 ) ) ;
#6336=( BOUNDED_CURVE ( )  B_SPLINE_CURVE ( 2, ( #15462, #53076, #21745, #4870, #64301, #26313, #69582, #63950, #15797, #58679, #5536 ),
 .UNSPECIFIED., .F., .F. ) 
 B_SPLINE_CURVE_WITH_KNOTS ( ( 3, 2, 2, 2, 2, 3 ),
 ( 0.07608695652173741442, 0.07826086956521563498, 0.08043478260869382779, 0.08260869565217204835, 0.08478260869565025504, 0.08695652173912847560 ),
 .UNSPECIFIED. ) 
 CURVE ( )  GEOMETRIC_REPRESENTATION_ITEM ( )  RATIONAL_B_SPLINE_CURVE ( ( 1.000000000000038636, 0.9510565162951147844, 1.000000000000000000, 0.9510565162951535312, 1.000000000000000000, 0.9510565162951535312, 1.000000000000000000, 0.9510565162951535312, 1.000000000000000000, 0.9510565162951976070, 0.9999999999999559241 ) ) 
 REPRESENTATION_ITEM ( '' )  );
#6338=CARTESIAN_POINT ( 'NONE',  ( -120.2929263765337993, 3.094860106618428031, -9.524999999999993250 ) ) ;
#6340=CARTESIAN_POINT ( 'NONE',  ( -146.8449999999999989, -7.632228543268599452, 2.479861379858951054 ) ) ;
#6341=DIRECTION ( 'NONE',  ( -1.000000000000000000, -0.000000000000000000, -0.000000000000000000 ) ) ;
#6345=CARTESIAN_POINT ( 'NONE',  ( -47.24499999999998323, -4.716976649647093289, -6.492361379858945902 ) ) ;
#6354=CYLINDRICAL_SURFACE ( 'NONE', #48341, 9.524999999999991473 ) ;
#6355=FACE_OUTER_BOUND ( 'NONE', #3639, .T. ) ;
#6356=CARTESIAN_POINT ( 'NONE',  ( -151.1929263765338192, -10.01517768586948698, 6.132527647946031529E-16 ) ) ;
#6358=CARTESIAN_POINT ( 'NONE',  ( -144.6549999999999727, -7.632228543268600340, -2.479861379858950166 ) ) ;
#6362=CARTESIAN_POINT ( 'NONE',  ( -195.0000000000000000, 0.000000000000000000, 9.524999999999991473 ) ) ;
#6365=LINE ( 'NONE', #41195, #34331 ) ;
#6370=CARTESIAN_POINT ( 'NONE',  ( -56.15499999999997982, 7.632228543268600340, 2.479861379858949277 ) ) ;
#6371=CARTESIAN_POINT ( 'NONE',  ( -115.4949999999999903, 6.826472737025113702, -4.959722759717902107 ) ) ;
#6380=DIRECTION ( 'NONE',  ( -1.000000000000000000, 0.000000000000000000, -0.000000000000000000 ) ) ;
#6386=CARTESIAN_POINT ( 'NONE',  ( -176.0049999999999670, 6.826472737025116366, 4.959722759717898555 ) ) ;
#6387=ORIENTED_EDGE ( 'NONE', *, *, #36149, .T. ) ;
#6388=CARTESIAN_POINT ( 'NONE',  ( -87.95707362346617231, 9.058813317711329915, -2.943386871421373119 ) ) ;
#6396=CARTESIAN_POINT ( 'NONE',  ( -84.20499999999995566, -2.607480562269071545, -8.024999999999991473 ) ) ;
#6401=CARTESIAN_POINT ( 'NONE',  ( -69.80707362346613820, 10.01517768586948698, -1.839758294383808571E-15 ) ) ;
#6408=CARTESIAN_POINT ( 'NONE',  ( -99.35499999999998977, -4.716976649647093289, -6.492361379858945902 ) ) ;
#6410=CARTESIAN_POINT ( 'NONE',  ( -120.2949999999999733, -2.607480562269069768, 8.024999999999991473 ) ) ;
#6413=CARTESIAN_POINT ( 'NONE',  ( -19.99982264573705493, 11.99992610239912949, 0.3333660036662020043 ) ) ;
#6415=CARTESIAN_POINT ( 'NONE',  ( -149.2429263765338021, 5.598654528085804216, 7.705886871421366635 ) ) ;
#6417=CARTESIAN_POINT ( 'NONE',  ( -175.9449999999999932, -9.827790563157499189E-16, -8.024999999999991473 ) ) ;
#6422=AXIS2_PLACEMENT_3D ( 'NONE', #7766, #35565, #7091 ) ;
#6429=CARTESIAN_POINT ( 'NONE',  ( -65.69292637653380496, 10.01517768586948698, -1.839758294383808571E-15 ) ) ;
#6433=CARTESIAN_POINT ( 'NONE',  ( -142.0429263765338135, -9.058813317711329915, -2.943386871421370898 ) ) ;
#6439=CARTESIAN_POINT ( 'NONE',  ( -171.6550000000000011, -7.632228543268600340, -2.479861379858950166 ) ) ;
#6448=CARTESIAN_POINT ( 'NONE',  ( -80.15499999999998693, 7.632228543268600340, 2.479861379858949277 ) ) ;
#6455=CARTESIAN_POINT ( 'NONE',  ( -61.94499999999998607, -9.827790563157499189E-16, -8.024999999999991473 ) ) ;
#6466=CARTESIAN_POINT ( 'NONE',  ( -114.2049999999999699, -2.607480562269071545, -8.024999999999991473 ) ) ;
#6471=CARTESIAN_POINT ( 'NONE',  ( -151.2570736234661979, 5.598654528085800663, -7.705886871421367523 ) ) ;
#6474=CARTESIAN_POINT ( 'NONE',  ( -91.25707362346616947, 5.598654528085800663, -7.705886871421367523 ) ) ;
#6476=ORIENTED_EDGE ( 'NONE', *, *, #34768, .T. ) ;
#6478=CARTESIAN_POINT ( 'NONE',  ( -132.9549999999999841, -7.632228543268599452, 2.479861379858951054 ) ) ;
#6480=CARTESIAN_POINT ( 'NONE',  ( -146.0929263765342796, 3.094860106626500240, 9.524999999994133049 ) ) ;
#6482=CARTESIAN_POINT ( 'NONE',  ( -143.3949999999999818, -6.826472737025115478, -4.959722759717899443 ) ) ;
#6483=CARTESIAN_POINT ( 'NONE',  ( -125.9949999999999903, -6.826472737025113702, 4.959722759717902107 ) ) ;
#6488=CARTESIAN_POINT ( 'NONE',  ( -180.4429263765338192, -1.166476076187852838E-15, -9.524999999999991473 ) ) ;
#6490=CARTESIAN_POINT ( 'NONE',  ( -55.04499999999998039, 7.632228543268600340, 2.479861379858949277 ) ) ;
#6496=CARTESIAN_POINT ( 'NONE',  ( -75.20707362346615810, 3.094860106618433360, 9.524999999999991473 ) ) ;
#6497=CARTESIAN_POINT ( 'NONE',  ( -93.89292637653379359, -8.102448949553172852, -5.886773742842741797 ) ) ;
#6500=DIRECTION ( 'NONE',  ( -1.000000000000000000, -0.000000000000000000, -0.000000000000000000 ) ) ;
#6522=CARTESIAN_POINT ( 'NONE',  ( -119.3070736234661808, -10.01517768586948698, 6.132527647946031529E-16 ) ) ;
#6525=CARTESIAN_POINT ( 'NONE',  ( -87.29500000000000171, -2.607480562269069768, 8.024999999999991473 ) ) ;
#6535=DIRECTION ( 'NONE',  ( 1.000000000000000000, 0.000000000000000000, 0.000000000000000000 ) ) ;
#6537=CARTESIAN_POINT ( 'NONE',  ( -166.1070736234661638, 8.102448949553172852, -5.886773742842744461 ) ) ;
#6541=CARTESIAN_POINT ( 'NONE',  ( -174.5070736234661695, 8.102448949553176405, 5.886773742842740909 ) ) ;
#6545=CARTESIAN_POINT ( 'NONE',  ( -68.54292637653379927, 9.058813317711329915, 2.943386871421369566 ) ) ;
#6551=CARTESIAN_POINT ( 'NONE',  ( -149.0070736234661979, -8.102448949553174629, -5.886773742842741797 ) ) ;
#6554=CARTESIAN_POINT ( 'NONE',  ( -161.3050000000000068, 8.437984349512085203, -1.550032578732815448E-15 ) ) ;
#6558=CARTESIAN_POINT ( 'NONE',  ( -169.9449999999999932, -9.827790563157499189E-16, -8.024999999999991473 ) ) ;
#6560=CARTESIAN_POINT ( 'NONE',  ( -159.7450000000000045, 4.716976649647094177, 6.492361379858945902 ) ) ;
#6564=CARTESIAN_POINT ( 'NONE',  ( -89.39292637653379359, 8.102448949553176405, 5.886773742842740909 ) ) ;
#6567=CARTESIAN_POINT ( 'NONE',  ( -69.80499999999996419, -8.437984349512085203, 5.166775262442717831E-16 ) ) ;
#6572=CARTESIAN_POINT ( 'NONE',  ( -70.49499999999996191, 6.826472737025113702, -4.959722759717902107 ) ) ;
#6576=CARTESIAN_POINT ( 'NONE',  ( -177.1429263765338078, 5.598654528085800663, -7.705886871421367523 ) ) ;
#6583=EDGE_CURVE ( 'NONE', #67626, #12224, #46344, .T. ) ;
#6597=CARTESIAN_POINT ( 'NONE',  ( -69.35707362346617799, 5.598654528085804216, 7.705886871421366635 ) ) ;
#6599=CARTESIAN_POINT ( 'NONE',  ( -114.2049999999999699, -2.607480562269071545, -8.024999999999991473 ) ) ;
#6605=ORIENTED_EDGE ( 'NONE', *, *, #67628, .T. ) ;
#6612=CARTESIAN_POINT ( 'NONE',  ( -152.4570736234661581, -9.058813317711329915, 2.943386871421371787 ) ) ;
#6621=ORIENTED_EDGE ( 'NONE', *, *, #67944, .T. ) ;
#6623=ORIENTED_EDGE ( 'NONE', *, *, #61298, .F. ) ;
#6627=DIRECTION ( 'NONE',  ( -1.000000000000000000, -0.000000000000000000, -0.000000000000000000 ) ) ;
#6628=CARTESIAN_POINT ( 'NONE',  ( -145.5549999999999784, 0.000000000000000000, 8.024999999999991473 ) ) ;
#6640=CARTESIAN_POINT ( 'NONE',  ( -60.05499999999998550, -9.827790563157499189E-16, -8.024999999999991473 ) ) ;
#6664=CARTESIAN_POINT ( 'NONE',  ( -108.8949999999999960, 6.826472737025115478, 4.959722759717899443 ) ) ;
#6666=CARTESIAN_POINT ( 'NONE',  ( -74.39499999999999602, -6.826472737025115478, -4.959722759717899443 ) ) ;
#6670=ADVANCED_FACE ( 'NONE', ( #16193 ), #26685, .T. ) ;
#6677=EDGE_CURVE ( 'NONE', #68888, #35268, #51243, .T. ) ;
#6678=CARTESIAN_POINT ( 'NONE',  ( -121.4929263765337879, -8.102448949553172852, 5.886773742842742685 ) ) ;
#6680=CARTESIAN_POINT ( 'NONE',  ( -141.5950000000000273, 2.607480562269073321, 8.024999999999991473 ) ) ;
#6695=CARTESIAN_POINT ( 'NONE',  ( -150.5929263765342512, -3.094860106625624052, -9.524999999994767208 ) ) ;
#6697=CARTESIAN_POINT ( 'NONE',  ( -140.1550000000000011, 7.632228543268600340, 2.479861379858949277 ) ) ;
#6711=CARTESIAN_POINT ( 'NONE',  ( -94.55707362346616662, -1.166476076187852838E-15, -9.524999999999991473 ) ) ;
#6713=CARTESIAN_POINT ( 'NONE',  ( -59.60499999999998977, 6.826472737025113702, -4.959722759717902107 ) ) ;
#6728=CARTESIAN_POINT ( 'NONE',  ( -171.5049999999999386, -6.826472737025115478, -4.959722759717899443 ) ) ;
#6741=CARTESIAN_POINT ( 'NONE',  ( -88.40499999999997272, -2.607480562269069768, 8.024999999999991473 ) ) ;
#6742=VERTEX_POINT ( 'NONE', #1973 ) ;
#6745=CARTESIAN_POINT ( 'NONE',  ( -52.25707362346618368, 5.598654528085800663, -7.705886871421367523 ) ) ;
#6747=( BOUNDED_CURVE ( )  B_SPLINE_CURVE ( 2, ( #63740, #15588, #47985 ),
 .UNSPECIFIED., .F., .F. ) 
 B_SPLINE_CURVE_WITH_KNOTS ( ( 3, 3 ),
 ( 0.9891304347826086474, 0.9913043478260870067 ),
 .UNSPECIFIED. ) 
 CURVE ( )  GEOMETRIC_REPRESENTATION_ITEM ( )  RATIONAL_B_SPLINE_CURVE ( ( 1.000000000000000000, 0.9510565162951535312, 1.000000000000000000 ) ) 
 REPRESENTATION_ITEM ( '' )  );
#6754=CARTESIAN_POINT ( 'NONE',  ( -103.0449999999999875, 7.632228543268600340, 2.479861379858949277 ) ) ;
#6760=CARTESIAN_POINT ( 'NONE',  ( -15.00000000000000000, 10.90871211463571200, -5.000000000000000000 ) ) ;
#6762=CARTESIAN_POINT ( 'NONE',  ( -154.1929263765338192, -10.01517768586948698, 6.132527647946031529E-16 ) ) ;
#6764=CARTESIAN_POINT ( 'NONE',  ( -180.1450000000000102, -4.716976649647092401, 6.492361379858946790 ) ) ;
#6773=CARTESIAN_POINT ( 'NONE',  ( -64.94292637653380496, 0.000000000000000000, 9.524999999999991473 ) ) ;
#6782=ORIENTED_EDGE ( 'NONE', *, *, #66531, .F. ) ;
#6783=CARTESIAN_POINT ( 'NONE',  ( -171.2049999999999557, -2.607480562269071545, -8.024999999999991473 ) ) ;
#6785=CARTESIAN_POINT ( 'NONE',  ( -112.1929263765338050, -10.01517768586948698, 6.132527647946031529E-16 ) ) ;
#6786=DIRECTION ( 'NONE',  ( 0.000000000000000000, 0.000000000000000000, 1.000000000000000000 ) ) ;
#6795=CARTESIAN_POINT ( 'NONE',  ( -80.75499999999999545, 4.716976649647091513, -6.492361379858946790 ) ) ;
#6797=FACE_OUTER_BOUND ( 'NONE', #43811, .T. ) ;
#6798=CARTESIAN_POINT ( 'NONE',  ( -73.55707362346616662, -1.166476076187852838E-15, -9.524999999999991473 ) ) ;
#6804=CARTESIAN_POINT ( 'NONE',  ( -139.5570736234661808, -1.166476076187852838E-15, -9.524999999999991473 ) ) ;
#6806=CARTESIAN_POINT ( 'NONE',  ( -58.64499999999998892, 4.716976649647091513, -6.492361379858946790 ) ) ;
#6807=VECTOR ( 'NONE', #9761, 1000.000000000000000 ) ;
#6818=CARTESIAN_POINT ( 'NONE',  ( -110.4549999999999841, 7.632228543268599452, -2.479861379858951942 ) ) ;
#6825=CARTESIAN_POINT ( 'NONE',  ( -195.0000000000000000, 1.166476076187852838E-15, -9.524999999999991473 ) ) ;
#6827=CARTESIAN_POINT ( 'NONE',  ( -147.9570736234661581, 9.058813317711329915, -2.943386871421373119 ) ) ;
#6831=CARTESIAN_POINT ( 'NONE',  ( -81.65707362346617515, 9.058813317711329915, 2.943386871421369566 ) ) ;
#6832=CARTESIAN_POINT ( 'NONE',  ( -175.8549999999999898, 4.716976649647094177, 6.492361379858945902 ) ) ;
#6842=CARTESIAN_POINT ( 'NONE',  ( -127.4049999999999869, -2.607480562269069768, 8.024999999999991473 ) ) ;
#6843=CARTESIAN_POINT ( 'NONE',  ( -164.2429263765338021, 5.598654528085804216, 7.705886871421366635 ) ) ;
#6846=CARTESIAN_POINT ( 'NONE',  ( -144.8949999999999818, 6.826472737025116366, 4.959722759717898555 ) ) ;
#6848=CARTESIAN_POINT ( 'NONE',  ( -133.6449999999999818, 4.716976649647091513, -6.492361379858946790 ) ) ;
#6855=CARTESIAN_POINT ( 'NONE',  ( -179.9929263765337453, 8.102448949553171076, -5.886773742842744461 ) ) ;
#6857=CARTESIAN_POINT ( 'NONE',  ( -63.59499999999997755, 2.607480562269073321, 8.024999999999991473 ) ) ;
#6862=CARTESIAN_POINT ( 'NONE',  ( -75.95707362346617231, 9.058813317711329915, -2.943386871421373119 ) ) ;
#6864=CARTESIAN_POINT ( 'NONE',  ( -91.34292637653381064, -9.058813317711329915, 2.943386871421371787 ) ) ;
#6866=CARTESIAN_POINT ( 'NONE',  ( -103.5570736234661808, -1.166476076187852838E-15, -9.524999999999991473 ) ) ;
#6867=DIRECTION ( 'NONE',  ( 0.000000000000000000, 0.000000000000000000, 1.000000000000000000 ) ) ;
#6870=CARTESIAN_POINT ( 'NONE',  ( -79.25707362346618368, 5.598654528085800663, -7.705886871421367523 ) ) ;
#6872=CARTESIAN_POINT ( 'NONE',  ( -91.55707362346616662, -1.166476076187852838E-15, -9.524999999999991473 ) ) ;
#6886=CARTESIAN_POINT ( 'NONE',  ( -116.7570736234661695, -5.598654528085801552, 7.705886871421367523 ) ) ;
#6888=ORIENTED_EDGE ( 'NONE', *, *, #53915, .T. ) ;
#6893=CARTESIAN_POINT ( 'NONE',  ( -94.94499999999999318, -9.827790563157499189E-16, -8.024999999999991473 ) ) ;
#6899=EDGE_LOOP ( 'NONE', ( #44931, #46945, #27793, #23962 ) ) ;
#6915=CARTESIAN_POINT ( 'NONE',  ( -114.6570736234661751, 9.058813317711329915, 2.943386871421369566 ) ) ;
#6923=EDGE_CURVE ( 'NONE', #23187, #51098, #39153, .T. ) ;
#6926=CARTESIAN_POINT ( 'NONE',  ( -161.1550000000000011, 7.632228543268600340, 2.479861379858949277 ) ) ;
#6930=CARTESIAN_POINT ( 'NONE',  ( -177.2950000000000159, -2.607480562269069768, 8.024999999999991473 ) ) ;
#6931=CARTESIAN_POINT ( 'NONE',  ( -158.8449999999999989, -7.632228543268599452, 2.479861379858951054 ) ) ;
#6936=CARTESIAN_POINT ( 'NONE',  ( -68.60499999999996135, 6.826472737025113702, -4.959722759717902107 ) ) ;
#6940=CARTESIAN_POINT ( 'NONE',  ( -69.29499999999998749, -2.607480562269069768, 8.024999999999991473 ) ) ;
#6945=CARTESIAN_POINT ( 'NONE',  ( -177.4429263765338192, -1.166476076187852838E-15, -9.524999999999991473 ) ) ;
#6968=CARTESIAN_POINT ( 'NONE',  ( -111.6549999999999869, -7.632228543268600340, -2.479861379858950166 ) ) ;
#6969=ORIENTED_EDGE ( 'NONE', *, *, #17028, .T. ) ;
#6991=DIRECTION ( 'NONE',  ( -1.000000000000000000, -0.000000000000000000, -0.000000000000000000 ) ) ;
#6995=ORIENTED_EDGE ( 'NONE', *, *, #16087, .F. ) ;
#6999=DIRECTION ( 'NONE',  ( 0.000000000000000000, 0.000000000000000000, 1.000000000000000000 ) ) ;
#7001=CARTESIAN_POINT ( 'NONE',  ( -138.0549999999999784, -9.827790563157499189E-16, -8.024999999999991473 ) ) ;
#7007=( NAMED_UNIT ( * ) PLANE_ANGLE_UNIT ( ) SI_UNIT ( $, .RADIAN. ) );
#7014=CARTESIAN_POINT ( 'NONE',  ( -51.50499999999999545, -6.826472737025115478, -4.959722759717899443 ) ) ;
#7026=CARTESIAN_POINT ( 'NONE',  ( -103.1949999999999932, 8.437984349512086979, -1.550032578732815448E-15 ) ) ;
#7028=CARTESIAN_POINT ( 'NONE',  ( -81.14499999999998181, -4.716976649647092401, 6.492361379858946790 ) ) ;
#7037=CARTESIAN_POINT ( 'NONE',  ( -119.6929263765338192, 10.01517768586948698, -1.839758294383808571E-15 ) ) ;
#7040=CARTESIAN_POINT ( 'NONE',  ( -141.4449999999999932, 0.000000000000000000, 8.024999999999991473 ) ) ;
#7057=CARTESIAN_POINT ( 'NONE',  ( -142.5549999999999784, 0.000000000000000000, 8.024999999999991473 ) ) ;
#7075=CARTESIAN_POINT ( 'NONE',  ( -54.80499999999999261, -8.437984349512086979, 5.166775262442717831E-16 ) ) ;
#7091=DIRECTION ( 'NONE',  ( -0.000000000000000000, 0.000000000000000000, 1.000000000000000000 ) ) ;
#7093=CARTESIAN_POINT ( 'NONE',  ( -158.7549999999999670, 4.716976649647091513, -6.492361379858946790 ) ) ;
#7103=CARTESIAN_POINT ( 'NONE',  ( -57.44292637653381206, -1.166476076187852838E-15, -9.524999999999991473 ) ) ;
#7105=CARTESIAN_POINT ( 'NONE',  ( -89.45499999999999829, 7.632228543268599452, -2.479861379858951942 ) ) ;
#7110=CARTESIAN_POINT ( 'NONE',  ( -151.1070736234661638, 8.102448949553172852, -5.886773742842744461 ) ) ;
#7118=CARTESIAN_POINT ( 'NONE',  ( -109.7950000000000017, 2.607480562269068880, -8.024999999999993250 ) ) ;
#7124=CARTESIAN_POINT ( 'NONE',  ( -152.0929263765338249, 3.094860106618433360, 9.524999999999991473 ) ) ;
#7125=AXIS2_PLACEMENT_3D ( 'NONE', #31619, #20738, #15480 ) ;
#7127=CARTESIAN_POINT ( 'NONE',  ( -162.7450000000000045, 4.716976649647094177, 6.492361379858945902 ) ) ;
#7133=CARTESIAN_POINT ( 'NONE',  ( -70.94292637653380496, 0.000000000000000000, 9.524999999999991473 ) ) ;
#7143=CARTESIAN_POINT ( 'NONE',  ( -167.4549999999999841, 7.632228543268599452, -2.479861379858951942 ) ) ;
#7158=CARTESIAN_POINT ( 'NONE',  ( -87.20499999999998408, -2.607480562269071545, -8.024999999999991473 ) ) ;
#7159=DIRECTION ( 'NONE',  ( -1.000000000000000000, -0.000000000000000000, -0.000000000000000000 ) ) ;
#7170=CARTESIAN_POINT ( 'NONE',  ( -139.8570736234661638, -5.598654528085803328, -7.705886871421366635 ) ) ;
#7172=CARTESIAN_POINT ( 'NONE',  ( -62.69499999999998607, -8.437984349512085203, 5.166775262442717831E-16 ) ) ;
#7181=CARTESIAN_POINT ( 'NONE',  ( -51.29499999999997328, -2.607480562269069768, 8.024999999999991473 ) ) ;
#7187=CARTESIAN_POINT ( 'NONE',  ( -110.3049999999999926, 8.437984349512085203, -1.550032578732815448E-15 ) ) ;
#7193=CARTESIAN_POINT ( 'NONE',  ( -155.0070736234661695, -8.102448949553172852, -5.886773742842741797 ) ) ;
#7196=CARTESIAN_POINT ( 'NONE',  ( -82.25707362346616947, 5.598654528085800663, -7.705886871421367523 ) ) ;
#7199=CARTESIAN_POINT ( 'NONE',  ( -95.84292637653379643, 9.058813317711329915, -2.943386871421373119 ) ) ;
#7204=CARTESIAN_POINT ( 'NONE',  ( -128.6049999999999898, 6.826472737025113702, -4.959722759717902107 ) ) ;
#7205=CARTESIAN_POINT ( 'NONE',  ( -165.2929263765340693, 3.094860106614496065, -9.525000000002851408 ) ) ;
#7208=CARTESIAN_POINT ( 'NONE',  ( -139.7950000000000159, 2.607480562269068880, -8.024999999999993250 ) ) ;
#7210=CARTESIAN_POINT ( 'NONE',  ( -129.8949999999999818, 6.826472737025115478, 4.959722759717899443 ) ) ;
#7216=CARTESIAN_POINT ( 'NONE',  ( -184.9429263765338192, 0.000000000000000000, 9.524999999999991473 ) ) ;
#7217=DIRECTION ( 'NONE',  ( 0.000000000000000000, 0.000000000000000000, 1.000000000000000000 ) ) ;
#7218=CARTESIAN_POINT ( 'NONE',  ( -47.39499999999998181, -6.826472737025115478, -4.959722759717899443 ) ) ;
#7225=CARTESIAN_POINT ( 'NONE',  ( -98.24292637653380211, 5.598654528085804216, 7.705886871421366635 ) ) ;
#7246=CARTESIAN_POINT ( 'NONE',  ( -115.5570736234661808, -1.166476076187852838E-15, -9.524999999999991473 ) ) ;
#7255=CARTESIAN_POINT ( 'NONE',  ( -96.14499999999999602, -4.716976649647092401, 6.492361379858946790 ) ) ;
#7272=CARTESIAN_POINT ( 'NONE',  ( -179.3070736234661524, -10.01517768586948698, 6.132527647946031529E-16 ) ) ;
#7276=CARTESIAN_POINT ( 'NONE',  ( -109.7070736234661581, -3.094860106618431139, -9.524999999999991473 ) ) ;
#7279=CARTESIAN_POINT ( 'NONE',  ( -85.40707362346616094, 3.094860106618428031, -9.524999999999993250 ) ) ;
#7286=CARTESIAN_POINT ( 'NONE',  ( -157.5550000000000068, 0.000000000000000000, 8.024999999999991473 ) ) ;
#7288=CARTESIAN_POINT ( 'NONE',  ( -183.7648598996489113, -7.758193185839872719, -4.080356100732527302 ) ) ;
#7289=CARTESIAN_POINT ( 'NONE',  ( -162.5949999999999704, 2.607480562269073321, 8.024999999999991473 ) ) ;
#7290=CARTESIAN_POINT ( 'NONE',  ( -156.7450000000000045, 4.716976649647094177, 6.492361379858945902 ) ) ;
#7293=CARTESIAN_POINT ( 'NONE',  ( -67.94292637653380496, 0.000000000000000000, 9.524999999999991473 ) ) ;
#7296=CARTESIAN_POINT ( 'NONE',  ( -73.70499999999998408, 2.607480562269073321, 8.024999999999991473 ) ) ;
#7300=CARTESIAN_POINT ( 'NONE',  ( -75.74499999999999034, 4.716976649647094177, 6.492361379858945902 ) ) ;
#7316=CARTESIAN_POINT ( 'NONE',  ( -119.5429263765338135, 9.058813317711329915, 2.943386871421369566 ) ) ;
#7328=CARTESIAN_POINT ( 'NONE',  ( -102.5049999999999812, -6.826472737025113702, -4.959722759717900331 ) ) ;
#7333=CARTESIAN_POINT ( 'NONE',  ( -68.75707362346616947, -5.598654528085801552, 7.705886871421367523 ) ) ;
#7343=EDGE_LOOP ( 'NONE', ( #49691, #5233, #33704, #53413 ) ) ;
#7350=EDGE_CURVE ( 'NONE', #55574, #54295, #58426, .T. ) ;
#7359=CARTESIAN_POINT ( 'NONE',  ( -136.4050000000000296, -2.607480562269069768, 8.024999999999991473 ) ) ;
#7363=DIRECTION ( 'NONE',  ( -1.000000000000000000, -0.000000000000000000, -0.000000000000000000 ) ) ;
#7369=CARTESIAN_POINT ( 'NONE',  ( -51.35499999999998266, -4.716976649647093289, -6.492361379858945902 ) ) ;
#7385=CARTESIAN_POINT ( 'NONE',  ( -101.0949999999999847, -2.607480562269071545, -8.024999999999991473 ) ) ;
#7387=CARTESIAN_POINT ( 'NONE',  ( -82.64499999999998181, 4.716976649647091513, -6.492361379858946790 ) ) ;
#7397=CARTESIAN_POINT ( 'NONE',  ( -118.1929263765337907, -10.01517768586948698, 6.132527647946031529E-16 ) ) ;
#7399=CARTESIAN_POINT ( 'NONE',  ( -139.1950000000000216, 8.437984349512085203, -1.550032578732815448E-15 ) ) ;
#7402=EDGE_CURVE ( 'NONE', #57125, #39571, #56148, .T. ) ;
#7418=CARTESIAN_POINT ( 'NONE',  ( -138.3550000000000182, -4.716976649647093289, -6.492361379858945902 ) ) ;
#7434=CARTESIAN_POINT ( 'NONE',  ( -54.20499999999997698, -2.607480562269071545, -8.024999999999991473 ) ) ;
#7447=CARTESIAN_POINT ( 'NONE',  ( -166.1049999999999898, -6.826472737025115478, 4.959722759717900331 ) ) ;
#7448=ORIENTED_EDGE ( 'NONE', *, *, #48281, .T. ) ;
#7457=CARTESIAN_POINT ( 'NONE',  ( -77.90500000000000114, 2.607480562269068880, -8.024999999999993250 ) ) ;
#7460=CARTESIAN_POINT ( 'NONE',  ( -84.05707362346618083, 0.000000000000000000, 9.524999999999991473 ) ) ;
#7468=CARTESIAN_POINT ( 'NONE',  ( -104.8449999999999989, -7.632228543268599452, 2.479861379858951054 ) ) ;
#7472=DIRECTION ( 'NONE',  ( -1.000000000000000000, -0.000000000000000000, -0.000000000000000000 ) ) ;
#7473=CARTESIAN_POINT ( 'NONE',  ( -155.9929263765338021, 8.102448949553171076, -5.886773742842744461 ) ) ;
#7474=CARTESIAN_POINT ( 'NONE',  ( -163.9449999999999932, -9.827790563157499189E-16, -8.024999999999991473 ) ) ;
#7481=CARTESIAN_POINT ( 'NONE',  ( -65.24292637653380211, 5.598654528085804216, 7.705886871421366635 ) ) ;
#7484=CARTESIAN_POINT ( 'NONE',  ( -141.4429263765337907, -1.166476076187852838E-15, -9.524999999999991473 ) ) ;
#7490=CARTESIAN_POINT ( 'NONE',  ( -168.8049999999999500, -8.437984349512086979, 5.166775262442717831E-16 ) ) ;
#7492=EDGE_LOOP ( 'NONE', ( #37708, #39844, #19222, #26498 ) ) ;
#7498=CARTESIAN_POINT ( 'NONE',  ( -87.95499999999999829, -7.632228543268599452, 2.479861379858951054 ) ) ;
#7511=CARTESIAN_POINT ( 'NONE',  ( -54.44499999999999318, 0.000000000000000000, 8.024999999999991473 ) ) ;
#7519=CARTESIAN_POINT ( 'NONE',  ( -55.04499999999998039, 7.632228543268600340, 2.479861379858949277 ) ) ;
#7523=CARTESIAN_POINT ( 'NONE',  ( -105.3549999999999898, -4.716976649647093289, -6.492361379858945902 ) ) ;
#7527=CARTESIAN_POINT ( 'NONE',  ( -152.7570736234661979, -5.598654528085801552, 7.705886871421367523 ) ) ;
#7528=CARTESIAN_POINT ( 'NONE',  ( -59.00707362346617657, -8.102448949553174629, -5.886773742842741797 ) ) ;
#7530=CARTESIAN_POINT ( 'NONE',  ( -80.60707362346614957, -8.102448949553172852, 5.886773742842742685 ) ) ;
#7533=ORIENTED_EDGE ( 'NONE', *, *, #35912, .F. ) ;
#7536=AXIS2_PLACEMENT_3D ( 'NONE', #44176, #53970, #5772 ) ;
#7537=CARTESIAN_POINT ( 'NONE',  ( -135.6550000000000011, -7.632228543268600340, -2.479861379858950166 ) ) ;
#7540=CARTESIAN_POINT ( 'NONE',  ( -147.4429263765338192, -1.166476076187852838E-15, -9.524999999999991473 ) ) ;
#7542=CARTESIAN_POINT ( 'NONE',  ( -139.4949999999999761, 6.826472737025113702, -4.959722759717902107 ) ) ;
#7544=CARTESIAN_POINT ( 'NONE',  ( -125.0949999999999847, -2.607480562269071545, -8.024999999999991473 ) ) ;
#7547=EDGE_CURVE ( 'NONE', #31166, #57680, #8522, .T. ) ;
#7550=CARTESIAN_POINT ( 'NONE',  ( -120.4429263765338050, -1.166476076187852838E-15, -9.524999999999991473 ) ) ;
#7551=CARTESIAN_POINT ( 'NONE',  ( -178.3429263765338249, -9.058813317711329915, 2.943386871421371787 ) ) ;
#7552=CARTESIAN_POINT ( 'NONE',  ( -51.44499999999999318, 0.000000000000000000, 8.024999999999991473 ) ) ;
#7560=CARTESIAN_POINT ( 'NONE',  ( -99.89292637653380780, -8.102448949553172852, -5.886773742842741797 ) ) ;
#7569=ORIENTED_EDGE ( 'NONE', *, *, #9138, .F. ) ;
#7573=ORIENTED_EDGE ( 'NONE', *, *, #35279, .T. ) ;
#7577=DIRECTION ( 'NONE',  ( -1.000000000000000000, -0.000000000000000000, -0.000000000000000000 ) ) ;
#7581=CARTESIAN_POINT ( 'NONE',  ( -94.49292637653380211, -8.102448949553174629, 5.886773742842742685 ) ) ;
#7586=CARTESIAN_POINT ( 'NONE',  ( -83.84499999999998465, -7.632228543268599452, 2.479861379858951054 ) ) ;
#7596=VERTEX_POINT ( 'NONE', #31654 ) ;
#7599=DIRECTION ( 'NONE',  ( -0.000000000000000000, 1.000000000000000000, -0.000000000000000000 ) ) ;
#7602=CARTESIAN_POINT ( 'NONE',  ( -177.5070736234661979, 8.102448949553176405, 5.886773742842740909 ) ) ;
#7604=CARTESIAN_POINT ( 'NONE',  ( -114.8070736234661808, 10.01517768586948698, -1.839758294383808571E-15 ) ) ;
#7611=CARTESIAN_POINT ( 'NONE',  ( -160.5550000000000068, 0.000000000000000000, 8.024999999999991473 ) ) ;
#7615=CARTESIAN_POINT ( 'NONE',  ( -167.6949999999999363, -8.437984349512085203, 5.166775262442717831E-16 ) ) ;
#7616=CARTESIAN_POINT ( 'NONE',  ( -161.3949999999999818, -6.826472737025113702, -4.959722759717900331 ) ) ;
#7617=ORIENTED_EDGE ( 'NONE', *, *, #43345, .T. ) ;
#7623=CARTESIAN_POINT ( 'NONE',  ( -72.50499999999998124, -6.826472737025115478, -4.959722759717899443 ) ) ;
#7627=CARTESIAN_POINT ( 'NONE',  ( -67.94499999999999318, -9.827790563157499189E-16, -8.024999999999991473 ) ) ;
#7630=EDGE_CURVE ( 'NONE', #19619, #41595, #29667, .T. ) ;
#7646=EDGE_LOOP ( 'NONE', ( #9050, #60160, #58101, #9662 ) ) ;
#7656=( BOUNDED_CURVE ( )  B_SPLINE_CURVE ( 2, ( #5868, #865, #65320, #48843, #69554, #38636, #541, #64960, #59684, #60040, #11852 ),
 .UNSPECIFIED., .F., .F. ) 
 B_SPLINE_CURVE_WITH_KNOTS ( ( 3, 2, 2, 2, 2, 3 ),
 ( 0.1630434782608656263, 0.1652173913043438191, 0.1673913043478220397, 0.1695652173913002603, 0.1717391304347784808, 0.1739130434782566736 ),
 .UNSPECIFIED. ) 
 CURVE ( )  GEOMETRIC_REPRESENTATION_ITEM ( )  RATIONAL_B_SPLINE_CURVE ( ( 1.000000000000088818, 0.9510565162950648244, 1.000000000000000000, 0.9510565162951535312, 1.000000000000000000, 0.9510565162951535312, 1.000000000000000000, 0.9510565162951535312, 1.000000000000000000, 0.9510565162952479001, 0.9999999999999056310 ) ) 
 REPRESENTATION_ITEM ( '' )  );
#7658=CARTESIAN_POINT ( 'NONE',  ( -118.9449999999999932, -9.827790563157499189E-16, -8.024999999999991473 ) ) ;
#7664=CARTESIAN_POINT ( 'NONE',  ( -10.04082649006660155, -11.98303716040044264, -0.6588920121501417038 ) ) ;
#7678=CARTESIAN_POINT ( 'NONE',  ( -134.9050000000000011, 2.607480562269068880, -8.024999999999993250 ) ) ;
#7682=VECTOR ( 'NONE', #36178, 1000.000000000000000 ) ;
#7686=CARTESIAN_POINT ( 'NONE',  ( -157.6429263765338078, -5.598654528085801552, 7.705886871421367523 ) ) ;
#7693=CARTESIAN_POINT ( 'NONE',  ( -49.10499999999998977, -6.826472737025115478, 4.959722759717900331 ) ) ;
#7695=CARTESIAN_POINT ( 'NONE',  ( -124.1070736234661638, 8.102448949553172852, -5.886773742842744461 ) ) ;
#7707=CARTESIAN_POINT ( 'NONE',  ( -101.7549999999999812, 4.716976649647091513, -6.492361379858946790 ) ) ;
#7712=CARTESIAN_POINT ( 'NONE',  ( -103.6449999999999818, 4.716976649647091513, -6.492361379858946790 ) ) ;
#7714=CARTESIAN_POINT ( 'NONE',  ( -76.34499999999998465, 7.632228543268599452, -2.479861379858951942 ) ) ;
#7718=CARTESIAN_POINT ( 'NONE',  ( -183.0000000000000000, 0.000000000000000000, 0.000000000000000000 ) ) ;
#7724=CARTESIAN_POINT ( 'NONE',  ( -119.3929263765337794, 8.102448949553176405, 5.886773742842740909 ) ) ;
#7725=ADVANCED_FACE ( 'NONE', ( #44682 ), #13298, .T. ) ;
#7726=CARTESIAN_POINT ( 'NONE',  ( -134.0949999999999420, -2.607480562269071545, -8.024999999999991473 ) ) ;
#7739=CARTESIAN_POINT ( 'NONE',  ( -126.8070736234661666, 10.01517768586948698, -1.839758294383808966E-15 ) ) ;
#7741=CARTESIAN_POINT ( 'NONE',  ( -136.4049999999999727, -2.607480562269069768, 8.024999999999991473 ) ) ;
#7744=CARTESIAN_POINT ( 'NONE',  ( -171.4429263765337907, -1.166476076187852838E-15, -9.524999999999991473 ) ) ;
#7752=CARTESIAN_POINT ( 'NONE',  ( -49.10499999999998266, -6.826472737025113702, 4.959722759717902107 ) ) ;
#7766=CARTESIAN_POINT ( 'NONE',  ( -190.0000000000000000, 5.499999999999984901, 0.000000000000000000 ) ) ;
#7768=CARTESIAN_POINT ( 'NONE',  ( -166.2549999999999955, -4.716976649647092401, 6.492361379858946790 ) ) ;
#7778=EDGE_LOOP ( 'NONE', ( #59862, #62005, #12499, #57393 ) ) ;
#7781=DIRECTION ( 'NONE',  ( 0.000000000000000000, 0.000000000000000000, 1.000000000000000000 ) ) ;
#7783=CARTESIAN_POINT ( 'NONE',  ( -74.15499999999998693, 7.632228543268600340, 2.479861379858949277 ) ) ;
#7787=CARTESIAN_POINT ( 'NONE',  ( -63.80707362346617373, 10.01517768586948698, -1.839758294383808966E-15 ) ) ;
#7797=CARTESIAN_POINT ( 'NONE',  ( -106.6449999999999960, 4.716976649647091513, -6.492361379858946790 ) ) ;
#7798=DIRECTION ( 'NONE',  ( 0.000000000000000000, 0.000000000000000000, 1.000000000000000000 ) ) ;
#7804=CARTESIAN_POINT ( 'NONE',  ( -147.2929263765338135, 3.094860106618428031, -9.524999999999993250 ) ) ;
#7805=CARTESIAN_POINT ( 'NONE',  ( -162.4449999999999932, 0.000000000000000000, 8.024999999999991473 ) ) ;
#7810=CYLINDRICAL_SURFACE ( 'NONE', #54034, 9.524999999999991473 ) ;
#7825=CARTESIAN_POINT ( 'NONE',  ( -164.0049999999999955, 6.826472737025115478, 4.959722759717899443 ) ) ;
#7837=CARTESIAN_POINT ( 'NONE',  ( -86.30499999999997840, 8.437984349512086979, -1.550032578732815448E-15 ) ) ;
#7843=EDGE_CURVE ( 'NONE', #18409, #40144, #64945, .T. ) ;
#7846=CARTESIAN_POINT ( 'NONE',  ( -54.14499999999999602, -4.716976649647092401, 6.492361379858946790 ) ) ;
#7854=CARTESIAN_POINT ( 'NONE',  ( -50.09499999999996334, -2.607480562269071545, -8.024999999999991473 ) ) ;
#7859=CARTESIAN_POINT ( 'NONE',  ( -109.2549999999999955, -4.716976649647092401, 6.492361379858946790 ) ) ;
#7866=CARTESIAN_POINT ( 'NONE',  ( -137.6070736234661922, -8.102448949553172852, 5.886773742842742685 ) ) ;
#7870=CARTESIAN_POINT ( 'NONE',  ( -80.15707362346617515, -9.058813317711329915, -2.943386871421370898 ) ) ;
#7872=CARTESIAN_POINT ( 'NONE',  ( -94.94292637653380496, 0.000000000000000000, 9.524999999999991473 ) ) ;
#7879=CARTESIAN_POINT ( 'NONE',  ( -117.8050000000000068, -8.437984349512085203, 5.166775262442717831E-16 ) ) ;
#7883=CARTESIAN_POINT ( 'NONE',  ( -135.1449999999999818, -4.716976649647092401, 6.492361379858946790 ) ) ;
#7886=CARTESIAN_POINT ( 'NONE',  ( -118.9449999999999932, -9.827790563157499189E-16, -8.024999999999991473 ) ) ;
#7889=CARTESIAN_POINT ( 'NONE',  ( -146.4570736234661865, -9.058813317711329915, 2.943386871421371787 ) ) ;
#7893=CARTESIAN_POINT ( 'NONE',  ( -176.5429263765338135, 9.058813317711329915, 2.943386871421369566 ) ) ;
#7903=CARTESIAN_POINT ( 'NONE',  ( -92.69292637653377653, 10.01517768586948698, -1.839758294383808571E-15 ) ) ;
#7918=CARTESIAN_POINT ( 'NONE',  ( -64.79292637653379927, -3.094860106618429807, 9.524999999999991473 ) ) ;
#7934=CARTESIAN_POINT ( 'NONE',  ( -79.64499999999999602, 4.716976649647091513, -6.492361379858946790 ) ) ;
#7937=EDGE_CURVE ( 'NONE', #37066, #33115, #20681, .T. ) ;
#7943=CARTESIAN_POINT ( 'NONE',  ( -76.04292637653379927, -9.058813317711329915, -2.943386871421370898 ) ) ;
#7950=DIRECTION ( 'NONE',  ( 0.000000000000000000, 0.000000000000000000, 1.000000000000000000 ) ) ;
#7953=CARTESIAN_POINT ( 'NONE',  ( -177.6570736234662036, 9.058813317711329915, 2.943386871421369566 ) ) ;
#7957=CARTESIAN_POINT ( 'NONE',  ( -110.3070736234661808, -10.01517768586948698, 6.132527647946031529E-16 ) ) ;
#7962=CARTESIAN_POINT ( 'NONE',  ( -84.80707362346619504, 10.01517768586948698, -1.839758294383808966E-15 ) ) ;
#7967=CARTESIAN_POINT ( 'NONE',  ( -154.5550000000000068, 0.000000000000000000, 8.024999999999991473 ) ) ;
#7971=CARTESIAN_POINT ( 'NONE',  ( -167.0949999999999704, -2.607480562269071545, -8.024999999999991473 ) ) ;
#7972=CARTESIAN_POINT ( 'NONE',  ( -157.7949999999999875, 2.607480562269069324, -8.024999999999993250 ) ) ;
#7979=CARTESIAN_POINT ( 'NONE',  ( -77.45499999999998408, 7.632228543268599452, -2.479861379858951942 ) ) ;
#7982=CARTESIAN_POINT ( 'NONE',  ( -168.2929263765340124, 3.094860106615100914, -9.525000000002410872 ) ) ;
#7983=CARTESIAN_POINT ( 'NONE',  ( -72.14499999999998181, -4.716976649647092401, 6.492361379858946790 ) ) ;
#7996=ORIENTED_EDGE ( 'NONE', *, *, #59623, .F. ) ;
#8002=ORIENTED_EDGE ( 'NONE', *, *, #65124, .T. ) ;
#8010=DIRECTION ( 'NONE',  ( -1.000000000000000000, -0.000000000000000000, -0.000000000000000000 ) ) ;
#8016=CARTESIAN_POINT ( 'NONE',  ( -107.9949999999999761, -6.826472737025115478, 4.959722759717900331 ) ) ;
#8018=ADVANCED_FACE ( 'NONE', ( #44601 ), #31909, .T. ) ;
#8021=CARTESIAN_POINT ( 'NONE',  ( -11.94445006289030786, -11.32557150108030619, 3.970945727933070657 ) ) ;
#8037=CARTESIAN_POINT ( 'NONE',  ( -137.1550000000000011, 7.632228543268600340, 2.479861379858949277 ) ) ;
#8038=DIRECTION ( 'NONE',  ( 0.000000000000000000, 0.000000000000000000, 1.000000000000000000 ) ) ;
#8045=CARTESIAN_POINT ( 'NONE',  ( -157.9429263765338192, 0.000000000000000000, 9.524999999999991473 ) ) ;
#8048=ORIENTED_EDGE ( 'NONE', *, *, #7547, .T. ) ;
#8055=CARTESIAN_POINT ( 'NONE',  ( -59.15707362346617515, -9.058813317711329915, -2.943386871421370898 ) ) ;
#8058=CARTESIAN_POINT ( 'NONE',  ( -178.1070736234661638, 8.102448949553172852, -5.886773742842744461 ) ) ;
#8060=CARTESIAN_POINT ( 'NONE',  ( -160.7070736234664423, -3.094860106623137153, -9.524999999996571987 ) ) ;
#8063=CARTESIAN_POINT ( 'NONE',  ( -104.9049999999999869, 2.607480562269068880, -8.024999999999993250 ) ) ;
#8068=CARTESIAN_POINT ( 'NONE',  ( -104.3949999999999818, -6.826472737025113702, -4.959722759717900331 ) ) ;
#8070=CARTESIAN_POINT ( 'NONE',  ( -82.04499999999998749, 7.632228543268600340, 2.479861379858949277 ) ) ;
#8082=CARTESIAN_POINT ( 'NONE',  ( -117.1429263765337936, 5.598654528085800663, -7.705886871421367523 ) ) ;
#8083=CARTESIAN_POINT ( 'NONE',  ( -133.7949999999999875, 2.607480562269068880, -8.024999999999993250 ) ) ;
#8089=ORIENTED_EDGE ( 'NONE', *, *, #9243, .T. ) ;
#8090=ORIENTED_EDGE ( 'NONE', *, *, #52589, .T. ) ;
#8093=CARTESIAN_POINT ( 'NONE',  ( -62.09292637653379643, 3.094860106618433360, 9.524999999999991473 ) ) ;
#8100=CARTESIAN_POINT ( 'NONE',  ( -128.9050000000000011, 2.607480562269069324, -8.024999999999993250 ) ) ;
#8104=CARTESIAN_POINT ( 'NONE',  ( -119.7570736234661695, -5.598654528085801552, 7.705886871421367523 ) ) ;
#8107=CARTESIAN_POINT ( 'NONE',  ( -172.9429263765337907, 0.000000000000000000, 9.524999999999991473 ) ) ;
#8129=EDGE_LOOP ( 'NONE', ( #48185, #53169, #30687, #54656 ) ) ;
#8132=EDGE_CURVE ( 'NONE', #67977, #26061, #15301, .T. ) ;
#8137=CARTESIAN_POINT ( 'NONE',  ( -164.9049999999999443, 2.607480562269068880, -8.024999999999993250 ) ) ;
#8150=CYLINDRICAL_SURFACE ( 'NONE', #49624, 9.524999999999991473 ) ;
#8154=CARTESIAN_POINT ( 'NONE',  ( -75.35499999999998977, -4.716976649647093289, -6.492361379858945902 ) ) ;
#8157=CARTESIAN_POINT ( 'NONE',  ( -64.10707362346616378, 8.102448949553172852, -5.886773742842744461 ) ) ;
#8158=CARTESIAN_POINT ( 'NONE',  ( -150.6570736234661751, 9.058813317711329915, 2.943386871421369566 ) ) ;
#8159=VECTOR ( 'NONE', #15960, 1000.000000000000000 ) ;
#8165=CARTESIAN_POINT ( 'NONE',  ( -103.4949999999999761, 6.826472737025113702, -4.959722759717902107 ) ) ;
#8169=ADVANCED_FACE ( 'NONE', ( #53260 ), #61086, .T. ) ;
#8173=CARTESIAN_POINT ( 'NONE',  ( -147.7429263765338021, -5.598654528085803328, -7.705886871421366635 ) ) ;
#8174=CARTESIAN_POINT ( 'NONE',  ( -169.6449999999999818, 4.716976649647091513, -6.492361379858946790 ) ) ;
#8182=ORIENTED_EDGE ( 'NONE', *, *, #41816, .T. ) ;
#8190=CARTESIAN_POINT ( 'NONE',  ( -164.7549999999999955, 4.716976649647091513, -6.492361379858946790 ) ) ;
#8198=FACE_OUTER_BOUND ( 'NONE', #63656, .T. ) ;
#8201=( BOUNDED_CURVE ( )  B_SPLINE_CURVE ( 2, ( #5121, #58252, #16425, #37188, #25883, #31500, #15383, #9747, #4070, #42135, #58953 ),
 .UNSPECIFIED., .F., .F. ) 
 B_SPLINE_CURVE_WITH_KNOTS ( ( 3, 2, 2, 2, 2, 3 ),
 ( 0.9565217391304348116, 0.9586956521739130599, 0.9608695652173913082, 0.9630434782608695565, 0.9652173913043478048, 0.9673913043478260532 ),
 .UNSPECIFIED. ) 
 CURVE ( )  GEOMETRIC_REPRESENTATION_ITEM ( )  RATIONAL_B_SPLINE_CURVE ( ( 1.000000000000000000, 0.9510565162951535312, 1.000000000000000000, 0.9510565162951535312, 1.000000000000000000, 0.9510565162951535312, 1.000000000000000000, 0.9510565162951535312, 1.000000000000000000, 0.9510565162951535312, 1.000000000000000000 ) ) 
 REPRESENTATION_ITEM ( '' )  );
#8207=CARTESIAN_POINT ( 'NONE',  ( -75.20499999999996987, -2.607480562269071545, -8.024999999999991473 ) ) ;
#8218=CARTESIAN_POINT ( 'NONE',  ( -49.49499999999997613, 6.826472737025113702, -4.959722759717902107 ) ) ;
#8227=CARTESIAN_POINT ( 'NONE',  ( -52.79499999999997328, 2.607480562269069324, -8.024999999999993250 ) ) ;
#8231=CARTESIAN_POINT ( 'NONE',  ( -104.0049999999999812, 6.826472737025116366, 4.959722759717898555 ) ) ;
#8237=CARTESIAN_POINT ( 'NONE',  ( -142.7070736234662149, -3.094860106618431139, -9.524999999999991473 ) ) ;
#8242=CARTESIAN_POINT ( 'NONE',  ( -87.95707362346617231, 9.058813317711329915, -2.943386871421373119 ) ) ;
#8250=CARTESIAN_POINT ( 'NONE',  ( -124.1049999999999756, -6.826472737025115478, 4.959722759717900331 ) ) ;
#8251=CARTESIAN_POINT ( 'NONE',  ( -158.8429263765337964, 9.058813317711329915, -2.943386871421373119 ) ) ;
#8253=CARTESIAN_POINT ( 'NONE',  ( -130.9449999999999648, -9.827790563157499189E-16, -8.024999999999991473 ) ) ;
#8254=CARTESIAN_POINT ( 'NONE',  ( -115.3449999999999847, 7.632228543268599452, -2.479861379858951942 ) ) ;
#8258=VECTOR ( 'NONE', #59330, 1000.000000000000000 ) ;
#8260=CARTESIAN_POINT ( 'NONE',  ( -167.9929263765338021, 8.102448949553171076, -5.886773742842744461 ) ) ;
#8261=CARTESIAN_POINT ( 'NONE',  ( -50.24499999999998323, -4.716976649647093289, -6.492361379858945902 ) ) ;
#8270=CARTESIAN_POINT ( 'NONE',  ( -86.54292637653379927, 9.058813317711329915, 2.943386871421369566 ) ) ;
#8276=DIRECTION ( 'NONE',  ( -1.000000000000000000, -0.000000000000000000, -0.000000000000000000 ) ) ;
#8278=CARTESIAN_POINT ( 'NONE',  ( -163.4929263765338021, -8.102448949553174629, 5.886773742842742685 ) ) ;
#8284=ORIENTED_EDGE ( 'NONE', *, *, #7843, .T. ) ;
#8291=LINE ( 'NONE', #18141, #61984 ) ;
#8303=CARTESIAN_POINT ( 'NONE',  ( -77.84499999999998465, -7.632228543268599452, 2.479861379858951054 ) ) ;
#8316=CYLINDRICAL_SURFACE ( 'NONE', #48784, 9.524999999999991473 ) ;
#8320=CARTESIAN_POINT ( 'NONE',  ( -170.9070736234662036, -3.094860106618429807, 9.524999999999991473 ) ) ;
#8323=CARTESIAN_POINT ( 'NONE',  ( -113.1570736234661751, -9.058813317711329915, -2.943386871421370898 ) ) ;
#8331=CARTESIAN_POINT ( 'NONE',  ( -154.8549999999999898, 4.716976649647094177, 6.492361379858945902 ) ) ;
#8333=CARTESIAN_POINT ( 'NONE',  ( -164.8449999999999989, -7.632228543268599452, 2.479861379858951054 ) ) ;
#8335=CARTESIAN_POINT ( 'NONE',  ( -150.4449999999999932, 0.000000000000000000, 8.024999999999991473 ) ) ;
#8340=CARTESIAN_POINT ( 'NONE',  ( -122.5429263765337993, 9.058813317711329915, 2.943386871421369566 ) ) ;
#8342=CARTESIAN_POINT ( 'NONE',  ( -67.10499999999997556, -6.826472737025115478, 4.959722759717900331 ) ) ;
#8346=CARTESIAN_POINT ( 'NONE',  ( -58.79499999999998749, 2.607480562269069324, -8.024999999999993250 ) ) ;
#8348=DIRECTION ( 'NONE',  ( 0.000000000000000000, 0.000000000000000000, 1.000000000000000000 ) ) ;
#8351=DIRECTION ( 'NONE',  ( -1.000000000000000000, -0.000000000000000000, -0.000000000000000000 ) ) ;
#8353=CARTESIAN_POINT ( 'NONE',  ( -159.2070736234664423, 3.094860106623441798, 9.524999999996355271 ) ) ;
#8356=CARTESIAN_POINT ( 'NONE',  ( -183.4449999999999932, 0.000000000000000000, 8.024999999999991473 ) ) ;
#8382=CARTESIAN_POINT ( 'NONE',  ( -106.7949999999999733, 2.607480562269068880, -8.024999999999993250 ) ) ;
#8391=CARTESIAN_POINT ( 'NONE',  ( -106.5570736234661666, -1.166476076187852838E-15, -9.524999999999991473 ) ) ;
#8399=CARTESIAN_POINT ( 'NONE',  ( -134.3050000000000352, 8.437984349512085203, -1.550032578732815448E-15 ) ) ;
#8408=VERTEX_POINT ( 'NONE', #5509 ) ;
#8414=ORIENTED_EDGE ( 'NONE', *, *, #20160, .F. ) ;
#8415=CARTESIAN_POINT ( 'NONE',  ( -182.4550000000000125, 7.632228543268599452, -2.479861379858951942 ) ) ;
#8418=CARTESIAN_POINT ( 'NONE',  ( -55.40707362346616094, 3.094860106618428031, -9.524999999999993250 ) ) ;
#8422=CARTESIAN_POINT ( 'NONE',  ( -176.0949999999999704, -2.607480562269071545, -8.024999999999991473 ) ) ;
#8423=CARTESIAN_POINT ( 'NONE',  ( -178.2570736234661695, 5.598654528085800663, -7.705886871421367523 ) ) ;
#8428=CARTESIAN_POINT ( 'NONE',  ( -91.10500000000000398, -6.826472737025115478, 4.959722759717900331 ) ) ;
#8430=CARTESIAN_POINT ( 'NONE',  ( -168.9570736234661865, 9.058813317711329915, -2.943386871421373119 ) ) ;
#8434=CARTESIAN_POINT ( 'NONE',  ( -100.6449999999999818, 4.716976649647091513, -6.492361379858946790 ) ) ;
#8436=CARTESIAN_POINT ( 'NONE',  ( -69.74499999999999034, 4.716976649647094177, 6.492361379858945902 ) ) ;
#8446=CARTESIAN_POINT ( 'NONE',  ( -116.3929263765338220, 8.102448949553176405, 5.886773742842740909 ) ) ;
#8447=CARTESIAN_POINT ( 'NONE',  ( -131.9949999999999477, -6.826472737025115478, 4.959722759717900331 ) ) ;
#8461=CARTESIAN_POINT ( 'NONE',  ( -126.6570736234661751, 9.058813317711329915, 2.943386871421369566 ) ) ;
#8463=CARTESIAN_POINT ( 'NONE',  ( -133.8549999999999898, 4.716976649647094177, 6.492361379858945902 ) ) ;
#8465=CARTESIAN_POINT ( 'NONE',  ( -184.0000000000000000, 9.524999999999982592, 0.000000000000000000 ) ) ;
#8466=CARTESIAN_POINT ( 'NONE',  ( -120.3570736234661780, 5.598654528085804216, 7.705886871421366635 ) ) ;
#8479=LINE ( 'NONE', #13733, #68754 ) ;
#8481=ORIENTED_EDGE ( 'NONE', *, *, #54574, .F. ) ;
#8489=CARTESIAN_POINT ( 'NONE',  ( -145.9429263765337907, 0.000000000000000000, 9.524999999999991473 ) ) ;
#8494=CARTESIAN_POINT ( 'NONE',  ( -160.4049999999999727, -2.607480562269069768, 8.024999999999991473 ) ) ;
#8500=CARTESIAN_POINT ( 'NONE',  ( -184.0000000000000000, 0.000000000000000000, 0.000000000000000000 ) ) ;
#8506=CARTESIAN_POINT ( 'NONE',  ( -77.60499999999996135, 6.826472737025113702, -4.959722759717902107 ) ) ;
#8518=CARTESIAN_POINT ( 'NONE',  ( -100.9449999999999932, -9.827790563157499189E-16, -8.024999999999991473 ) ) ;
#8522=( BOUNDED_CURVE ( )  B_SPLINE_CURVE ( 2, ( #29302, #29671, #51833, #2531, #19804, #30004, #35997, #2882, #14519, #45190, #18761 ),
 .UNSPECIFIED., .F., .F. ) 
 B_SPLINE_CURVE_WITH_KNOTS ( ( 3, 2, 2, 2, 2, 3 ),
 ( 0.7065217391304348116, 0.7086956521739130599, 0.7108695652173913082, 0.7130434782608695565, 0.7152173913043478048, 0.7173913043478260532 ),
 .UNSPECIFIED. ) 
 CURVE ( )  GEOMETRIC_REPRESENTATION_ITEM ( )  RATIONAL_B_SPLINE_CURVE ( ( 1.000000000000000000, 0.9510565162951535312, 1.000000000000000000, 0.9510565162951535312, 1.000000000000000000, 0.9510565162951535312, 1.000000000000000000, 0.9510565162951535312, 1.000000000000000000, 0.9510565162951535312, 1.000000000000000000 ) ) 
 REPRESENTATION_ITEM ( '' )  );
#8525=CARTESIAN_POINT ( 'NONE',  ( -70.94292637653380496, 0.000000000000000000, 9.524999999999991473 ) ) ;
#8526=CARTESIAN_POINT ( 'NONE',  ( -140.6929263765338192, 10.01517768586948698, -1.839758294383808571E-15 ) ) ;
#8529=CARTESIAN_POINT ( 'NONE',  ( -165.4450000000000216, 0.000000000000000000, 8.024999999999991473 ) ) ;
#8545=CARTESIAN_POINT ( 'NONE',  ( -164.3049999999999784, 8.437984349512086979, -1.550032578732815448E-15 ) ) ;
#8548=ORIENTED_EDGE ( 'NONE', *, *, #41407, .T. ) ;
#8555=CARTESIAN_POINT ( 'NONE',  ( -76.55499999999997840, 0.000000000000000000, 8.024999999999991473 ) ) ;
#8556=CARTESIAN_POINT ( 'NONE',  ( -79.70707362346615810, -3.094860106618431139, -9.524999999999991473 ) ) ;
#8568=CARTESIAN_POINT ( 'NONE',  ( -48.29499999999997328, -2.607480562269069768, 8.024999999999991473 ) ) ;
#8579=CARTESIAN_POINT ( 'NONE',  ( -108.6549999999999869, -7.632228543268600340, -2.479861379858950166 ) ) ;
#8582=CARTESIAN_POINT ( 'NONE',  ( -141.3570736234661638, 5.598654528085804216, 7.705886871421366635 ) ) ;
#8586=CARTESIAN_POINT ( 'NONE',  ( -71.75707362346616947, -5.598654528085801552, 7.705886871421367523 ) ) ;
#8588=CARTESIAN_POINT ( 'NONE',  ( -93.44292637653380496, -1.166476076187852838E-15, -9.524999999999991473 ) ) ;
#8590=CARTESIAN_POINT ( 'NONE',  ( -16.30447726496212368, -10.98532143068888622, 4.829644968601866317 ) ) ;
#8593=CARTESIAN_POINT ( 'NONE',  ( -118.4049999999999869, -2.607480562269069768, 8.024999999999991473 ) ) ;
#8595=CARTESIAN_POINT ( 'NONE',  ( -158.6929263765338192, 10.01517768586948698, -1.839758294383808966E-15 ) ) ;
#8597=CARTESIAN_POINT ( 'NONE',  ( -134.0949999999999420, -2.607480562269071545, -8.024999999999991473 ) ) ;
#8598=CARTESIAN_POINT ( 'NONE',  ( -123.7449999999999903, 4.716976649647094177, 6.492361379858945902 ) ) ;
#8604=CARTESIAN_POINT ( 'NONE',  ( -175.6429263765338078, -5.598654528085801552, 7.705886871421367523 ) ) ;
#8605=CARTESIAN_POINT ( 'NONE',  ( -52.19499999999999318, 8.437984349512085203, -1.550032578732815448E-15 ) ) ;
#8614=CARTESIAN_POINT ( 'NONE',  ( -88.19292637653379074, -10.01517768586948698, 6.132527647946031529E-16 ) ) ;
#8622=ORIENTED_EDGE ( 'NONE', *, *, #36046, .F. ) ;
#8623=DIRECTION ( 'NONE',  ( -1.000000000000000000, -0.000000000000000000, -0.000000000000000000 ) ) ;
#8632=CARTESIAN_POINT ( 'NONE',  ( -101.9049999999999869, 2.607480562269069324, -8.024999999999993250 ) ) ;
#8641=DIRECTION ( 'NONE',  ( -0.000000000000000000, 1.000000000000000000, -0.000000000000000000 ) ) ;
#8642=CARTESIAN_POINT ( 'NONE',  ( -85.64499999999998181, 4.716976649647091513, -6.492361379858946790 ) ) ;
#8657=CARTESIAN_POINT ( 'NONE',  ( -136.5570736234661808, -1.166476076187852838E-15, -9.524999999999991473 ) ) ;
#8658=CARTESIAN_POINT ( 'NONE',  ( -171.9570736234661865, 9.058813317711329915, -2.943386871421373119 ) ) ;
#8661=CARTESIAN_POINT ( 'NONE',  ( -107.9070736234661894, -3.094860106618429807, 9.524999999999991473 ) ) ;
#8664=CARTESIAN_POINT ( 'NONE',  ( -66.05707362346618083, 0.000000000000000000, 9.524999999999991473 ) ) ;
#8667=CARTESIAN_POINT ( 'NONE',  ( -107.9929263765337879, 8.102448949553172852, -5.886773742842744461 ) ) ;
#8668=CARTESIAN_POINT ( 'NONE',  ( -82.79292637653381348, -3.094860106618429807, 9.524999999999991473 ) ) ;
#8674=CARTESIAN_POINT ( 'NONE',  ( -149.6050000000000182, 6.826472737025113702, -4.959722759717902107 ) ) ;
#8676=CARTESIAN_POINT ( 'NONE',  ( -148.6429263765338078, -5.598654528085801552, 7.705886871421367523 ) ) ;
#8677=CARTESIAN_POINT ( 'NONE',  ( -162.7450000000000045, 4.716976649647094177, 6.492361379858945902 ) ) ;
#8678=CARTESIAN_POINT ( 'NONE',  ( -145.6450000000000102, 4.716976649647091513, -6.492361379858946790 ) ) ;
#8682=CARTESIAN_POINT ( 'NONE',  ( -61.70499999999997698, 2.607480562269073321, 8.024999999999991473 ) ) ;
#8685=CARTESIAN_POINT ( 'NONE',  ( -63.89499999999998181, 6.826472737025115478, 4.959722759717899443 ) ) ;
#8699=VERTEX_POINT ( 'NONE', #48078 ) ;
#8701=CARTESIAN_POINT ( 'NONE',  ( -60.95707362346616520, 9.058813317711329915, -2.943386871421373119 ) ) ;
#8711=CARTESIAN_POINT ( 'NONE',  ( -145.9429263765337907, 0.000000000000000000, 9.524999999999991473 ) ) ;
#8715=CARTESIAN_POINT ( 'NONE',  ( -108.1449999999999960, -4.716976649647092401, 6.492361379858946790 ) ) ;
#8733=CARTESIAN_POINT ( 'NONE',  ( -126.9549999999999841, -7.632228543268599452, 2.479861379858951054 ) ) ;
#8735=DIRECTION ( 'NONE',  ( 0.000000000000000000, 0.000000000000000000, 1.000000000000000000 ) ) ;
#8750=CARTESIAN_POINT ( 'NONE',  ( -181.8549999999999898, 4.716976649647094177, 6.492361379858945902 ) ) ;
#8752=CARTESIAN_POINT ( 'NONE',  ( -60.35707362346616378, 5.598654528085804216, 7.705886871421366635 ) ) ;
#8755=CARTESIAN_POINT ( 'NONE',  ( -172.6449999999999818, 4.716976649647091513, -6.492361379858946790 ) ) ;
#8762=CARTESIAN_POINT ( 'NONE',  ( -90.50499999999999545, -6.826472737025115478, -4.959722759717899443 ) ) ;
#8767=CARTESIAN_POINT ( 'NONE',  ( -94.34499999999998465, 7.632228543268599452, -2.479861379858951942 ) ) ;
#8769=CARTESIAN_POINT ( 'NONE',  ( -66.14499999999998181, -4.716976649647092401, 6.492361379858946790 ) ) ;
#8777=CARTESIAN_POINT ( 'NONE',  ( -110.3929263765337936, 8.102448949553176405, 5.886773742842740909 ) ) ;
#8778=CARTESIAN_POINT ( 'NONE',  ( -133.0449999999999875, 7.632228543268600340, 2.479861379858949277 ) ) ;
#8785=CARTESIAN_POINT ( 'NONE',  ( -195.0000000000000000, 0.000000000000000000, 0.000000000000000000 ) ) ;
#8791=CARTESIAN_POINT ( 'NONE',  ( -133.7049999999999557, 2.607480562269072433, 8.024999999999991473 ) ) ;
#8792=ORIENTED_EDGE ( 'NONE', *, *, #28967, .F. ) ;
#8794=CARTESIAN_POINT ( 'NONE',  ( -123.3570736234661780, 5.598654528085804216, 7.705886871421366635 ) ) ;
#8804=CARTESIAN_POINT ( 'NONE',  ( -48.50499999999998835, -6.826472737025113702, -4.959722759717900331 ) ) ;
#8808=CARTESIAN_POINT ( 'NONE',  ( -52.55707362346618083, -1.166476076187852838E-15, -9.524999999999991473 ) ) ;
#8819=CARTESIAN_POINT ( 'NONE',  ( -150.0550000000000068, -9.827790563157499189E-16, -8.024999999999991473 ) ) ;
#8834=CARTESIAN_POINT ( 'NONE',  ( -75.20499999999995566, -2.607480562269071545, -8.024999999999991473 ) ) ;
#8853=CARTESIAN_POINT ( 'NONE',  ( -98.84499999999998465, -7.632228543268599452, 2.479861379858951054 ) ) ;
#8858=CARTESIAN_POINT ( 'NONE',  ( -141.2929263765338419, 3.094860106618428031, -9.524999999999993250 ) ) ;
#8860=CARTESIAN_POINT ( 'NONE',  ( -152.5449999999999875, -7.632228543268600340, -2.479861379858950166 ) ) ;
#8866=ORIENTED_EDGE ( 'NONE', *, *, #32461, .T. ) ;
#8874=CARTESIAN_POINT ( 'NONE',  ( -162.3549999999999898, -4.716976649647093289, -6.492361379858945902 ) ) ;
#8882=EDGE_LOOP ( 'NONE', ( #64853, #34799, #63560, #769 ) ) ;
#8883=CARTESIAN_POINT ( 'NONE',  ( -58.04292637653379927, -9.058813317711329915, -2.943386871421370898 ) ) ;
#8885=CARTESIAN_POINT ( 'NONE',  ( -73.25499999999998124, -4.716976649647092401, 6.492361379858946790 ) ) ;
#8886=CARTESIAN_POINT ( 'NONE',  ( -79.55707362346616662, -1.166476076187852838E-15, -9.524999999999991473 ) ) ;
#8895=EDGE_CURVE ( 'NONE', #59074, #32584, #9755, .T. ) ;
#8901=LINE ( 'NONE', #58141, #59761 ) ;
#8902=CARTESIAN_POINT ( 'NONE',  ( -53.54499999999998039, -7.632228543268600340, -2.479861379858950166 ) ) ;
#8907=DIRECTION ( 'NONE',  ( 0.7071067811865426878, 0.000000000000000000, -0.7071067811865524577 ) ) ;
#8912=ORIENTED_EDGE ( 'NONE', *, *, #44992, .F. ) ;
#8914=CARTESIAN_POINT ( 'NONE',  ( -108.9549999999999983, -7.632228543268599452, 2.479861379858951054 ) ) ;
#8919=CARTESIAN_POINT ( 'NONE',  ( -143.6070736234661354, -8.102448949553172852, 5.886773742842742685 ) ) ;
#8921=CARTESIAN_POINT ( 'NONE',  ( -76.85707362346616378, -5.598654528085803328, -7.705886871421366635 ) ) ;
#8927=CARTESIAN_POINT ( 'NONE',  ( -17.22313415847698082, -11.12901830060570063, 4.490355093446679824 ) ) ;
#8931=CARTESIAN_POINT ( 'NONE',  ( -125.4549999999999841, 7.632228543268599452, -2.479861379858951942 ) ) ;
#8934=CARTESIAN_POINT ( 'NONE',  ( -121.3449999999999989, 7.632228543268599452, -2.479861379858951942 ) ) ;
#8937=CARTESIAN_POINT ( 'NONE',  ( -122.8449999999999847, -7.632228543268599452, 2.479861379858951054 ) ) ;
#8939=ORIENTED_EDGE ( 'NONE', *, *, #1471, .T. ) ;
#8945=CARTESIAN_POINT ( 'NONE',  ( -172.3429263765338249, -9.058813317711329915, 2.943386871421371787 ) ) ;
#8947=CARTESIAN_POINT ( 'NONE',  ( -181.9449999999999932, -9.827790563157499189E-16, -8.024999999999991473 ) ) ;
#8954=CARTESIAN_POINT ( 'NONE',  ( -82.94292637653380496, 0.000000000000000000, 9.524999999999991473 ) ) ;
#8964=ORIENTED_EDGE ( 'NONE', *, *, #2997, .T. ) ;
#8968=CARTESIAN_POINT ( 'NONE',  ( -184.0000000000000000, 0.000000000000000000, 0.000000000000000000 ) ) ;
#8975=CARTESIAN_POINT ( 'NONE',  ( -103.4049999999999869, -2.607480562269069768, 8.024999999999991473 ) ) ;
#8980=CARTESIAN_POINT ( 'NONE',  ( -104.4570736234661723, -9.058813317711329915, 2.943386871421371787 ) ) ;
#8987=CARTESIAN_POINT ( 'NONE',  ( -82.64499999999998181, 4.716976649647091513, -6.492361379858946790 ) ) ;
#9007=CARTESIAN_POINT ( 'NONE',  ( -169.2570736234661695, 5.598654528085800663, -7.705886871421367523 ) ) ;
#9009=CARTESIAN_POINT ( 'NONE',  ( -104.6070736234661922, -8.102448949553172852, 5.886773742842742685 ) ) ;
#9015=CARTESIAN_POINT ( 'NONE',  ( -81.59292637653378222, -3.094860106618431139, -9.524999999999991473 ) ) ;
#9018=CARTESIAN_POINT ( 'NONE',  ( -150.9550000000000125, -7.632228543268599452, 2.479861379858951054 ) ) ;
#9020=CARTESIAN_POINT ( 'NONE',  ( -151.6450000000000102, 4.716976649647091513, -6.492361379858946790 ) ) ;
#9021=CARTESIAN_POINT ( 'NONE',  ( -143.3949999999999818, -6.826472737025113702, -4.959722759717900331 ) ) ;
#9024=( BOUNDED_CURVE ( )  B_SPLINE_CURVE ( 2, ( #8588, #51849, #42028, #45886, #19820, #19468, #25784, #36401, #47296, #3972, #68724 ),
 .UNSPECIFIED., .F., .F. ) 
 B_SPLINE_CURVE_WITH_KNOTS ( ( 3, 2, 2, 2, 2, 3 ),
 ( 0.6630434782608538580, 0.6652173913043321063, 0.6673913043478103546, 0.6695652173912884919, 0.6717391304347667402, 0.6739130434782448775 ),
 .UNSPECIFIED. ) 
 CURVE ( )  GEOMETRIC_REPRESENTATION_ITEM ( )  RATIONAL_B_SPLINE_CURVE ( ( 1.000000000000352385, 0.9510565162948011464, 1.000000000000000000, 0.9510565162951535312, 1.000000000000000000, 0.9510565162951535312, 1.000000000000000000, 0.9510565162951535312, 1.000000000000000000, 0.9510565162955134655, 0.9999999999996400657 ) ) 
 REPRESENTATION_ITEM ( '' )  );
#9029=CARTESIAN_POINT ( 'NONE',  ( -60.35499999999998977, -4.716976649647093289, -6.492361379858945902 ) ) ;
#9031=CARTESIAN_POINT ( 'NONE',  ( -167.2429263765338305, 5.598654528085804216, 7.705886871421366635 ) ) ;
#9032=CARTESIAN_POINT ( 'NONE',  ( -61.34499999999998465, 7.632228543268599452, -2.479861379858951942 ) ) ;
#9034=CARTESIAN_POINT ( 'NONE',  ( -143.9070736234666299, -3.094860106610496597, 9.525000000005753975 ) ) ;
#9050=ORIENTED_EDGE ( 'NONE', *, *, #35592, .F. ) ;
#9056=CARTESIAN_POINT ( 'NONE',  ( -78.05707362346616662, 0.000000000000000000, 9.524999999999991473 ) ) ;
#9071=CARTESIAN_POINT ( 'NONE',  ( -113.0949999999999989, -2.607480562269071545, -8.024999999999991473 ) ) ;
#9074=CARTESIAN_POINT ( 'NONE',  ( -165.0570736234661524, 0.000000000000000000, 9.524999999999991473 ) ) ;
#9077=CARTESIAN_POINT ( 'NONE',  ( -179.4570736234661865, -9.058813317711329915, 2.943386871421371787 ) ) ;
#9083=ORIENTED_EDGE ( 'NONE', *, *, #2507, .T. ) ;
#9089=CARTESIAN_POINT ( 'NONE',  ( -140.6929263765337907, 10.01517768586948698, -1.839758294383808966E-15 ) ) ;
#9090=CARTESIAN_POINT ( 'NONE',  ( -158.4570736234661581, -9.058813317711329915, 2.943386871421371787 ) ) ;
#9091=CARTESIAN_POINT ( 'NONE',  ( -128.0049999999999670, 6.826472737025116366, 4.959722759717898555 ) ) ;
#9092=CARTESIAN_POINT ( 'NONE',  ( -184.0000000000000568, -3.735988484587566827, 7.112865090842599436 ) ) ;
#9106=CARTESIAN_POINT ( 'NONE',  ( -183.0550000000000068, -9.827790563157499189E-16, -8.024999999999991473 ) ) ;
#9107=DIRECTION ( 'NONE',  ( -1.000000000000000000, -0.000000000000000000, -0.000000000000000000 ) ) ;
#9110=CARTESIAN_POINT ( 'NONE',  ( -47.90707362346616094, -3.094860106618429807, 9.524999999999991473 ) ) ;
#9111=CARTESIAN_POINT ( 'NONE',  ( -178.3449999999999989, 7.632228543268599452, -2.479861379858951942 ) ) ;
#9118=CARTESIAN_POINT ( 'NONE',  ( -88.10499999999998977, -6.826472737025115478, 4.959722759717900331 ) ) ;
#9120=CARTESIAN_POINT ( 'NONE',  ( -169.5570736234661808, -1.166476076187852838E-15, -9.524999999999991473 ) ) ;
#9122=CARTESIAN_POINT ( 'NONE',  ( -86.84499999999998465, -7.632228543268599452, 2.479861379858951054 ) ) ;
#9124=CARTESIAN_POINT ( 'NONE',  ( -67.49499999999999034, 6.826472737025113702, -4.959722759717902107 ) ) ;
#9131=ORIENTED_EDGE ( 'NONE', *, *, #4618, .F. ) ;
#9132=CARTESIAN_POINT ( 'NONE',  ( -101.3929263765337794, 8.102448949553176405, 5.886773742842740909 ) ) ;
#9133=PRODUCT ( '4. Adjustment Screw', '4. Adjustment Screw', '', ( #1535 ) ) ;
#9134=CARTESIAN_POINT ( 'NONE',  ( -125.5449999999999875, -7.632228543268600340, -2.479861379858950166 ) ) ;
#9138=EDGE_CURVE ( 'NONE', #32880, #13067, #36887, .T. ) ;
#9149=CARTESIAN_POINT ( 'NONE',  ( -98.30707362346616662, -10.01517768586948698, 6.132527647946031529E-16 ) ) ;
#9154=CARTESIAN_POINT ( 'NONE',  ( -124.7049999999999841, 2.607480562269072433, 8.024999999999991473 ) ) ;
#9157=CARTESIAN_POINT ( 'NONE',  ( -127.7070736234661581, -3.094860106618431139, -9.524999999999991473 ) ) ;
#9167=DIRECTION ( 'NONE',  ( -1.000000000000000000, -0.000000000000000000, -0.000000000000000000 ) ) ;
#9178=ORIENTED_EDGE ( 'NONE', *, *, #44645, .F. ) ;
#9180=VERTEX_POINT ( 'NONE', #30381 ) ;
#9181=CARTESIAN_POINT ( 'NONE',  ( -59.24292637653380211, 5.598654528085804216, 7.705886871421366635 ) ) ;
#9185=CARTESIAN_POINT ( 'NONE',  ( -147.9550000000000125, -7.632228543268599452, 2.479861379858951054 ) ) ;
#9186=ORIENTED_EDGE ( 'NONE', *, *, #5795, .F. ) ;
#9189=FACE_OUTER_BOUND ( 'NONE', #69551, .T. ) ;
#9198=CARTESIAN_POINT ( 'NONE',  ( -65.75499999999998124, 4.716976649647091513, -6.492361379858946790 ) ) ;
#9202=CYLINDRICAL_SURFACE ( 'NONE', #10452, 9.524999999999991473 ) ;
#9211=CARTESIAN_POINT ( 'NONE',  ( -95.99499999999996191, -6.826472737025115478, 4.959722759717900331 ) ) ;
#9214=CARTESIAN_POINT ( 'NONE',  ( -132.4429263765338192, -1.166476076187852838E-15, -9.524999999999991473 ) ) ;
#9218=CARTESIAN_POINT ( 'NONE',  ( -143.8429263765338249, 9.058813317711329915, -2.943386871421373119 ) ) ;
#9220=CARTESIAN_POINT ( 'NONE',  ( -156.5949999999999704, 2.607480562269073321, 8.024999999999991473 ) ) ;
#9223=DIRECTION ( 'NONE',  ( 0.000000000000000000, 0.000000000000000000, 1.000000000000000000 ) ) ;
#9224=CARTESIAN_POINT ( 'NONE',  ( -132.5929263765344785, -3.094860106629523600, -9.524999999991933919 ) ) ;
#9235=ORIENTED_EDGE ( 'NONE', *, *, #27044, .T. ) ;
#9236=CARTESIAN_POINT ( 'NONE',  ( -157.1049999999999898, -6.826472737025113702, 4.959722759717902107 ) ) ;
#9243=EDGE_CURVE ( 'NONE', #52329, #51279, #40292, .T. ) ;
#9244=CARTESIAN_POINT ( 'NONE',  ( -195.0000000000000000, 1.166476076187852838E-15, -9.524999999999991473 ) ) ;
#9254=CARTESIAN_POINT ( 'NONE',  ( -74.75499999999998124, 4.716976649647091513, -6.492361379858946790 ) ) ;
#9264=EDGE_LOOP ( 'NONE', ( #6312, #55581, #43130, #32895, #69047 ) ) ;
#9267=CARTESIAN_POINT ( 'NONE',  ( -179.7549999999999955, 4.716976649647091513, -6.492361379858946790 ) ) ;
#9274=CARTESIAN_POINT ( 'NONE',  ( -94.40500000000000114, -2.607480562269069768, 8.024999999999991473 ) ) ;
#9276=FACE_OUTER_BOUND ( 'NONE', #55975, .T. ) ;
#9278=CARTESIAN_POINT ( 'NONE',  ( -136.1070736234661922, 8.102448949553171076, -5.886773742842744461 ) ) ;
#9281=CARTESIAN_POINT ( 'NONE',  ( -79.70707362346614389, -3.094860106618431139, -9.524999999999991473 ) ) ;
#9289=CARTESIAN_POINT ( 'NONE',  ( -119.6049999999999756, 6.826472737025113702, -4.959722759717902107 ) ) ;
#9293=CARTESIAN_POINT ( 'NONE',  ( -123.8949999999999676, 6.826472737025116366, 4.959722759717898555 ) ) ;
#9300=CARTESIAN_POINT ( 'NONE',  ( -176.6929263765338192, 10.01517768586948698, -1.839758294383808571E-15 ) ) ;
#9311=CARTESIAN_POINT ( 'NONE',  ( -83.54292637653381348, 9.058813317711329915, 2.943386871421369566 ) ) ;
#9315=CARTESIAN_POINT ( 'NONE',  ( -165.4429263765337907, -1.166476076187852838E-15, -9.524999999999991473 ) ) ;
#9317=( BOUNDED_CURVE ( )  B_SPLINE_CURVE ( 2, ( #44639, #50569, #18205, #49890, #40369, #13609, #7316, #28030, #1630, #39689, #45674 ),
 .UNSPECIFIED., .F., .F. ) 
 B_SPLINE_CURVE_WITH_KNOTS ( ( 3, 2, 2, 2, 2, 3 ),
 ( 0.4673913043478149509, 0.4695652173912931437, 0.4717391304347713366, 0.4739130434782495849, 0.4760869565217278332, 0.4782608695652060260 ),
 .UNSPECIFIED. ) 
 CURVE ( )  GEOMETRIC_REPRESENTATION_ITEM ( )  RATIONAL_B_SPLINE_CURVE ( ( 1.000000000000251132, 0.9510565162949022877, 1.000000000000000000, 0.9510565162951535312, 1.000000000000000000, 0.9510565162951535312, 1.000000000000000000, 0.9510565162951535312, 1.000000000000000000, 0.9510565162954097707, 0.9999999999997437605 ) ) 
 REPRESENTATION_ITEM ( '' )  );
#9325=VERTEX_POINT ( 'NONE', #45926 ) ;
#9330=CARTESIAN_POINT ( 'NONE',  ( -101.0070736234661695, -8.102448949553174629, -5.886773742842741797 ) ) ;
#9332=CARTESIAN_POINT ( 'NONE',  ( -107.1549999999999869, 7.632228543268600340, 2.479861379858949277 ) ) ;
#9343=CARTESIAN_POINT ( 'NONE',  ( -68.09499999999998465, -2.607480562269071545, -8.024999999999991473 ) ) ;
#9356=DIRECTION ( 'NONE',  ( -1.000000000000000000, -0.000000000000000000, -0.000000000000000000 ) ) ;
#9359=CARTESIAN_POINT ( 'NONE',  ( -149.8429263765337964, 9.058813317711329915, -2.943386871421373119 ) ) ;
#9361=CARTESIAN_POINT ( 'NONE',  ( -172.7070736234661581, -3.094860106618431139, -9.524999999999991473 ) ) ;
#9364=CARTESIAN_POINT ( 'NONE',  ( -102.5070736234661837, 8.102448949553176405, 5.886773742842740909 ) ) ;
#9374=CARTESIAN_POINT ( 'NONE',  ( -152.9049999999999727, 2.607480562269068880, -8.024999999999993250 ) ) ;
#9377=CARTESIAN_POINT ( 'NONE',  ( -152.6949999999999932, -8.437984349512085203, 5.166775262442717831E-16 ) ) ;
#9380=CARTESIAN_POINT ( 'NONE',  ( -152.2450000000000045, -4.716976649647093289, -6.492361379858945902 ) ) ;
#9382=CARTESIAN_POINT ( 'NONE',  ( -180.2070736234662434, 3.094860106619025775, 9.524999999999563371 ) ) ;
#9387=CARTESIAN_POINT ( 'NONE',  ( -67.70499999999998408, 2.607480562269073321, 8.024999999999991473 ) ) ;
#9389=CARTESIAN_POINT ( 'NONE',  ( -153.0570736234661808, 0.000000000000000000, 9.524999999999991473 ) ) ;
#9391=CARTESIAN_POINT ( 'NONE',  ( -60.59499999999997755, 2.607480562269072433, 8.024999999999991473 ) ) ;
#9396=CARTESIAN_POINT ( 'NONE',  ( -112.9429263765338050, 0.000000000000000000, 9.524999999999991473 ) ) ;
#9404=CARTESIAN_POINT ( 'NONE',  ( -178.1929263765338192, -10.01517768586948698, 6.132527647946031529E-16 ) ) ;
#9423=CARTESIAN_POINT ( 'NONE',  ( -85.19292637653380496, -10.01517768586948698, 6.132527647946031529E-16 ) ) ;
#9426=CARTESIAN_POINT ( 'NONE',  ( -103.6449999999999818, 4.716976649647091513, -6.492361379858946790 ) ) ;
#9429=AXIS2_PLACEMENT_3D ( 'NONE', #58071, #64366, #10566 ) ;
#9438=CARTESIAN_POINT ( 'NONE',  ( -120.3549999999999898, -4.716976649647093289, -6.492361379858945902 ) ) ;
#9443=( BOUNDED_CURVE ( )  B_SPLINE_CURVE ( 2, ( #16941, #37743, #54544, #59827, #59124, #6356, #10612, #10946, #53521, #6695, #44402 ),
 .UNSPECIFIED., .F., .F. ) 
 B_SPLINE_CURVE_WITH_KNOTS ( ( 3, 2, 2, 2, 2, 3 ),
 ( 0.2391304347826030130, 0.2413043478260812058, 0.2434782608695594264, 0.2456521739130376469, 0.2478260869565158675, 0.2499999999999940603 ),
 .UNSPECIFIED. ) 
 CURVE ( )  GEOMETRIC_REPRESENTATION_ITEM ( )  RATIONAL_B_SPLINE_CURVE ( ( 1.000000000000128120, 0.9510565162950255225, 1.000000000000000000, 0.9510565162951535312, 1.000000000000000000, 0.9510565162951535312, 1.000000000000000000, 0.9510565162951535312, 1.000000000000000000, 0.9510565162952872020, 0.9999999999998663291 ) ) 
 REPRESENTATION_ITEM ( '' )  );
#9456=CARTESIAN_POINT ( 'NONE',  ( -175.7049999999999557, 2.607480562269073321, 8.024999999999991473 ) ) ;
#9459=CARTESIAN_POINT ( 'NONE',  ( -47.45707362346615810, -9.058813317711329915, 2.943386871421371787 ) ) ;
#9461=CARTESIAN_POINT ( 'NONE',  ( -180.5949999999999704, 2.607480562269072433, 8.024999999999991473 ) ) ;
#9463=EDGE_LOOP ( 'NONE', ( #28404, #48874, #54744, #17323 ) ) ;
#9468=CARTESIAN_POINT ( 'NONE',  ( -11.23379897725272336, 11.53847739608159806, -3.304761116138219545 ) ) ;
#9469=CARTESIAN_POINT ( 'NONE',  ( -96.65499999999998693, -7.632228543268600340, -2.479861379858950166 ) ) ;
#9475=CARTESIAN_POINT ( 'NONE',  ( -85.94499999999999318, -9.827790563157499189E-16, -8.024999999999991473 ) ) ;
#9478=CARTESIAN_POINT ( 'NONE',  ( -64.19499999999999318, 8.437984349512085203, -1.550032578732815448E-15 ) ) ;
#9489=CARTESIAN_POINT ( 'NONE',  ( -101.2429263765338021, 5.598654528085804216, 7.705886871421366635 ) ) ;
#9490=CARTESIAN_POINT ( 'NONE',  ( -127.3449999999999847, 7.632228543268599452, -2.479861379858951942 ) ) ;
#9504=DIRECTION ( 'NONE',  ( 0.000000000000000000, 0.000000000000000000, 1.000000000000000000 ) ) ;
#9507=ORIENTED_EDGE ( 'NONE', *, *, #62089, .T. ) ;
#9508=CARTESIAN_POINT ( 'NONE',  ( -123.2049999999999699, -2.607480562269071545, -8.024999999999991473 ) ) ;
#9512=CARTESIAN_POINT ( 'NONE',  ( -125.0070736234661979, -8.102448949553172852, -5.886773742842741797 ) ) ;
#9537=CARTESIAN_POINT ( 'NONE',  ( -60.59292637653378932, -3.094860106618431139, -9.524999999999991473 ) ) ;
#9542=CARTESIAN_POINT ( 'NONE',  ( -152.0050000000000239, 6.826472737025116366, 4.959722759717898555 ) ) ;
#9543=ORIENTED_EDGE ( 'NONE', *, *, #39131, .F. ) ;
#9554=CARTESIAN_POINT ( 'NONE',  ( -70.40499999999997272, -2.607480562269069768, 8.024999999999991473 ) ) ;
#9560=CARTESIAN_POINT ( 'NONE',  ( -124.4929263765337879, -8.102448949553174629, 5.886773742842742685 ) ) ;
#9563=EDGE_CURVE ( 'NONE', #13981, #63556, #58843, .T. ) ;
#9571=CARTESIAN_POINT ( 'NONE',  ( -98.69499999999999318, -8.437984349512085203, 5.166775262442717831E-16 ) ) ;
#9575=AXIS2_PLACEMENT_3D ( 'NONE', #560, #53417, #21377 ) ;
#9578=CARTESIAN_POINT ( 'NONE',  ( -133.1929263765337339, -10.01517768586948698, 6.132527647946031529E-16 ) ) ;
#9580=CARTESIAN_POINT ( 'NONE',  ( -154.0449999999999875, 7.632228543268600340, 2.479861379858949277 ) ) ;
#9597=CARTESIAN_POINT ( 'NONE',  ( -152.3050000000000068, 8.437984349512086979, -1.550032578732815448E-15 ) ) ;
#9609=CARTESIAN_POINT ( 'NONE',  ( -69.35499999999998977, -4.716976649647093289, -6.492361379858945902 ) ) ;
#9611=ORIENTED_EDGE ( 'NONE', *, *, #35763, .T. ) ;
#9614=CYLINDRICAL_SURFACE ( 'NONE', #29887, 9.524999999999991473 ) ;
#9622=CARTESIAN_POINT ( 'NONE',  ( -47.99499999999998323, -6.826472737025115478, 4.959722759717900331 ) ) ;
#9632=CARTESIAN_POINT ( 'NONE',  ( -99.65499999999998693, -7.632228543268600340, -2.479861379858950166 ) ) ;
#9635=EDGE_CURVE ( 'NONE', #49320, #64348, #53984, .T. ) ;
#9638=CARTESIAN_POINT ( 'NONE',  ( -129.6570736234661751, 9.058813317711329915, 2.943386871421369566 ) ) ;
#9641=CARTESIAN_POINT ( 'NONE',  ( -73.70707362346615810, -3.094860106618431139, -9.524999999999991473 ) ) ;
#9642=CARTESIAN_POINT ( 'NONE',  ( -160.5570736234661808, -1.166476076187852838E-15, -9.524999999999991473 ) ) ;
#9643=VERTEX_POINT ( 'NONE', #66941 ) ;
#9645=CARTESIAN_POINT ( 'NONE',  ( -15.00000000000000000, -10.90871211463571200, 5.000000000000000000 ) ) ;
#9646=LINE ( 'NONE', #31062, #13346 ) ;
#9649=CARTESIAN_POINT ( 'NONE',  ( -114.9549999999999841, -7.632228543268599452, 2.479861379858951054 ) ) ;
#9650=EDGE_CURVE ( 'NONE', #6742, #34526, #14165, .T. ) ;
#9653=CARTESIAN_POINT ( 'NONE',  ( -123.7449999999999903, 4.716976649647094177, 6.492361379858945902 ) ) ;
#9658=( BOUNDED_CURVE ( )  B_SPLINE_CURVE ( 2, ( #59101, #1335, #44011, #33074, #11951, #43663, #22513, #33408, #27061, #26720, #58762 ),
 .UNSPECIFIED., .F., .F. ) 
 B_SPLINE_CURVE_WITH_KNOTS ( ( 3, 2, 2, 2, 2, 3 ),
 ( 0.4021739130434686116, 0.4043478260869468044, 0.4065217391304249972, 0.4086956521739032455, 0.4108695652173814383, 0.4130434782608596311 ),
 .UNSPECIFIED. ) 
 CURVE ( )  GEOMETRIC_REPRESENTATION_ITEM ( )  RATIONAL_B_SPLINE_CURVE ( ( 1.000000000000217382, 0.9510565162949360385, 1.000000000000000000, 0.9510565162951535312, 1.000000000000000000, 0.9510565162951535312, 1.000000000000000000, 0.9510565162951535312, 1.000000000000000000, 0.9510565162953772411, 0.9999999999997762901 ) ) 
 REPRESENTATION_ITEM ( '' )  );
#9662=ORIENTED_EDGE ( 'NONE', *, *, #12925, .F. ) ;
#9665=CARTESIAN_POINT ( 'NONE',  ( -161.5429263765338135, 9.058813317711329915, 2.943386871421369566 ) ) ;
#9671=CARTESIAN_POINT ( 'NONE',  ( -87.44292637653380496, -1.166476076187852838E-15, -9.524999999999991473 ) ) ;
#9679=CARTESIAN_POINT ( 'NONE',  ( -176.1550000000000011, 7.632228543268600340, 2.479861379858949277 ) ) ;
#9692=CARTESIAN_POINT ( 'NONE',  ( -98.90499999999998693, 2.607480562269069324, -8.024999999999993250 ) ) ;
#9701=CARTESIAN_POINT ( 'NONE',  ( -74.69499999999997897, -8.437984349512085203, 5.166775262442717831E-16 ) ) ;
#9704=CARTESIAN_POINT ( 'NONE',  ( -120.2070736234669397, 3.094860106631407426, 9.524999999990566124 ) ) ;
#9710=ORIENTED_EDGE ( 'NONE', *, *, #33973, .F. ) ;
#9717=CARTESIAN_POINT ( 'NONE',  ( -164.7570736234661695, -5.598654528085801552, 7.705886871421367523 ) ) ;
#9720=CARTESIAN_POINT ( 'NONE',  ( -101.1570736234661609, -9.058813317711329915, -2.943386871421370898 ) ) ;
#9724=CARTESIAN_POINT ( 'NONE',  ( -65.60707362346616378, -8.102448949553174629, 5.886773742842742685 ) ) ;
#9730=CARTESIAN_POINT ( 'NONE',  ( -114.6570736234661751, 9.058813317711329915, 2.943386871421369566 ) ) ;
#9732=CARTESIAN_POINT ( 'NONE',  ( -137.6049999999999329, 6.826472737025113702, -4.959722759717902107 ) ) ;
#9737=CARTESIAN_POINT ( 'NONE',  ( -150.7449999999999761, 4.716976649647094177, 6.492361379858945902 ) ) ;
#9740=CARTESIAN_POINT ( 'NONE',  ( -150.5949999999999704, 2.607480562269072433, 8.024999999999991473 ) ) ;
#9745=CARTESIAN_POINT ( 'NONE',  ( -62.90499999999997982, 2.607480562269068880, -8.024999999999993250 ) ) ;
#9747=CARTESIAN_POINT ( 'NONE',  ( -51.89292637653380069, -8.102448949553174629, -5.886773742842741797 ) ) ;
#9752=CARTESIAN_POINT ( 'NONE',  ( -88.85707362346617799, -5.598654528085803328, -7.705886871421366635 ) ) ;
#9755=LINE ( 'NONE', #36141, #17318 ) ;
#9761=DIRECTION ( 'NONE',  ( -1.000000000000000000, -0.000000000000000000, -0.000000000000000000 ) ) ;
#9775=CARTESIAN_POINT ( 'NONE',  ( -96.29500000000000171, -2.607480562269069768, 8.024999999999991473 ) ) ;
#9777=FACE_OUTER_BOUND ( 'NONE', #20860, .T. ) ;
#9804=CARTESIAN_POINT ( 'NONE',  ( -182.3929263765338078, 8.102448949553176405, 5.886773742842740909 ) ) ;
#9808=CARTESIAN_POINT ( 'NONE',  ( -181.5550000000000068, 0.000000000000000000, 8.024999999999991473 ) ) ;
#9811=CARTESIAN_POINT ( 'NONE',  ( -179.0949999999999704, -2.607480562269071545, -8.024999999999991473 ) ) ;
#9813=CARTESIAN_POINT ( 'NONE',  ( -180.8949999999999818, 6.826472737025115478, 4.959722759717899443 ) ) ;
#9816=EDGE_CURVE ( 'NONE', #64678, #66633, #47616, .T. ) ;
#9818=CARTESIAN_POINT ( 'NONE',  ( -95.15499999999998693, 7.632228543268600340, 2.479861379858949277 ) ) ;
#9822=CARTESIAN_POINT ( 'NONE',  ( -94.64499999999999602, 4.716976649647091513, -6.492361379858946790 ) ) ;
#9825=CARTESIAN_POINT ( 'NONE',  ( -64.04499999999998749, 7.632228543268600340, 2.479861379858949277 ) ) ;
#9830=ORIENTED_EDGE ( 'NONE', *, *, #1612, .F. ) ;
#9845=CARTESIAN_POINT ( 'NONE',  ( -118.8549999999999898, 4.716976649647094177, 6.492361379858945902 ) ) ;
#9863=CARTESIAN_POINT ( 'NONE',  ( -46.70707362346617941, -3.094860106618431139, -9.524999999999991473 ) ) ;
#9865=CARTESIAN_POINT ( 'NONE',  ( -195.0000000000000000, 1.166476076187852838E-15, -9.524999999999991473 ) ) ;
#9874=CARTESIAN_POINT ( 'NONE',  ( -54.59292637653378222, -3.094860106618431139, -9.524999999999991473 ) ) ;
#9877=CARTESIAN_POINT ( 'NONE',  ( -155.9049999999999443, 2.607480562269068880, -8.024999999999993250 ) ) ;
#9888=ORIENTED_EDGE ( 'NONE', *, *, #44930, .T. ) ;
#9892=CARTESIAN_POINT ( 'NONE',  ( -67.70499999999998408, 2.607480562269073321, 8.024999999999991473 ) ) ;
#9907=CARTESIAN_POINT ( 'NONE',  ( -97.79500000000000171, 2.607480562269068880, -8.024999999999993250 ) ) ;
#9912=VECTOR ( 'NONE', #3515, 1000.000000000000000 ) ;
#9913=CARTESIAN_POINT ( 'NONE',  ( -133.6429263765338078, -5.598654528085801552, 7.705886871421367523 ) ) ;
#9914=FACE_OUTER_BOUND ( 'NONE', #14594, .T. ) ;
#9915=CARTESIAN_POINT ( 'NONE',  ( -154.7950000000000159, 2.607480562269068880, -8.024999999999993250 ) ) ;
#9930=CARTESIAN_POINT ( 'NONE',  ( -155.0049999999999955, 6.826472737025115478, 4.959722759717899443 ) ) ;
#9940=CARTESIAN_POINT ( 'NONE',  ( -64.70499999999998408, 2.607480562269072433, 8.024999999999991473 ) ) ;
#9945=DIRECTION ( 'NONE',  ( 0.000000000000000000, 0.000000000000000000, 1.000000000000000000 ) ) ;
#9954=CARTESIAN_POINT ( 'NONE',  ( -183.5049999999999955, -6.826472737025115478, -4.959722759717899443 ) ) ;
#9956=( BOUNDED_CURVE ( )  B_SPLINE_CURVE ( 2, ( #193, #17509, #10821, #38288, #17165, #26955, #11153, #16484, #64636, #60376, #43233 ),
 .UNSPECIFIED., .F., .F. ) 
 B_SPLINE_CURVE_WITH_KNOTS ( ( 3, 2, 2, 2, 2, 3 ),
 ( 0.9673913043478260532, 0.9695652173913043015, 0.9717391304347826608, 0.9739130434782609091, 0.9760869565217391575, 0.9782608695652174058 ),
 .UNSPECIFIED. ) 
 CURVE ( )  GEOMETRIC_REPRESENTATION_ITEM ( )  RATIONAL_B_SPLINE_CURVE ( ( 1.000000000000000000, 0.9510565162951535312, 1.000000000000000000, 0.9510565162951535312, 1.000000000000000000, 0.9510565162951535312, 1.000000000000000000, 0.9510565162951535312, 1.000000000000000000, 0.9510565162951535312, 1.000000000000000000 ) ) 
 REPRESENTATION_ITEM ( '' )  );
#9959=CARTESIAN_POINT ( 'NONE',  ( 0.000000000000000000, 0.000000000000000000, 10.99999999999995381 ) ) ;
#9968=CARTESIAN_POINT ( 'NONE',  ( -95.00499999999998124, 6.826472737025116366, 4.959722759717898555 ) ) ;
#9973=CARTESIAN_POINT ( 'NONE',  ( -131.1570736234661751, -9.058813317711329915, -2.943386871421370898 ) ) ;
#9976=CARTESIAN_POINT ( 'NONE',  ( -77.15707362346617515, -9.058813317711329915, -2.943386871421370898 ) ) ;
#9979=CARTESIAN_POINT ( 'NONE',  ( -16.62496282464071840, -11.02508589828193131, -4.739834931414112162 ) ) ;
#9982=CARTESIAN_POINT ( 'NONE',  ( -113.3049999999999784, 8.437984349512085203, -1.550032578732815448E-15 ) ) ;
#9983=CARTESIAN_POINT ( 'NONE',  ( -195.0000000000000000, 0.000000000000000000, 9.524999999999991473 ) ) ;
#9986=CARTESIAN_POINT ( 'NONE',  ( -129.1449999999999818, -4.716976649647092401, 6.492361379858946790 ) ) ;
#9988=CARTESIAN_POINT ( 'NONE',  ( -118.9429263765338050, 0.000000000000000000, 9.524999999999991473 ) ) ;
#9991=CARTESIAN_POINT ( 'NONE',  ( -159.2929263765337851, 3.094860106618428031, -9.524999999999993250 ) ) ;
#9992=FILL_AREA_STYLE ('',( #4315 ) ) ;
#10001=CARTESIAN_POINT ( 'NONE',  ( -73.19292637653380496, -10.01517768586948698, 6.132527647946031529E-16 ) ) ;
#10008=CARTESIAN_POINT ( 'NONE',  ( -175.4049999999999727, -2.607480562269069768, 8.024999999999991473 ) ) ;
#10015=CARTESIAN_POINT ( 'NONE',  ( -103.4929263765337879, -8.102448949553174629, 5.886773742842742685 ) ) ;
#10023=CARTESIAN_POINT ( 'NONE',  ( -94.40500000000000114, -2.607480562269069768, 8.024999999999991473 ) ) ;
#10027=EDGE_CURVE ( 'NONE', #49213, #40311, #53504, .T. ) ;
#10032=CARTESIAN_POINT ( 'NONE',  ( -76.64499999999999602, 4.716976649647091513, -6.492361379858946790 ) ) ;
#10035=CARTESIAN_POINT ( 'NONE',  ( -120.3570736234661780, 5.598654528085804216, 7.705886871421366635 ) ) ;
#10048=CARTESIAN_POINT ( 'NONE',  ( -148.9429263765338192, 0.000000000000000000, 9.524999999999991473 ) ) ;
#10050=CARTESIAN_POINT ( 'NONE',  ( -158.1570736234661751, -9.058813317711329915, -2.943386871421370898 ) ) ;
#10055=CARTESIAN_POINT ( 'NONE',  ( -105.6570736234661751, 9.058813317711329915, 2.943386871421369566 ) ) ;
#10062=CARTESIAN_POINT ( 'NONE',  ( -115.1070736234661638, 8.102448949553172852, -5.886773742842744461 ) ) ;
#10063=CARTESIAN_POINT ( 'NONE',  ( -142.4049999999999443, -2.607480562269069768, 8.024999999999991473 ) ) ;
#10065=CARTESIAN_POINT ( 'NONE',  ( -159.4449999999999932, 0.000000000000000000, 8.024999999999991473 ) ) ;
#10067=CARTESIAN_POINT ( 'NONE',  ( -138.7450000000000045, 4.716976649647094177, 6.492361379858945902 ) ) ;
#10069=AXIS2_PLACEMENT_3D ( 'NONE', #35243, #10255, #58779 ) ;
#10074=CARTESIAN_POINT ( 'NONE',  ( -52.10499999999998266, -6.826472737025115478, 4.959722759717900331 ) ) ;
#10076=CARTESIAN_POINT ( 'NONE',  ( -144.0570736234661808, 0.000000000000000000, 9.524999999999991473 ) ) ;
#10083=CARTESIAN_POINT ( 'NONE',  ( -81.50707362346616947, 8.102448949553176405, 5.886773742842740909 ) ) ;
#10108=CARTESIAN_POINT ( 'NONE',  ( -84.44292637653380496, -1.166476076187852838E-15, -9.524999999999991473 ) ) ;
#10114=CARTESIAN_POINT ( 'NONE',  ( -98.84499999999998465, -7.632228543268599452, 2.479861379858951054 ) ) ;
#10118=CARTESIAN_POINT ( 'NONE',  ( -164.6070736234661922, -8.102448949553174629, 5.886773742842742685 ) ) ;
#10140=CARTESIAN_POINT ( 'NONE',  ( -165.0550000000000068, -9.827790563157499189E-16, -8.024999999999991473 ) ) ;
#10144=CARTESIAN_POINT ( 'NONE',  ( -48.65707362346616094, 9.058813317711329915, 2.943386871421369566 ) ) ;
#10146=CARTESIAN_POINT ( 'NONE',  ( -163.7949999999999875, 2.607480562269069324, -8.024999999999993250 ) ) ;
#10149=DIRECTION ( 'NONE',  ( -1.000000000000000000, -0.000000000000000000, -0.000000000000000000 ) ) ;
#10152=CARTESIAN_POINT ( 'NONE',  ( -13.68927517661561133, 10.98243962888954428, -4.836436941715524185 ) ) ;
#10153=CARTESIAN_POINT ( 'NONE',  ( -82.10499999999998977, -6.826472737025115478, 4.959722759717900331 ) ) ;
#10157=CARTESIAN_POINT ( 'NONE',  ( -94.79499999999997328, 2.607480562269069324, -8.024999999999993250 ) ) ;
#10166=ORIENTED_EDGE ( 'NONE', *, *, #33064, .F. ) ;
#10170=CARTESIAN_POINT ( 'NONE',  ( -131.8429263765337964, 9.058813317711329915, -2.943386871421373119 ) ) ;
#10174=VERTEX_POINT ( 'NONE', #34484 ) ;
#10182=CARTESIAN_POINT ( 'NONE',  ( -123.9549999999999841, -7.632228543268599452, 2.479861379858951054 ) ) ;
#10184=CARTESIAN_POINT ( 'NONE',  ( -137.3070736234661808, -10.01517768586948698, 6.132527647946031529E-16 ) ) ;
#10207=CARTESIAN_POINT ( 'NONE',  ( -99.14292637653380780, 5.598654528085800663, -7.705886871421367523 ) ) ;
#10213=CARTESIAN_POINT ( 'NONE',  ( -54.14292637653381490, 5.598654528085800663, -7.705886871421367523 ) ) ;
#10215=CARTESIAN_POINT ( 'NONE',  ( -150.3549999999999898, -4.716976649647093289, -6.492361379858945902 ) ) ;
#10229=CARTESIAN_POINT ( 'NONE',  ( -67.10499999999997556, -6.826472737025115478, 4.959722759717900331 ) ) ;
#10235=CARTESIAN_POINT ( 'NONE',  ( -124.6429263765338078, -5.598654528085801552, 7.705886871421367523 ) ) ;
#10238=EDGE_CURVE ( 'NONE', #31166, #12387, #30932, .T. ) ;
#10242=CARTESIAN_POINT ( 'NONE',  ( -195.0000000000000000, 0.000000000000000000, 0.000000000000000000 ) ) ;
#10246=CARTESIAN_POINT ( 'NONE',  ( -122.5449999999999875, -7.632228543268600340, -2.479861379858950166 ) ) ;
#10248=CARTESIAN_POINT ( 'NONE',  ( -84.29499999999998749, -2.607480562269069768, 8.024999999999991473 ) ) ;
#10255=DIRECTION ( 'NONE',  ( -0.000000000000000000, 1.000000000000000000, 0.000000000000000000 ) ) ;
#10257=CARTESIAN_POINT ( 'NONE',  ( -130.3429263765337964, -9.058813317711329915, 2.943386871421371787 ) ) ;
#10259=CARTESIAN_POINT ( 'NONE',  ( -153.4449999999999932, 0.000000000000000000, 8.024999999999991473 ) ) ;
#10273=ORIENTED_EDGE ( 'NONE', *, *, #42909, .T. ) ;
#10274=CARTESIAN_POINT ( 'NONE',  ( -153.0550000000000068, -9.827790563157499189E-16, -8.024999999999991473 ) ) ;
#10288=CARTESIAN_POINT ( 'NONE',  ( -66.20499999999996987, -2.607480562269071545, -8.024999999999991473 ) ) ;
#10303=CARTESIAN_POINT ( 'NONE',  ( -183.9550000000000125, -7.632228543268599452, 2.479861379858951054 ) ) ;
#10313=CARTESIAN_POINT ( 'NONE',  ( -127.7070736234668260, -3.094860106629993890, -9.524999999991592858 ) ) ;
#10315=CARTESIAN_POINT ( 'NONE',  ( -91.40500000000000114, -2.607480562269069768, 8.024999999999991473 ) ) ;
#10320=CARTESIAN_POINT ( 'NONE',  ( -130.8570736234661922, -5.598654528085803328, -7.705886871421366635 ) ) ;
#10322=CARTESIAN_POINT ( 'NONE',  ( -61.70707362346615810, -3.094860106618431139, -9.524999999999991473 ) ) ;
#10323=EDGE_CURVE ( 'NONE', #18337, #62258, #27777, .T. ) ;
#10329=CARTESIAN_POINT ( 'NONE',  ( -110.4549999999999841, 7.632228543268599452, -2.479861379858951942 ) ) ;
#10331=CARTESIAN_POINT ( 'NONE',  ( -113.6949999999999790, -8.437984349512085203, 5.166775262442717831E-16 ) ) ;
#10334=CARTESIAN_POINT ( 'NONE',  ( -117.8929263765337794, -8.102448949553174629, -5.886773742842741797 ) ) ;
#10339=CARTESIAN_POINT ( 'NONE',  ( -160.4929263765338305, -8.102448949553172852, 5.886773742842742685 ) ) ;
#10340=( LENGTH_UNIT ( ) NAMED_UNIT ( * ) SI_UNIT ( .MILLI., .METRE. ) );
#10345=DIRECTION ( 'NONE',  ( 0.000000000000000000, 0.000000000000000000, 1.000000000000000000 ) ) ;
#10351=CARTESIAN_POINT ( 'NONE',  ( -71.54292637653379927, 9.058813317711329915, 2.943386871421369566 ) ) ;
#10358=DIRECTION ( 'NONE',  ( -1.000000000000000000, -0.000000000000000000, -0.000000000000000000 ) ) ;
#10361=CARTESIAN_POINT ( 'NONE',  ( -182.0049999999999670, 6.826472737025115478, 4.959722759717899443 ) ) ;
#10369=( BOUNDED_CURVE ( )  B_SPLINE_CURVE ( 2, ( #57906, #41750, #51934, #10062, #47033, #36483, #9730, #31137, #2981, #62466, #67400 ),
 .UNSPECIFIED., .F., .F. ) 
 B_SPLINE_CURVE_WITH_KNOTS ( ( 3, 2, 2, 2, 2, 3 ),
 ( 0.4891304347825972121, 0.4913043478260754049, 0.4934782608695535977, 0.4956521739130318460, 0.4978260869565100388, 0.4999999999999882316 ),
 .UNSPECIFIED. ) 
 CURVE ( )  GEOMETRIC_REPRESENTATION_ITEM ( )  RATIONAL_B_SPLINE_CURVE ( ( 1.000000000000258682, 0.9510565162948948492, 1.000000000000000000, 0.9510565162951535312, 1.000000000000000000, 0.9510565162951535312, 1.000000000000000000, 0.9510565162951535312, 1.000000000000000000, 0.9510565162954184304, 0.9999999999997351008 ) ) 
 REPRESENTATION_ITEM ( '' )  );
#10370=CARTESIAN_POINT ( 'NONE',  ( -181.8570736234661638, -5.598654528085803328, -7.705886871421366635 ) ) ;
#10375=CARTESIAN_POINT ( 'NONE',  ( -95.90499999999998693, 2.607480562269069324, -8.024999999999993250 ) ) ;
#10381=CARTESIAN_POINT ( 'NONE',  ( -103.5570736234661808, -1.166476076187852838E-15, -9.524999999999991473 ) ) ;
#10384=ORIENTED_EDGE ( 'NONE', *, *, #9563, .F. ) ;
#10387=CARTESIAN_POINT ( 'NONE',  ( -73.94499999999997897, -9.827790563157499189E-16, -8.024999999999991473 ) ) ;
#10397=EDGE_LOOP ( 'NONE', ( #35111, #15687, #19596, #69541 ) ) ;
#10402=CARTESIAN_POINT ( 'NONE',  ( -159.3570736234661922, 5.598654528085804216, 7.705886871421366635 ) ) ;
#10405=CARTESIAN_POINT ( 'NONE',  ( -91.70707362346614389, -3.094860106618431139, -9.524999999999991473 ) ) ;
#10411=CARTESIAN_POINT ( 'NONE',  ( -138.3550000000000182, -4.716976649647093289, -6.492361379858945902 ) ) ;
#10415=EDGE_CURVE ( 'NONE', #51275, #20383, #35003, .T. ) ;
#10416=CARTESIAN_POINT ( 'NONE',  ( -156.4449999999999932, 0.000000000000000000, 8.024999999999991473 ) ) ;
#10417=CARTESIAN_POINT ( 'NONE',  ( -139.7950000000000159, 2.607480562269069324, -8.024999999999993250 ) ) ;
#10424=CARTESIAN_POINT ( 'NONE',  ( -56.45499999999997698, 7.632228543268599452, -2.479861379858951942 ) ) ;
#10445=LINE ( 'NONE', #36523, #39443 ) ;
#10450=CARTESIAN_POINT ( 'NONE',  ( -109.2570736234661837, 5.598654528085800663, -7.705886871421367523 ) ) ;
#10452=AXIS2_PLACEMENT_3D ( 'NONE', #15198, #36662, #58087 ) ;
#10460=CARTESIAN_POINT ( 'NONE',  ( -102.5949999999999704, 2.607480562269073321, 8.024999999999991473 ) ) ;
#10464=CARTESIAN_POINT ( 'NONE',  ( -140.0070736234661695, -8.102448949553174629, -5.886773742842741797 ) ) ;
#10468=LINE ( 'NONE', #69209, #7682 ) ;
#10481=CARTESIAN_POINT ( 'NONE',  ( -114.4429263765338050, -1.166476076187852838E-15, -9.524999999999991473 ) ) ;
#10486=CARTESIAN_POINT ( 'NONE',  ( -100.5570736234661808, -1.166476076187852838E-15, -9.524999999999991473 ) ) ;
#10489=CARTESIAN_POINT ( 'NONE',  ( -170.0049999999999955, 6.826472737025116366, 4.959722759717898555 ) ) ;
#10493=CARTESIAN_POINT ( 'NONE',  ( -181.1949999999999648, 8.437984349512085203, -1.550032578732815448E-15 ) ) ;
#10495=CARTESIAN_POINT ( 'NONE',  ( -166.0449999999999875, 7.632228543268600340, 2.479861379858949277 ) ) ;
#10501=CARTESIAN_POINT ( 'NONE',  ( -86.30499999999997840, 8.437984349512085203, -1.550032578732815448E-15 ) ) ;
#10506=CARTESIAN_POINT ( 'NONE',  ( -84.14499999999998181, -4.716976649647092401, 6.492361379858946790 ) ) ;
#10510=CARTESIAN_POINT ( 'NONE',  ( -170.6929263765337623, 10.01517768586948698, -1.839758294383808966E-15 ) ) ;
#10512=DIRECTION ( 'NONE',  ( 0.000000000000000000, 0.000000000000000000, 1.000000000000000000 ) ) ;
#10532=CARTESIAN_POINT ( 'NONE',  ( -120.0549999999999926, -9.827790563157499189E-16, -8.024999999999991473 ) ) ;
#10544=ORIENTED_EDGE ( 'NONE', *, *, #35592, .T. ) ;
#10548=ORIENTED_EDGE ( 'NONE', *, *, #19704, .F. ) ;
#10558=CARTESIAN_POINT ( 'NONE',  ( -59.99292637653379501, 8.102448949553171076, -5.886773742842744461 ) ) ;
#10561=CARTESIAN_POINT ( 'NONE',  ( -145.1049999999999898, -6.826472737025115478, 4.959722759717900331 ) ) ;
#10566=DIRECTION ( 'NONE',  ( 0.000000000000000000, 0.000000000000000000, 1.000000000000000000 ) ) ;
#10574=CARTESIAN_POINT ( 'NONE',  ( -63.20499999999998408, -2.607480562269071545, -8.024999999999991473 ) ) ;
#10582=EDGE_CURVE ( 'NONE', #1270, #57659, #5391, .T. ) ;
#10587=CARTESIAN_POINT ( 'NONE',  ( -112.0449999999999875, 7.632228543268600340, 2.479861379858949277 ) ) ;
#10589=CARTESIAN_POINT ( 'NONE',  ( -85.49499999999999034, 6.826472737025113702, -4.959722759717902107 ) ) ;
#10599=CARTESIAN_POINT ( 'NONE',  ( -138.4429263765337907, -1.166476076187852838E-15, -9.524999999999991473 ) ) ;
#10601=CARTESIAN_POINT ( 'NONE',  ( -143.8449999999999989, -7.632228543268599452, 2.479861379858951054 ) ) ;
#10603=CARTESIAN_POINT ( 'NONE',  ( -47.69499999999998607, -8.437984349512086979, 5.166775262442717831E-16 ) ) ;
#10612=CARTESIAN_POINT ( 'NONE',  ( -151.0429263765337851, -9.058813317711329915, -2.943386871421370898 ) ) ;
#10614=CARTESIAN_POINT ( 'NONE',  ( -148.2549999999999955, -4.716976649647092401, 6.492361379858946790 ) ) ;
#10624=EDGE_CURVE ( 'NONE', #54061, #1147, #49022, .T. ) ;
#10628=CARTESIAN_POINT ( 'NONE',  ( -67.25499999999998124, -4.716976649647092401, 6.492361379858946790 ) ) ;
#10629=CARTESIAN_POINT ( 'NONE',  ( -122.3949999999999818, -6.826472737025115478, -4.959722759717899443 ) ) ;
#10642=CARTESIAN_POINT ( 'NONE',  ( -175.4049999999999727, -2.607480562269069768, 8.024999999999991473 ) ) ;
#10651=CARTESIAN_POINT ( 'NONE',  ( -96.35499999999997556, -4.716976649647093289, -6.492361379858945902 ) ) ;
#10656=CARTESIAN_POINT ( 'NONE',  ( -131.3070736234661524, -10.01517768586948698, 6.132527647946031529E-16 ) ) ;
#10659=CARTESIAN_POINT ( 'NONE',  ( -67.70707362346617231, -3.094860106618431139, -9.524999999999991473 ) ) ;
#10666=CARTESIAN_POINT ( 'NONE',  ( -115.4049999999999727, -2.607480562269069768, 8.024999999999991473 ) ) ;
#10668=CARTESIAN_POINT ( 'NONE',  ( -114.8949999999999818, 6.826472737025116366, 4.959722759717898555 ) ) ;
#10673=FACE_OUTER_BOUND ( 'NONE', #38150, .T. ) ;
#10676=CARTESIAN_POINT ( 'NONE',  ( -167.0929263765338249, 3.094860106618433360, 9.524999999999991473 ) ) ;
#10678=CARTESIAN_POINT ( 'NONE',  ( -174.8950000000000102, 6.826472737025116366, 4.959722759717898555 ) ) ;
#10680=CARTESIAN_POINT ( 'NONE',  ( -109.5570736234661666, -1.166476076187852838E-15, -9.524999999999991473 ) ) ;
#10685=CARTESIAN_POINT ( 'NONE',  ( -76.49292637653381632, -8.102448949553172852, 5.886773742842742685 ) ) ;
#10694=CARTESIAN_POINT ( 'NONE',  ( -180.2049999999999841, -2.607480562269071545, -8.024999999999991473 ) ) ;
#10705=CARTESIAN_POINT ( 'NONE',  ( -94.70499999999998408, 2.607480562269072433, 8.024999999999991473 ) ) ;
#10716=CARTESIAN_POINT ( 'NONE',  ( -68.99499999999999034, -6.826472737025115478, 4.959722759717900331 ) ) ;
#10721=CARTESIAN_POINT ( 'NONE',  ( -125.9070736234668715, -3.094860106606598382, 9.525000000008585488 ) ) ;
#10729=CARTESIAN_POINT ( 'NONE',  ( -119.3049999999999926, 8.437984349512085203, -1.550032578732815448E-15 ) ) ;
#10738=CARTESIAN_POINT ( 'NONE',  ( -161.0070736234661410, -8.102448949553172852, -5.886773742842741797 ) ) ;
#10741=CARTESIAN_POINT ( 'NONE',  ( -95.00707362346616947, -8.102448949553172852, -5.886773742842741797 ) ) ;
#10747=ADVANCED_FACE ( 'NONE', ( #68427 ), #20938, .F. ) ;
#10751=CARTESIAN_POINT ( 'NONE',  ( -139.2549999999999955, -4.716976649647092401, 6.492361379858946790 ) ) ;
#10752=CARTESIAN_POINT ( 'NONE',  ( -85.55707362346618083, -1.166476076187852838E-15, -9.524999999999991473 ) ) ;
#10755=CARTESIAN_POINT ( 'NONE',  ( -144.7449999999999761, 4.716976649647094177, 6.492361379858945902 ) ) ;
#10756=CARTESIAN_POINT ( 'NONE',  ( -138.1449999999999818, -4.716976649647092401, 6.492361379858946790 ) ) ;
#10757=ORIENTED_EDGE ( 'NONE', *, *, #68917, .T. ) ;
#10761=CARTESIAN_POINT ( 'NONE',  ( -55.85499999999998977, 4.716976649647094177, 6.492361379858945902 ) ) ;
#10762=CARTESIAN_POINT ( 'NONE',  ( -138.8929263765338078, -8.102448949553174629, -5.886773742842741797 ) ) ;
#10767=CARTESIAN_POINT ( 'NONE',  ( -190.0000000000000000, 0.000000000000000000, 7.499999999999985789 ) ) ;
#10769=CARTESIAN_POINT ( 'NONE',  ( -107.8429263765338106, 9.058813317711329915, -2.943386871421373119 ) ) ;
#10796=CARTESIAN_POINT ( 'NONE',  ( -104.3949999999999960, -6.826472737025115478, -4.959722759717899443 ) ) ;
#10797=EDGE_LOOP ( 'NONE', ( #67933, #3816, #21896, #45681 ) ) ;
#10821=CARTESIAN_POINT ( 'NONE',  ( -49.25707362346617657, 5.598654528085800663, -7.705886871421367523 ) ) ;
#10828=CARTESIAN_POINT ( 'NONE',  ( -168.0550000000000068, -9.827790563157499189E-16, -8.024999999999991473 ) ) ;
#10829=CARTESIAN_POINT ( 'NONE',  ( -195.0000000000000000, 0.000000000000000000, 0.000000000000000000 ) ) ;
#10831=CARTESIAN_POINT ( 'NONE',  ( -176.3949999999999818, -6.826472737025115478, -4.959722759717899443 ) ) ;
#10833=CARTESIAN_POINT ( 'NONE',  ( -163.9449999999999932, -9.827790563157499189E-16, -8.024999999999991473 ) ) ;
#10838=CARTESIAN_POINT ( 'NONE',  ( -83.45499999999998408, 7.632228543268599452, -2.479861379858951942 ) ) ;
#10839=CARTESIAN_POINT ( 'NONE',  ( -195.0000000000000000, 0.000000000000000000, 0.000000000000000000 ) ) ;
#10842=CARTESIAN_POINT ( 'NONE',  ( -81.29499999999997328, -2.607480562269069768, 8.024999999999991473 ) ) ;
#10850=CARTESIAN_POINT ( 'NONE',  ( -74.24292637653380211, 5.598654528085804216, 7.705886871421366635 ) ) ;
#10852=ORIENTED_EDGE ( 'NONE', *, *, #65124, .F. ) ;
#10868=CARTESIAN_POINT ( 'NONE',  ( -115.2549999999999955, -4.716976649647092401, 6.492361379858946790 ) ) ;
#10870=CARTESIAN_POINT ( 'NONE',  ( -138.0570736234661808, 0.000000000000000000, 9.524999999999991473 ) ) ;
#10885=CARTESIAN_POINT ( 'NONE',  ( -181.7929263765338135, -3.094860106617829398, 9.525000000000428457 ) ) ;
#10895=ORIENTED_EDGE ( 'NONE', *, *, #20439, .F. ) ;
#10899=CARTESIAN_POINT ( 'NONE',  ( -140.6050000000000182, 6.826472737025113702, -4.959722759717902107 ) ) ;
#10905=SURFACE_STYLE_FILL_AREA ( #53797 ) ;
#10906=ORIENTED_EDGE ( 'NONE', *, *, #42864, .T. ) ;
#10912=CARTESIAN_POINT ( 'NONE',  ( -56.60499999999998266, 6.826472737025113702, -4.959722759717902107 ) ) ;
#10925=CARTESIAN_POINT ( 'NONE',  ( -104.9949999999999761, -6.826472737025113702, 4.959722759717902107 ) ) ;
#10927=CARTESIAN_POINT ( 'NONE',  ( -84.74499999999999034, 4.716976649647094177, 6.492361379858945902 ) ) ;
#10932=CARTESIAN_POINT ( 'NONE',  ( -153.0570736234661808, 0.000000000000000000, 9.524999999999991473 ) ) ;
#10934=CARTESIAN_POINT ( 'NONE',  ( -133.7929263765338135, -3.094860106618429807, 9.524999999999991473 ) ) ;
#10935=CARTESIAN_POINT ( 'NONE',  ( -151.4949999999999761, 6.826472737025113702, -4.959722759717902107 ) ) ;
#10937=CARTESIAN_POINT ( 'NONE',  ( -66.80707362346618083, 10.01517768586948698, -1.839758294383808966E-15 ) ) ;
#10942=CARTESIAN_POINT ( 'NONE',  ( -133.1070736234661922, 8.102448949553172852, -5.886773742842744461 ) ) ;
#10946=CARTESIAN_POINT ( 'NONE',  ( -150.8929263765337794, -8.102448949553174629, -5.886773742842741797 ) ) ;
#10948=CARTESIAN_POINT ( 'NONE',  ( -151.8549999999999898, 4.716976649647094177, 6.492361379858945902 ) ) ;
#10961=LINE ( 'NONE', #38780, #49876 ) ;
#10963=CARTESIAN_POINT ( 'NONE',  ( -64.55499999999999261, 0.000000000000000000, 8.024999999999991473 ) ) ;
#10964=CARTESIAN_POINT ( 'NONE',  ( -120.4449999999999932, 0.000000000000000000, 8.024999999999991473 ) ) ;
#10980=CARTESIAN_POINT ( 'NONE',  ( -174.0549999999999784, -9.827790563157499189E-16, -8.024999999999991473 ) ) ;
#10990=CARTESIAN_POINT ( 'NONE',  ( -128.3070736234661524, -10.01517768586948698, 6.132527647946031529E-16 ) ) ;
#10992=CARTESIAN_POINT ( 'NONE',  ( -87.35499999999998977, -4.716976649647093289, -6.492361379858945902 ) ) ;
#10994=CARTESIAN_POINT ( 'NONE',  ( -62.30707362346616662, -10.01517768586948698, 6.132527647946031529E-16 ) ) ;
#11002=CARTESIAN_POINT ( 'NONE',  ( -109.8549999999999898, 4.716976649647094177, 6.492361379858945902 ) ) ;
#11004=CARTESIAN_POINT ( 'NONE',  ( -116.9949999999999761, -6.826472737025115478, 4.959722759717900331 ) ) ;
#11008=CARTESIAN_POINT ( 'NONE',  ( -165.5929263765337964, -3.094860106618431139, -9.524999999999991473 ) ) ;
#11009=CARTESIAN_POINT ( 'NONE',  ( -178.4949999999999477, 6.826472737025113702, -4.959722759717902107 ) ) ;
#11014=VERTEX_POINT ( 'NONE', #48972 ) ;
#11015=CARTESIAN_POINT ( 'NONE',  ( -76.19292637653380496, -10.01517768586948698, 6.132527647946031529E-16 ) ) ;
#11018=FACE_OUTER_BOUND ( 'NONE', #3769, .T. ) ;
#11019=CARTESIAN_POINT ( 'NONE',  ( -45.99999999999999289, 1.166476076187854022E-15, -9.525000000000000355 ) ) ;
#11022=CARTESIAN_POINT ( 'NONE',  ( -179.7549999999999955, 4.716976649647091513, -6.492361379858946790 ) ) ;
#11032=CARTESIAN_POINT ( 'NONE',  ( -92.75499999999999545, 4.716976649647091513, -6.492361379858946790 ) ) ;
#11039=CARTESIAN_POINT ( 'NONE',  ( -127.9429263765338192, 0.000000000000000000, 9.524999999999991473 ) ) ;
#11045=CARTESIAN_POINT ( 'NONE',  ( -62.54499999999998749, -7.632228543268600340, -2.479861379858950166 ) ) ;
#11057=CARTESIAN_POINT ( 'NONE',  ( -121.8549999999999898, 4.716976649647094177, 6.492361379858945902 ) ) ;
#11060=CARTESIAN_POINT ( 'NONE',  ( -159.7429263765338021, -5.598654528085803328, -7.705886871421366635 ) ) ;
#11062=CARTESIAN_POINT ( 'NONE',  ( -163.8570736234661922, -5.598654528085803328, -7.705886871421366635 ) ) ;
#11064=CARTESIAN_POINT ( 'NONE',  ( -98.00707362346618368, -8.102448949553172852, -5.886773742842741797 ) ) ;
#11071=CARTESIAN_POINT ( 'NONE',  ( -140.9050000000000011, 2.607480562269068880, -8.024999999999993250 ) ) ;
#11076=CARTESIAN_POINT ( 'NONE',  ( -142.9449999999999932, -9.827790563157499189E-16, -8.024999999999991473 ) ) ;
#11078=CARTESIAN_POINT ( 'NONE',  ( -139.0450000000000159, 7.632228543268600340, 2.479861379858949277 ) ) ;
#11084=CARTESIAN_POINT ( 'NONE',  ( -57.50499999999997414, -6.826472737025115478, -4.959722759717899443 ) ) ;
#11087=CARTESIAN_POINT ( 'NONE',  ( -55.19499999999998607, 8.437984349512085203, -1.550032578732815448E-15 ) ) ;
#11090=CARTESIAN_POINT ( 'NONE',  ( -124.9429263765338192, 0.000000000000000000, 9.524999999999991473 ) ) ;
#11094=CARTESIAN_POINT ( 'NONE',  ( -109.0429263765337993, -9.058813317711329915, -2.943386871421370898 ) ) ;
#11109=DIRECTION ( 'NONE',  ( -1.000000000000000000, -0.000000000000000000, -0.000000000000000000 ) ) ;
#11116=CYLINDRICAL_SURFACE ( 'NONE', #42259, 9.524999999999991473 ) ;
#11117=CYLINDRICAL_SURFACE ( 'NONE', #27510, 9.524999999999991473 ) ;
#11125=CARTESIAN_POINT ( 'NONE',  ( -89.84499999999999886, -7.632228543268599452, 2.479861379858951054 ) ) ;
#11131=CARTESIAN_POINT ( 'NONE',  ( -175.6429263765338078, -5.598654528085801552, 7.705886871421367523 ) ) ;
#11147=CARTESIAN_POINT ( 'NONE',  ( -69.44292637653380496, -1.166476076187852838E-15, -9.524999999999991473 ) ) ;
#11153=CARTESIAN_POINT ( 'NONE',  ( -48.65707362346616094, 9.058813317711329915, 2.943386871421369566 ) ) ;
#11158=CARTESIAN_POINT ( 'NONE',  ( -164.6049999999999898, 6.826472737025113702, -4.959722759717902107 ) ) ;
#11161=CARTESIAN_POINT ( 'NONE',  ( -173.3950000000000102, -6.826472737025115478, -4.959722759717899443 ) ) ;
#11162=CARTESIAN_POINT ( 'NONE',  ( -165.8949999999999818, 6.826472737025115478, 4.959722759717899443 ) ) ;
#11165=( BOUNDED_CURVE ( )  B_SPLINE_CURVE ( 2, ( #66885, #45466, #29213, #34850, #17989, #35208, #61244, #23607, #39477, #34172, #60882 ),
 .UNSPECIFIED., .F., .F. ) 
 B_SPLINE_CURVE_WITH_KNOTS ( ( 3, 2, 2, 2, 2, 3 ),
 ( 0.4347826086956419478, 0.4369565217391201406, 0.4391304347825983889, 0.4413043478260766372, 0.4434782608695548300, 0.4456521739130330229 ),
 .UNSPECIFIED. ) 
 CURVE ( )  GEOMETRIC_REPRESENTATION_ITEM ( )  RATIONAL_B_SPLINE_CURVE ( ( 1.000000000000230038, 0.9510565162949236040, 1.000000000000000000, 0.9510565162951535312, 1.000000000000000000, 0.9510565162951535312, 1.000000000000000000, 0.9510565162951535312, 1.000000000000000000, 0.9510565162953884544, 0.9999999999997650768 ) ) 
 REPRESENTATION_ITEM ( '' )  );
#11172=CARTESIAN_POINT ( 'NONE',  ( -82.55499999999999261, 0.000000000000000000, 8.024999999999991473 ) ) ;
#11175=CARTESIAN_POINT ( 'NONE',  ( -76.19499999999997897, 8.437984349512086979, -1.550032578732815448E-15 ) ) ;
#11177=CARTESIAN_POINT ( 'NONE',  ( -133.7070736234668118, -3.094860106628716245, -9.524999999992518340 ) ) ;
#11182=CARTESIAN_POINT ( 'NONE',  ( -75.29292637653379927, 3.094860106618428031, -9.524999999999993250 ) ) ;
#11183=VECTOR ( 'NONE', #8623, 1000.000000000000000 ) ;
#11193=CARTESIAN_POINT ( 'NONE',  ( -195.0000000000000000, 0.000000000000000000, 0.000000000000000000 ) ) ;
#11206=ORIENTED_EDGE ( 'NONE', *, *, #39836, .F. ) ;
#11207=CARTESIAN_POINT ( 'NONE',  ( -109.5549999999999926, 0.000000000000000000, 8.024999999999991473 ) ) ;
#11211=EDGE_LOOP ( 'NONE', ( #8182, #41378 ) ) ;
#11218=FACE_OUTER_BOUND ( 'NONE', #41533, .T. ) ;
#11219=CARTESIAN_POINT ( 'NONE',  ( -151.5570736234661808, -1.166476076187852838E-15, -9.524999999999991473 ) ) ;
#11222=ORIENTED_EDGE ( 'NONE', *, *, #41087, .T. ) ;
#11235=CARTESIAN_POINT ( 'NONE',  ( -195.0000000000000000, 0.000000000000000000, 0.000000000000000000 ) ) ;
#11237=CARTESIAN_POINT ( 'NONE',  ( -146.3049999999999784, 8.437984349512085203, -1.550032578732815448E-15 ) ) ;
#11243=ORIENTED_EDGE ( 'NONE', *, *, #64252, .F. ) ;
#11248=CARTESIAN_POINT ( 'NONE',  ( -56.15499999999997982, 7.632228543268600340, 2.479861379858949277 ) ) ;
#11262=CARTESIAN_POINT ( 'NONE',  ( -111.4449999999999932, 0.000000000000000000, 8.024999999999991473 ) ) ;
#11264=CARTESIAN_POINT ( 'NONE',  ( -92.24499999999999034, -4.716976649647093289, -6.492361379858945902 ) ) ;
#11270=( BOUNDED_CURVE ( )  B_SPLINE_CURVE ( 2, ( #36557, #35812, #57256, #36884, #20678, #9089, #3759, #30505, #57974, #4113, #52003 ),
 .UNSPECIFIED., .F., .F. ) 
 B_SPLINE_CURVE_WITH_KNOTS ( ( 3, 2, 2, 2, 2, 3 ),
 ( 0.3152173913043403997, 0.3173913043478185925, 0.3195652173912967853, 0.3217391304347749781, 0.3239130434782532264, 0.3260869565217314192 ),
 .UNSPECIFIED. ) 
 CURVE ( )  GEOMETRIC_REPRESENTATION_ITEM ( )  RATIONAL_B_SPLINE_CURVE ( ( 1.000000000000167422, 0.9510565162949861095, 1.000000000000000000, 0.9510565162951535312, 1.000000000000000000, 0.9510565162951535312, 1.000000000000000000, 0.9510565162951535312, 1.000000000000000000, 0.9510565162953272811, 0.9999999999998262501 ) ) 
 REPRESENTATION_ITEM ( '' )  );
#11275=CARTESIAN_POINT ( 'NONE',  ( -122.0929263765338106, 3.094860106618433360, 9.524999999999991473 ) ) ;
#11276=CARTESIAN_POINT ( 'NONE',  ( -143.5449999999999875, -7.632228543268600340, -2.479861379858950166 ) ) ;
#11287=CARTESIAN_POINT ( 'NONE',  ( -155.5429263765338135, 9.058813317711329915, 2.943386871421369566 ) ) ;
#11290=CARTESIAN_POINT ( 'NONE',  ( -116.2429263765338021, 5.598654528085804216, 7.705886871421366635 ) ) ;
#11293=ORIENTED_EDGE ( 'NONE', *, *, #27044, .F. ) ;
#11294=CARTESIAN_POINT ( 'NONE',  ( -137.4549999999999841, 7.632228543268599452, -2.479861379858951942 ) ) ;
#11299=VERTEX_POINT ( 'NONE', #27744 ) ;
#11307=DIRECTION ( 'NONE',  ( -1.000000000000000000, -0.000000000000000000, -0.000000000000000000 ) ) ;
#11309=CARTESIAN_POINT ( 'NONE',  ( -56.90499999999998693, 2.607480562269069324, -8.024999999999993250 ) ) ;
#11310=CARTESIAN_POINT ( 'NONE',  ( -119.9949999999999903, -6.826472737025115478, 4.959722759717900331 ) ) ;
#11312=EDGE_LOOP ( 'NONE', ( #27949, #56843, #14730, #30559 ) ) ;
#11319=VERTEX_POINT ( 'NONE', #28437 ) ;
#11322=CARTESIAN_POINT ( 'NONE',  ( -172.5549999999999784, 0.000000000000000000, 8.024999999999991473 ) ) ;
#11325=CARTESIAN_POINT ( 'NONE',  ( -183.9999999999999147, -7.795498455245760461, 2.554623800884867624 ) ) ;
#11330=CARTESIAN_POINT ( 'NONE',  ( -86.45499999999998408, 7.632228543268599452, -2.479861379858951942 ) ) ;
#11337=CARTESIAN_POINT ( 'NONE',  ( -69.35707362346617799, 5.598654528085804216, 7.705886871421366635 ) ) ;
#11340=DIRECTION ( 'NONE',  ( -1.000000000000000000, -0.000000000000000000, -0.000000000000000000 ) ) ;
#11343=CARTESIAN_POINT ( 'NONE',  ( -106.2549999999999955, -4.716976649647092401, 6.492361379858946790 ) ) ;
#11345=CARTESIAN_POINT ( 'NONE',  ( -118.6449999999999818, 4.716976649647091513, -6.492361379858946790 ) ) ;
#11352=CARTESIAN_POINT ( 'NONE',  ( -156.7429263765338021, -5.598654528085803328, -7.705886871421366635 ) ) ;
#11353=CARTESIAN_POINT ( 'NONE',  ( -176.8449999999999989, -7.632228543268599452, 2.479861379858951054 ) ) ;
#11363=EDGE_CURVE ( 'NONE', #54295, #55506, #66016, .T. ) ;
#11364=CARTESIAN_POINT ( 'NONE',  ( -77.84292637653379643, 9.058813317711329915, -2.943386871421373119 ) ) ;
#11374=CARTESIAN_POINT ( 'NONE',  ( -78.74292637653380211, -5.598654528085803328, -7.705886871421366635 ) ) ;
#11376=CARTESIAN_POINT ( 'NONE',  ( -166.8549999999999898, 4.716976649647094177, 6.492361379858945902 ) ) ;
#11379=FACE_OUTER_BOUND ( 'NONE', #7343, .T. ) ;
#11386=CARTESIAN_POINT ( 'NONE',  ( -93.65499999999998693, -7.632228543268600340, -2.479861379858950166 ) ) ;
#11395=CARTESIAN_POINT ( 'NONE',  ( -62.09499999999998465, -2.607480562269071545, -8.024999999999991473 ) ) ;
#11408=CARTESIAN_POINT ( 'NONE',  ( -111.2049999999999983, -2.607480562269071545, -8.024999999999991473 ) ) ;
#11414=CARTESIAN_POINT ( 'NONE',  ( -152.9070736234662036, -3.094860106618429807, 9.524999999999991473 ) ) ;
#11417=CARTESIAN_POINT ( 'NONE',  ( -90.50707362346618368, 8.102448949553176405, 5.886773742842740909 ) ) ;
#11420=ORIENTED_EDGE ( 'NONE', *, *, #35925, .F. ) ;
#11425=CARTESIAN_POINT ( 'NONE',  ( -129.8050000000000068, -8.437984349512085203, 5.166775262442717831E-16 ) ) ;
#11430=CARTESIAN_POINT ( 'NONE',  ( -148.1950000000000216, 8.437984349512085203, -1.550032578732815448E-15 ) ) ;
#11432=CARTESIAN_POINT ( 'NONE',  ( -138.2949999999999875, -2.607480562269069768, 8.024999999999991473 ) ) ;
#11437=CARTESIAN_POINT ( 'NONE',  ( -51.05499999999999261, -9.827790563157499189E-16, -8.024999999999991473 ) ) ;
#11440=CARTESIAN_POINT ( 'NONE',  ( -57.44499999999999318, 0.000000000000000000, 8.024999999999991473 ) ) ;
#11446=EDGE_CURVE ( 'NONE', #55926, #11014, #19802, .T. ) ;
#11449=CARTESIAN_POINT ( 'NONE',  ( -107.5429263765337993, 9.058813317711329915, 2.943386871421369566 ) ) ;
#11478=CARTESIAN_POINT ( 'NONE',  ( -88.34499999999999886, 7.632228543268599452, -2.479861379858951942 ) ) ;
#11486=CARTESIAN_POINT ( 'NONE',  ( -174.8929263765337794, -8.102448949553174629, -5.886773742842741797 ) ) ;
#11492=AXIS2_PLACEMENT_3D ( 'NONE', #59784, #28432, #12262 ) ;
#11508=CARTESIAN_POINT ( 'NONE',  ( -166.8549999999999898, 4.716976649647094177, 6.492361379858945902 ) ) ;
#11512=CARTESIAN_POINT ( 'NONE',  ( -170.9950000000000330, -6.826472737025115478, 4.959722759717900331 ) ) ;
#11514=CARTESIAN_POINT ( 'NONE',  ( -169.3449999999999989, 7.632228543268599452, -2.479861379858951942 ) ) ;
#11519=CARTESIAN_POINT ( 'NONE',  ( -82.85499999999998977, 4.716976649647094177, 6.492361379858945902 ) ) ;
#11522=CARTESIAN_POINT ( 'NONE',  ( -82.04499999999998749, 7.632228543268600340, 2.479861379858949277 ) ) ;
#11535=CARTESIAN_POINT ( 'NONE',  ( -49.94292637653380496, 0.000000000000000000, 9.524999999999991473 ) ) ;
#11544=( BOUNDED_CURVE ( )  B_SPLINE_CURVE ( 2, ( #61259, #34523, #55977, #8157, #40180, #7787, #29236, #56685, #61578, #34873, #67231 ),
 .UNSPECIFIED., .F., .F. ) 
 B_SPLINE_CURVE_WITH_KNOTS ( ( 3, 2, 2, 2, 2, 3 ),
 ( 0.8586956521739130821, 0.8608695652173913304, 0.8630434782608695787, 0.8652173913043478271, 0.8673913043478260754, 0.8695652173913043237 ),
 .UNSPECIFIED. ) 
 CURVE ( )  GEOMETRIC_REPRESENTATION_ITEM ( )  RATIONAL_B_SPLINE_CURVE ( ( 1.000000000000000000, 0.9510565162951535312, 1.000000000000000000, 0.9510565162951535312, 1.000000000000000000, 0.9510565162951535312, 1.000000000000000000, 0.9510565162951535312, 1.000000000000000000, 0.9510565162951535312, 1.000000000000000000 ) ) 
 REPRESENTATION_ITEM ( '' )  );
#11546=CARTESIAN_POINT ( 'NONE',  ( -70.10707362346617799, 8.102448949553172852, -5.886773742842744461 ) ) ;
#11548=CARTESIAN_POINT ( 'NONE',  ( -116.4549999999999841, 7.632228543268599452, -2.479861379858951942 ) ) ;
#11560=ORIENTED_EDGE ( 'NONE', *, *, #52752, .T. ) ;
#11564=CARTESIAN_POINT ( 'NONE',  ( -117.3570736234661780, 5.598654528085804216, 7.705886871421366635 ) ) ;
#11566=CARTESIAN_POINT ( 'NONE',  ( -130.7929263765344956, -3.094860106607001171, 9.525000000008295942 ) ) ;
#11575=CARTESIAN_POINT ( 'NONE',  ( -52.49292637653380211, -8.102448949553172852, 5.886773742842742685 ) ) ;
#11578=CARTESIAN_POINT ( 'NONE',  ( -138.9549999999999841, -7.632228543268599452, 2.479861379858951054 ) ) ;
#11595=CARTESIAN_POINT ( 'NONE',  ( -54.80499999999999261, -8.437984349512085203, 5.166775262442717831E-16 ) ) ;
#11603=CARTESIAN_POINT ( 'NONE',  ( -97.19292637653379074, -10.01517768586948698, 6.132527647946031529E-16 ) ) ;
#11614=CARTESIAN_POINT ( 'NONE',  ( -111.7449999999999903, 4.716976649647094177, 6.492361379858945902 ) ) ;
#11616=CARTESIAN_POINT ( 'NONE',  ( -89.24499999999999034, -4.716976649647093289, -6.492361379858945902 ) ) ;
#11618=CARTESIAN_POINT ( 'NONE',  ( -190.0000000000000000, 6.735557395310424274E-16, -5.499999999999984901 ) ) ;
#11626=CARTESIAN_POINT ( 'NONE',  ( -127.1929263765338050, -10.01517768586948698, 6.132527647946031529E-16 ) ) ;
#11627=CARTESIAN_POINT ( 'NONE',  ( -145.1949999999999648, 8.437984349512085203, -1.550032578732815448E-15 ) ) ;
#11629=CARTESIAN_POINT ( 'NONE',  ( -47.84499999999997044, -7.632228543268599452, 2.479861379858951054 ) ) ;
#11642=CARTESIAN_POINT ( 'NONE',  ( -136.7049999999999841, 2.607480562269072433, 8.024999999999991473 ) ) ;
#11654=CARTESIAN_POINT ( 'NONE',  ( -94.85707362346616378, -5.598654528085803328, -7.705886871421366635 ) ) ;
#11656=CARTESIAN_POINT ( 'NONE',  ( -51.05499999999999261, -9.827790563157499189E-16, -8.024999999999991473 ) ) ;
#11657=CARTESIAN_POINT ( 'NONE',  ( -117.8949999999999676, 6.826472737025116366, 4.959722759717898555 ) ) ;
#11670=CARTESIAN_POINT ( 'NONE',  ( -173.7549999999999955, 4.716976649647091513, -6.492361379858946790 ) ) ;
#11672=CARTESIAN_POINT ( 'NONE',  ( -87.80707362346616662, 10.01517768586948698, -1.839758294383808966E-15 ) ) ;
#11682=CARTESIAN_POINT ( 'NONE',  ( -84.65500000000000114, -7.632228543268600340, -2.479861379858950166 ) ) ;
#11685=LINE ( 'NONE', #16311, #8159 ) ;
#11689=CARTESIAN_POINT ( 'NONE',  ( -66.65707362346616094, 9.058813317711329915, 2.943386871421369566 ) ) ;
#11691=( BOUNDED_CURVE ( )  B_SPLINE_CURVE ( 2, ( #9074, #68168, #68509, #10118, #25568, #62168, #30493, #47443, #4818, #63227, #40752 ),
 .UNSPECIFIED., .F., .F. ) 
 B_SPLINE_CURVE_WITH_KNOTS ( ( 3, 2, 2, 2, 2, 3 ),
 ( 0.1304347826086927065, 0.1326086956521709270, 0.1347826086956491198, 0.1369565217391273404, 0.1391304347826055610, 0.1413043478260837538 ),
 .UNSPECIFIED. ) 
 CURVE ( )  GEOMETRIC_REPRESENTATION_ITEM ( )  RATIONAL_B_SPLINE_CURVE ( ( 1.000000000000066169, 0.9510565162950872509, 1.000000000000000000, 0.9510565162951535312, 1.000000000000000000, 0.9510565162951535312, 1.000000000000000000, 0.9510565162951535312, 1.000000000000000000, 0.9510565162952253626, 0.9999999999999281686 ) ) 
 REPRESENTATION_ITEM ( '' )  );
#11698=CARTESIAN_POINT ( 'NONE',  ( -105.9549999999999983, -7.632228543268599452, 2.479861379858951054 ) ) ;
#11700=CARTESIAN_POINT ( 'NONE',  ( -113.3949999999999818, -6.826472737025115478, -4.959722759717899443 ) ) ;
#11707=CARTESIAN_POINT ( 'NONE',  ( -155.6929263765338192, 10.01517768586948698, -1.839758294383808571E-15 ) ) ;
#11709=CARTESIAN_POINT ( 'NONE',  ( -173.0949999999999989, -2.607480562269071545, -8.024999999999991473 ) ) ;
#11716=EDGE_LOOP ( 'NONE', ( #17657, #30621, #44474, #5405 ) ) ;
#11717=CARTESIAN_POINT ( 'NONE',  ( -70.04292637653379927, -9.058813317711329915, -2.943386871421370898 ) ) ;
#11723=CYLINDRICAL_SURFACE ( 'NONE', #58337, 9.524999999999991473 ) ;
#11726=CARTESIAN_POINT ( 'NONE',  ( -174.8049999999999784, -8.437984349512086979, 5.166775262442717831E-16 ) ) ;
#11736=CARTESIAN_POINT ( 'NONE',  ( -79.85499999999997556, 4.716976649647094177, 6.492361379858945902 ) ) ;
#11745=CARTESIAN_POINT ( 'NONE',  ( -65.99499999999996191, -6.826472737025115478, 4.959722759717900331 ) ) ;
#11746=ORIENTED_EDGE ( 'NONE', *, *, #59964, .T. ) ;
#11747=FACE_OUTER_BOUND ( 'NONE', #477, .T. ) ;
#11758=CARTESIAN_POINT ( 'NONE',  ( -115.8549999999999898, 4.716976649647094177, 6.492361379858945902 ) ) ;
#11761=CARTESIAN_POINT ( 'NONE',  ( -72.44292637653379074, -1.166476076187852838E-15, -9.524999999999991473 ) ) ;
#11766=CARTESIAN_POINT ( 'NONE',  ( -146.9070736234661467, -3.094860106618429807, 9.524999999999991473 ) ) ;
#11768=EDGE_CURVE ( 'NONE', #30865, #23696, #42718, .T. ) ;
#11770=CARTESIAN_POINT ( 'NONE',  ( -96.80707362346618083, 10.01517768586948698, -1.839758294383808571E-15 ) ) ;
#11771=EDGE_CURVE ( 'NONE', #59012, #36722, #61935, .T. ) ;
#11780=CARTESIAN_POINT ( 'NONE',  ( -128.9050000000000011, 2.607480562269068880, -8.024999999999993250 ) ) ;
#11783=CARTESIAN_POINT ( 'NONE',  ( -149.3949999999999818, -6.826472737025115478, -4.959722759717899443 ) ) ;
#11784=CARTESIAN_POINT ( 'NONE',  ( -133.1950000000000216, 8.437984349512086979, -1.550032578732815448E-15 ) ) ;
#11790=CARTESIAN_POINT ( 'NONE',  ( -48.35499999999998266, -4.716976649647093289, -6.492361379858945902 ) ) ;
#11791=CARTESIAN_POINT ( 'NONE',  ( -57.29499999999998039, -2.607480562269069768, 8.024999999999991473 ) ) ;
#11795=CARTESIAN_POINT ( 'NONE',  ( -91.19292637653380496, -10.01517768586948698, 6.132527647946031529E-16 ) ) ;
#11822=CARTESIAN_POINT ( 'NONE',  ( -95.84499999999998465, -7.632228543268599452, 2.479861379858951054 ) ) ;
#11831=CARTESIAN_POINT ( 'NONE',  ( -174.4429263765337907, -1.166476076187852838E-15, -9.524999999999991473 ) ) ;
#11844=CARTESIAN_POINT ( 'NONE',  ( -182.4570736234661865, -9.058813317711329915, 2.943386871421371787 ) ) ;
#11850=CARTESIAN_POINT ( 'NONE',  ( -114.5929263765346917, -3.094860106633086083, -9.524999999989345767 ) ) ;
#11852=CARTESIAN_POINT ( 'NONE',  ( -160.9429263765338192, 0.000000000000000000, 9.524999999999991473 ) ) ;
#11859=CARTESIAN_POINT ( 'NONE',  ( -162.0550000000000068, -9.827790563157499189E-16, -8.024999999999991473 ) ) ;
#11862=CARTESIAN_POINT ( 'NONE',  ( -178.6450000000000102, 4.716976649647091513, -6.492361379858946790 ) ) ;
#11865=CARTESIAN_POINT ( 'NONE',  ( -162.2949999999999875, -2.607480562269069768, 8.024999999999991473 ) ) ;
#11870=CARTESIAN_POINT ( 'NONE',  ( -69.05499999999999261, -9.827790563157499189E-16, -8.024999999999991473 ) ) ;
#11874=CARTESIAN_POINT ( 'NONE',  ( -81.44499999999999318, 0.000000000000000000, 8.024999999999991473 ) ) ;
#11881=( BOUNDED_CURVE ( )  B_SPLINE_CURVE ( 2, ( #53718, #42886, #64279, #26293, #69231, #47832, #16131, #53051, #4845, #15437, #37607 ),
 .UNSPECIFIED., .F., .F. ) 
 B_SPLINE_CURVE_WITH_KNOTS ( ( 3, 2, 2, 2, 2, 3 ),
 ( 0.08695652173912847560, 0.08913043478260668229, 0.09130434782608488897, 0.09347826086956310954, 0.09565217391304131622, 0.09782608695651952291 ),
 .UNSPECIFIED. ) 
 CURVE ( )  GEOMETRIC_REPRESENTATION_ITEM ( )  RATIONAL_B_SPLINE_CURVE ( ( 1.000000000000044187, 0.9510565162951095664, 1.000000000000000000, 0.9510565162951535312, 1.000000000000000000, 0.9510565162951535312, 1.000000000000000000, 0.9510565162951535312, 1.000000000000000000, 0.9510565162952034912, 0.9999999999999500400 ) ) 
 REPRESENTATION_ITEM ( '' )  );
#11897=CARTESIAN_POINT ( 'NONE',  ( -70.55707362346616662, -1.166476076187852838E-15, -9.524999999999991473 ) ) ;
#11899=CARTESIAN_POINT ( 'NONE',  ( -107.7549999999999955, 4.716976649647091513, -6.492361379858946790 ) ) ;
#11900=ORIENTED_EDGE ( 'NONE', *, *, #23989, .F. ) ;
#11912=ORIENTED_EDGE ( 'NONE', *, *, #19932, .F. ) ;
#11917=CARTESIAN_POINT ( 'NONE',  ( -153.0570736234661808, 0.000000000000000000, 9.524999999999991473 ) ) ;
#11918=CARTESIAN_POINT ( 'NONE',  ( -180.5929263765338817, -3.094860106619338413, -9.524999999999332445 ) ) ;
#11935=CARTESIAN_POINT ( 'NONE',  ( -141.2050000000000125, -2.607480562269071545, -8.024999999999991473 ) ) ;
#11937=ORIENTED_EDGE ( 'NONE', *, *, #65936, .F. ) ;
#11943=ORIENTED_EDGE ( 'NONE', *, *, #9650, .F. ) ;
#11946=CARTESIAN_POINT ( 'NONE',  ( -52.10499999999998266, -6.826472737025115478, 4.959722759717900331 ) ) ;
#11951=CARTESIAN_POINT ( 'NONE',  ( -128.8429263765337964, 9.058813317711329915, -2.943386871421373119 ) ) ;
#11952=ORIENTED_EDGE ( 'NONE', *, *, #20439, .T. ) ;
#11953=CARTESIAN_POINT ( 'NONE',  ( -144.8070736234661808, 10.01517768586948698, -1.839758294383808966E-15 ) ) ;
#11959=CARTESIAN_POINT ( 'NONE',  ( -113.8449999999999847, -7.632228543268599452, 2.479861379858951054 ) ) ;
#11962=CARTESIAN_POINT ( 'NONE',  ( -74.54499999999998749, -7.632228543268600340, -2.479861379858950166 ) ) ;
#11970=CARTESIAN_POINT ( 'NONE',  ( -124.9429263765338192, 0.000000000000000000, 9.524999999999991473 ) ) ;
#11971=CARTESIAN_POINT ( 'NONE',  ( -152.0949999999999420, -2.607480562269071545, -8.024999999999991473 ) ) ;
#11985=CARTESIAN_POINT ( 'NONE',  ( -141.0549999999999784, -9.827790563157499189E-16, -8.024999999999991473 ) ) ;
#11992=ORIENTED_EDGE ( 'NONE', *, *, #63706, .F. ) ;
#12001=CARTESIAN_POINT ( 'NONE',  ( -52.25499999999999545, -4.716976649647092401, 6.492361379858946790 ) ) ;
#12017=CARTESIAN_POINT ( 'NONE',  ( -176.1550000000000011, 7.632228543268600340, 2.479861379858949277 ) ) ;
#12025=ORIENTED_EDGE ( 'NONE', *, *, #12369, .T. ) ;
#12028=CARTESIAN_POINT ( 'NONE',  ( -85.10499999999997556, -6.826472737025115478, 4.959722759717900331 ) ) ;
#12032=CARTESIAN_POINT ( 'NONE',  ( -55.10707362346616378, 8.102448949553171076, -5.886773742842744461 ) ) ;
#12037=CARTESIAN_POINT ( 'NONE',  ( -106.1949999999999932, 8.437984349512085203, -1.550032578732815448E-15 ) ) ;
#12039=CARTESIAN_POINT ( 'NONE',  ( -15.00000000000000000, 10.90871211463577239, 5.000000000000000888 ) ) ;
#12040=CARTESIAN_POINT ( 'NONE',  ( -148.9429263765338192, 0.000000000000000000, 9.524999999999991473 ) ) ;
#12041=CARTESIAN_POINT ( 'NONE',  ( -180.8949999999999534, 6.826472737025116366, 4.959722759717898555 ) ) ;
#12050=CARTESIAN_POINT ( 'NONE',  ( -68.39292637653380780, 8.102448949553176405, 5.886773742842740909 ) ) ;
#12058=CARTESIAN_POINT ( 'NONE',  ( -79.34292637653379643, -9.058813317711329915, 2.943386871421371787 ) ) ;
#12061=CARTESIAN_POINT ( 'NONE',  ( -167.7549999999999955, 4.716976649647091513, -6.492361379858946790 ) ) ;
#12071=CARTESIAN_POINT ( 'NONE',  ( -85.10499999999997556, -6.826472737025113702, 4.959722759717902107 ) ) ;
#12073=EDGE_CURVE ( 'NONE', #39475, #59038, #63349, .T. ) ;
#12074=CARTESIAN_POINT ( 'NONE',  ( -72.80707362346615241, 10.01517768586948698, -1.839758294383808966E-15 ) ) ;
#12077=VERTEX_POINT ( 'NONE', #15204 ) ;
#12080=CARTESIAN_POINT ( 'NONE',  ( -67.19499999999999318, 8.437984349512085203, -1.550032578732815448E-15 ) ) ;
#12083=CARTESIAN_POINT ( 'NONE',  ( -48.89292637653380780, -8.102448949553174629, -5.886773742842741797 ) ) ;
#12092=CARTESIAN_POINT ( 'NONE',  ( -115.7049999999999983, 2.607480562269073321, 8.024999999999991473 ) ) ;
#12094=EDGE_CURVE ( 'NONE', #9643, #48114, #69658, .T. ) ;
#12100=CARTESIAN_POINT ( 'NONE',  ( -148.2570736234661979, 5.598654528085800663, -7.705886871421367523 ) ) ;
#12104=CARTESIAN_POINT ( 'NONE',  ( -82.55707362346618083, -1.166476076187852838E-15, -9.524999999999991473 ) ) ;
#12114=CARTESIAN_POINT ( 'NONE',  ( -131.6049999999999898, 6.826472737025113702, -4.959722759717902107 ) ) ;
#12118=CARTESIAN_POINT ( 'NONE',  ( -149.0949999999999704, -2.607480562269071545, -8.024999999999991473 ) ) ;
#12119=CARTESIAN_POINT ( 'NONE',  ( -128.5449999999999875, -7.632228543268600340, -2.479861379858950166 ) ) ;
#12121=CARTESIAN_POINT ( 'NONE',  ( -195.0000000000000000, 0.000000000000000000, 0.000000000000000000 ) ) ;
#12125=CARTESIAN_POINT ( 'NONE',  ( -47.75499999999999545, 4.716976649647091513, -6.492361379858946790 ) ) ;
#12126=CARTESIAN_POINT ( 'NONE',  ( -62.69499999999998607, -8.437984349512085203, 5.166775262442717831E-16 ) ) ;
#12131=CARTESIAN_POINT ( 'NONE',  ( -97.49292637653380211, -8.102448949553172852, 5.886773742842742685 ) ) ;
#12134=CARTESIAN_POINT ( 'NONE',  ( -81.05707362346618083, 0.000000000000000000, 9.524999999999991473 ) ) ;
#12156=CARTESIAN_POINT ( 'NONE',  ( -92.39499999999998181, -6.826472737025115478, -4.959722759717899443 ) ) ;
#12160=VECTOR ( 'NONE', #16579, 1000.000000000000000 ) ;
#12172=CARTESIAN_POINT ( 'NONE',  ( -178.1070736234661922, 8.102448949553171076, -5.886773742842744461 ) ) ;
#12176=CARTESIAN_POINT ( 'NONE',  ( -84.20707362346615810, 3.094860106618433360, 9.524999999999991473 ) ) ;
#12185=CARTESIAN_POINT ( 'NONE',  ( -155.7549999999999955, 4.716976649647091513, -6.492361379858946790 ) ) ;
#12188=CARTESIAN_POINT ( 'NONE',  ( -174.1449999999999818, -4.716976649647092401, 6.492361379858946790 ) ) ;
#12189=CARTESIAN_POINT ( 'NONE',  ( -155.9949999999999761, -6.826472737025113702, 4.959722759717902107 ) ) ;
#12194=CARTESIAN_POINT ( 'NONE',  ( -75.50499999999998124, -6.826472737025115478, -4.959722759717899443 ) ) ;
#12197=CARTESIAN_POINT ( 'NONE',  ( -66.89499999999996760, 6.826472737025115478, 4.959722759717899443 ) ) ;
#12211=VECTOR ( 'NONE', #35498, 1000.000000000000000 ) ;
#12224=VERTEX_POINT ( 'NONE', #38739 ) ;
#12225=CARTESIAN_POINT ( 'NONE',  ( -117.0549999999999926, -9.827790563157499189E-16, -8.024999999999991473 ) ) ;
#12233=CARTESIAN_POINT ( 'NONE',  ( -139.5570736234661808, -1.166476076187852838E-15, -9.524999999999991473 ) ) ;
#12240=CARTESIAN_POINT ( 'NONE',  ( -151.7070736234666128, -3.094860106624918394, -9.524999999995278799 ) ) ;
#12244=DIRECTION ( 'NONE',  ( -1.000000000000000000, -0.000000000000000000, -0.000000000000000000 ) ) ;
#12245=CARTESIAN_POINT ( 'NONE',  ( -46.55707362346617373, -1.166476076187852838E-15, -9.524999999999991473 ) ) ;
#12249=ORIENTED_EDGE ( 'NONE', *, *, #26378, .F. ) ;
#12254=CARTESIAN_POINT ( 'NONE',  ( -130.2549999999999955, -4.716976649647092401, 6.492361379858946790 ) ) ;
#12262=DIRECTION ( 'NONE',  ( 0.000000000000000000, 0.000000000000000000, 1.000000000000000000 ) ) ;
#12263=CARTESIAN_POINT ( 'NONE',  ( -55.85499999999998977, 4.716976649647094177, 6.492361379858945902 ) ) ;
#12269=FACE_OUTER_BOUND ( 'NONE', #38475, .T. ) ;
#12282=CARTESIAN_POINT ( 'NONE',  ( -95.99499999999997613, -6.826472737025113702, 4.959722759717902107 ) ) ;
#12284=CARTESIAN_POINT ( 'NONE',  ( -78.89499999999999602, 6.826472737025116366, 4.959722759717898555 ) ) ;
#12287=LINE ( 'NONE', #49268, #54129 ) ;
#12295=CARTESIAN_POINT ( 'NONE',  ( -121.3429263765338106, -9.058813317711329915, 2.943386871421371787 ) ) ;
#12296=CARTESIAN_POINT ( 'NONE',  ( -142.1949999999999932, 8.437984349512085203, -1.550032578732815448E-15 ) ) ;
#12299=CARTESIAN_POINT ( 'NONE',  ( -173.2429263765338305, 5.598654528085804216, 7.705886871421366635 ) ) ;
#12307=CARTESIAN_POINT ( 'NONE',  ( -98.90707362346724096, -3.094860106601085459, 9.525000000012594725 ) ) ;
#12311=CARTESIAN_POINT ( 'NONE',  ( -139.5549999999999784, 0.000000000000000000, 8.024999999999991473 ) ) ;
#12319=CIRCLE ( 'NONE', #69632, 9.525000000000000355 ) ;
#12325=CARTESIAN_POINT ( 'NONE',  ( -58.85499999999998977, 4.716976649647094177, 6.492361379858945902 ) ) ;
#12333=DIRECTION ( 'NONE',  ( -1.000000000000000000, -0.000000000000000000, -0.000000000000000000 ) ) ;
#12342=CARTESIAN_POINT ( 'NONE',  ( -160.1049999999999613, -6.826472737025115478, 4.959722759717900331 ) ) ;
#12348=DIRECTION ( 'NONE',  ( -1.000000000000000000, -0.000000000000000000, -0.000000000000000000 ) ) ;
#12354=CARTESIAN_POINT ( 'NONE',  ( -184.0000000000000000, 0.000000000000000000, 8.024999999999991473 ) ) ;
#12355=CARTESIAN_POINT ( 'NONE',  ( -111.0570736234661808, 0.000000000000000000, 9.524999999999991473 ) ) ;
#12356=CARTESIAN_POINT ( 'NONE',  ( -81.05499999999999261, -9.827790563157499189E-16, -8.024999999999991473 ) ) ;
#12369=EDGE_CURVE ( 'NONE', #13981, #47647, #45401, .T. ) ;
#12371=CARTESIAN_POINT ( 'NONE',  ( -111.5949999999999704, 2.607480562269073321, 8.024999999999991473 ) ) ;
#12378=CARTESIAN_POINT ( 'NONE',  ( -157.1929263765337907, -10.01517768586948698, 6.132527647946031529E-16 ) ) ;
#12379=CARTESIAN_POINT ( 'NONE',  ( -163.0449999999999875, 7.632228543268600340, 2.479861379858949277 ) ) ;
#12387=VERTEX_POINT ( 'NONE', #40110 ) ;
#12388=CARTESIAN_POINT ( 'NONE',  ( -63.89292637653380780, -8.102448949553172852, -5.886773742842741797 ) ) ;
#12398=EDGE_LOOP ( 'NONE', ( #29461, #6969, #12696, #43690 ) ) ;
#12399=CARTESIAN_POINT ( 'NONE',  ( -168.6550000000000011, -7.632228543268600340, -2.479861379858950166 ) ) ;
#12401=CARTESIAN_POINT ( 'NONE',  ( -111.4429263765338050, -1.166476076187852838E-15, -9.524999999999991473 ) ) ;
#12409=CARTESIAN_POINT ( 'NONE',  ( -85.40499999999998693, -2.607480562269069768, 8.024999999999991473 ) ) ;
#12415=CARTESIAN_POINT ( 'NONE',  ( -169.7929263765340124, -3.094860106615421547, 9.525000000002178169 ) ) ;
#12420=CARTESIAN_POINT ( 'NONE',  ( -66.89499999999996760, 6.826472737025116366, 4.959722759717898555 ) ) ;
#12429=CARTESIAN_POINT ( 'NONE',  ( -54.29499999999998039, -2.607480562269069768, 8.024999999999991473 ) ) ;
#12434=CARTESIAN_POINT ( 'NONE',  ( -111.5049999999999955, -6.826472737025115478, -4.959722759717899443 ) ) ;
#12441=CARTESIAN_POINT ( 'NONE',  ( -149.0070736234661979, -8.102448949553172852, -5.886773742842741797 ) ) ;
#12445=CARTESIAN_POINT ( 'NONE',  ( -84.65707362346616094, 9.058813317711329915, 2.943386871421369566 ) ) ;
#12453=CARTESIAN_POINT ( 'NONE',  ( -130.2549999999999955, -4.716976649647092401, 6.492361379858946790 ) ) ;
#12456=CARTESIAN_POINT ( 'NONE',  ( -55.34292637653378932, -9.058813317711329915, 2.943386871421371787 ) ) ;
#12457=CARTESIAN_POINT ( 'NONE',  ( -138.4449999999999932, 0.000000000000000000, 8.024999999999991473 ) ) ;
#12458=CARTESIAN_POINT ( 'NONE',  ( -131.6949999999999648, -8.437984349512086979, 5.166775262442717831E-16 ) ) ;
#12461=CARTESIAN_POINT ( 'NONE',  ( -146.9070736234666015, -3.094860106611035722, 9.525000000005366729 ) ) ;
#12464=EDGE_CURVE ( 'NONE', #11299, #37145, #63692, .T. ) ;
#12467=CARTESIAN_POINT ( 'NONE',  ( -48.95499999999996987, -7.632228543268599452, 2.479861379858951054 ) ) ;
#12468=CARTESIAN_POINT ( 'NONE',  ( -47.84499999999997044, -7.632228543268599452, 2.479861379858951054 ) ) ;
#12476=CARTESIAN_POINT ( 'NONE',  ( -98.69292637653380496, 10.01517768586948698, -1.839758294383808571E-15 ) ) ;
#12487=AXIS2_PLACEMENT_3D ( 'NONE', #23425, #7599, #7950 ) ;
#12495=DIRECTION ( 'NONE',  ( -1.000000000000000000, -0.000000000000000000, -0.000000000000000000 ) ) ;
#12499=ORIENTED_EDGE ( 'NONE', *, *, #2893, .T. ) ;
#12500=CARTESIAN_POINT ( 'NONE',  ( -93.05707362346616662, 0.000000000000000000, 9.524999999999991473 ) ) ;
#12502=CARTESIAN_POINT ( 'NONE',  ( -88.49500000000000455, 6.826472737025113702, -4.959722759717902107 ) ) ;
#12518=LINE ( 'NONE', #29394, #4668 ) ;
#12521=CARTESIAN_POINT ( 'NONE',  ( -181.2570736234661979, 5.598654528085800663, -7.705886871421367523 ) ) ;
#12526=CARTESIAN_POINT ( 'NONE',  ( -111.3570736234661780, 5.598654528085804216, 7.705886871421366635 ) ) ;
#12528=CARTESIAN_POINT ( 'NONE',  ( -84.95707362346617231, 9.058813317711329915, -2.943386871421373119 ) ) ;
#12536=EDGE_CURVE ( 'NONE', #20383, #2500, #1250, .T. ) ;
#12538=CARTESIAN_POINT ( 'NONE',  ( -156.0550000000000068, -9.827790563157499189E-16, -8.024999999999991473 ) ) ;
#12539=DIRECTION ( 'NONE',  ( 1.000000000000000000, 0.000000000000000000, 0.000000000000000000 ) ) ;
#12542=CARTESIAN_POINT ( 'NONE',  ( -168.8949999999999818, 6.826472737025116366, 4.959722759717898555 ) ) ;
#12543=CARTESIAN_POINT ( 'NONE',  ( -153.4449999999999932, 0.000000000000000000, 8.024999999999991473 ) ) ;
#12547=CARTESIAN_POINT ( 'NONE',  ( -76.10500000000000398, -6.826472737025115478, 4.959722759717900331 ) ) ;
#12551=CARTESIAN_POINT ( 'NONE',  ( -70.64499999999998181, 4.716976649647091513, -6.492361379858946790 ) ) ;
#12555=CARTESIAN_POINT ( 'NONE',  ( -176.2429263765338021, 5.598654528085804216, 7.705886871421366635 ) ) ;
#12576=CARTESIAN_POINT ( 'NONE',  ( -104.7549999999999812, 4.716976649647091513, -6.492361379858946790 ) ) ;
#12582=CARTESIAN_POINT ( 'NONE',  ( -56.69292637653380496, 10.01517768586948698, -1.839758294383808966E-15 ) ) ;
#12610=CARTESIAN_POINT ( 'NONE',  ( -129.5049999999999670, -6.826472737025115478, -4.959722759717899443 ) ) ;
#12611=CARTESIAN_POINT ( 'NONE',  ( -195.0000000000000000, 0.000000000000000000, 0.000000000000000000 ) ) ;
#12613=ORIENTED_EDGE ( 'NONE', *, *, #52743, .T. ) ;
#12622=ORIENTED_EDGE ( 'NONE', *, *, #19130, .T. ) ;
#12630=CARTESIAN_POINT ( 'NONE',  ( -182.2450000000000045, -4.716976649647093289, -6.492361379858945902 ) ) ;
#12632=VERTEX_POINT ( 'NONE', #50213 ) ;
#12635=CARTESIAN_POINT ( 'NONE',  ( -144.5070736234661695, 8.102448949553176405, 5.886773742842740909 ) ) ;
#12642=CARTESIAN_POINT ( 'NONE',  ( -100.9449999999999932, -9.827790563157499189E-16, -8.024999999999991473 ) ) ;
#12644=CARTESIAN_POINT ( 'NONE',  ( -74.99499999999999034, -6.826472737025115478, 4.959722759717900331 ) ) ;
#12650=CYLINDRICAL_SURFACE ( 'NONE', #39770, 9.524999999999991473 ) ;
#12652=CARTESIAN_POINT ( 'NONE',  ( -127.4929263765338163, -8.102448949553172852, 5.886773742842742685 ) ) ;
#12654=CARTESIAN_POINT ( 'NONE',  ( -138.5949999999999420, 2.607480562269073321, 8.024999999999991473 ) ) ;
#12667=CARTESIAN_POINT ( 'NONE',  ( -126.0570736234661808, 0.000000000000000000, 9.524999999999991473 ) ) ;
#12669=CARTESIAN_POINT ( 'NONE',  ( -139.1049999999999898, -6.826472737025113702, 4.959722759717902107 ) ) ;
#12676=LINE ( 'NONE', #54882, #57898 ) ;
#12682=CARTESIAN_POINT ( 'NONE',  ( -52.70499999999996277, 2.607480562269072433, 8.024999999999991473 ) ) ;
#12687=CARTESIAN_POINT ( 'NONE',  ( -88.64292637653380780, -5.598654528085801552, 7.705886871421367523 ) ) ;
#12696=ORIENTED_EDGE ( 'NONE', *, *, #63706, .T. ) ;
#12698=DIRECTION ( 'NONE',  ( -1.000000000000000000, -0.000000000000000000, -0.000000000000000000 ) ) ;
#12699=CARTESIAN_POINT ( 'NONE',  ( -157.5550000000000068, 0.000000000000000000, 8.024999999999991473 ) ) ;
#12701=EDGE_CURVE ( 'NONE', #31165, #56538, #34578, .T. ) ;
#12702=( BOUNDED_CURVE ( )  B_SPLINE_CURVE ( 2, ( #54307, #49745, #32493, #23012, #53955, #60286, #33555, #12083, #65912, #28604, #48743 ),
 .UNSPECIFIED., .F., .F. ) 
 B_SPLINE_CURVE_WITH_KNOTS ( ( 3, 2, 2, 2, 2, 3 ),
 ( 0.9782608695652174058, 0.9804347826086956541, 0.9826086956521739024, 0.9847826086956521507, 0.9869565217391303991, 0.9891304347826086474 ),
 .UNSPECIFIED. ) 
 CURVE ( )  GEOMETRIC_REPRESENTATION_ITEM ( )  RATIONAL_B_SPLINE_CURVE ( ( 1.000000000000000000, 0.9510565162951535312, 1.000000000000000000, 0.9510565162951535312, 1.000000000000000000, 0.9510565162951535312, 1.000000000000000000, 0.9510565162951535312, 1.000000000000000000, 0.9510565162951535312, 1.000000000000000000 ) ) 
 REPRESENTATION_ITEM ( '' )  );
#12708=VERTEX_POINT ( 'NONE', #5117 ) ;
#12711=CARTESIAN_POINT ( 'NONE',  ( -76.25499999999999545, -4.716976649647092401, 6.492361379858946790 ) ) ;
#12729=CARTESIAN_POINT ( 'NONE',  ( -110.8449999999999847, -7.632228543268599452, 2.479861379858951054 ) ) ;
#12734=CARTESIAN_POINT ( 'NONE',  ( -156.4429263765338192, -1.166476076187852838E-15, -9.524999999999991473 ) ) ;
#12737=CARTESIAN_POINT ( 'NONE',  ( -165.8949999999999818, 6.826472737025116366, 4.959722759717898555 ) ) ;
#12744=CARTESIAN_POINT ( 'NONE',  ( -67.34292637653379643, -9.058813317711329915, 2.943386871421371787 ) ) ;
#12751=CARTESIAN_POINT ( 'NONE',  ( -174.3549999999999898, -4.716976649647093289, -6.492361379858945902 ) ) ;
#12752=VERTEX_POINT ( 'NONE', #58948 ) ;
#12764=CARTESIAN_POINT ( 'NONE',  ( -83.45499999999998408, 7.632228543268599452, -2.479861379858951942 ) ) ;
#12767=CYLINDRICAL_SURFACE ( 'NONE', #19485, 9.524999999999991473 ) ;
#12770=CARTESIAN_POINT ( 'NONE',  ( -73.25707362346616947, 5.598654528085800663, -7.705886871421367523 ) ) ;
#12772=ADVANCED_FACE ( 'NONE', ( #20257 ), #47044, .T. ) ;
#12775=CARTESIAN_POINT ( 'NONE',  ( -113.6070736234661638, -8.102448949553174629, 5.886773742842742685 ) ) ;
#12779=CARTESIAN_POINT ( 'NONE',  ( -53.09499999999997755, -2.607480562269071545, -8.024999999999991473 ) ) ;
#12782=AXIS2_PLACEMENT_3D ( 'NONE', #49155, #43561, #37935 ) ;
#12787=CARTESIAN_POINT ( 'NONE',  ( -54.44499999999999318, 0.000000000000000000, 8.024999999999991473 ) ) ;
#12793=CARTESIAN_POINT ( 'NONE',  ( -104.4549999999999983, 7.632228543268599452, -2.479861379858951942 ) ) ;
#12799=CARTESIAN_POINT ( 'NONE',  ( -150.5070736234661410, 8.102448949553176405, 5.886773742842740909 ) ) ;
#12802=CARTESIAN_POINT ( 'NONE',  ( -80.75707362346616947, -5.598654528085801552, 7.705886871421367523 ) ) ;
#12811=CARTESIAN_POINT ( 'NONE',  ( -132.2049999999999841, -2.607480562269071545, -8.024999999999991473 ) ) ;
#12813=CARTESIAN_POINT ( 'NONE',  ( -146.2429263765338021, 5.598654528085804216, 7.705886871421366635 ) ) ;
#12815=CARTESIAN_POINT ( 'NONE',  ( -134.2450000000000045, -4.716976649647093289, -6.492361379858945902 ) ) ;
#12817=CARTESIAN_POINT ( 'NONE',  ( -130.3449999999999989, 7.632228543268599452, -2.479861379858951942 ) ) ;
#12823=CARTESIAN_POINT ( 'NONE',  ( -182.6929263765338192, 10.01517768586948698, -1.839758294383808571E-15 ) ) ;
#12824=CARTESIAN_POINT ( 'NONE',  ( -46.64499999999998892, 4.716976649647091513, -6.492361379858946790 ) ) ;
#12832=CARTESIAN_POINT ( 'NONE',  ( -95.99292637653377369, 8.102448949553171076, -5.886773742842744461 ) ) ;
#12842=ORIENTED_EDGE ( 'NONE', *, *, #34366, .T. ) ;
#12846=EDGE_LOOP ( 'NONE', ( #28392, #29939, #16482, #51287 ) ) ;
#12856=CARTESIAN_POINT ( 'NONE',  ( -94.64292637653380780, -5.598654528085801552, 7.705886871421367523 ) ) ;
#12864=CARTESIAN_POINT ( 'NONE',  ( -82.19499999999999318, 8.437984349512085203, -1.550032578732815448E-15 ) ) ;
#12873=ORIENTED_EDGE ( 'NONE', *, *, #8895, .T. ) ;
#12880=CARTESIAN_POINT ( 'NONE',  ( -175.5570736234661808, -1.166476076187852838E-15, -9.524999999999991473 ) ) ;
#12885=CARTESIAN_POINT ( 'NONE',  ( -116.0070736234661553, -8.102448949553172852, -5.886773742842741797 ) ) ;
#12895=CARTESIAN_POINT ( 'NONE',  ( -155.1550000000000011, 7.632228543268600340, 2.479861379858949277 ) ) ;
#12896=CARTESIAN_POINT ( 'NONE',  ( -183.3769980489784643, -0.6272992113221751431, -9.148001951021605294 ) ) ;
#12897=CARTESIAN_POINT ( 'NONE',  ( -168.7450000000000045, 4.716976649647094177, 6.492361379858945902 ) ) ;
#12898=CARTESIAN_POINT ( 'NONE',  ( -157.3449999999999989, 7.632228543268599452, -2.479861379858951942 ) ) ;
#12904=CARTESIAN_POINT ( 'NONE',  ( -77.75499999999999545, 4.716976649647091513, -6.492361379858946790 ) ) ;
#12906=CARTESIAN_POINT ( 'NONE',  ( -167.8429263765337964, 9.058813317711329915, -2.943386871421373119 ) ) ;
#12908=CARTESIAN_POINT ( 'NONE',  ( -68.69499999999999318, -8.437984349512086979, 5.166775262442717831E-16 ) ) ;
#12925=EDGE_CURVE ( 'NONE', #51005, #53684, #32532, .T. ) ;
#12941=CARTESIAN_POINT ( 'NONE',  ( -122.8449999999999847, -7.632228543268599452, 2.479861379858951054 ) ) ;
#12946=CARTESIAN_POINT ( 'NONE',  ( -10.44806848068614258, -11.82018413492187747, 2.075183112132959362 ) ) ;
#12964=CARTESIAN_POINT ( 'NONE',  ( -133.5549999999999784, 0.000000000000000000, 8.024999999999991473 ) ) ;
#12974=CARTESIAN_POINT ( 'NONE',  ( -51.65707362346616804, 9.058813317711329915, 2.943386871421369566 ) ) ;
#12975=CARTESIAN_POINT ( 'NONE',  ( -48.50499999999998835, -6.826472737025115478, -4.959722759717899443 ) ) ;
#12978=CARTESIAN_POINT ( 'NONE',  ( -184.1049999999999613, -6.826472737025115478, 4.959722759717900331 ) ) ;
#12986=VERTEX_POINT ( 'NONE', #1869 ) ;
#12991=CARTESIAN_POINT ( 'NONE',  ( -103.5549999999999926, 0.000000000000000000, 8.024999999999991473 ) ) ;
#12995=CARTESIAN_POINT ( 'NONE',  ( -104.8449999999999989, -7.632228543268599452, 2.479861379858951054 ) ) ;
#12997=CARTESIAN_POINT ( 'NONE',  ( -77.54499999999998749, -7.632228543268600340, -2.479861379858950166 ) ) ;
#13005=CARTESIAN_POINT ( 'NONE',  ( -117.4429263765338050, -1.166476076187852838E-15, -9.524999999999991473 ) ) ;
#13007=CARTESIAN_POINT ( 'NONE',  ( -134.8449999999999989, -7.632228543268599452, 2.479861379858951054 ) ) ;
#13016=( BOUNDED_CURVE ( )  B_SPLINE_CURVE ( 2, ( #5126, #32217, #52321, #68473, #64218, #53665, #37560, #41775, #26902, #63193, #36507 ),
 .UNSPECIFIED., .F., .F. ) 
 B_SPLINE_CURVE_WITH_KNOTS ( ( 3, 2, 2, 2, 2, 3 ),
 ( 0.2282608695652119657, 0.2304347826086901863, 0.2326086956521683791, 0.2347826086956465996, 0.2369565217391247924, 0.2391304347826030130 ),
 .UNSPECIFIED. ) 
 CURVE ( )  GEOMETRIC_REPRESENTATION_ITEM ( )  RATIONAL_B_SPLINE_CURVE ( ( 1.000000000000121680, 0.9510565162950315177, 1.000000000000000000, 0.9510565162951535312, 1.000000000000000000, 0.9510565162951535312, 1.000000000000000000, 0.9510565162951535312, 1.000000000000000000, 0.9510565162952816509, 0.9999999999998718803 ) ) 
 REPRESENTATION_ITEM ( '' )  );
#13018=CARTESIAN_POINT ( 'NONE',  ( -62.39292637653380069, 8.102448949553176405, 5.886773742842740909 ) ) ;
#13024=CARTESIAN_POINT ( 'NONE',  ( -135.2050000000000125, -2.607480562269071545, -8.024999999999991473 ) ) ;
#13041=CARTESIAN_POINT ( 'NONE',  ( -50.00499999999998835, 6.826472737025115478, 4.959722759717899443 ) ) ;
#13047=CARTESIAN_POINT ( 'NONE',  ( -88.79292637653379927, -3.094860106618429807, 9.524999999999991473 ) ) ;
#13052=DIRECTION ( 'NONE',  ( -1.000000000000000000, -0.000000000000000000, -0.000000000000000000 ) ) ;
#13054=CARTESIAN_POINT ( 'NONE',  ( -195.0000000000000000, 0.000000000000000000, 9.524999999999991473 ) ) ;
#13055=CARTESIAN_POINT ( 'NONE',  ( -159.6550000000000011, -7.632228543268600340, -2.479861379858950166 ) ) ;
#13066=CARTESIAN_POINT ( 'NONE',  ( -75.05499999999997840, -9.827790563157499189E-16, -8.024999999999991473 ) ) ;
#13067=VERTEX_POINT ( 'NONE', #44878 ) ;
#13070=CARTESIAN_POINT ( 'NONE',  ( -151.4070736234665162, 3.094860106611941220, -9.525000000004705925 ) ) ;
#13074=CARTESIAN_POINT ( 'NONE',  ( -53.15707362346616804, -9.058813317711329915, -2.943386871421370898 ) ) ;
#13078=CARTESIAN_POINT ( 'NONE',  ( -103.3449999999999989, 7.632228543268599452, -2.479861379858951942 ) ) ;
#13081=CARTESIAN_POINT ( 'NONE',  ( -18.97010937149592280, 11.60744552740335855, 3.056979887745398194 ) ) ;
#13082=CARTESIAN_POINT ( 'NONE',  ( -146.2429263765338021, 5.598654528085804216, 7.705886871421366635 ) ) ;
#13084=CARTESIAN_POINT ( 'NONE',  ( -167.8449999999999989, -7.632228543268599452, 2.479861379858951054 ) ) ;
#13085=EDGE_CURVE ( 'NONE', #56538, #3684, #6241, .T. ) ;
#13097=CARTESIAN_POINT ( 'NONE',  ( -158.1550000000000011, 7.632228543268600340, 2.479861379858949277 ) ) ;
#13104=EDGE_CURVE ( 'NONE', #16901, #29002, #49395, .T. ) ;
#13107=ADVANCED_FACE ( 'NONE', ( #30362 ), #20173, .T. ) ;
#13110=( BOUNDED_CURVE ( )  B_SPLINE_CURVE ( 2, ( #37033, #52159, #35961, #47608, #3916, #21145, #15229, #4619, #20822, #31009, #30652 ),
 .UNSPECIFIED., .F., .F. ) 
 B_SPLINE_CURVE_WITH_KNOTS ( ( 3, 2, 2, 2, 2, 3 ),
 ( 0.2934782608695582495, 0.2956521739130364423, 0.2978260869565146907, 0.2999999999999928835, 0.3021739130434711318, 0.3043478260869493801 ),
 .UNSPECIFIED. ) 
 CURVE ( )  GEOMETRIC_REPRESENTATION_ITEM ( )  RATIONAL_B_SPLINE_CURVE ( ( 1.000000000000157430, 0.9510565162949961016, 1.000000000000000000, 0.9510565162951535312, 1.000000000000000000, 0.9510565162951535312, 1.000000000000000000, 0.9510565162951535312, 1.000000000000000000, 0.9510565162953147356, 0.9999999999998387956 ) ) 
 REPRESENTATION_ITEM ( '' )  );
#13115=CARTESIAN_POINT ( 'NONE',  ( -87.50499999999995282, -6.826472737025113702, -4.959722759717900331 ) ) ;
#13117=UNCERTAINTY_MEASURE_WITH_UNIT (LENGTH_MEASURE( 1.000000000000000082E-05 ), #18254, 'distance_accuracy_value', 'NONE');
#13121=CARTESIAN_POINT ( 'NONE',  ( -113.4570736234661723, -9.058813317711329915, 2.943386871421371787 ) ) ;
#13123=DIRECTION ( 'NONE',  ( 0.000000000000000000, 0.000000000000000000, -1.000000000000000000 ) ) ;
#13125=CARTESIAN_POINT ( 'NONE',  ( -50.39499999999999602, -6.826472737025115478, -4.959722759717899443 ) ) ;
#13133=CARTESIAN_POINT ( 'NONE',  ( -50.84499999999997044, -7.632228543268599452, 2.479861379858951054 ) ) ;
#13137=CARTESIAN_POINT ( 'NONE',  ( -99.95499999999998408, -7.632228543268599452, 2.479861379858951054 ) ) ;
#13141=CARTESIAN_POINT ( 'NONE',  ( -141.0570736234661808, 0.000000000000000000, 9.524999999999991473 ) ) ;
#13144=CARTESIAN_POINT ( 'NONE',  ( -83.45707362346617231, -9.058813317711329915, 2.943386871421371787 ) ) ;
#13145=CARTESIAN_POINT ( 'NONE',  ( -95.69292637653379074, 10.01517768586948698, -1.839758294383808966E-15 ) ) ;
#13146=CARTESIAN_POINT ( 'NONE',  ( -43.99999999999999289, 0.000000000000000000, 9.525000000000000355 ) ) ;
#13149=CARTESIAN_POINT ( 'NONE',  ( -122.7549999999999955, 4.716976649647091513, -6.492361379858946790 ) ) ;
#13153=CARTESIAN_POINT ( 'NONE',  ( -136.0449999999999875, 7.632228543268600340, 2.479861379858949277 ) ) ;
#13154=CARTESIAN_POINT ( 'NONE',  ( -122.3949999999999818, -6.826472737025113702, -4.959722759717900331 ) ) ;
#13160=CARTESIAN_POINT ( 'NONE',  ( -179.5429263765338135, 9.058813317711329915, 2.943386871421369566 ) ) ;
#13170=CARTESIAN_POINT ( 'NONE',  ( -93.44292637653380496, -1.166476076187852838E-15, -9.524999999999991473 ) ) ;
#13177=CARTESIAN_POINT ( 'NONE',  ( -195.0000000000000000, 0.000000000000000000, 0.000000000000000000 ) ) ;
#13191=ORIENTED_EDGE ( 'NONE', *, *, #9650, .T. ) ;
#13201=CARTESIAN_POINT ( 'NONE',  ( -80.09499999999998465, -2.607480562269071545, -8.024999999999991473 ) ) ;
#13211=VERTEX_POINT ( 'NONE', #26731 ) ;
#13213=CARTESIAN_POINT ( 'NONE',  ( -137.2429263765338021, 5.598654528085804216, 7.705886871421366635 ) ) ;
#13216=CARTESIAN_POINT ( 'NONE',  ( -178.8570736234661638, -5.598654528085803328, -7.705886871421366635 ) ) ;
#13219=CARTESIAN_POINT ( 'NONE',  ( -109.1070736234661922, 8.102448949553171076, -5.886773742842744461 ) ) ;
#13221=CARTESIAN_POINT ( 'NONE',  ( -183.1015393889102256, 5.789891952623192672, -7.443705283220353408 ) ) ;
#13228=CARTESIAN_POINT ( 'NONE',  ( -148.1049999999999898, -6.826472737025115478, 4.959722759717900331 ) ) ;
#13230=CARTESIAN_POINT ( 'NONE',  ( -183.7787065195572609, -7.888957336882999272, -3.789685084752649313 ) ) ;
#13231=CARTESIAN_POINT ( 'NONE',  ( -168.1449999999999818, -4.716976649647092401, 6.492361379858946790 ) ) ;
#13232=CARTESIAN_POINT ( 'NONE',  ( -161.0949999999999704, -2.607480562269071545, -8.024999999999991473 ) ) ;
#13234=CARTESIAN_POINT ( 'NONE',  ( -66.44292637653380496, -1.166476076187852838E-15, -9.524999999999991473 ) ) ;
#13237=CARTESIAN_POINT ( 'NONE',  ( -122.3929263765337936, 8.102448949553176405, 5.886773742842740909 ) ) ;
#13238=CARTESIAN_POINT ( 'NONE',  ( -70.40499999999997272, -2.607480562269069768, 8.024999999999991473 ) ) ;
#13244=CARTESIAN_POINT ( 'NONE',  ( -68.24499999999999034, -4.716976649647093289, -6.492361379858945902 ) ) ;
#13270=ORIENTED_EDGE ( 'NONE', *, *, #728, .F. ) ;
#13274=CARTESIAN_POINT ( 'NONE',  ( -82.85707362346616378, -5.598654528085803328, -7.705886871421366635 ) ) ;
#13276=CARTESIAN_POINT ( 'NONE',  ( -108.8949999999999960, 6.826472737025116366, 4.959722759717898555 ) ) ;
#13281=CARTESIAN_POINT ( 'NONE',  ( -10.06570109130832336, -11.97273657574575090, -0.8246214522176227302 ) ) ;
#13289=CARTESIAN_POINT ( 'NONE',  ( -141.0570736234661808, 0.000000000000000000, 9.524999999999991473 ) ) ;
#13295=CARTESIAN_POINT ( 'NONE',  ( -168.4429263765337907, -1.166476076187852838E-15, -9.524999999999991473 ) ) ;
#13297=CARTESIAN_POINT ( 'NONE',  ( -135.8049999999999500, -8.437984349512085203, 5.166775262442717831E-16 ) ) ;
#13298=CYLINDRICAL_SURFACE ( 'NONE', #17411, 5.499999999999985789 ) ;
#13316=CARTESIAN_POINT ( 'NONE',  ( -57.35707362346617799, 5.598654528085804216, 7.705886871421366635 ) ) ;
#13325=CARTESIAN_POINT ( 'NONE',  ( -97.70499999999998408, 2.607480562269073321, 8.024999999999991473 ) ) ;
#13331=CARTESIAN_POINT ( 'NONE',  ( -101.3949999999999676, -6.826472737025113702, -4.959722759717900331 ) ) ;
#13334=CARTESIAN_POINT ( 'NONE',  ( -75.74499999999999034, 4.716976649647094177, 6.492361379858945902 ) ) ;
#13342=CARTESIAN_POINT ( 'NONE',  ( -113.2429263765338163, 5.598654528085804216, 7.705886871421366635 ) ) ;
#13343=CARTESIAN_POINT ( 'NONE',  ( -138.2949999999999591, -2.607480562269069768, 8.024999999999991473 ) ) ;
#13346=VECTOR ( 'NONE', #58504, 1000.000000000000000 ) ;
#13349=CARTESIAN_POINT ( 'NONE',  ( -174.1429263765338078, 5.598654528085800663, -7.705886871421367523 ) ) ;
#13356=FACE_OUTER_BOUND ( 'NONE', #14020, .T. ) ;
#13360=CARTESIAN_POINT ( 'NONE',  ( -129.2049999999999841, -2.607480562269071545, -8.024999999999991473 ) ) ;
#13362=CARTESIAN_POINT ( 'NONE',  ( -121.1070736234661922, 8.102448949553171076, -5.886773742842744461 ) ) ;
#13391=CARTESIAN_POINT ( 'NONE',  ( -158.1550000000000011, 7.632228543268600340, 2.479861379858949277 ) ) ;
#13399=( BOUNDED_CURVE ( )  B_SPLINE_CURVE ( 2, ( #68436, #14628, #24804, #41041, #9359, #41735, #31473, #3317, #63160, #26203, #10048 ),
 .UNSPECIFIED., .F., .F. ) 
 B_SPLINE_CURVE_WITH_KNOTS ( ( 3, 2, 2, 2, 2, 3 ),
 ( 0.2499999999999940603, 0.2521739130434722531, 0.2543478260869504459, 0.2565217391304287498, 0.2586956521739069426, 0.2608695652173851354 ),
 .UNSPECIFIED. ) 
 CURVE ( )  GEOMETRIC_REPRESENTATION_ITEM ( )  RATIONAL_B_SPLINE_CURVE ( ( 1.000000000000133671, 0.9510565162950198603, 1.000000000000000000, 0.9510565162951535312, 1.000000000000000000, 0.9510565162951535312, 1.000000000000000000, 0.9510565162951535312, 1.000000000000000000, 0.9510565162952923091, 0.9999999999998612221 ) ) 
 REPRESENTATION_ITEM ( '' )  );
#13402=CARTESIAN_POINT ( 'NONE',  ( -47.75499999999999545, 4.716976649647091513, -6.492361379858946790 ) ) ;
#13404=CARTESIAN_POINT ( 'NONE',  ( -80.30499999999999261, 8.437984349512085203, -1.550032578732815448E-15 ) ) ;
#13416=ADVANCED_FACE ( 'NONE', ( #50304 ), #29156, .T. ) ;
#13418=CARTESIAN_POINT ( 'NONE',  ( -103.9449999999999932, -9.827790563157499189E-16, -8.024999999999991473 ) ) ;
#13421=CARTESIAN_POINT ( 'NONE',  ( -97.10707362346616378, 8.102448949553172852, -5.886773742842744461 ) ) ;
#13424=CARTESIAN_POINT ( 'NONE',  ( -145.4929263765338021, -8.102448949553172852, 5.886773742842742685 ) ) ;
#13425=CARTESIAN_POINT ( 'NONE',  ( -166.4950000000000045, 6.826472737025113702, -4.959722759717902107 ) ) ;
#13444=CARTESIAN_POINT ( 'NONE',  ( -158.4549999999999841, 7.632228543268599452, -2.479861379858951942 ) ) ;
#13456=CARTESIAN_POINT ( 'NONE',  ( -77.60499999999997556, 6.826472737025113702, -4.959722759717902107 ) ) ;
#13467=CARTESIAN_POINT ( 'NONE',  ( -50.24499999999998323, -4.716976649647093289, -6.492361379858945902 ) ) ;
#13475=CARTESIAN_POINT ( 'NONE',  ( -54.89499999999997470, 6.826472737025115478, 4.959722759717899443 ) ) ;
#13478=CARTESIAN_POINT ( 'NONE',  ( -108.2049999999999983, -2.607480562269071545, -8.024999999999991473 ) ) ;
#13484=CARTESIAN_POINT ( 'NONE',  ( -141.5070736234661126, 8.102448949553176405, 5.886773742842740909 ) ) ;
#13488=CARTESIAN_POINT ( 'NONE',  ( -89.45707362346618652, -9.058813317711329915, 2.943386871421371787 ) ) ;
#13490=CARTESIAN_POINT ( 'NONE',  ( -95.99292637653378790, 8.102448949553172852, -5.886773742842744461 ) ) ;
#13494=CARTESIAN_POINT ( 'NONE',  ( -117.2049999999999841, -2.607480562269071545, -8.024999999999991473 ) ) ;
#13496=CARTESIAN_POINT ( 'NONE',  ( -133.9449999999999932, -9.827790563157499189E-16, -8.024999999999991473 ) ) ;
#13498=AXIS2_PLACEMENT_3D ( 'NONE', #67884, #14764, #30557 ) ;
#13499=CARTESIAN_POINT ( 'NONE',  ( -115.9449999999999932, -9.827790563157499189E-16, -8.024999999999991473 ) ) ;
#13508=CARTESIAN_POINT ( 'NONE',  ( -168.2929263765337851, 3.094860106618428031, -9.524999999999993250 ) ) ;
#13510=CARTESIAN_POINT ( 'NONE',  ( -52.94499999999999318, -9.827790563157499189E-16, -8.024999999999991473 ) ) ;
#13518=CARTESIAN_POINT ( 'NONE',  ( -86.84292637653381064, 9.058813317711329915, -2.943386871421373119 ) ) ;
#13521=( BOUNDED_CURVE ( )  B_SPLINE_CURVE ( 2, ( #6798, #66236, #12770, #55696, #18062, #12074, #21966, #17732, #50090, #28225, #39547 ),
 .UNSPECIFIED., .F., .F. ) 
 B_SPLINE_CURVE_WITH_KNOTS ( ( 3, 2, 2, 2, 2, 3 ),
 ( 0.7934782608695651884, 0.7956521739130434367, 0.7978260869565216851, 0.8000000000000000444, 0.8021739130434782927, 0.8043478260869565410 ),
 .UNSPECIFIED. ) 
 CURVE ( )  GEOMETRIC_REPRESENTATION_ITEM ( )  RATIONAL_B_SPLINE_CURVE ( ( 1.000000000000000000, 0.9510565162951535312, 1.000000000000000000, 0.9510565162951535312, 1.000000000000000000, 0.9510565162951535312, 1.000000000000000000, 0.9510565162951535312, 1.000000000000000000, 0.9510565162951535312, 1.000000000000000000 ) ) 
 REPRESENTATION_ITEM ( '' )  );
#13527=CARTESIAN_POINT ( 'NONE',  ( -124.5570736234661808, -1.166476076187852838E-15, -9.524999999999991473 ) ) ;
#13535=VECTOR ( 'NONE', #44647, 1000.000000000000000 ) ;
#13547=CARTESIAN_POINT ( 'NONE',  ( -83.39499999999998181, -6.826472737025115478, -4.959722759717899443 ) ) ;
#13555=CARTESIAN_POINT ( 'NONE',  ( -76.19292637653380496, -10.01517768586948698, 6.132527647946031529E-16 ) ) ;
#13564=CARTESIAN_POINT ( 'NONE',  ( -174.2070736234661581, 3.094860106618433360, 9.524999999999991473 ) ) ;
#13569=CARTESIAN_POINT ( 'NONE',  ( -113.6070736234661780, -8.102448949553172852, 5.886773742842742685 ) ) ;
#13570=CARTESIAN_POINT ( 'NONE',  ( -183.2934834974413718, 1.440814635842406100, -9.147492737475964475 ) ) ;
#13579=CARTESIAN_POINT ( 'NONE',  ( -153.6549999999999727, -7.632228543268600340, -2.479861379858950166 ) ) ;
#13583=CARTESIAN_POINT ( 'NONE',  ( -160.0449999999999875, 7.632228543268600340, 2.479861379858949277 ) ) ;
#13585=CARTESIAN_POINT ( 'NONE',  ( -152.8449999999999989, -7.632228543268599452, 2.479861379858951054 ) ) ;
#13590=CARTESIAN_POINT ( 'NONE',  ( -121.9429263765338050, 0.000000000000000000, 9.524999999999991473 ) ) ;
#13591=CARTESIAN_POINT ( 'NONE',  ( -62.60499999999998266, 6.826472737025113702, -4.959722759717902107 ) ) ;
#13593=CARTESIAN_POINT ( 'NONE',  ( -167.0929263765340238, 3.094860106622062901, 9.524999999997353584 ) ) ;
#13594=CARTESIAN_POINT ( 'NONE',  ( -75.89499999999998181, 6.826472737025115478, 4.959722759717899443 ) ) ;
#13599=UNCERTAINTY_MEASURE_WITH_UNIT (LENGTH_MEASURE( 1.000000000000000082E-05 ), #10340, 'distance_accuracy_value', 'NONE');
#13602=CARTESIAN_POINT ( 'NONE',  ( -160.5570736234661808, -1.166476076187852838E-15, -9.524999999999991473 ) ) ;
#13609=CARTESIAN_POINT ( 'NONE',  ( -119.6929263765338050, 10.01517768586948698, -1.839758294383808966E-15 ) ) ;
#13626=CARTESIAN_POINT ( 'NONE',  ( -195.0000000000000000, 0.000000000000000000, 9.524999999999991473 ) ) ;
#13632=CARTESIAN_POINT ( 'NONE',  ( -109.6449999999999960, 4.716976649647091513, -6.492361379858946790 ) ) ;
#13637=CARTESIAN_POINT ( 'NONE',  ( -14.67032170310171146, -10.90871211463571200, -5.000000000000000000 ) ) ;
#13646=ADVANCED_FACE ( 'NONE', ( #21746 ), #4503, .T. ) ;
#13654=CARTESIAN_POINT ( 'NONE',  ( -136.2549999999999955, -4.716976649647092401, 6.492361379858946790 ) ) ;
#13669=CARTESIAN_POINT ( 'NONE',  ( -48.20499999999999829, -2.607480562269071545, -8.024999999999991473 ) ) ;
#13672=CARTESIAN_POINT ( 'NONE',  ( -176.3050000000000068, 8.437984349512085203, -1.550032578732815448E-15 ) ) ;
#13674=CARTESIAN_POINT ( 'NONE',  ( -59.00707362346616236, -8.102448949553172852, -5.886773742842741797 ) ) ;
#13677=CARTESIAN_POINT ( 'NONE',  ( -181.1949999999999363, 8.437984349512086979, -1.550032578732815448E-15 ) ) ;
#13685=CARTESIAN_POINT ( 'NONE',  ( -104.4549999999999983, 7.632228543268599452, -2.479861379858951942 ) ) ;
#13690=CARTESIAN_POINT ( 'NONE',  ( -100.1949999999999790, 8.437984349512086979, -1.550032578732815448E-15 ) ) ;
#13692=CARTESIAN_POINT ( 'NONE',  ( -65.09499999999998465, -2.607480562269071545, -8.024999999999991473 ) ) ;
#13694=CARTESIAN_POINT ( 'NONE',  ( -56.60707362346617089, -8.102448949553174629, 5.886773742842742685 ) ) ;
#13700=CARTESIAN_POINT ( 'NONE',  ( -112.4929263765337879, -8.102448949553172852, 5.886773742842742685 ) ) ;
#13701=CARTESIAN_POINT ( 'NONE',  ( -127.9449999999999790, -9.827790563157499189E-16, -8.024999999999991473 ) ) ;
#13708=ORIENTED_EDGE ( 'NONE', *, *, #35192, .F. ) ;
#13710=CARTESIAN_POINT ( 'NONE',  ( -63.14292637653380780, 5.598654528085800663, -7.705886871421367523 ) ) ;
#13718=CARTESIAN_POINT ( 'NONE',  ( -135.8049999999999784, -8.437984349512086979, 5.166775262442717831E-16 ) ) ;
#13721=CARTESIAN_POINT ( 'NONE',  ( -121.5570736234661808, -1.166476076187852838E-15, -9.524999999999991473 ) ) ;
#13729=ORIENTED_EDGE ( 'NONE', *, *, #49812, .F. ) ;
#13733=CARTESIAN_POINT ( 'NONE',  ( -195.0000000000000000, 1.166476076187852838E-15, -9.524999999999991473 ) ) ;
#13740=DIRECTION ( 'NONE',  ( 0.000000000000000000, 0.000000000000000000, 1.000000000000000000 ) ) ;
#13741=EDGE_CURVE ( 'NONE', #2194, #1270, #26946, .T. ) ;
#13747=CARTESIAN_POINT ( 'NONE',  ( -195.0000000000000000, 1.166476076187852838E-15, -9.524999999999991473 ) ) ;
#13749=CARTESIAN_POINT ( 'NONE',  ( -195.0000000000000000, 0.000000000000000000, 9.524999999999991473 ) ) ;
#13750=CARTESIAN_POINT ( 'NONE',  ( -161.3050000000000068, 8.437984349512085203, -1.550032578732815448E-15 ) ) ;
#13766=CARTESIAN_POINT ( 'NONE',  ( -78.65499999999998693, -7.632228543268600340, -2.479861379858950166 ) ) ;
#13780=CARTESIAN_POINT ( 'NONE',  ( -101.8449999999999847, -7.632228543268599452, 2.479861379858951054 ) ) ;
#13787=FACE_OUTER_BOUND ( 'NONE', #27493, .T. ) ;
#13789=CARTESIAN_POINT ( 'NONE',  ( -147.1429263765338078, 5.598654528085800663, -7.705886871421367523 ) ) ;
#13791=CARTESIAN_POINT ( 'NONE',  ( -167.2450000000000045, -4.716976649647093289, -6.492361379858945902 ) ) ;
#13804=CARTESIAN_POINT ( 'NONE',  ( -157.8549999999999898, 4.716976649647094177, 6.492361379858945902 ) ) ;
#13808=DIRECTION ( 'NONE',  ( -1.000000000000000000, -0.000000000000000000, -0.000000000000000000 ) ) ;
#13810=ORIENTED_EDGE ( 'NONE', *, *, #45943, .T. ) ;
#13818=CARTESIAN_POINT ( 'NONE',  ( -75.35499999999998977, -4.716976649647093289, -6.492361379858945902 ) ) ;
#13820=( BOUNDED_CURVE ( )  B_SPLINE_CURVE ( 2, ( #8045, #1677, #7686, #60127, #38720, #34761, #65752, #28428, #55540, #49940, #50274 ),
 .UNSPECIFIED., .F., .F. ) 
 B_SPLINE_CURVE_WITH_KNOTS ( ( 3, 2, 2, 2, 2, 3 ),
 ( 0.1956521739130387683, 0.1978260869565169611, 0.1999999999999951816, 0.2021739130434734022, 0.2043478260869516228, 0.2065217391304298156 ),
 .UNSPECIFIED. ) 
 CURVE ( )  GEOMETRIC_REPRESENTATION_ITEM ( )  RATIONAL_B_SPLINE_CURVE ( ( 1.000000000000106137, 0.9510565162950472828, 1.000000000000000000, 0.9510565162951535312, 1.000000000000000000, 0.9510565162951535312, 1.000000000000000000, 0.9510565162951535312, 1.000000000000000000, 0.9510565162952654417, 0.9999999999998880895 ) ) 
 REPRESENTATION_ITEM ( '' )  );
#13833=CARTESIAN_POINT ( 'NONE',  ( -48.59499999999997755, 2.607480562269073321, 8.024999999999991473 ) ) ;
#13839=CARTESIAN_POINT ( 'NONE',  ( -52.94499999999999318, -9.827790563157499189E-16, -8.024999999999991473 ) ) ;
#13843=CARTESIAN_POINT ( 'NONE',  ( -103.8549999999999898, 4.716976649647094177, 6.492361379858945902 ) ) ;
#13848=CARTESIAN_POINT ( 'NONE',  ( -138.5070736234661695, 8.102448949553176405, 5.886773742842740909 ) ) ;
#13852=CARTESIAN_POINT ( 'NONE',  ( -72.95707362346617231, 9.058813317711329915, -2.943386871421373119 ) ) ;
#13856=CARTESIAN_POINT ( 'NONE',  ( -18.97318813750202082, -11.60852854622079455, -3.052579355033961495 ) ) ;
#13860=CARTESIAN_POINT ( 'NONE',  ( -120.2049999999999983, -2.607480562269071545, -8.024999999999991473 ) ) ;
#13862=CARTESIAN_POINT ( 'NONE',  ( -138.1449999999999818, -4.716976649647092401, 6.492361379858946790 ) ) ;
#13863=CARTESIAN_POINT ( 'NONE',  ( -120.2949999999999733, -2.607480562269069768, 8.024999999999991473 ) ) ;
#13871=CARTESIAN_POINT ( 'NONE',  ( -171.8929263765338078, -8.102448949553172852, -5.886773742842741797 ) ) ;
#13872=CARTESIAN_POINT ( 'NONE',  ( -51.89499999999998892, 6.826472737025116366, 4.959722759717898555 ) ) ;
#13879=CARTESIAN_POINT ( 'NONE',  ( -85.94292637653380496, 0.000000000000000000, 9.524999999999991473 ) ) ;
#13888=CARTESIAN_POINT ( 'NONE',  ( -157.2570736234661979, 5.598654528085800663, -7.705886871421367523 ) ) ;
#13895=DIRECTION ( 'NONE',  ( -1.000000000000000000, -0.000000000000000000, -0.000000000000000000 ) ) ;
#13901=CARTESIAN_POINT ( 'NONE',  ( -105.9549999999999983, -7.632228543268599452, 2.479861379858951054 ) ) ;
#13906=AXIS2_PLACEMENT_3D ( 'NONE', #24168, #54776, #2294 ) ;
#13911=EDGE_CURVE ( 'NONE', #67626, #1545, #14303, .T. ) ;
#13913=CARTESIAN_POINT ( 'NONE',  ( -81.89499999999999602, 6.826472737025116366, 4.959722759717898555 ) ) ;
#13918=ORIENTED_EDGE ( 'NONE', *, *, #32313, .F. ) ;
#13924=CARTESIAN_POINT ( 'NONE',  ( -44.00000000000000000, 11.99999999999999467, 0.000000000000000000 ) ) ;
#13925=CARTESIAN_POINT ( 'NONE',  ( -195.0000000000000000, 0.000000000000000000, 9.524999999999991473 ) ) ;
#13928=CARTESIAN_POINT ( 'NONE',  ( -166.1070736234661638, 8.102448949553171076, -5.886773742842744461 ) ) ;
#13931=CARTESIAN_POINT ( 'NONE',  ( -111.6570736234661751, 9.058813317711329915, 2.943386871421369566 ) ) ;
#13932=CARTESIAN_POINT ( 'NONE',  ( -183.3230534119037429, 0.7217949698500222278, -9.201946588096255653 ) ) ;
#13941=CARTESIAN_POINT ( 'NONE',  ( -151.7049999999999841, 2.607480562269073321, 8.024999999999991473 ) ) ;
#13944=CARTESIAN_POINT ( 'NONE',  ( -162.4449999999999932, 0.000000000000000000, 8.024999999999991473 ) ) ;
#13945=CARTESIAN_POINT ( 'NONE',  ( -148.3449999999999989, 7.632228543268599452, -2.479861379858951942 ) ) ;
#13948=CARTESIAN_POINT ( 'NONE',  ( -67.64292637653379359, -5.598654528085801552, 7.705886871421367523 ) ) ;
#13952=CARTESIAN_POINT ( 'NONE',  ( -62.45499999999998408, 7.632228543268599452, -2.479861379858951942 ) ) ;
#13956=CARTESIAN_POINT ( 'NONE',  ( -62.99499999999996902, -6.826472737025113702, 4.959722759717902107 ) ) ;
#13979=EDGE_CURVE ( 'NONE', #32866, #52425, #32319, .T. ) ;
#13980=VERTEX_POINT ( 'NONE', #10767 ) ;
#13981=VERTEX_POINT ( 'NONE', #9396 ) ;
#13987=CARTESIAN_POINT ( 'NONE',  ( -65.39292637653379359, 8.102448949553176405, 5.886773742842740909 ) ) ;
#13995=CARTESIAN_POINT ( 'NONE',  ( -109.0449999999999875, 7.632228543268600340, 2.479861379858949277 ) ) ;
#14012=CARTESIAN_POINT ( 'NONE',  ( -128.1550000000000011, 7.632228543268600340, 2.479861379858949277 ) ) ;
#14013=CARTESIAN_POINT ( 'NONE',  ( -184.0000000000000000, -0.7817472717335689492, 8.024999999999995026 ) ) ;
#14020=EDGE_LOOP ( 'NONE', ( #4051, #21678, #51554, #46044 ) ) ;
#14027=ORIENTED_EDGE ( 'NONE', *, *, #41407, .F. ) ;
#14029=CARTESIAN_POINT ( 'NONE',  ( -177.2050000000000125, -2.607480562269071545, -8.024999999999991473 ) ) ;
#14032=CARTESIAN_POINT ( 'NONE',  ( -58.85707362346617799, -5.598654528085803328, -7.705886871421366635 ) ) ;
#14035=CARTESIAN_POINT ( 'NONE',  ( -176.6949999999999363, -8.437984349512086979, 5.166775262442717831E-16 ) ) ;
#14039=CARTESIAN_POINT ( 'NONE',  ( -195.0000000000000000, 1.166476076187852838E-15, -9.524999999999991473 ) ) ;
#14041=CARTESIAN_POINT ( 'NONE',  ( -96.35499999999997556, -4.716976649647093289, -6.492361379858945902 ) ) ;
#14046=CARTESIAN_POINT ( 'NONE',  ( -94.04499999999998749, 7.632228543268600340, 2.479861379858949277 ) ) ;
#14048=CARTESIAN_POINT ( 'NONE',  ( -69.59499999999999886, 2.607480562269073321, 8.024999999999991473 ) ) ;
#14056=CARTESIAN_POINT ( 'NONE',  ( -114.1429263765338078, 5.598654528085800663, -7.705886871421367523 ) ) ;
#14058=CARTESIAN_POINT ( 'NONE',  ( -127.0449999999999875, 7.632228543268600340, 2.479861379858949277 ) ) ;
#14059=CARTESIAN_POINT ( 'NONE',  ( -15.00000000000000000, -10.90871211463571022, -5.000000000000000000 ) ) ;
#14061=DIRECTION ( 'NONE',  ( -1.000000000000000000, -0.000000000000000000, -0.000000000000000000 ) ) ;
#14063=DIRECTION ( 'NONE',  ( 0.000000000000000000, -1.224646799147353454E-16, 1.000000000000000000 ) ) ;
#14075=CARTESIAN_POINT ( 'NONE',  ( -134.4549999999999841, 7.632228543268599452, -2.479861379858951942 ) ) ;
#14079=CARTESIAN_POINT ( 'NONE',  ( -124.4070736234661751, 3.094860106618428031, -9.524999999999993250 ) ) ;
#14110=CARTESIAN_POINT ( 'NONE',  ( -154.1049999999999898, -6.826472737025115478, 4.959722759717900331 ) ) ;
#14122=CARTESIAN_POINT ( 'NONE',  ( -79.70499999999995566, 2.607480562269073321, 8.024999999999991473 ) ) ;
#14136=CARTESIAN_POINT ( 'NONE',  ( -97.04499999999998749, 7.632228543268600340, 2.479861379858949277 ) ) ;
#14143=CARTESIAN_POINT ( 'NONE',  ( -144.8929263765338362, -8.102448949553172852, -5.886773742842741797 ) ) ;
#14144=CARTESIAN_POINT ( 'NONE',  ( -152.9950000000000045, -6.826472737025115478, 4.959722759717900331 ) ) ;
#14150=ORIENTED_EDGE ( 'NONE', *, *, #37482, .T. ) ;
#14155=SHAPE_REPRESENTATION ( '4. Adjustment Screw', ( #42840 ), #4621 ) ;
#14159=CARTESIAN_POINT ( 'NONE',  ( -110.3070736234661666, -10.01517768586948698, 6.132527647946031529E-16 ) ) ;
#14163=CARTESIAN_POINT ( 'NONE',  ( -159.2049999999999841, -2.607480562269071545, -8.024999999999991473 ) ) ;
#14165=LINE ( 'NONE', #56357, #66106 ) ;
#14170=CARTESIAN_POINT ( 'NONE',  ( -58.25707362346617657, 5.598654528085800663, -7.705886871421367523 ) ) ;
#14174=CARTESIAN_POINT ( 'NONE',  ( -58.19292637653381206, -10.01517768586948698, 6.132527647946031529E-16 ) ) ;
#14176=CARTESIAN_POINT ( 'NONE',  ( -70.55499999999999261, 0.000000000000000000, 8.024999999999991473 ) ) ;
#14185=EDGE_LOOP ( 'NONE', ( #58156, #37787, #58043, #51362 ) ) ;
#14188=CARTESIAN_POINT ( 'NONE',  ( -57.44499999999999318, 0.000000000000000000, 8.024999999999991473 ) ) ;
#14194=ORIENTED_EDGE ( 'NONE', *, *, #35912, .T. ) ;
#14197=CARTESIAN_POINT ( 'NONE',  ( -106.8549999999999898, 4.716976649647094177, 6.492361379858945902 ) ) ;
#14202=CARTESIAN_POINT ( 'NONE',  ( -139.7070736234661865, -3.094860106618431139, -9.524999999999991473 ) ) ;
#14204=CARTESIAN_POINT ( 'NONE',  ( -79.55707362346616662, -1.166476076187852838E-15, -9.524999999999991473 ) ) ;
#14210=CARTESIAN_POINT ( 'NONE',  ( -18.76557388412283345, -11.53827662439787005, -3.305441448926072390 ) ) ;
#14212=CARTESIAN_POINT ( 'NONE',  ( -124.2549999999999955, -4.716976649647092401, 6.492361379858946790 ) ) ;
#14215=CARTESIAN_POINT ( 'NONE',  ( -121.7949999999999875, 2.607480562269068880, -8.024999999999993250 ) ) ;
#14216=CARTESIAN_POINT ( 'NONE',  ( -118.1949999999999790, 8.437984349512086979, -1.550032578732815448E-15 ) ) ;
#14222=CARTESIAN_POINT ( 'NONE',  ( -170.2429263765338305, 5.598654528085804216, 7.705886871421366635 ) ) ;
#14232=CARTESIAN_POINT ( 'NONE',  ( -89.24292637653380211, 5.598654528085804216, 7.705886871421366635 ) ) ;
#14235=CARTESIAN_POINT ( 'NONE',  ( -178.9429263765338192, 0.000000000000000000, 9.524999999999991473 ) ) ;
#14249=CARTESIAN_POINT ( 'NONE',  ( -107.0049999999999955, 6.826472737025115478, 4.959722759717899443 ) ) ;
#14258=CARTESIAN_POINT ( 'NONE',  ( -80.69499999999999318, -8.437984349512085203, 5.166775262442717831E-16 ) ) ;
#14267=CARTESIAN_POINT ( 'NONE',  ( -47.75499999999999545, 4.716976649647091513, -6.492361379858946790 ) ) ;
#14275=CARTESIAN_POINT ( 'NONE',  ( -171.6570736234661751, 9.058813317711329915, 2.943386871421369566 ) ) ;
#14277=CARTESIAN_POINT ( 'NONE',  ( -108.5070736234661695, 8.102448949553176405, 5.886773742842740909 ) ) ;
#14278=CARTESIAN_POINT ( 'NONE',  ( -65.15707362346617515, -9.058813317711329915, -2.943386871421370898 ) ) ;
#14279=ORIENTED_EDGE ( 'NONE', *, *, #41816, .F. ) ;
#14280=CARTESIAN_POINT ( 'NONE',  ( -108.1429263765338078, 5.598654528085800663, -7.705886871421367523 ) ) ;
#14281=CARTESIAN_POINT ( 'NONE',  ( -82.94292637653380496, 0.000000000000000000, 9.524999999999991473 ) ) ;
#14286=CARTESIAN_POINT ( 'NONE',  ( -150.2049999999999841, -2.607480562269071545, -8.024999999999991473 ) ) ;
#14287=CARTESIAN_POINT ( 'NONE',  ( -148.0429263765338135, -9.058813317711329915, -2.943386871421370898 ) ) ;
#14289=CARTESIAN_POINT ( 'NONE',  ( -152.3950000000000102, -6.826472737025115478, -4.959722759717899443 ) ) ;
#14290=CARTESIAN_POINT ( 'NONE',  ( -148.1949999999999932, 8.437984349512086979, -1.550032578732815448E-15 ) ) ;
#14291=ORIENTED_EDGE ( 'NONE', *, *, #39509, .T. ) ;
#14293=DIRECTION ( 'NONE',  ( 0.000000000000000000, 0.000000000000000000, 1.000000000000000000 ) ) ;
#14297=CARTESIAN_POINT ( 'NONE',  ( -60.80499999999998550, -8.437984349512085203, 5.166775262442717831E-16 ) ) ;
#14300=CARTESIAN_POINT ( 'NONE',  ( -63.29499999999998749, -2.607480562269069768, 8.024999999999991473 ) ) ;
#14303=LINE ( 'NONE', #50904, #48107 ) ;
#14325=ORIENTED_EDGE ( 'NONE', *, *, #64658, .T. ) ;
#14328=ORIENTED_EDGE ( 'NONE', *, *, #68478, .T. ) ;
#14330=CARTESIAN_POINT ( 'NONE',  ( -111.5949999999999704, 2.607480562269073321, 8.024999999999991473 ) ) ;
#14340=EDGE_LOOP ( 'NONE', ( #38261, #49779, #55542, #30168 ) ) ;
#14342=ORIENTED_EDGE ( 'NONE', *, *, #43114, .F. ) ;
#14345=CARTESIAN_POINT ( 'NONE',  ( -157.8570736234661922, -5.598654528085803328, -7.705886871421366635 ) ) ;
#14346=CARTESIAN_POINT ( 'NONE',  ( -119.9049999999999869, 2.607480562269068880, -8.024999999999993250 ) ) ;
#14350=CARTESIAN_POINT ( 'NONE',  ( -125.2429263765338021, 5.598654528085804216, 7.705886871421366635 ) ) ;
#14359=CARTESIAN_POINT ( 'NONE',  ( -175.8549999999999898, 4.716976649647094177, 6.492361379858945902 ) ) ;
#14363=CARTESIAN_POINT ( 'NONE',  ( -53.75707362346618368, -5.598654528085801552, 7.705886871421367523 ) ) ;
#14365=CARTESIAN_POINT ( 'NONE',  ( -181.4949999999999761, 6.826472737025113702, -4.959722759717902107 ) ) ;
#14370=CARTESIAN_POINT ( 'NONE',  ( -91.25499999999999545, -4.716976649647092401, 6.492361379858946790 ) ) ;
#14375=CARTESIAN_POINT ( 'NONE',  ( -87.14499999999998181, -4.716976649647092401, 6.492361379858946790 ) ) ;
#14377=CARTESIAN_POINT ( 'NONE',  ( -71.39499999999998181, -6.826472737025115478, -4.959722759717899443 ) ) ;
#14380=CARTESIAN_POINT ( 'NONE',  ( -55.85707362346617799, -5.598654528085803328, -7.705886871421366635 ) ) ;
#14386=CARTESIAN_POINT ( 'NONE',  ( -119.2429263765338021, 5.598654528085804216, 7.705886871421366635 ) ) ;
#14387=CARTESIAN_POINT ( 'NONE',  ( -127.1949999999999932, 8.437984349512085203, -1.550032578732815448E-15 ) ) ;
#14392=EDGE_LOOP ( 'NONE', ( #29974, #56544 ) ) ;
#14393=CARTESIAN_POINT ( 'NONE',  ( -61.94292637653379785, 0.000000000000000000, 9.524999999999991473 ) ) ;
#14402=CARTESIAN_POINT ( 'NONE',  ( -126.9549999999999841, -7.632228543268599452, 2.479861379858951054 ) ) ;
#14404=CARTESIAN_POINT ( 'NONE',  ( -124.7070736234661723, -3.094860106618431139, -9.524999999999991473 ) ) ;
#14428=CARTESIAN_POINT ( 'NONE',  ( -54.89292637653381490, -8.102448949553172852, -5.886773742842741797 ) ) ;
#14430=CARTESIAN_POINT ( 'NONE',  ( -148.5550000000000068, 0.000000000000000000, 8.024999999999991473 ) ) ;
#14442=DIRECTION ( 'NONE',  ( 0.000000000000000000, 0.000000000000000000, 1.000000000000000000 ) ) ;
#14445=CARTESIAN_POINT ( 'NONE',  ( -62.60499999999998266, 6.826472737025113702, -4.959722759717902107 ) ) ;
#14462=CARTESIAN_POINT ( 'NONE',  ( -99.29499999999997328, -2.607480562269069768, 8.024999999999991473 ) ) ;
#14470=CARTESIAN_POINT ( 'NONE',  ( -143.0929263765338249, 3.094860106618433360, 9.524999999999991473 ) ) ;
#14473=CARTESIAN_POINT ( 'NONE',  ( -159.4449999999999932, 0.000000000000000000, 8.024999999999991473 ) ) ;
#14485=CARTESIAN_POINT ( 'NONE',  ( -109.5570736234661666, -1.166476076187852838E-15, -9.524999999999991473 ) ) ;
#14489=CARTESIAN_POINT ( 'NONE',  ( -156.0550000000000068, -9.827790563157499189E-16, -8.024999999999991473 ) ) ;
#14504=CARTESIAN_POINT ( 'NONE',  ( -72.80499999999997840, -8.437984349512086979, 5.166775262442717831E-16 ) ) ;
#14512=ORIENTED_EDGE ( 'NONE', *, *, #15800, .T. ) ;
#14515=CARTESIAN_POINT ( 'NONE',  ( -182.9050000000000011, 2.607480562269068880, -8.024999999999993250 ) ) ;
#14519=CARTESIAN_POINT ( 'NONE',  ( -86.24292637653380211, 5.598654528085804216, 7.705886871421366635 ) ) ;
#14522=DIRECTION ( 'NONE',  ( 0.000000000000000000, 0.000000000000000000, -1.000000000000000000 ) ) ;
#14525=DIRECTION ( 'NONE',  ( -1.000000000000000000, -0.000000000000000000, -0.000000000000000000 ) ) ;
#14528=CARTESIAN_POINT ( 'NONE',  ( -93.65499999999998693, -7.632228543268600340, -2.479861379858950166 ) ) ;
#14532=CARTESIAN_POINT ( 'NONE',  ( -137.0070736234661410, -8.102448949553172852, -5.886773742842741797 ) ) ;
#14537=CARTESIAN_POINT ( 'NONE',  ( -75.65707362346617515, 9.058813317711329915, 2.943386871421369566 ) ) ;
#14544=CARTESIAN_POINT ( 'NONE',  ( -20.00036572459219997, -12.00015238516981952, -0.3288021958098223396 ) ) ;
#14548=CARTESIAN_POINT ( 'NONE',  ( -121.4049999999999869, -2.607480562269069768, 8.024999999999991473 ) ) ;
#14551=CARTESIAN_POINT ( 'NONE',  ( -124.0449999999999875, 7.632228543268600340, 2.479861379858949277 ) ) ;
#14564=CARTESIAN_POINT ( 'NONE',  ( -167.8429263765337964, 9.058813317711329915, -2.943386871421373119 ) ) ;
#14566=CARTESIAN_POINT ( 'NONE',  ( -181.7949999999999875, 2.607480562269068880, -8.024999999999993250 ) ) ;
#14574=CARTESIAN_POINT ( 'NONE',  ( -85.49292637653380211, -8.102448949553172852, 5.886773742842742685 ) ) ;
#14576=AXIS2_PLACEMENT_3D ( 'NONE', #26490, #43755, #21568 ) ;
#14594=EDGE_LOOP ( 'NONE', ( #53526, #23578, #65693, #5011 ) ) ;
#14597=CARTESIAN_POINT ( 'NONE',  ( -100.8549999999999898, 4.716976649647094177, 6.492361379858945902 ) ) ;
#14608=CARTESIAN_POINT ( 'NONE',  ( -68.69500000000000739, -8.437984349512085203, 5.166775262442717831E-16 ) ) ;
#14628=CARTESIAN_POINT ( 'NONE',  ( -150.2929263765342114, 3.094860106611235562, -9.525000000005221068 ) ) ;
#14631=CARTESIAN_POINT ( 'NONE',  ( -173.9070736234662036, -3.094860106618429807, 9.524999999999991473 ) ) ;
#14634=CARTESIAN_POINT ( 'NONE',  ( -108.6570736234661751, 9.058813317711329915, 2.943386871421369566 ) ) ;
#14635=CYLINDRICAL_SURFACE ( 'NONE', #44830, 9.524999999999991473 ) ;
#14636=EDGE_CURVE ( 'NONE', #36632, #67977, #25141, .T. ) ;
#14637=CARTESIAN_POINT ( 'NONE',  ( -64.85707362346616378, -5.598654528085803328, -7.705886871421366635 ) ) ;
#14640=CARTESIAN_POINT ( 'NONE',  ( -107.8429263765338106, 9.058813317711329915, -2.943386871421373119 ) ) ;
#14641=CARTESIAN_POINT ( 'NONE',  ( -81.74292637653380211, -5.598654528085803328, -7.705886871421366635 ) ) ;
#14645=CARTESIAN_POINT ( 'NONE',  ( -145.4050000000000296, -2.607480562269069768, 8.024999999999991473 ) ) ;
#14647=CARTESIAN_POINT ( 'NONE',  ( -148.3429263765338249, -9.058813317711329915, 2.943386871421371787 ) ) ;
#14648=CARTESIAN_POINT ( 'NONE',  ( -158.3949999999999818, -6.826472737025115478, -4.959722759717899443 ) ) ;
#14649=CARTESIAN_POINT ( 'NONE',  ( -147.7449999999999761, 4.716976649647094177, 6.492361379858945902 ) ) ;
#14655=CARTESIAN_POINT ( 'NONE',  ( -59.60499999999998977, 6.826472737025113702, -4.959722759717902107 ) ) ;
#14657=CARTESIAN_POINT ( 'NONE',  ( -59.84499999999998465, -7.632228543268599452, 2.479861379858951054 ) ) ;
#14662=CARTESIAN_POINT ( 'NONE',  ( -155.4570736234661581, -9.058813317711329915, 2.943386871421371787 ) ) ;
#14670=CARTESIAN_POINT ( 'NONE',  ( -43.99999999999998579, 0.000000000000000000, 0.000000000000000000 ) ) ;
#14683=CARTESIAN_POINT ( 'NONE',  ( -77.90707362346617515, -3.094860106618429807, 9.524999999999991473 ) ) ;
#14686=CARTESIAN_POINT ( 'NONE',  ( -108.6570736234661751, 9.058813317711329915, 2.943386871421369566 ) ) ;
#14689=ORIENTED_EDGE ( 'NONE', *, *, #38372, .F. ) ;
#14695=CARTESIAN_POINT ( 'NONE',  ( -107.3949999999999960, -6.826472737025115478, -4.959722759717899443 ) ) ;
#14714=CARTESIAN_POINT ( 'NONE',  ( -122.1549999999999869, 7.632228543268600340, 2.479861379858949277 ) ) ;
#14715=CARTESIAN_POINT ( 'NONE',  ( -183.9999999999999716, -5.054410645616873587, 6.281779722895938889 ) ) ;
#14728=EDGE_CURVE ( 'NONE', #23874, #47647, #10369, .T. ) ;
#14730=ORIENTED_EDGE ( 'NONE', *, *, #56521, .T. ) ;
#14732=CARTESIAN_POINT ( 'NONE',  ( -174.6550000000000011, -7.632228543268600340, -2.479861379858950166 ) ) ;
#14735=CARTESIAN_POINT ( 'NONE',  ( -47.75707362346617657, -5.598654528085801552, 7.705886871421367523 ) ) ;
#14736=CARTESIAN_POINT ( 'NONE',  ( -175.0450000000000159, 7.632228543268600340, 2.479861379858949277 ) ) ;
#14743=CARTESIAN_POINT ( 'NONE',  ( -90.65499999999998693, -7.632228543268600340, -2.479861379858950166 ) ) ;
#14747=CARTESIAN_POINT ( 'NONE',  ( -86.54499999999998749, -7.632228543268600340, -2.479861379858950166 ) ) ;
#14749=CARTESIAN_POINT ( 'NONE',  ( -69.29499999999995907, -2.607480562269069768, 8.024999999999991473 ) ) ;
#14757=CARTESIAN_POINT ( 'NONE',  ( -104.9929263765337879, 8.102448949553171076, -5.886773742842744461 ) ) ;
#14760=CARTESIAN_POINT ( 'NONE',  ( -126.5949999999999847, 2.607480562269073321, 8.024999999999991473 ) ) ;
#14764=DIRECTION ( 'NONE',  ( -1.000000000000000000, -0.000000000000000000, -0.000000000000000000 ) ) ;
#14767=ORIENTED_EDGE ( 'NONE', *, *, #31288, .F. ) ;
#14776=CARTESIAN_POINT ( 'NONE',  ( -122.7549999999999955, 4.716976649647091513, -6.492361379858946790 ) ) ;
#14779=CARTESIAN_POINT ( 'NONE',  ( -123.0570736234661808, 0.000000000000000000, 9.524999999999991473 ) ) ;
#14803=CARTESIAN_POINT ( 'NONE',  ( -59.39292637653377938, 8.102448949553176405, 5.886773742842740909 ) ) ;
#14807=CARTESIAN_POINT ( 'NONE',  ( -151.1049999999999613, -6.826472737025115478, 4.959722759717900331 ) ) ;
#14816=CARTESIAN_POINT ( 'NONE',  ( -70.64292637653379359, -5.598654528085801552, 7.705886871421367523 ) ) ;
#14823=CARTESIAN_POINT ( 'NONE',  ( -65.45499999999998408, 7.632228543268599452, -2.479861379858951942 ) ) ;
#14829=CARTESIAN_POINT ( 'NONE',  ( -91.40707362346728360, 3.094860106599739868, -9.525000000013571722 ) ) ;
#14839=CARTESIAN_POINT ( 'NONE',  ( -93.14499999999999602, -4.716976649647092401, 6.492361379858946790 ) ) ;
#14846=CARTESIAN_POINT ( 'NONE',  ( -137.3929263765337510, 8.102448949553176405, 5.886773742842740909 ) ) ;
#14848=CARTESIAN_POINT ( 'NONE',  ( -160.3449999999999989, 7.632228543268599452, -2.479861379858951942 ) ) ;
#14865=CARTESIAN_POINT ( 'NONE',  ( -153.3549999999999898, -4.716976649647093289, -6.492361379858945902 ) ) ;
#14873=CARTESIAN_POINT ( 'NONE',  ( -57.50707362346616236, 8.102448949553176405, 5.886773742842740909 ) ) ;
#14877=EDGE_LOOP ( 'NONE', ( #60090, #28299 ) ) ;
#14879=CARTESIAN_POINT ( 'NONE',  ( -57.44292637653381206, -1.166476076187852838E-15, -9.524999999999991473 ) ) ;
#14881=CARTESIAN_POINT ( 'NONE',  ( -71.15499999999998693, 7.632228543268600340, 2.479861379858949277 ) ) ;
#14897=CARTESIAN_POINT ( 'NONE',  ( -182.3049999999999500, 8.437984349512085203, -1.550032578732815448E-15 ) ) ;
#14899=( BOUNDED_CURVE ( )  B_SPLINE_CURVE ( 2, ( #31135, #62464, #14280, #8667, #14640, #36817, #30095, #4052, #35746, #4388, #58235 ),
 .UNSPECIFIED., .F., .F. ) 
 B_SPLINE_CURVE_WITH_KNOTS ( ( 3, 2, 2, 2, 2, 3 ),
 ( 0.5543478260869434404, 0.5565217391304216887, 0.5586956521738998260, 0.5608695652173780744, 0.5630434782608562116, 0.5652173913043344600 ),
 .UNSPECIFIED. ) 
 CURVE ( )  GEOMETRIC_REPRESENTATION_ITEM ( )  RATIONAL_B_SPLINE_CURVE ( ( 1.000000000000294875, 0.9510565162948585449, 1.000000000000000000, 0.9510565162951535312, 1.000000000000000000, 0.9510565162951535312, 1.000000000000000000, 0.9510565162951535312, 1.000000000000000000, 0.9510565162954535134, 0.9999999999997000177 ) ) 
 REPRESENTATION_ITEM ( '' )  );
#14902=EDGE_CURVE ( 'NONE', #57697, #54371, #17564, .T. ) ;
#14907=CARTESIAN_POINT ( 'NONE',  ( -128.1570736234661751, -9.058813317711329915, -2.943386871421370898 ) ) ;
#14909=CARTESIAN_POINT ( 'NONE',  ( -98.75499999999999545, 4.716976649647091513, -6.492361379858946790 ) ) ;
#14912=CARTESIAN_POINT ( 'NONE',  ( -130.4070736234661751, 3.094860106618428031, -9.524999999999993250 ) ) ;
#14915=CARTESIAN_POINT ( 'NONE',  ( -74.60707362346617799, -8.102448949553172852, 5.886773742842742685 ) ) ;
#14920=CARTESIAN_POINT ( 'NONE',  ( -19.48783162866786611, -11.79520720594569738, -2.229038028308376607 ) ) ;
#14922=CARTESIAN_POINT ( 'NONE',  ( -116.0049999999999955, 6.826472737025116366, 4.959722759717898555 ) ) ;
#14927=CARTESIAN_POINT ( 'NONE',  ( -123.4449999999999932, 0.000000000000000000, 8.024999999999991473 ) ) ;
#14929=CARTESIAN_POINT ( 'NONE',  ( -112.2570736234661837, 5.598654528085800663, -7.705886871421367523 ) ) ;
#14936=CARTESIAN_POINT ( 'NONE',  ( -175.3429263765338249, -9.058813317711329915, 2.943386871421371787 ) ) ;
#14946=CARTESIAN_POINT ( 'NONE',  ( -83.39292637653379359, 8.102448949553176405, 5.886773742842740909 ) ) ;
#14952=CARTESIAN_POINT ( 'NONE',  ( -162.4429263765338192, -1.166476076187852838E-15, -9.524999999999991473 ) ) ;
#14954=ORIENTED_EDGE ( 'NONE', *, *, #42310, .F. ) ;
#14955=CARTESIAN_POINT ( 'NONE',  ( -136.9429263765338192, 0.000000000000000000, 9.524999999999991473 ) ) ;
#14958=CARTESIAN_POINT ( 'NONE',  ( -103.3429263765338106, -9.058813317711329915, 2.943386871421371787 ) ) ;
#14968=CARTESIAN_POINT ( 'NONE',  ( -99.35499999999998977, -4.716976649647093289, -6.492361379858945902 ) ) ;
#14980=CARTESIAN_POINT ( 'NONE',  ( -76.34499999999998465, 7.632228543268599452, -2.479861379858951942 ) ) ;
#14981=EDGE_LOOP ( 'NONE', ( #13918, #17624, #24550, #43874 ) ) ;
#14983=CARTESIAN_POINT ( 'NONE',  ( -121.4070736234669283, 3.094860106605790140, -9.525000000009175238 ) ) ;
#14984=CARTESIAN_POINT ( 'NONE',  ( -124.8570736234661780, -5.598654528085803328, -7.705886871421366635 ) ) ;
#14995=ORIENTED_EDGE ( 'NONE', *, *, #40551, .T. ) ;
#14998=CARTESIAN_POINT ( 'NONE',  ( -169.4070736234661751, 3.094860106618428031, -9.524999999999993250 ) ) ;
#15002=CARTESIAN_POINT ( 'NONE',  ( -101.7570736234661695, -5.598654528085801552, 7.705886871421367523 ) ) ;
#15008=CARTESIAN_POINT ( 'NONE',  ( -61.19292637653379074, -10.01517768586948698, 6.132527647946031529E-16 ) ) ;
#15010=CARTESIAN_POINT ( 'NONE',  ( -141.9549999999999841, -7.632228543268599452, 2.479861379858951054 ) ) ;
#15012=CARTESIAN_POINT ( 'NONE',  ( -152.5449999999999875, -7.632228543268600340, -2.479861379858950166 ) ) ;
#15016=CARTESIAN_POINT ( 'NONE',  ( -150.2949999999999875, -2.607480562269069768, 8.024999999999991473 ) ) ;
#15017=ORIENTED_EDGE ( 'NONE', *, *, #1471, .F. ) ;
#15022=CARTESIAN_POINT ( 'NONE',  ( -195.0000000000000000, 0.000000000000000000, 0.000000000000000000 ) ) ;
#15024=CARTESIAN_POINT ( 'NONE',  ( -65.15499999999998693, 7.632228543268600340, 2.479861379858949277 ) ) ;
#15025=B_SPLINE_CURVE_WITH_KNOTS ( 'NONE', 1,
 ( #2962, #14267 ),
 .UNSPECIFIED., .F., .F.,
 ( 2, 2 ),
 ( 0.000000000000000000, 1.000000000000000000 ),
 .UNSPECIFIED. ) ;
#15027=CARTESIAN_POINT ( 'NONE',  ( -61.64499999999998892, 4.716976649647091513, -6.492361379858946790 ) ) ;
#15059=CARTESIAN_POINT ( 'NONE',  ( -109.4070736234670704, 3.094860106603370298, -9.525000000010933832 ) ) ;
#15069=CARTESIAN_POINT ( 'NONE',  ( -99.89499999999998181, 6.826472737025116366, 4.959722759717898555 ) ) ;
#15098=CARTESIAN_POINT ( 'NONE',  ( -182.8429263765338249, 9.058813317711329915, -2.943386871421373119 ) ) ;
#15102=CARTESIAN_POINT ( 'NONE',  ( -153.7429263765338021, -5.598654528085803328, -7.705886871421366635 ) ) ;
#15103=CARTESIAN_POINT ( 'NONE',  ( -177.3549999999999898, -4.716976649647093289, -6.492361379858945902 ) ) ;
#15106=CARTESIAN_POINT ( 'NONE',  ( -180.7449999999999761, 4.716976649647094177, 6.492361379858945902 ) ) ;
#15107=CARTESIAN_POINT ( 'NONE',  ( -180.4449999999999932, 0.000000000000000000, 8.024999999999991473 ) ) ;
#15113=CARTESIAN_POINT ( 'NONE',  ( -10.00004746342556317, 11.99998022357284810, -0.3303491890816930843 ) ) ;
#15114=CARTESIAN_POINT ( 'NONE',  ( -93.95499999999998408, -7.632228543268599452, 2.479861379858951054 ) ) ;
#15117=CARTESIAN_POINT ( 'NONE',  ( -90.44499999999997897, 0.000000000000000000, 8.024999999999991473 ) ) ;
#15119=CARTESIAN_POINT ( 'NONE',  ( -70.34499999999998465, 7.632228543268599452, -2.479861379858951942 ) ) ;
#15126=CARTESIAN_POINT ( 'NONE',  ( -74.84292637653381064, 9.058813317711329915, -2.943386871421373119 ) ) ;
#15129=CARTESIAN_POINT ( 'NONE',  ( -129.1449999999999818, -4.716976649647092401, 6.492361379858946790 ) ) ;
#15134=CYLINDRICAL_SURFACE ( 'NONE', #13498, 9.524999999999991473 ) ;
#15146=CARTESIAN_POINT ( 'NONE',  ( -124.4049999999999869, -2.607480562269069768, 8.024999999999991473 ) ) ;
#15147=EDGE_LOOP ( 'NONE', ( #29169, #45727, #28111, #56989 ) ) ;
#15150=CARTESIAN_POINT ( 'NONE',  ( -105.0570736234661666, 0.000000000000000000, 9.524999999999991473 ) ) ;
#15176=CARTESIAN_POINT ( 'NONE',  ( -55.64292637653381490, -5.598654528085801552, 7.705886871421367523 ) ) ;
#15181=CARTESIAN_POINT ( 'NONE',  ( -149.9050000000000296, 2.607480562269068880, -8.024999999999993250 ) ) ;
#15193=CARTESIAN_POINT ( 'NONE',  ( -69.50499999999996703, -6.826472737025115478, -4.959722759717899443 ) ) ;
#15198=CARTESIAN_POINT ( 'NONE',  ( -195.0000000000000000, 0.000000000000000000, 0.000000000000000000 ) ) ;
#15204=CARTESIAN_POINT ( 'NONE',  ( -169.9429263765337907, 0.000000000000000000, 9.524999999999991473 ) ) ;
#15208=CARTESIAN_POINT ( 'NONE',  ( -98.09499999999997044, -2.607480562269071545, -8.024999999999991473 ) ) ;
#15210=DIRECTION ( 'NONE',  ( -1.000000000000000000, -0.000000000000000000, -0.000000000000000000 ) ) ;
#15216=CARTESIAN_POINT ( 'NONE',  ( -131.3929263765338078, 8.102448949553176405, 5.886773742842740909 ) ) ;
#15219=CARTESIAN_POINT ( 'NONE',  ( -157.6449999999999818, 4.716976649647091513, -6.492361379858946790 ) ) ;
#15225=ORIENTED_EDGE ( 'NONE', *, *, #63207, .T. ) ;
#15229=CARTESIAN_POINT ( 'NONE',  ( -143.5429263765338135, 9.058813317711329915, 2.943386871421369566 ) ) ;
#15231=CARTESIAN_POINT ( 'NONE',  ( -174.0570736234661808, 0.000000000000000000, 9.524999999999991473 ) ) ;
#15234=CARTESIAN_POINT ( 'NONE',  ( -146.1549999999999727, 7.632228543268600340, 2.479861379858949277 ) ) ;
#15244=CARTESIAN_POINT ( 'NONE',  ( -57.59292637653379643, -3.094860106618431139, -9.524999999999991473 ) ) ;
#15246=CARTESIAN_POINT ( 'NONE',  ( -60.35499999999998977, -4.716976649647093289, -6.492361379858945902 ) ) ;
#15247=VECTOR ( 'NONE', #65953, 1000.000000000000000 ) ;
#15257=DIRECTION ( 'NONE',  ( -1.000000000000000000, -0.000000000000000000, -0.000000000000000000 ) ) ;
#15258=CARTESIAN_POINT ( 'NONE',  ( -47.84499999999997044, -7.632228543268599452, 2.479861379858951054 ) ) ;
#15268=CARTESIAN_POINT ( 'NONE',  ( -128.6070736234661922, -8.102448949553174629, 5.886773742842742685 ) ) ;
#15271=CARTESIAN_POINT ( 'NONE',  ( -97.10499999999998977, -6.826472737025115478, 4.959722759717900331 ) ) ;
#15275=CARTESIAN_POINT ( 'NONE',  ( -133.8570736234661638, -5.598654528085803328, -7.705886871421366635 ) ) ;
#15279=CARTESIAN_POINT ( 'NONE',  ( -72.35707362346617799, 5.598654528085804216, 7.705886871421366635 ) ) ;
#15287=CARTESIAN_POINT ( 'NONE',  ( -114.5050000000000097, -6.826472737025115478, -4.959722759717899443 ) ) ;
#15290=CARTESIAN_POINT ( 'NONE',  ( -127.6450000000000102, 4.716976649647091513, -6.492361379858946790 ) ) ;
#15299=CARTESIAN_POINT ( 'NONE',  ( -166.7929263765337851, -3.094860106618429807, 9.524999999999991473 ) ) ;
#15301=LINE ( 'NONE', #63096, #30873 ) ;
#15310=CARTESIAN_POINT ( 'NONE',  ( -73.64292637653380780, -5.598654528085801552, 7.705886871421367523 ) ) ;
#15318=CARTESIAN_POINT ( 'NONE',  ( -184.0000000000000000, -7.358988424933670558, 3.200923985616050071 ) ) ;
#15322=CARTESIAN_POINT ( 'NONE',  ( -110.8429263765337964, 9.058813317711329915, -2.943386871421373119 ) ) ;
#15329=CARTESIAN_POINT ( 'NONE',  ( -91.25499999999999545, -4.716976649647092401, 6.492361379858946790 ) ) ;
#15335=CARTESIAN_POINT ( 'NONE',  ( -83.75707362346616947, -5.598654528085801552, 7.705886871421367523 ) ) ;
#15338=ORIENTED_EDGE ( 'NONE', *, *, #65927, .F. ) ;
#15340=CARTESIAN_POINT ( 'NONE',  ( -72.29499999999998749, -2.607480562269069768, 8.024999999999991473 ) ) ;
#15357=CARTESIAN_POINT ( 'NONE',  ( -162.0570736234661808, 0.000000000000000000, 9.524999999999991473 ) ) ;
#15359=CARTESIAN_POINT ( 'NONE',  ( -104.0070736234661695, -8.102448949553172852, -5.886773742842741797 ) ) ;
#15368=CARTESIAN_POINT ( 'NONE',  ( -144.8049999999999216, -8.437984349512085203, 5.166775262442717831E-16 ) ) ;
#15372=CARTESIAN_POINT ( 'NONE',  ( -152.9950000000000045, -6.826472737025115478, 4.959722759717900331 ) ) ;
#15375=CARTESIAN_POINT ( 'NONE',  ( -141.8949999999999818, 6.826472737025115478, 4.959722759717899443 ) ) ;
#15381=CARTESIAN_POINT ( 'NONE',  ( -54.95499999999997698, -7.632228543268599452, 2.479861379858951054 ) ) ;
#15383=CARTESIAN_POINT ( 'NONE',  ( -52.04292637653379217, -9.058813317711329915, -2.943386871421370898 ) ) ;
#15384=CARTESIAN_POINT ( 'NONE',  ( -143.4570736234661865, -9.058813317711329915, 2.943386871421371787 ) ) ;
#15411=CARTESIAN_POINT ( 'NONE',  ( -104.5449999999999875, -7.632228543268600340, -2.479861379858950166 ) ) ;
#15413=( BOUNDED_CURVE ( )  B_SPLINE_CURVE ( 2, ( #45348, #25836, #15335, #37140, #40067, #45691, #18893, #40391, #13274, #61799, #35091 ),
 .UNSPECIFIED., .F., .F. ) 
 B_SPLINE_CURVE_WITH_KNOTS ( ( 3, 2, 2, 2, 2, 3 ),
 ( 0.7173913043478260532, 0.7195652173913043015, 0.7217391304347826608, 0.7239130434782609091, 0.7260869565217391575, 0.7282608695652174058 ),
 .UNSPECIFIED. ) 
 CURVE ( )  GEOMETRIC_REPRESENTATION_ITEM ( )  RATIONAL_B_SPLINE_CURVE ( ( 1.000000000000000000, 0.9510565162951535312, 1.000000000000000000, 0.9510565162951535312, 1.000000000000000000, 0.9510565162951535312, 1.000000000000000000, 0.9510565162951535312, 1.000000000000000000, 0.9510565162951535312, 1.000000000000000000 ) ) 
 REPRESENTATION_ITEM ( '' )  );
#15433=ORIENTED_EDGE ( 'NONE', *, *, #42612, .F. ) ;
#15437=CARTESIAN_POINT ( 'NONE',  ( -169.7070736234663570, -3.094860106621120988, -9.524999999998039257 ) ) ;
#15440=CARTESIAN_POINT ( 'NONE',  ( -154.0429263765338135, -9.058813317711329915, -2.943386871421370898 ) ) ;
#15441=CARTESIAN_POINT ( 'NONE',  ( -168.5049999999999955, -6.826472737025115478, -4.959722759717899443 ) ) ;
#15444=CARTESIAN_POINT ( 'NONE',  ( -148.2570736234661979, 5.598654528085800663, -7.705886871421367523 ) ) ;
#15445=CARTESIAN_POINT ( 'NONE',  ( -182.6949999999999648, -8.437984349512085203, 5.166775262442717831E-16 ) ) ;
#15446=CARTESIAN_POINT ( 'NONE',  ( -169.4949999999999761, 6.826472737025113702, -4.959722759717902107 ) ) ;
#15450=CARTESIAN_POINT ( 'NONE',  ( -12.34763874847350529, 11.22577880721510368, -4.241592803799083988 ) ) ;
#15451=CARTESIAN_POINT ( 'NONE',  ( -83.15499999999998693, 7.632228543268600340, 2.479861379858949277 ) ) ;
#15453=CARTESIAN_POINT ( 'NONE',  ( -169.2570736234661695, 5.598654528085800663, -7.705886871421367523 ) ) ;
#15457=CARTESIAN_POINT ( 'NONE',  ( -91.49499999999997613, 6.826472737025113702, -4.959722759717902107 ) ) ;
#15461=ADVANCED_FACE ( 'NONE', ( #23541 ), #28451, .T. ) ;
#15462=CARTESIAN_POINT ( 'NONE',  ( -172.5570736234661808, -1.166476076187852838E-15, -9.524999999999991473 ) ) ;
#15464=CARTESIAN_POINT ( 'NONE',  ( -75.44292637653379074, -1.166476076187852838E-15, -9.524999999999991473 ) ) ;
#15471=CARTESIAN_POINT ( 'NONE',  ( -63.29292637653379927, 3.094860106618428031, -9.524999999999993250 ) ) ;
#15476=CARTESIAN_POINT ( 'NONE',  ( -134.0929263765344501, 3.094860106629121699, 9.524999999992225241 ) ) ;
#15480=DIRECTION ( 'NONE',  ( 0.000000000000000000, 0.000000000000000000, 1.000000000000000000 ) ) ;
#15482=CARTESIAN_POINT ( 'NONE',  ( -120.6549999999999869, -7.632228543268600340, -2.479861379858950166 ) ) ;
#15485=CARTESIAN_POINT ( 'NONE',  ( -105.2070736234671386, 3.094860106634298447, 9.524999999988466470 ) ) ;
#15494=CARTESIAN_POINT ( 'NONE',  ( -54.80707362346617373, 10.01517768586948698, -1.839758294383808966E-15 ) ) ;
#15496=CARTESIAN_POINT ( 'NONE',  ( -135.3570736234661638, 5.598654528085804216, 7.705886871421366635 ) ) ;
#15507=EDGE_LOOP ( 'NONE', ( #48796, #61931 ) ) ;
#15508=CARTESIAN_POINT ( 'NONE',  ( -60.74292637653380922, -5.598654528085803328, -7.705886871421366635 ) ) ;
#15512=CARTESIAN_POINT ( 'NONE',  ( -150.8050000000000068, -8.437984349512085203, 5.166775262442717831E-16 ) ) ;
#15524=CARTESIAN_POINT ( 'NONE',  ( -69.65499999999998693, -7.632228543268600340, -2.479861379858950166 ) ) ;
#15530=CARTESIAN_POINT ( 'NONE',  ( -123.8929263765337936, -8.102448949553174629, -5.886773742842741797 ) ) ;
#15534=LINE ( 'NONE', #38035, #12160 ) ;
#15539=CARTESIAN_POINT ( 'NONE',  ( -114.5949999999999704, 2.607480562269072433, 8.024999999999991473 ) ) ;
#15541=CARTESIAN_POINT ( 'NONE',  ( -85.19500000000000739, 8.437984349512085203, -1.550032578732815448E-15 ) ) ;
#15543=DIRECTION ( 'NONE',  ( 0.000000000000000000, 0.000000000000000000, 1.000000000000000000 ) ) ;
#15546=CARTESIAN_POINT ( 'NONE',  ( -134.5429263765338135, 9.058813317711329915, 2.943386871421369566 ) ) ;
#15547=DIRECTION ( 'NONE',  ( -1.000000000000000000, -0.000000000000000000, -0.000000000000000000 ) ) ;
#15548=CARTESIAN_POINT ( 'NONE',  ( -157.3449999999999989, 7.632228543268599452, -2.479861379858951942 ) ) ;
#15566=CARTESIAN_POINT ( 'NONE',  ( -155.3050000000000068, 8.437984349512086979, -1.550032578732815448E-15 ) ) ;
#15575=CARTESIAN_POINT ( 'NONE',  ( -64.85499999999997556, 4.716976649647094177, 6.492361379858945902 ) ) ;
#15577=CARTESIAN_POINT ( 'NONE',  ( -1.000000000000028644, 0.000000000000000000, 0.000000000000000000 ) ) ;
#15588=CARTESIAN_POINT ( 'NONE',  ( -46.40707362346616094, 3.094860106618428031, -9.524999999999993250 ) ) ;
#15589=CARTESIAN_POINT ( 'NONE',  ( -48.14499999999999602, -4.716976649647092401, 6.492361379858946790 ) ) ;
#15604=CARTESIAN_POINT ( 'NONE',  ( -93.05499999999997840, -9.827790563157499189E-16, -8.024999999999991473 ) ) ;
#15609=CARTESIAN_POINT ( 'NONE',  ( -131.4570736234661865, -9.058813317711329915, 2.943386871421371787 ) ) ;
#15612=CARTESIAN_POINT ( 'NONE',  ( -62.75707362346616236, -5.598654528085801552, 7.705886871421367523 ) ) ;
#15616=CARTESIAN_POINT ( 'NONE',  ( -184.0000000000000000, 0.000000000000000000, 0.000000000000000000 ) ) ;
#15620=CARTESIAN_POINT ( 'NONE',  ( -109.7049999999999699, 2.607480562269073321, 8.024999999999991473 ) ) ;
#15622=CARTESIAN_POINT ( 'NONE',  ( -123.5949999999999704, 2.607480562269073321, 8.024999999999991473 ) ) ;
#15624=CARTESIAN_POINT ( 'NONE',  ( -118.0429263765338135, -9.058813317711329915, -2.943386871421370898 ) ) ;
#15627=CARTESIAN_POINT ( 'NONE',  ( -161.6929263765337907, 10.01517768586948698, -1.839758294383808571E-15 ) ) ;
#15635=CARTESIAN_POINT ( 'NONE',  ( -77.39292637653380780, 8.102448949553176405, 5.886773742842740909 ) ) ;
#15644=CARTESIAN_POINT ( 'NONE',  ( -180.9550000000000125, -7.632228543268599452, 2.479861379858951054 ) ) ;
#15651=ORIENTED_EDGE ( 'NONE', *, *, #44930, .F. ) ;
#15653=CARTESIAN_POINT ( 'NONE',  ( -96.50499999999998124, -6.826472737025113702, -4.959722759717900331 ) ) ;
#15662=CARTESIAN_POINT ( 'NONE',  ( -74.09499999999998465, -2.607480562269071545, -8.024999999999991473 ) ) ;
#15668=FACE_OUTER_BOUND ( 'NONE', #59740, .T. ) ;
#15671=ADVANCED_FACE ( 'NONE', ( #28014 ), #22087, .T. ) ;
#15679=CARTESIAN_POINT ( 'NONE',  ( -156.2070736234661581, 3.094860106618433360, 9.524999999999991473 ) ) ;
#15683=CARTESIAN_POINT ( 'NONE',  ( -101.3070736234661950, -10.01517768586948698, 6.132527647946031529E-16 ) ) ;
#15687=ORIENTED_EDGE ( 'NONE', *, *, #59147, .F. ) ;
#15692=CARTESIAN_POINT ( 'NONE',  ( -138.5049999999999955, -6.826472737025115478, -4.959722759717899443 ) ) ;
#15694=CARTESIAN_POINT ( 'NONE',  ( -158.0949999999999704, -2.607480562269071545, -8.024999999999991473 ) ) ;
#15696=CARTESIAN_POINT ( 'NONE',  ( -142.7949999999999875, 2.607480562269069324, -8.024999999999993250 ) ) ;
#15703=CARTESIAN_POINT ( 'NONE',  ( -49.55499999999998550, 0.000000000000000000, 8.024999999999991473 ) ) ;
#15710=AXIS2_PLACEMENT_3D ( 'NONE', #57525, #31116, #4366 ) ;
#15713=( BOUNDED_CURVE ( )  B_SPLINE_CURVE ( 2, ( #35944, #57392, #25030, #20081, #45822, #30634, #52142, #3897, #3168, #25373, #8525 ),
 .UNSPECIFIED., .F., .F. ) 
 B_SPLINE_CURVE_WITH_KNOTS ( ( 3, 2, 2, 2, 2, 3 ),
 ( 0.8152173913043477826, 0.8173913043478261420, 0.8195652173913043903, 0.8217391304347826386, 0.8239130434782608869, 0.8260869565217391353 ),
 .UNSPECIFIED. ) 
 CURVE ( )  GEOMETRIC_REPRESENTATION_ITEM ( )  RATIONAL_B_SPLINE_CURVE ( ( 1.000000000000000000, 0.9510565162951535312, 1.000000000000000000, 0.9510565162951535312, 1.000000000000000000, 0.9510565162951535312, 1.000000000000000000, 0.9510565162951535312, 1.000000000000000000, 0.9510565162951535312, 1.000000000000000000 ) ) 
 REPRESENTATION_ITEM ( '' )  );
#15728=CARTESIAN_POINT ( 'NONE',  ( -195.0000000000000000, 0.000000000000000000, 9.524999999999991473 ) ) ;
#15742=CARTESIAN_POINT ( 'NONE',  ( -104.9949999999999761, -6.826472737025115478, 4.959722759717900331 ) ) ;
#15755=CARTESIAN_POINT ( 'NONE',  ( -195.0000000000000000, 0.000000000000000000, 0.000000000000000000 ) ) ;
#15763=CARTESIAN_POINT ( 'NONE',  ( -195.0000000000000000, 0.000000000000000000, 0.000000000000000000 ) ) ;
#15767=CARTESIAN_POINT ( 'NONE',  ( -125.3929263765338220, 8.102448949553176405, 5.886773742842740909 ) ) ;
#15776=ORIENTED_EDGE ( 'NONE', *, *, #35675, .F. ) ;
#15777=CARTESIAN_POINT ( 'NONE',  ( -174.0549999999999784, -9.827790563157499189E-16, -8.024999999999991473 ) ) ;
#15780=CARTESIAN_POINT ( 'NONE',  ( -47.60707362346616378, -8.102448949553172852, 5.886773742842742685 ) ) ;
#15781=CARTESIAN_POINT ( 'NONE',  ( -165.7450000000000045, 4.716976649647094177, 6.492361379858945902 ) ) ;
#15787=CARTESIAN_POINT ( 'NONE',  ( -11.94747633183538937, 11.32477212104151221, 3.973188058064621497 ) ) ;
#15788=CARTESIAN_POINT ( 'NONE',  ( -78.80500000000000682, -8.437984349512085203, 5.166775262442717831E-16 ) ) ;
#15792=CARTESIAN_POINT ( 'NONE',  ( -83.69499999999997897, -8.437984349512086979, 5.166775262442717831E-16 ) ) ;
#15797=CARTESIAN_POINT ( 'NONE',  ( -171.3570736234661922, 5.598654528085804216, 7.705886871421366635 ) ) ;
#15800=EDGE_CURVE ( 'NONE', #64678, #30575, #63357, .T. ) ;
#15813=( BOUNDED_CURVE ( )  B_SPLINE_CURVE ( 2, ( #34389, #55495, #1636, #10942, #39353, #38062, #32378, #2680, #44978, #18210, #23474 ),
 .UNSPECIFIED., .F., .F. ) 
 B_SPLINE_CURVE_WITH_KNOTS ( ( 3, 2, 2, 2, 2, 3 ),
 ( 0.3586956521739045334, 0.3608695652173827817, 0.3630434782608609745, 0.3652173913043392228, 0.3673913043478174156, 0.3695652173912956084 ),
 .UNSPECIFIED. ) 
 CURVE ( )  GEOMETRIC_REPRESENTATION_ITEM ( )  RATIONAL_B_SPLINE_CURVE ( ( 1.000000000000191180, 0.9510565162949623508, 1.000000000000000000, 0.9510565162951535312, 1.000000000000000000, 0.9510565162951535312, 1.000000000000000000, 0.9510565162951535312, 1.000000000000000000, 0.9510565162953497076, 0.9999999999998038236 ) ) 
 REPRESENTATION_ITEM ( '' )  );
#15820=ORIENTED_EDGE ( 'NONE', *, *, #66531, .T. ) ;
#15821=CARTESIAN_POINT ( 'NONE',  ( -121.5549999999999926, 0.000000000000000000, 8.024999999999991473 ) ) ;
#15824=CARTESIAN_POINT ( 'NONE',  ( -136.7070736234667265, -3.094860106627910223, -9.524999999993106314 ) ) ;
#15836=AXIS2_PLACEMENT_3D ( 'NONE', #14670, #67787, #24850 ) ;
#15841=ORIENTED_EDGE ( 'NONE', *, *, #65936, .T. ) ;
#15852=CARTESIAN_POINT ( 'NONE',  ( -58.64292637653378648, -5.598654528085801552, 7.705886871421367523 ) ) ;
#15854=CARTESIAN_POINT ( 'NONE',  ( -141.8050000000000068, -8.437984349512085203, 5.166775262442717831E-16 ) ) ;
#15867=CARTESIAN_POINT ( 'NONE',  ( -70.25499999999998124, -4.716976649647092401, 6.492361379858946790 ) ) ;
#15873=CARTESIAN_POINT ( 'NONE',  ( -97.79292637653489351, -3.094860106600278993, 9.525000000013179147 ) ) ;
#15877=DIRECTION ( 'NONE',  ( -1.000000000000000000, -0.000000000000000000, -0.000000000000000000 ) ) ;
#15880=CARTESIAN_POINT ( 'NONE',  ( -109.6449999999999960, 4.716976649647091513, -6.492361379858946790 ) ) ;
#15882=CARTESIAN_POINT ( 'NONE',  ( -91.19499999999999318, 8.437984349512085203, -1.550032578732815448E-15 ) ) ;
#15885=CARTESIAN_POINT ( 'NONE',  ( -183.0000000000000000, 0.000000000000000000, 0.000000000000000000 ) ) ;
#15888=EDGE_CURVE ( 'NONE', #52425, #16179, #41403, .T. ) ;
#15892=CARTESIAN_POINT ( 'NONE',  ( -135.1429263765338078, 5.598654528085800663, -7.705886871421367523 ) ) ;
#15894=DIRECTION ( 'NONE',  ( 0.000000000000000000, 0.000000000000000000, 1.000000000000000000 ) ) ;
#15895=CARTESIAN_POINT ( 'NONE',  ( -146.3950000000000102, -6.826472737025115478, -4.959722759717899443 ) ) ;
#15898=AXIS2_PLACEMENT_3D ( 'NONE', #54399, #48480, #37241 ) ;
#15910=CARTESIAN_POINT ( 'NONE',  ( -60.44292637653379785, -1.166476076187852838E-15, -9.524999999999991473 ) ) ;
#15914=CARTESIAN_POINT ( 'NONE',  ( -154.8549999999999898, 4.716976649647094177, 6.492361379858945902 ) ) ;
#15915=ADVANCED_FACE ( 'NONE', ( #10673 ), #44940, .F. ) ;
#15926=CARTESIAN_POINT ( 'NONE',  ( -96.05707362346618083, 0.000000000000000000, 9.524999999999991473 ) ) ;
#15930=CARTESIAN_POINT ( 'NONE',  ( -59.90499999999997982, 2.607480562269069324, -8.024999999999993250 ) ) ;
#15931=CARTESIAN_POINT ( 'NONE',  ( -116.9949999999999761, -6.826472737025115478, 4.959722759717900331 ) ) ;
#15945=CARTESIAN_POINT ( 'NONE',  ( -184.1049999999999613, -6.826472737025115478, 4.959722759717900331 ) ) ;
#15958=CARTESIAN_POINT ( 'NONE',  ( -96.20499999999996987, -2.607480562269071545, -8.024999999999991473 ) ) ;
#15960=DIRECTION ( 'NONE',  ( -1.000000000000000000, -0.000000000000000000, -0.000000000000000000 ) ) ;
#15963=CARTESIAN_POINT ( 'NONE',  ( -132.6570736234661751, 9.058813317711329915, 2.943386871421369566 ) ) ;
#15966=CARTESIAN_POINT ( 'NONE',  ( -65.15707362346617515, -9.058813317711329915, -2.943386871421370898 ) ) ;
#15968=CARTESIAN_POINT ( 'NONE',  ( -80.09292637653379643, 3.094860106618433360, 9.524999999999991473 ) ) ;
#15973=CARTESIAN_POINT ( 'NONE',  ( -112.8550000000000040, 4.716976649647094177, 6.492361379858945902 ) ) ;
#15975=CARTESIAN_POINT ( 'NONE',  ( -118.0450000000000017, 7.632228543268600340, 2.479861379858949277 ) ) ;
#15982=CARTESIAN_POINT ( 'NONE',  ( -158.5429263765338135, 9.058813317711329915, 2.943386871421369566 ) ) ;
#15984=CARTESIAN_POINT ( 'NONE',  ( -175.7950000000000159, 2.607480562269068880, -8.024999999999993250 ) ) ;
#15992=CARTESIAN_POINT ( 'NONE',  ( -75.59292637653379643, -3.094860106618431139, -9.524999999999991473 ) ) ;
#15994=CARTESIAN_POINT ( 'NONE',  ( -165.8929263765338078, -8.102448949553174629, -5.886773742842741797 ) ) ;
#16000=CARTESIAN_POINT ( 'NONE',  ( -183.0550000000000068, -9.827790563157499189E-16, -8.024999999999991473 ) ) ;
#16003=ORIENTED_EDGE ( 'NONE', *, *, #24665, .T. ) ;
#16004=CONICAL_SURFACE ( 'NONE', #28286, 11.99999999999999645, 0.7853981633974552734 ) ;
#16013=CARTESIAN_POINT ( 'NONE',  ( -90.35499999999998977, -4.716976649647093289, -6.492361379858945902 ) ) ;
#16026=CARTESIAN_POINT ( 'NONE',  ( -70.04499999999998749, 7.632228543268600340, 2.479861379858949277 ) ) ;
#16035=CARTESIAN_POINT ( 'NONE',  ( -126.2049999999999841, -2.607480562269071545, -8.024999999999991473 ) ) ;
#16037=EDGE_CURVE ( 'NONE', #55165, #27373, #23298, .T. ) ;
#16043=CARTESIAN_POINT ( 'NONE',  ( -155.4570736234661581, -9.058813317711329915, 2.943386871421371787 ) ) ;
#16044=EDGE_CURVE ( 'NONE', #37145, #11299, #23200, .T. ) ;
#16046=CARTESIAN_POINT ( 'NONE',  ( -89.60707362346614957, -8.102448949553172852, 5.886773742842742685 ) ) ;
#16053=CARTESIAN_POINT ( 'NONE',  ( -136.7050000000000125, 2.607480562269073321, 8.024999999999991473 ) ) ;
#16058=CARTESIAN_POINT ( 'NONE',  ( -143.5449999999999875, -7.632228543268600340, -2.479861379858950166 ) ) ;
#16059=CARTESIAN_POINT ( 'NONE',  ( -136.7949999999999875, 2.607480562269069324, -8.024999999999993250 ) ) ;
#16065=CARTESIAN_POINT ( 'NONE',  ( -53.45499999999997698, 7.632228543268599452, -2.479861379858951942 ) ) ;
#16072=CARTESIAN_POINT ( 'NONE',  ( -155.1570736234661751, -9.058813317711329915, -2.943386871421370898 ) ) ;
#16073=CARTESIAN_POINT ( 'NONE',  ( -109.4929263765337879, -8.102448949553172852, 5.886773742842742685 ) ) ;
#16083=ORIENTED_EDGE ( 'NONE', *, *, #47294, .T. ) ;
#16087=EDGE_CURVE ( 'NONE', #42918, #38125, #15713, .T. ) ;
#16096=DIRECTION ( 'NONE',  ( -1.000000000000000000, -0.000000000000000000, -0.000000000000000000 ) ) ;
#16104=CARTESIAN_POINT ( 'NONE',  ( -101.3949999999999676, -6.826472737025115478, -4.959722759717899443 ) ) ;
#16113=CARTESIAN_POINT ( 'NONE',  ( -62.90707362346616804, -3.094860106618429807, 9.524999999999991473 ) ) ;
#16131=CARTESIAN_POINT ( 'NONE',  ( -170.1570736234661751, -9.058813317711329915, -2.943386871421370898 ) ) ;
#16135=CARTESIAN_POINT ( 'NONE',  ( -165.6550000000000011, -7.632228543268600340, -2.479861379858950166 ) ) ;
#16138=CARTESIAN_POINT ( 'NONE',  ( -183.1450000000000102, -4.716976649647092401, 6.492361379858946790 ) ) ;
#16139=AXIS2_PLACEMENT_3D ( 'NONE', #51386, #35566, #29214 ) ;
#16140=CARTESIAN_POINT ( 'NONE',  ( -169.7949999999999875, 2.607480562269069324, -8.024999999999993250 ) ) ;
#16144=CARTESIAN_POINT ( 'NONE',  ( -86.60500000000000398, 6.826472737025113702, -4.959722759717902107 ) ) ;
#16149=CARTESIAN_POINT ( 'NONE',  ( -82.19499999999999318, 8.437984349512086979, -1.550032578732815448E-15 ) ) ;
#16158=ORIENTED_EDGE ( 'NONE', *, *, #14728, .F. ) ;
#16171=ADVANCED_FACE ( 'NONE', ( #13787 ), #35601, .F. ) ;
#16177=FACE_OUTER_BOUND ( 'NONE', #4487, .T. ) ;
#16179=VERTEX_POINT ( 'NONE', #10932 ) ;
#16180=CARTESIAN_POINT ( 'NONE',  ( -126.3549999999999898, -4.716976649647093289, -6.492361379858945902 ) ) ;
#16183=CARTESIAN_POINT ( 'NONE',  ( -82.94292637653380496, 0.000000000000000000, 9.524999999999991473 ) ) ;
#16193=FACE_OUTER_BOUND ( 'NONE', #58740, .T. ) ;
#16210=CARTESIAN_POINT ( 'NONE',  ( -144.0549999999999784, -9.827790563157499189E-16, -8.024999999999991473 ) ) ;
#16220=ORIENTED_EDGE ( 'NONE', *, *, #47874, .T. ) ;
#16224=CARTESIAN_POINT ( 'NONE',  ( -59.30499999999999972, 8.437984349512085203, -1.550032578732815448E-15 ) ) ;
#16225=ORIENTED_EDGE ( 'NONE', *, *, #33436, .F. ) ;
#16229=AXIS2_PLACEMENT_3D ( 'NONE', #46741, #47067, #41431 ) ;
#16232=ORIENTED_EDGE ( 'NONE', *, *, #12464, .F. ) ;
#16238=CARTESIAN_POINT ( 'NONE',  ( -106.9449999999999790, -9.827790563157499189E-16, -8.024999999999991473 ) ) ;
#16240=CARTESIAN_POINT ( 'NONE',  ( -85.34499999999998465, 7.632228543268599452, -2.479861379858951942 ) ) ;
#16244=CARTESIAN_POINT ( 'NONE',  ( -168.0570736234661808, 0.000000000000000000, 9.524999999999991473 ) ) ;
#16247=( BOUNDED_CURVE ( )  B_SPLINE_CURVE ( 2, ( #41513, #42244, #5218, #26664, #48187, #63634, #20371, #68576, #25985, #15476, #4163 ),
 .UNSPECIFIED., .F., .F. ) 
 B_SPLINE_CURVE_WITH_KNOTS ( ( 3, 2, 2, 2, 2, 3 ),
 ( 0.3586956521739044224, 0.3608695652173826707, 0.3630434782608608635, 0.3652173913043391118, 0.3673913043478173046, 0.3695652173912954974 ),
 .UNSPECIFIED. ) 
 CURVE ( )  GEOMETRIC_REPRESENTATION_ITEM ( )  RATIONAL_B_SPLINE_CURVE ( ( 1.000000000000193623, 0.9510565162949597973, 1.000000000000000000, 0.9510565162951535312, 1.000000000000000000, 0.9510565162951535312, 1.000000000000000000, 0.9510565162951535312, 1.000000000000000000, 0.9510565162953522611, 0.9999999999998012701 ) ) 
 REPRESENTATION_ITEM ( '' )  );
#16251=CARTESIAN_POINT ( 'NONE',  ( -134.9929263765337737, 8.102448949553171076, -5.886773742842744461 ) ) ;
#16254=CARTESIAN_POINT ( 'NONE',  ( -149.9949999999999193, -6.826472737025115478, 4.959722759717900331 ) ) ;
#16258=CARTESIAN_POINT ( 'NONE',  ( -47.09499999999999886, -2.607480562269071545, -8.024999999999991473 ) ) ;
#16265=CARTESIAN_POINT ( 'NONE',  ( -155.8429263765337964, 9.058813317711329915, -2.943386871421373119 ) ) ;
#16268=CARTESIAN_POINT ( 'NONE',  ( -116.9929263765337879, 8.102448949553172852, -5.886773742842744461 ) ) ;
#16271=CARTESIAN_POINT ( 'NONE',  ( -146.9049999999999727, 2.607480562269069324, -8.024999999999993250 ) ) ;
#16285=CARTESIAN_POINT ( 'NONE',  ( -61.85499999999998266, 4.716976649647094177, 6.492361379858945902 ) ) ;
#16286=CARTESIAN_POINT ( 'NONE',  ( -120.5949999999999704, 2.607480562269073321, 8.024999999999991473 ) ) ;
#16300=CARTESIAN_POINT ( 'NONE',  ( -168.5049999999999955, -6.826472737025115478, -4.959722759717899443 ) ) ;
#16301=ORIENTED_EDGE ( 'NONE', *, *, #28177, .F. ) ;
#16302=CARTESIAN_POINT ( 'NONE',  ( -144.4429263765337907, -1.166476076187852838E-15, -9.524999999999991473 ) ) ;
#16309=CARTESIAN_POINT ( 'NONE',  ( -88.25499999999998124, -4.716976649647092401, 6.492361379858946790 ) ) ;
#16311=CARTESIAN_POINT ( 'NONE',  ( -195.0000000000000000, 1.166476076187852838E-15, -9.524999999999991473 ) ) ;
#16314=CARTESIAN_POINT ( 'NONE',  ( -64.25707362346616947, 5.598654528085800663, -7.705886871421367523 ) ) ;
#16323=CARTESIAN_POINT ( 'NONE',  ( -113.1549999999999869, 7.632228543268600340, 2.479861379858949277 ) ) ;
#16326=CARTESIAN_POINT ( 'NONE',  ( -112.1949999999999932, 8.437984349512085203, -1.550032578732815448E-15 ) ) ;
#16333=CARTESIAN_POINT ( 'NONE',  ( -164.3929263765337510, 8.102448949553176405, 5.886773742842740909 ) ) ;
#16334=CARTESIAN_POINT ( 'NONE',  ( -179.2449999999999761, -4.716976649647093289, -6.492361379858945902 ) ) ;
#16341=CARTESIAN_POINT ( 'NONE',  ( -61.79292637653379217, -3.094860106618429807, 9.524999999999991473 ) ) ;
#16344=CARTESIAN_POINT ( 'NONE',  ( -80.39292637653379359, 8.102448949553176405, 5.886773742842740909 ) ) ;
#16353=CARTESIAN_POINT ( 'NONE',  ( -183.5049999999999955, -6.826472737025113702, -4.959722759717900331 ) ) ;
#16356=CARTESIAN_POINT ( 'NONE',  ( -74.00707362346615525, -8.102448949553174629, -5.886773742842741797 ) ) ;
#16361=CARTESIAN_POINT ( 'NONE',  ( -101.4570736234661723, -9.058813317711329915, 2.943386871421371787 ) ) ;
#16362=CARTESIAN_POINT ( 'NONE',  ( -90.20499999999999829, -2.607480562269071545, -8.024999999999991473 ) ) ;
#16365=CARTESIAN_POINT ( 'NONE',  ( -93.05707362346616662, 0.000000000000000000, 9.524999999999991473 ) ) ;
#16367=CARTESIAN_POINT ( 'NONE',  ( -141.4429263765337907, -1.166476076187852838E-15, -9.524999999999991473 ) ) ;
#16375=CARTESIAN_POINT ( 'NONE',  ( -63.74499999999998323, 4.716976649647094177, 6.492361379858945902 ) ) ;
#16385=DIRECTION ( 'NONE',  ( -1.000000000000000000, -0.000000000000000000, -0.000000000000000000 ) ) ;
#16386=CARTESIAN_POINT ( 'NONE',  ( -125.6050000000000040, 6.826472737025113702, -4.959722759717902107 ) ) ;
#16393=CARTESIAN_POINT ( 'NONE',  ( -161.9070736234662036, -3.094860106618429807, 9.524999999999991473 ) ) ;
#16396=CARTESIAN_POINT ( 'NONE',  ( -90.65707362346617515, 9.058813317711329915, 2.943386871421369566 ) ) ;
#16407=CARTESIAN_POINT ( 'NONE',  ( -145.2549999999999955, -4.716976649647092401, 6.492361379858946790 ) ) ;
#16412=CARTESIAN_POINT ( 'NONE',  ( -148.0449999999999875, 7.632228543268600340, 2.479861379858949277 ) ) ;
#16413=CARTESIAN_POINT ( 'NONE',  ( -137.6949999999999932, -8.437984349512086979, 5.166775262442717831E-16 ) ) ;
#16415=LINE ( 'NONE', #38214, #27967 ) ;
#16420=CARTESIAN_POINT ( 'NONE',  ( -56.75499999999997414, 4.716976649647091513, -6.492361379858946790 ) ) ;
#16421=CARTESIAN_POINT ( 'NONE',  ( -55.49499999999999034, 6.826472737025113702, -4.959722759717902107 ) ) ;
#16425=CARTESIAN_POINT ( 'NONE',  ( -52.64292637653380780, -5.598654528085801552, 7.705886871421367523 ) ) ;
#16432=CARTESIAN_POINT ( 'NONE',  ( -107.0929263765337964, 3.094860106618433360, 9.524999999999991473 ) ) ;
#16453=CARTESIAN_POINT ( 'NONE',  ( -101.5429263765338135, 9.058813317711329915, 2.943386871421369566 ) ) ;
#16457=DIRECTION ( 'NONE',  ( 0.000000000000000000, 0.000000000000000000, 1.000000000000000000 ) ) ;
#16458=CARTESIAN_POINT ( 'NONE',  ( -102.1449999999999818, -4.716976649647092401, 6.492361379858946790 ) ) ;
#16464=CARTESIAN_POINT ( 'NONE',  ( -175.9429263765337907, 0.000000000000000000, 9.524999999999991473 ) ) ;
#16474=CYLINDRICAL_SURFACE ( 'NONE', #67233, 9.524999999999991473 ) ;
#16481=CARTESIAN_POINT ( 'NONE',  ( -115.1929263765338050, -10.01517768586948698, 6.132527647946031529E-16 ) ) ;
#16482=ORIENTED_EDGE ( 'NONE', *, *, #27401, .F. ) ;
#16484=CARTESIAN_POINT ( 'NONE',  ( -48.50707362346618368, 8.102448949553176405, 5.886773742842740909 ) ) ;
#16491=CARTESIAN_POINT ( 'NONE',  ( -173.7549999999999955, 4.716976649647091513, -6.492361379858946790 ) ) ;
#16494=CARTESIAN_POINT ( 'NONE',  ( -176.9950000000000045, -6.826472737025115478, 4.959722759717900331 ) ) ;
#16495=CARTESIAN_POINT ( 'NONE',  ( -163.4949999999999761, 6.826472737025113702, -4.959722759717902107 ) ) ;
#16499=CARTESIAN_POINT ( 'NONE',  ( -79.25499999999999545, -4.716976649647092401, 6.492361379858946790 ) ) ;
#16500=DIRECTION ( 'NONE',  ( -1.000000000000000000, -0.000000000000000000, -0.000000000000000000 ) ) ;
#16503=CARTESIAN_POINT ( 'NONE',  ( -76.34499999999998465, 7.632228543268599452, -2.479861379858951942 ) ) ;
#16523=( BOUNDED_CURVE ( )  B_SPLINE_CURVE ( 2, ( #2122, #65177, #44479, #17026, #33189, #54621, #6433, #65883, #66210, #39523, #7484 ),
 .UNSPECIFIED., .F., .F. ) 
 B_SPLINE_CURVE_WITH_KNOTS ( ( 3, 2, 2, 2, 2, 3 ),
 ( 0.3043478260869493801, 0.3065217391304275729, 0.3086956521739057657, 0.3108695652173839585, 0.3130434782608622069, 0.3152173913043403997 ),
 .UNSPECIFIED. ) 
 CURVE ( )  GEOMETRIC_REPRESENTATION_ITEM ( )  RATIONAL_B_SPLINE_CURVE ( ( 1.000000000000161204, 0.9510565162949923268, 1.000000000000000000, 0.9510565162951535312, 1.000000000000000000, 0.9510565162951535312, 1.000000000000000000, 0.9510565162951535312, 1.000000000000000000, 0.9510565162953209528, 0.9999999999998325784 ) ) 
 REPRESENTATION_ITEM ( '' )  );
#16525=CARTESIAN_POINT ( 'NONE',  ( -109.7049999999999699, 2.607480562269072433, 8.024999999999991473 ) ) ;
#16551=EDGE_LOOP ( 'NONE', ( #65651, #54945 ) ) ;
#16552=CARTESIAN_POINT ( 'NONE',  ( -51.59292637653378932, -3.094860106618431139, -9.524999999999991473 ) ) ;
#16555=CARTESIAN_POINT ( 'NONE',  ( -146.6049999999999329, 6.826472737025113702, -4.959722759717902107 ) ) ;
#16556=CARTESIAN_POINT ( 'NONE',  ( -175.7070736234663002, -3.094860106619918838, -9.524999999998913225 ) ) ;
#16567=CARTESIAN_POINT ( 'NONE',  ( -53.75499999999999545, 4.716976649647091513, -6.492361379858946790 ) ) ;
#16573=EDGE_CURVE ( 'NONE', #1147, #10174, #68295, .T. ) ;
#16579=DIRECTION ( 'NONE',  ( -0.7071067811865426878, 8.659560562354994488E-17, -0.7071067811865524577 ) ) ;
#16584=CARTESIAN_POINT ( 'NONE',  ( -114.1449999999999960, -4.716976649647092401, 6.492361379858946790 ) ) ;
#16586=CARTESIAN_POINT ( 'NONE',  ( -85.79499999999997328, 2.607480562269068880, -8.024999999999993250 ) ) ;
#16593=CARTESIAN_POINT ( 'NONE',  ( -122.8429263765338106, 9.058813317711329915, -2.943386871421373119 ) ) ;
#16594=CARTESIAN_POINT ( 'NONE',  ( -144.8949999999999818, 6.826472737025116366, 4.959722759717898555 ) ) ;
#16601=DIRECTION ( 'NONE',  ( -1.000000000000000000, -0.000000000000000000, -0.000000000000000000 ) ) ;
#16603=CARTESIAN_POINT ( 'NONE',  ( -116.0929263765346775, 3.094860106632819186, 9.524999999989539390 ) ) ;
#16607=CARTESIAN_POINT ( 'NONE',  ( -137.7549999999999955, 4.716976649647091513, -6.492361379858946790 ) ) ;
#16619=CARTESIAN_POINT ( 'NONE',  ( -62.45499999999998408, 7.632228543268599452, -2.479861379858951942 ) ) ;
#16620=CARTESIAN_POINT ( 'NONE',  ( -118.7950000000000017, 2.607480562269068880, -8.024999999999993250 ) ) ;
#16622=VERTEX_POINT ( 'NONE', #5206 ) ;
#16634=CARTESIAN_POINT ( 'NONE',  ( -176.3050000000000068, 8.437984349512085203, -1.550032578732815448E-15 ) ) ;
#16644=DIRECTION ( 'NONE',  ( 0.000000000000000000, 0.000000000000000000, 1.000000000000000000 ) ) ;
#16645=CARTESIAN_POINT ( 'NONE',  ( -83.45499999999998408, 7.632228543268599452, -2.479861379858951942 ) ) ;
#16652=CARTESIAN_POINT ( 'NONE',  ( -60.95707362346616520, 9.058813317711329915, -2.943386871421373119 ) ) ;
#16657=ORIENTED_EDGE ( 'NONE', *, *, #7937, .T. ) ;
#16663=CARTESIAN_POINT ( 'NONE',  ( -106.7049999999999983, 2.607480562269073321, 8.024999999999991473 ) ) ;
#16665=CARTESIAN_POINT ( 'NONE',  ( -112.0449999999999875, 7.632228543268600340, 2.479861379858949277 ) ) ;
#16669=CARTESIAN_POINT ( 'NONE',  ( -157.6429263765338078, -5.598654528085801552, 7.705886871421367523 ) ) ;
#16670=CARTESIAN_POINT ( 'NONE',  ( -173.2449999999999761, -4.716976649647093289, -6.492361379858945902 ) ) ;
#16679=CARTESIAN_POINT ( 'NONE',  ( -80.69292637653380496, 10.01517768586948698, -1.839758294383808571E-15 ) ) ;
#16687=CARTESIAN_POINT ( 'NONE',  ( -176.3049999999999784, 8.437984349512086979, -1.550032578732815448E-15 ) ) ;
#16693=CARTESIAN_POINT ( 'NONE',  ( -182.8766231262712552, -3.603138673335301689, 9.155714005206574413 ) ) ;
#16697=CARTESIAN_POINT ( 'NONE',  ( -88.85499999999998977, 4.716976649647094177, 6.492361379858945902 ) ) ;
#16700=CIRCLE ( 'NONE', #33493, 1.000000000000000888 ) ;
#16701=ORIENTED_EDGE ( 'NONE', *, *, #2917, .F. ) ;
#16705=CARTESIAN_POINT ( 'NONE',  ( -127.6429263765337936, -5.598654528085801552, 7.705886871421367523 ) ) ;
#16711=CARTESIAN_POINT ( 'NONE',  ( -65.84499999999998465, -7.632228543268599452, 2.479861379858951054 ) ) ;
#16724=CARTESIAN_POINT ( 'NONE',  ( -111.6549999999999869, -7.632228543268600340, -2.479861379858950166 ) ) ;
#16726=CARTESIAN_POINT ( 'NONE',  ( -72.89292637653380780, -8.102448949553174629, -5.886773742842741797 ) ) ;
#16730=CARTESIAN_POINT ( 'NONE',  ( -161.6070736234661354, -8.102448949553172852, 5.886773742842742685 ) ) ;
#16732=CARTESIAN_POINT ( 'NONE',  ( -95.75707362346618368, -5.598654528085801552, 7.705886871421367523 ) ) ;
#16734=EDGE_CURVE ( 'NONE', #42940, #59896, #5811, .T. ) ;
#16738=CARTESIAN_POINT ( 'NONE',  ( -131.0049999999999670, 6.826472737025116366, 4.959722759717898555 ) ) ;
#16741=CARTESIAN_POINT ( 'NONE',  ( -54.74292637653380211, -5.598654528085803328, -7.705886871421366635 ) ) ;
#16742=CARTESIAN_POINT ( 'NONE',  ( -144.5950000000000273, 2.607480562269073321, 8.024999999999991473 ) ) ;
#16745=CARTESIAN_POINT ( 'NONE',  ( -139.3449999999999989, 7.632228543268599452, -2.479861379858951942 ) ) ;
#16749=CARTESIAN_POINT ( 'NONE',  ( -55.25499999999999545, -4.716976649647092401, 6.492361379858946790 ) ) ;
#16751=CARTESIAN_POINT ( 'NONE',  ( -55.94499999999999318, -9.827790563157499189E-16, -8.024999999999991473 ) ) ;
#16754=CARTESIAN_POINT ( 'NONE',  ( -102.8070736234661666, 10.01517768586948698, -1.839758294383808966E-15 ) ) ;
#16757=CARTESIAN_POINT ( 'NONE',  ( -102.2929263765338135, 3.094860106618428031, -9.524999999999993250 ) ) ;
#16763=CARTESIAN_POINT ( 'NONE',  ( -99.50707362346614104, 8.102448949553176405, 5.886773742842740909 ) ) ;
#16788=CARTESIAN_POINT ( 'NONE',  ( -91.94499999999997897, -9.827790563157499189E-16, -8.024999999999991473 ) ) ;
#16805=LINE ( 'NONE', #42871, #50674 ) ;
#16818=ORIENTED_EDGE ( 'NONE', *, *, #9816, .F. ) ;
#16819=CARTESIAN_POINT ( 'NONE',  ( -169.1049999999999613, -6.826472737025115478, 4.959722759717900331 ) ) ;
#16822=CARTESIAN_POINT ( 'NONE',  ( -178.0450000000000159, 7.632228543268600340, 2.479861379858949277 ) ) ;
#16823=CARTESIAN_POINT ( 'NONE',  ( -165.4450000000000216, 0.000000000000000000, 8.024999999999991473 ) ) ;
#16824=EDGE_CURVE ( 'NONE', #30575, #16901, #46726, .T. ) ;
#16831=CARTESIAN_POINT ( 'NONE',  ( -78.20499999999996987, -2.607480562269071545, -8.024999999999991473 ) ) ;
#16835=CARTESIAN_POINT ( 'NONE',  ( -78.44499999999999318, 0.000000000000000000, 8.024999999999991473 ) ) ;
#16846=CARTESIAN_POINT ( 'NONE',  ( -50.39292637653380780, 8.102448949553176405, 5.886773742842740909 ) ) ;
#16861=CARTESIAN_POINT ( 'NONE',  ( -108.0549999999999784, -9.827790563157499189E-16, -8.024999999999991473 ) ) ;
#16876=CARTESIAN_POINT ( 'NONE',  ( -117.8070736234661808, 10.01517768586948698, -1.839758294383808966E-15 ) ) ;
#16888=CARTESIAN_POINT ( 'NONE',  ( -50.99292637653380211, 8.102448949553171076, -5.886773742842744461 ) ) ;
#16892=CARTESIAN_POINT ( 'NONE',  ( -142.4049999999999443, -2.607480562269069768, 8.024999999999991473 ) ) ;
#16901=VERTEX_POINT ( 'NONE', #26573 ) ;
#16903=CARTESIAN_POINT ( 'NONE',  ( -55.25499999999999545, -4.716976649647092401, 6.492361379858946790 ) ) ;
#16908=EDGE_CURVE ( 'NONE', #11014, #32568, #13016, .T. ) ;
#16917=CARTESIAN_POINT ( 'NONE',  ( -109.3449999999999847, 7.632228543268599452, -2.479861379858951942 ) ) ;
#16919=CARTESIAN_POINT ( 'NONE',  ( -90.89499999999999602, 6.826472737025116366, 4.959722759717898555 ) ) ;
#16927=CARTESIAN_POINT ( 'NONE',  ( -126.2929263765338135, 3.094860106618428031, -9.524999999999993250 ) ) ;
#16929=CARTESIAN_POINT ( 'NONE',  ( -151.6450000000000102, 4.716976649647091513, -6.492361379858946790 ) ) ;
#16931=EDGE_CURVE ( 'NONE', #43539, #63360, #22469, .T. ) ;
#16939=CARTESIAN_POINT ( 'NONE',  ( -129.3570736234661922, 5.598654528085804216, 7.705886871421366635 ) ) ;
#16940=CARTESIAN_POINT ( 'NONE',  ( -1.000000000000028644, 0.000000000000000000, 0.000000000000000000 ) ) ;
#16941=CARTESIAN_POINT ( 'NONE',  ( -151.9429263765338192, 0.000000000000000000, 9.524999999999991473 ) ) ;
#16943=CARTESIAN_POINT ( 'NONE',  ( -140.7549999999999955, 4.716976649647091513, -6.492361379858946790 ) ) ;
#16952=CARTESIAN_POINT ( 'NONE',  ( 0.000000000000000000, 0.000000000000000000, 0.000000000000000000 ) ) ;
#16956=ORIENTED_EDGE ( 'NONE', *, *, #34366, .F. ) ;
#16959=ADVANCED_FACE ( 'NONE', ( #59268 ), #60662, .T. ) ;
#16960=CARTESIAN_POINT ( 'NONE',  ( -56.75499999999997414, 4.716976649647091513, -6.492361379858946790 ) ) ;
#16961=CARTESIAN_POINT ( 'NONE',  ( -115.9449999999999932, -9.827790563157499189E-16, -8.024999999999991473 ) ) ;
#16969=VERTEX_POINT ( 'NONE', #32547 ) ;
#16972=CARTESIAN_POINT ( 'NONE',  ( -169.5549999999999784, 0.000000000000000000, 8.024999999999991473 ) ) ;
#16983=CARTESIAN_POINT ( 'NONE',  ( -89.00499999999999545, 6.826472737025116366, 4.959722759717898555 ) ) ;
#16990=CARTESIAN_POINT ( 'NONE',  ( -64.70707362346617231, -3.094860106618431139, -9.524999999999991473 ) ) ;
#16996=CARTESIAN_POINT ( 'NONE',  ( -106.4049999999999727, -2.607480562269069768, 8.024999999999991473 ) ) ;
#16998=CARTESIAN_POINT ( 'NONE',  ( -116.0949999999999704, -2.607480562269071545, -8.024999999999991473 ) ) ;
#17005=CARTESIAN_POINT ( 'NONE',  ( -153.4429263765338192, -1.166476076187852838E-15, -9.524999999999991473 ) ) ;
#17008=CARTESIAN_POINT ( 'NONE',  ( -178.9449999999999932, -9.827790563157499189E-16, -8.024999999999991473 ) ) ;
#17018=CARTESIAN_POINT ( 'NONE',  ( -66.29292637653381348, 3.094860106618428031, -9.524999999999993250 ) ) ;
#17026=CARTESIAN_POINT ( 'NONE',  ( -142.4929263765338590, -8.102448949553174629, 5.886773742842742685 ) ) ;
#17028=EDGE_CURVE ( 'NONE', #2194, #51098, #65616, .T. ) ;
#17032=CARTESIAN_POINT ( 'NONE',  ( -172.7049999999999841, 2.607480562269072433, 8.024999999999991473 ) ) ;
#17038=CARTESIAN_POINT ( 'NONE',  ( -127.1070736234661780, 8.102448949553172852, -5.886773742842744461 ) ) ;
#17047=CARTESIAN_POINT ( 'NONE',  ( -83.15499999999998693, 7.632228543268600340, 2.479861379858949277 ) ) ;
#17049=CARTESIAN_POINT ( 'NONE',  ( -92.30707362346618083, -10.01517768586948698, 6.132527647946031529E-16 ) ) ;
#17050=CARTESIAN_POINT ( 'NONE',  ( -168.7429263765338305, -5.598654528085803328, -7.705886871421366635 ) ) ;
#17057=CARTESIAN_POINT ( 'NONE',  ( -62.39499999999998181, -6.826472737025115478, -4.959722759717899443 ) ) ;
#17064=FACE_OUTER_BOUND ( 'NONE', #69456, .T. ) ;
#17069=CARTESIAN_POINT ( 'NONE',  ( -115.1049999999999756, -6.826472737025115478, 4.959722759717900331 ) ) ;
#17072=CARTESIAN_POINT ( 'NONE',  ( -72.74292637653380211, -5.598654528085803328, -7.705886871421366635 ) ) ;
#17076=CARTESIAN_POINT ( 'NONE',  ( -148.5570736234661808, -1.166476076187852838E-15, -9.524999999999991473 ) ) ;
#17079=CARTESIAN_POINT ( 'NONE',  ( -95.90707362346618936, -3.094860106618429807, 9.524999999999991473 ) ) ;
#17090=CARTESIAN_POINT ( 'NONE',  ( -132.5049999999999670, -6.826472737025115478, -4.959722759717899443 ) ) ;
#17092=CARTESIAN_POINT ( 'NONE',  ( -146.5429263765338135, 9.058813317711329915, 2.943386871421369566 ) ) ;
#17093=CARTESIAN_POINT ( 'NONE',  ( -140.5450000000000159, -7.632228543268600340, -2.479861379858950166 ) ) ;
#17094=CARTESIAN_POINT ( 'NONE',  ( -128.3949999999999534, -6.826472737025113702, -4.959722759717900331 ) ) ;
#17097=CARTESIAN_POINT ( 'NONE',  ( -123.4429263765338192, -1.166476076187852838E-15, -9.524999999999991473 ) ) ;
#17102=CARTESIAN_POINT ( 'NONE',  ( -183.2929263765338135, 3.094860106618428031, -9.524999999999993250 ) ) ;
#17104=CARTESIAN_POINT ( 'NONE',  ( -55.79499999999998039, 2.607480562269068880, -8.024999999999993250 ) ) ;
#17107=CARTESIAN_POINT ( 'NONE',  ( -139.4929263765338021, -8.102448949553174629, 5.886773742842742685 ) ) ;
#17112=CARTESIAN_POINT ( 'NONE',  ( -75.80707362346616662, 10.01517768586948698, -1.839758294383808966E-15 ) ) ;
#17113=CARTESIAN_POINT ( 'NONE',  ( -106.4929263765338163, -8.102448949553172852, 5.886773742842742685 ) ) ;
#17135=CARTESIAN_POINT ( 'NONE',  ( -116.4570736234661723, -9.058813317711329915, 2.943386871421371787 ) ) ;
#17140=CARTESIAN_POINT ( 'NONE',  ( -91.79500000000000171, 2.607480562269068880, -8.024999999999993250 ) ) ;
#17158=CARTESIAN_POINT ( 'NONE',  ( -175.4070736234662036, 3.094860106618428031, -9.524999999999993250 ) ) ;
#17163=CARTESIAN_POINT ( 'NONE',  ( -115.7929263765346519, -3.094860106604043981, 9.525000000010443557 ) ) ;
#17165=CARTESIAN_POINT ( 'NONE',  ( -48.95707362346615810, 9.058813317711329915, -2.943386871421373119 ) ) ;
#17170=CARTESIAN_POINT ( 'NONE',  ( -158.0049999999999955, 6.826472737025116366, 4.959722759717898555 ) ) ;
#17173=CARTESIAN_POINT ( 'NONE',  ( -170.2450000000000045, -4.716976649647093289, -6.492361379858945902 ) ) ;
#17176=CARTESIAN_POINT ( 'NONE',  ( -158.6949999999999648, -8.437984349512086979, 5.166775262442717831E-16 ) ) ;
#17177=ORIENTED_EDGE ( 'NONE', *, *, #67014, .F. ) ;
#17178=CARTESIAN_POINT ( 'NONE',  ( -88.94292637653380496, 0.000000000000000000, 9.524999999999991473 ) ) ;
#17182=CARTESIAN_POINT ( 'NONE',  ( -69.50499999999996703, -6.826472737025115478, -4.959722759717899443 ) ) ;
#17187=CARTESIAN_POINT ( 'NONE',  ( -84.89499999999996760, 6.826472737025115478, 4.959722759717899443 ) ) ;
#17189=EDGE_CURVE ( 'NONE', #30575, #3787, #20198, .T. ) ;
#17194=CARTESIAN_POINT ( 'NONE',  ( -176.3929263765338078, 8.102448949553176405, 5.886773742842740909 ) ) ;
#17210=ORIENTED_EDGE ( 'NONE', *, *, #61855, .T. ) ;
#17219=CARTESIAN_POINT ( 'NONE',  ( -113.7549999999999955, 4.716976649647091513, -6.492361379858946790 ) ) ;
#17233=CARTESIAN_POINT ( 'NONE',  ( -117.5070736234661553, 8.102448949553176405, 5.886773742842740909 ) ) ;
#17246=CARTESIAN_POINT ( 'NONE',  ( -52.64292637653380780, -5.598654528085801552, 7.705886871421367523 ) ) ;
#17250=CARTESIAN_POINT ( 'NONE',  ( -146.4550000000000125, 7.632228543268599452, -2.479861379858951942 ) ) ;
#17252=CARTESIAN_POINT ( 'NONE',  ( -176.7570736234661695, -5.598654528085801552, 7.705886871421367523 ) ) ;
#17260=ORIENTED_EDGE ( 'NONE', *, *, #43114, .T. ) ;
#17264=CARTESIAN_POINT ( 'NONE',  ( -58.85499999999998977, 4.716976649647094177, 6.492361379858945902 ) ) ;
#17265=EDGE_LOOP ( 'NONE', ( #45547, #23103, #37917, #1269 ) ) ;
#17279=CARTESIAN_POINT ( 'NONE',  ( -111.2949999999999733, -2.607480562269069768, 8.024999999999991473 ) ) ;
#17281=CARTESIAN_POINT ( 'NONE',  ( -76.49500000000000455, 6.826472737025113702, -4.959722759717902107 ) ) ;
#17289=CARTESIAN_POINT ( 'NONE',  ( -124.6429263765338078, -5.598654528085801552, 7.705886871421367523 ) ) ;
#17290=CARTESIAN_POINT ( 'NONE',  ( -148.9449999999999932, -9.827790563157499189E-16, -8.024999999999991473 ) ) ;
#17300=AXIS2_PLACEMENT_3D ( 'NONE', #588, #43607, #38330 ) ;
#17302=CARTESIAN_POINT ( 'NONE',  ( -195.0000000000000000, 0.000000000000000000, 0.000000000000000000 ) ) ;
#17307=CARTESIAN_POINT ( 'NONE',  ( -141.5049999999999955, -6.826472737025113702, -4.959722759717900331 ) ) ;
#17310=VERTEX_POINT ( 'NONE', #48711 ) ;
#17312=VECTOR ( 'NONE', #9167, 1000.000000000000000 ) ;
#17318=VECTOR ( 'NONE', #55927, 1000.000000000000000 ) ;
#17321=CARTESIAN_POINT ( 'NONE',  ( -52.55499999999999261, 0.000000000000000000, 8.024999999999991473 ) ) ;
#17323=ORIENTED_EDGE ( 'NONE', *, *, #32115, .T. ) ;
#17335=CARTESIAN_POINT ( 'NONE',  ( -167.3049999999999784, 8.437984349512085203, -1.550032578732815448E-15 ) ) ;
#17337=CARTESIAN_POINT ( 'NONE',  ( -88.55707362346616662, -1.166476076187852838E-15, -9.524999999999991473 ) ) ;
#17340=DIRECTION ( 'NONE',  ( 0.000000000000000000, 0.000000000000000000, 1.000000000000000000 ) ) ;
#17342=CARTESIAN_POINT ( 'NONE',  ( -78.14292637653380780, 5.598654528085800663, -7.705886871421367523 ) ) ;
#17347=CARTESIAN_POINT ( 'NONE',  ( -81.65499999999998693, -7.632228543268600340, -2.479861379858950166 ) ) ;
#17352=CARTESIAN_POINT ( 'NONE',  ( -54.80707362346617373, 10.01517768586948698, -1.839758294383808571E-15 ) ) ;
#17357=ADVANCED_FACE ( 'NONE', ( #11018 ), #27859, .T. ) ;
#17359=CARTESIAN_POINT ( 'NONE',  ( -114.2950000000000017, -2.607480562269069768, 8.024999999999991473 ) ) ;
#17364=CARTESIAN_POINT ( 'NONE',  ( -17.07366864973394982, 11.10307524832556503, -4.552615482027356109 ) ) ;
#17366=CARTESIAN_POINT ( 'NONE',  ( -154.0429263765338135, -9.058813317711329915, -2.943386871421370898 ) ) ;
#17367=CARTESIAN_POINT ( 'NONE',  ( -178.3449999999999989, 7.632228543268599452, -2.479861379858951942 ) ) ;
#17370=CARTESIAN_POINT ( 'NONE',  ( -64.55707362346618083, -1.166476076187852838E-15, -9.524999999999991473 ) ) ;
#17377=CARTESIAN_POINT ( 'NONE',  ( -70.49292637653378790, -8.102448949553172852, 5.886773742842742685 ) ) ;
#17382=CARTESIAN_POINT ( 'NONE',  ( -79.49292637653380211, -8.102448949553174629, 5.886773742842742685 ) ) ;
#17384=CARTESIAN_POINT ( 'NONE',  ( -172.8550000000000182, 4.716976649647094177, 6.492361379858945902 ) ) ;
#17396=CARTESIAN_POINT ( 'NONE',  ( -86.00499999999998124, 6.826472737025115478, 4.959722759717899443 ) ) ;
#17399=CARTESIAN_POINT ( 'NONE',  ( -91.85707362346617799, -5.598654528085803328, -7.705886871421366635 ) ) ;
#17407=CARTESIAN_POINT ( 'NONE',  ( -59.39499999999998892, -6.826472737025115478, -4.959722759717899443 ) ) ;
#17411=AXIS2_PLACEMENT_3D ( 'NONE', #12611, #56210, #8038 ) ;
#17414=ORIENTED_EDGE ( 'NONE', *, *, #30657, .T. ) ;
#17418=CARTESIAN_POINT ( 'NONE',  ( -111.0549999999999926, -9.827790563157499189E-16, -8.024999999999991473 ) ) ;
#17426=CARTESIAN_POINT ( 'NONE',  ( -153.8070736234661808, 10.01517768586948698, -1.839758294383808571E-15 ) ) ;
#17429=EDGE_CURVE ( 'NONE', #23235, #29534, #48400, .T. ) ;
#17430=CARTESIAN_POINT ( 'NONE',  ( -83.75707362346616947, -5.598654528085801552, 7.705886871421367523 ) ) ;
#17432=ORIENTED_EDGE ( 'NONE', *, *, #2507, .F. ) ;
#17438=CARTESIAN_POINT ( 'NONE',  ( -132.3549999999999898, -4.716976649647093289, -6.492361379858945902 ) ) ;
#17442=CARTESIAN_POINT ( 'NONE',  ( -149.5449999999999875, -7.632228543268600340, -2.479861379858950166 ) ) ;
#17445=CARTESIAN_POINT ( 'NONE',  ( -130.9449999999999648, -9.827790563157499189E-16, -8.024999999999991473 ) ) ;
#17451=CARTESIAN_POINT ( 'NONE',  ( -182.8429263765338249, 9.058813317711329915, -2.943386871421373119 ) ) ;
#17452=CARTESIAN_POINT ( 'NONE',  ( -61.19499999999997897, 8.437984349512085203, -1.550032578732815448E-15 ) ) ;
#17457=CARTESIAN_POINT ( 'NONE',  ( -94.34292637653379643, -9.058813317711329915, 2.943386871421371787 ) ) ;
#17464=CARTESIAN_POINT ( 'NONE',  ( -100.5570736234661808, -1.166476076187852838E-15, -9.524999999999991473 ) ) ;
#17469=EDGE_LOOP ( 'NONE', ( #28874, #21576, #8964, #23625 ) ) ;
#17479=B_SPLINE_CURVE_WITH_KNOTS ( 'NONE', 3,
 ( #64702, #37999, #32668, #54123, #5934, #3027, #18589, #8021, #56192, #24192, #29096, #18898, #34409, #46037, #12946, #50592, #2327, #67113, #61138, #23849, #2699, #7664, #13281, #55862, #34737, #45006, #45356, #1972, #29820, #50941, #35100, #40398, #24521, #29471, #66774, #61806, #45697, #56547, #13637, #51285 ),
 .UNSPECIFIED., .F., .F.,
 ( 4, 2, 2, 2, 2, 2, 2, 2, 2, 2, 2, 2, 2, 2, 2, 2, 2, 2, 2, 4 ),
 ( 0.007910652177015307582, 0.008898557670442612533, 0.009886463163869915749, 0.01087436865729721897, 0.01186227415072452392, 0.01285017964415182713, 0.01334413239086547701, 0.01383808513757912861, 0.01482599063100643183, 0.01581389612443373505, 0.01630784887114738319, 0.01680180161786103479, 0.01778970711128833801, 0.01828365985800198962, 0.01877761260471563776, 0.01976551809814294097, 0.02075342359157024419, 0.02174132908499755087, 0.02272923457842485409, 0.02371714007185216078 ),
 .UNSPECIFIED. ) ;
#17484=CARTESIAN_POINT ( 'NONE',  ( -89.09499999999998465, -2.607480562269071545, -8.024999999999991473 ) ) ;
#17498=CARTESIAN_POINT ( 'NONE',  ( -138.4429263765337907, -1.166476076187852838E-15, -9.524999999999991473 ) ) ;
#17500=CYLINDRICAL_SURFACE ( 'NONE', #46536, 9.524999999999991473 ) ;
#17502=CARTESIAN_POINT ( 'NONE',  ( -181.4070736234661183, 3.094860106618428031, -9.524999999999993250 ) ) ;
#17505=ADVANCED_FACE ( 'NONE', ( #57665 ), #15134, .T. ) ;
#17509=CARTESIAN_POINT ( 'NONE',  ( -49.40707362346615383, 3.094860106618428031, -9.524999999999993250 ) ) ;
#17511=CARTESIAN_POINT ( 'NONE',  ( -148.5570736234661808, -1.166476076187852838E-15, -9.524999999999991473 ) ) ;
#17514=CARTESIAN_POINT ( 'NONE',  ( -162.5049999999999386, -6.826472737025115478, -4.959722759717899443 ) ) ;
#17517=CARTESIAN_POINT ( 'NONE',  ( -172.4950000000000045, 6.826472737025113702, -4.959722759717902107 ) ) ;
#17521=CARTESIAN_POINT ( 'NONE',  ( -154.7949999999999875, 2.607480562269069324, -8.024999999999993250 ) ) ;
#17527=CARTESIAN_POINT ( 'NONE',  ( -76.55499999999997840, 0.000000000000000000, 8.024999999999991473 ) ) ;
#17531=CARTESIAN_POINT ( 'NONE',  ( -74.24499999999999034, -4.716976649647093289, -6.492361379858945902 ) ) ;
#17541=CIRCLE ( 'NONE', #24235, 7.499999999999985789 ) ;
#17543=CARTESIAN_POINT ( 'NONE',  ( -54.05707362346618083, 0.000000000000000000, 9.524999999999991473 ) ) ;
#17553=CARTESIAN_POINT ( 'NONE',  ( -116.1550000000000011, 7.632228543268600340, 2.479861379858949277 ) ) ;
#17559=CARTESIAN_POINT ( 'NONE',  ( -67.70707362346617231, -3.094860106618431139, -9.524999999999991473 ) ) ;
#17564=( BOUNDED_CURVE ( )  B_SPLINE_CURVE ( 2, ( #45891, #46252, #19472, #67319, #19825, #40974, #40614, #31063, #62394, #62029, #25788 ),
 .UNSPECIFIED., .F., .F. ) 
 B_SPLINE_CURVE_WITH_KNOTS ( ( 3, 2, 2, 2, 2, 3 ),
 ( 0.6086956521738985382, 0.6108695652173767865, 0.6130434782608549238, 0.6152173913043331721, 0.6173913043478113094, 0.6195652173912895577 ),
 .UNSPECIFIED. ) 
 CURVE ( )  GEOMETRIC_REPRESENTATION_ITEM ( )  RATIONAL_B_SPLINE_CURVE ( ( 1.000000000000327516, 0.9510565162948261264, 1.000000000000000000, 0.9510565162951535312, 1.000000000000000000, 0.9510565162951535312, 1.000000000000000000, 0.9510565162951535312, 1.000000000000000000, 0.9510565162954859320, 0.9999999999996675992 ) ) 
 REPRESENTATION_ITEM ( '' )  );
#17586=CARTESIAN_POINT ( 'NONE',  ( -131.1550000000000011, 7.632228543268600340, 2.479861379858949277 ) ) ;
#17591=EDGE_CURVE ( 'NONE', #57659, #41595, #36931, .T. ) ;
#17592=CARTESIAN_POINT ( 'NONE',  ( -106.0429263765337993, -9.058813317711329915, -2.943386871421370898 ) ) ;
#17593=CARTESIAN_POINT ( 'NONE',  ( -107.4570736234661865, -9.058813317711329915, 2.943386871421371787 ) ) ;
#17599=CARTESIAN_POINT ( 'NONE',  ( -60.35499999999998977, -4.716976649647093289, -6.492361379858945902 ) ) ;
#17612=DIRECTION ( 'NONE',  ( -1.000000000000000000, -0.000000000000000000, -0.000000000000000000 ) ) ;
#17614=CARTESIAN_POINT ( 'NONE',  ( -98.99499999999997613, -6.826472737025113702, 4.959722759717902107 ) ) ;
#17617=CARTESIAN_POINT ( 'NONE',  ( -81.44499999999999318, 0.000000000000000000, 8.024999999999991473 ) ) ;
#17624=ORIENTED_EDGE ( 'NONE', *, *, #17189, .F. ) ;
#17625=CARTESIAN_POINT ( 'NONE',  ( -128.5429263765338135, 9.058813317711329915, 2.943386871421369566 ) ) ;
#17626=CARTESIAN_POINT ( 'NONE',  ( -134.5449999999999875, -7.632228543268600340, -2.479861379858950166 ) ) ;
#17641=CARTESIAN_POINT ( 'NONE',  ( -140.6049999999999613, 6.826472737025113702, -4.959722759717902107 ) ) ;
#17655=CARTESIAN_POINT ( 'NONE',  ( -54.95499999999997698, -7.632228543268599452, 2.479861379858951054 ) ) ;
#17657=ORIENTED_EDGE ( 'NONE', *, *, #19217, .F. ) ;
#17660=CARTESIAN_POINT ( 'NONE',  ( -88.49292637653380211, -8.102448949553174629, 5.886773742842742685 ) ) ;
#17670=CARTESIAN_POINT ( 'NONE',  ( -172.2549999999999955, -4.716976649647092401, 6.492361379858946790 ) ) ;
#17673=( BOUNDED_CURVE ( )  B_SPLINE_CURVE ( 2, ( #63144, #14983, #31813, #53299, #20936, #57883, #48055, #47355, #10035, #9704, #68786 ),
 .UNSPECIFIED., .F., .F. ) 
 B_SPLINE_CURVE_WITH_KNOTS ( ( 3, 2, 2, 2, 2, 3 ),
 ( 0.4456521739130330229, 0.4478260869565112712, 0.4499999999999894640, 0.4521739130434676568, 0.4543478260869458496, 0.4565217391304240424 ),
 .UNSPECIFIED. ) 
 CURVE ( )  GEOMETRIC_REPRESENTATION_ITEM ( )  RATIONAL_B_SPLINE_CURVE ( ( 1.000000000000234923, 0.9510565162949186080, 1.000000000000000000, 0.9510565162951535312, 1.000000000000000000, 0.9510565162951535312, 1.000000000000000000, 0.9510565162951535312, 1.000000000000000000, 0.9510565162953947826, 0.9999999999997587485 ) ) 
 REPRESENTATION_ITEM ( '' )  );
#17684=CARTESIAN_POINT ( 'NONE',  ( -81.50499999999999545, -6.826472737025115478, -4.959722759717899443 ) ) ;
#17694=CARTESIAN_POINT ( 'NONE',  ( -102.4449999999999932, 0.000000000000000000, 8.024999999999991473 ) ) ;
#17698=CARTESIAN_POINT ( 'NONE',  ( -148.3429263765338249, -9.058813317711329915, 2.943386871421371787 ) ) ;
#17700=CARTESIAN_POINT ( 'NONE',  ( -168.1449999999999818, -4.716976649647092401, 6.492361379858946790 ) ) ;
#17709=CARTESIAN_POINT ( 'NONE',  ( -67.79292637653381348, -3.094860106618429807, 9.524999999999991473 ) ) ;
#17715=CARTESIAN_POINT ( 'NONE',  ( -170.1550000000000011, 7.632228543268600340, 2.479861379858949277 ) ) ;
#17727=CARTESIAN_POINT ( 'NONE',  ( -79.10499999999998977, -6.826472737025113702, 4.959722759717902107 ) ) ;
#17730=CARTESIAN_POINT ( 'NONE',  ( -91.70707362346730918, -3.094860106637120190, -9.524999999986416555 ) ) ;
#17732=CARTESIAN_POINT ( 'NONE',  ( -72.50707362346616947, 8.102448949553176405, 5.886773742842740909 ) ) ;
#17733=CARTESIAN_POINT ( 'NONE',  ( -113.5429263765338135, 9.058813317711329915, 2.943386871421369566 ) ) ;
#17737=CARTESIAN_POINT ( 'NONE',  ( -67.34499999999998465, 7.632228543268599452, -2.479861379858951942 ) ) ;
#17744=CARTESIAN_POINT ( 'NONE',  ( -50.69499999999998607, -8.437984349512086979, 5.166775262442717831E-16 ) ) ;
#17748=ADVANCED_FACE ( 'NONE', ( #2005 ), #27370, .T. ) ;
#17750=CARTESIAN_POINT ( 'NONE',  ( -118.4049999999999869, -2.607480562269069768, 8.024999999999991473 ) ) ;
#17753=CYLINDRICAL_SURFACE ( 'NONE', #53332, 9.524999999999991473 ) ;
#17756=CARTESIAN_POINT ( 'NONE',  ( -145.7070736234661297, -3.094860106618431139, -9.524999999999991473 ) ) ;
#17759=CARTESIAN_POINT ( 'NONE',  ( -89.15707362346617515, -9.058813317711329915, -2.943386871421370898 ) ) ;
#17767=CARTESIAN_POINT ( 'NONE',  ( -128.7549999999999955, 4.716976649647091513, -6.492361379858946790 ) ) ;
#17771=CARTESIAN_POINT ( 'NONE',  ( -135.5949999999999989, 2.607480562269073321, 8.024999999999991473 ) ) ;
#17772=CARTESIAN_POINT ( 'NONE',  ( -126.7449999999999903, 4.716976649647094177, 6.492361379858945902 ) ) ;
#17774=ORIENTED_EDGE ( 'NONE', *, *, #47398, .T. ) ;
#17778=CARTESIAN_POINT ( 'NONE',  ( -177.5929263765337680, -3.094860106618431139, -9.524999999999991473 ) ) ;
#17779=CARTESIAN_POINT ( 'NONE',  ( -57.14499999999997470, -4.716976649647092401, 6.492361379858946790 ) ) ;
#17785=CARTESIAN_POINT ( 'NONE',  ( -94.94292637653380496, 0.000000000000000000, 9.524999999999991473 ) ) ;
#17790=CARTESIAN_POINT ( 'NONE',  ( -163.3429263765337964, -9.058813317711329915, 2.943386871421371787 ) ) ;
#17808=FACE_OUTER_BOUND ( 'NONE', #32806, .T. ) ;
#17809=CARTESIAN_POINT ( 'NONE',  ( -90.14499999999999602, -4.716976649647092401, 6.492361379858946790 ) ) ;
#17822=FACE_OUTER_BOUND ( 'NONE', #14981, .T. ) ;
#17826=CARTESIAN_POINT ( 'NONE',  ( -180.0570736234661808, 0.000000000000000000, 9.524999999999991473 ) ) ;
#17829=CARTESIAN_POINT ( 'NONE',  ( -110.4570736234661723, -9.058813317711329915, 2.943386871421371787 ) ) ;
#17839=CARTESIAN_POINT ( 'NONE',  ( -160.2549999999999670, -4.716976649647092401, 6.492361379858946790 ) ) ;
#17841=CARTESIAN_POINT ( 'NONE',  ( -169.7949999999999875, 2.607480562269068880, -8.024999999999993250 ) ) ;
#17843=CARTESIAN_POINT ( 'NONE',  ( -154.0449999999999875, 7.632228543268600340, 2.479861379858949277 ) ) ;
#17845=CARTESIAN_POINT ( 'NONE',  ( -66.89292637653377938, -8.102448949553174629, -5.886773742842741797 ) ) ;
#17848=CARTESIAN_POINT ( 'NONE',  ( -73.40500000000000114, -2.607480562269069768, 8.024999999999991473 ) ) ;
#17852=CARTESIAN_POINT ( 'NONE',  ( -75.14499999999999602, -4.716976649647092401, 6.492361379858946790 ) ) ;
#17876=CARTESIAN_POINT ( 'NONE',  ( -111.8049999999999784, -8.437984349512086979, 5.166775262442717831E-16 ) ) ;
#17891=LINE ( 'NONE', #45696, #29446 ) ;
#17904=CARTESIAN_POINT ( 'NONE',  ( -129.0549999999999784, -9.827790563157499189E-16, -8.024999999999991473 ) ) ;
#17909=CARTESIAN_POINT ( 'NONE',  ( -106.8570736234661780, -5.598654528085803328, -7.705886871421366635 ) ) ;
#17911=ORIENTED_EDGE ( 'NONE', *, *, #54468, .T. ) ;
#17922=ORIENTED_EDGE ( 'NONE', *, *, #19932, .T. ) ;
#17931=CARTESIAN_POINT ( 'NONE',  ( -103.3449999999999989, 7.632228543268599452, -2.479861379858951942 ) ) ;
#17933=CARTESIAN_POINT ( 'NONE',  ( -79.34499999999998465, 7.632228543268599452, -2.479861379858951942 ) ) ;
#17943=CARTESIAN_POINT ( 'NONE',  ( -125.5429263765337993, 9.058813317711329915, 2.943386871421369566 ) ) ;
#17945=CARTESIAN_POINT ( 'NONE',  ( -136.7949999999999875, 2.607480562269068880, -8.024999999999993250 ) ) ;
#17964=CARTESIAN_POINT ( 'NONE',  ( -144.2050000000000125, -2.607480562269071545, -8.024999999999991473 ) ) ;
#17977=CARTESIAN_POINT ( 'NONE',  ( -55.85499999999998977, 4.716976649647094177, 6.492361379858945902 ) ) ;
#17985=VERTEX_POINT ( 'NONE', #37937 ) ;
#17989=CARTESIAN_POINT ( 'NONE',  ( -122.4570736234661723, -9.058813317711329915, 2.943386871421371787 ) ) ;
#17990=CARTESIAN_POINT ( 'NONE',  ( -158.0049999999999955, 6.826472737025116366, 4.959722759717898555 ) ) ;
#18000=CARTESIAN_POINT ( 'NONE',  ( -80.60499999999996135, 6.826472737025113702, -4.959722759717902107 ) ) ;
#18013=CARTESIAN_POINT ( 'NONE',  ( -105.1449999999999818, -4.716976649647092401, 6.492361379858946790 ) ) ;
#18021=CARTESIAN_POINT ( 'NONE',  ( -152.6929263765337907, 10.01517768586948698, -1.839758294383808571E-15 ) ) ;
#18024=CARTESIAN_POINT ( 'NONE',  ( -167.9950000000000045, -6.826472737025115478, 4.959722759717900331 ) ) ;
#18025=ADVANCED_FACE ( 'NONE', ( #54732 ), #38278, .T. ) ;
#18026=EDGE_CURVE ( 'NONE', #29002, #64619, #50825, .T. ) ;
#18032=CARTESIAN_POINT ( 'NONE',  ( -70.79292637653379927, -3.094860106618429807, 9.524999999999991473 ) ) ;
#18041=EDGE_CURVE ( 'NONE', #49292, #41299, #16805, .T. ) ;
#18042=ORIENTED_EDGE ( 'NONE', *, *, #34166, .T. ) ;
#18043=CARTESIAN_POINT ( 'NONE',  ( -170.0049999999999955, 6.826472737025115478, 4.959722759717899443 ) ) ;
#18045=CARTESIAN_POINT ( 'NONE',  ( -112.6429263765338078, -5.598654528085801552, 7.705886871421367523 ) ) ;
#18048=VECTOR ( 'NONE', #4839, 1000.000000000000000 ) ;
#18051=( BOUNDED_CURVE ( )  B_SPLINE_CURVE ( 2, ( #60489, #61886, #13349, #28475, #39440, #34469, #44727, #55924, #12299, #2035, #44392 ),
 .UNSPECIFIED., .F., .F. ) 
 B_SPLINE_CURVE_WITH_KNOTS ( ( 3, 2, 2, 2, 2, 3 ),
 ( 0.07608695652173738666, 0.07826086956521560722, 0.08043478260869380003, 0.08260869565217202060, 0.08478260869565022728, 0.08695652173912844785 ),
 .UNSPECIFIED. ) 
 CURVE ( )  GEOMETRIC_REPRESENTATION_ITEM ( )  RATIONAL_B_SPLINE_CURVE ( ( 1.000000000000039302, 0.9510565162951140072, 1.000000000000000000, 0.9510565162951535312, 1.000000000000000000, 0.9510565162951535312, 1.000000000000000000, 0.9510565162951535312, 1.000000000000000000, 0.9510565162951981621, 0.9999999999999553690 ) ) 
 REPRESENTATION_ITEM ( '' )  );
#18053=VECTOR ( 'NONE', #53195, 1000.000000000000000 ) ;
#18056=CARTESIAN_POINT ( 'NONE',  ( -87.05499999999999261, -9.827790563157499189E-16, -8.024999999999991473 ) ) ;
#18062=CARTESIAN_POINT ( 'NONE',  ( -72.95707362346617231, 9.058813317711329915, -2.943386871421373119 ) ) ;
#18067=CARTESIAN_POINT ( 'NONE',  ( -140.6070736234661922, -8.102448949553174629, 5.886773742842742685 ) ) ;
#18069=CARTESIAN_POINT ( 'NONE',  ( -51.89499999999998892, 6.826472737025116366, 4.959722759717898555 ) ) ;
#18078=CARTESIAN_POINT ( 'NONE',  ( -53.69499999999999318, -8.437984349512086979, 5.166775262442717831E-16 ) ) ;
#18082=CARTESIAN_POINT ( 'NONE',  ( -117.2049999999999841, -2.607480562269071545, -8.024999999999991473 ) ) ;
#18088=CARTESIAN_POINT ( 'NONE',  ( -150.9570736234661581, 9.058813317711329915, -2.943386871421373119 ) ) ;
#18092=CARTESIAN_POINT ( 'NONE',  ( -81.05707362346618083, 0.000000000000000000, 9.524999999999991473 ) ) ;
#18098=CARTESIAN_POINT ( 'NONE',  ( -131.7549999999999955, 4.716976649647091513, -6.492361379858946790 ) ) ;
#18102=CARTESIAN_POINT ( 'NONE',  ( -136.4949999999999477, 6.826472737025113702, -4.959722759717902107 ) ) ;
#18103=CARTESIAN_POINT ( 'NONE',  ( -127.1950000000000074, 8.437984349512086979, -1.550032578732815448E-15 ) ) ;
#18112=CARTESIAN_POINT ( 'NONE',  ( -179.0929263765338249, 3.094860106618433360, 9.524999999999991473 ) ) ;
#18114=CARTESIAN_POINT ( 'NONE',  ( -53.39499999999998892, -6.826472737025115478, -4.959722759717899443 ) ) ;
#18122=CARTESIAN_POINT ( 'NONE',  ( -96.14292637653380780, 5.598654528085800663, -7.705886871421367523 ) ) ;
#18130=ADVANCED_FACE ( 'NONE', ( #55446 ), #1910, .F. ) ;
#18141=CARTESIAN_POINT ( 'NONE',  ( -195.0000000000000000, 1.166476076187852838E-15, -9.524999999999991473 ) ) ;
#18146=ADVANCED_FACE ( 'NONE', ( #17822 ), #66338, .T. ) ;
#18148=CARTESIAN_POINT ( 'NONE',  ( -72.05707362346616662, 0.000000000000000000, 9.524999999999991473 ) ) ;
#18150=CARTESIAN_POINT ( 'NONE',  ( -92.69499999999996476, -8.437984349512085203, 5.166775262442717831E-16 ) ) ;
#18161=CARTESIAN_POINT ( 'NONE',  ( -182.3070736234662093, -10.01517768586948698, 6.132527647946031529E-16 ) ) ;
#18165=CARTESIAN_POINT ( 'NONE',  ( -111.0570736234661808, 0.000000000000000000, 9.524999999999991473 ) ) ;
#18170=CARTESIAN_POINT ( 'NONE',  ( -195.0000000000000000, 1.166476076187852838E-15, -9.524999999999991473 ) ) ;
#18175=CARTESIAN_POINT ( 'NONE',  ( -156.5050000000000239, -6.826472737025115478, -4.959722759717899443 ) ) ;
#18178=EDGE_CURVE ( 'NONE', #4472, #32880, #43677, .T. ) ;
#18179=CARTESIAN_POINT ( 'NONE',  ( -159.7450000000000045, 4.716976649647094177, 6.492361379858945902 ) ) ;
#18180=CARTESIAN_POINT ( 'NONE',  ( -158.3949999999999818, -6.826472737025113702, -4.959722759717900331 ) ) ;
#18182=DIRECTION ( 'NONE',  ( -1.000000000000000000, -0.000000000000000000, -0.000000000000000000 ) ) ;
#18185=CARTESIAN_POINT ( 'NONE',  ( -74.60500000000000398, 6.826472737025113702, -4.959722759717902107 ) ) ;
#18190=CARTESIAN_POINT ( 'NONE',  ( -73.19499999999997897, 8.437984349512086979, -1.550032578732815448E-15 ) ) ;
#18194=EDGE_CURVE ( 'NONE', #10174, #51919, #12518, .T. ) ;
#18205=CARTESIAN_POINT ( 'NONE',  ( -120.1429263765338078, 5.598654528085800663, -7.705886871421367523 ) ) ;
#18208=CARTESIAN_POINT ( 'NONE',  ( -60.05707362346616662, 0.000000000000000000, 9.524999999999991473 ) ) ;
#18210=CARTESIAN_POINT ( 'NONE',  ( -132.2070736234668686, 3.094860106628988028, 9.524999999992326494 ) ) ;
#18217=CARTESIAN_POINT ( 'NONE',  ( -99.80499999999997840, -8.437984349512086979, 5.166775262442717831E-16 ) ) ;
#18223=CARTESIAN_POINT ( 'NONE',  ( -65.54292637653379927, 9.058813317711329915, 2.943386871421369566 ) ) ;
#18228=CARTESIAN_POINT ( 'NONE',  ( -123.2949999999999875, -2.607480562269069768, 8.024999999999991473 ) ) ;
#18229=ORIENTED_EDGE ( 'NONE', *, *, #42617, .F. ) ;
#18230=EDGE_LOOP ( 'NONE', ( #65539, #50043, #54162, #20228 ) ) ;
#18248=CARTESIAN_POINT ( 'NONE',  ( -134.1550000000000011, 7.632228543268600340, 2.479861379858949277 ) ) ;
#18254=( LENGTH_UNIT ( ) NAMED_UNIT ( * ) SI_UNIT ( .MILLI., .METRE. ) );
#18260=CARTESIAN_POINT ( 'NONE',  ( -51.95707362346615810, 9.058813317711329915, -2.943386871421373119 ) ) ;
#18263=CARTESIAN_POINT ( 'NONE',  ( -123.5070736234661695, 8.102448949553176405, 5.886773742842740909 ) ) ;
#18264=CARTESIAN_POINT ( 'NONE',  ( -184.2549999999999955, -4.716976649647092401, 6.492361379858946790 ) ) ;
#18265=CARTESIAN_POINT ( 'NONE',  ( -91.94292637653380496, 0.000000000000000000, 9.524999999999991473 ) ) ;
#18267=FACE_OUTER_BOUND ( 'NONE', #33288, .T. ) ;
#18278=CARTESIAN_POINT ( 'NONE',  ( -99.20499999999999829, -2.607480562269071545, -8.024999999999991473 ) ) ;
#18286=CARTESIAN_POINT ( 'NONE',  ( -97.79499999999998749, 2.607480562269069324, -8.024999999999993250 ) ) ;
#18288=CARTESIAN_POINT ( 'NONE',  ( -73.94499999999997897, -9.827790563157499189E-16, -8.024999999999991473 ) ) ;
#18289=EDGE_CURVE ( 'NONE', #23696, #60435, #58031, .T. ) ;
#18299=CARTESIAN_POINT ( 'NONE',  ( -114.7429263765338021, -5.598654528085803328, -7.705886871421366635 ) ) ;
#18301=CARTESIAN_POINT ( 'NONE',  ( -140.2450000000000045, -4.716976649647093289, -6.492361379858945902 ) ) ;
#18318=CARTESIAN_POINT ( 'NONE',  ( -132.8050000000000068, -8.437984349512086979, 5.166775262442717831E-16 ) ) ;
#18322=LINE ( 'NONE', #6362, #36638 ) ;
#18335=CARTESIAN_POINT ( 'NONE',  ( -51.95499999999996987, -7.632228543268599452, 2.479861379858951054 ) ) ;
#18337=VERTEX_POINT ( 'NONE', #7103 ) ;
#18346=DIRECTION ( 'NONE',  ( -0.000000000000000000, 1.000000000000000000, -0.000000000000000000 ) ) ;
#18351=CARTESIAN_POINT ( 'NONE',  ( -161.0050000000000239, 6.826472737025116366, 4.959722759717898555 ) ) ;
#18356=CARTESIAN_POINT ( 'NONE',  ( -99.05707362346618083, 0.000000000000000000, 9.524999999999991473 ) ) ;
#18358=( BOUNDED_CURVE ( )  B_SPLINE_CURVE ( 2, ( #18148, #35014, #56465, #66686, #2612, #67727, #66325, #29742, #41025, #61718, #50508 ),
 .UNSPECIFIED., .F., .F. ) 
 B_SPLINE_CURVE_WITH_KNOTS ( ( 3, 2, 2, 2, 2, 3 ),
 ( 0.8043478260869565410, 0.8065217391304347894, 0.8086956521739130377, 0.8108695652173912860, 0.8130434782608695343, 0.8152173913043477826 ),
 .UNSPECIFIED. ) 
 CURVE ( )  GEOMETRIC_REPRESENTATION_ITEM ( )  RATIONAL_B_SPLINE_CURVE ( ( 1.000000000000000000, 0.9510565162951535312, 1.000000000000000000, 0.9510565162951535312, 1.000000000000000000, 0.9510565162951535312, 1.000000000000000000, 0.9510565162951535312, 1.000000000000000000, 0.9510565162951535312, 1.000000000000000000 ) ) 
 REPRESENTATION_ITEM ( '' )  );
#18362=CARTESIAN_POINT ( 'NONE',  ( -78.05499999999997840, -9.827790563157499189E-16, -8.024999999999991473 ) ) ;
#18378=CARTESIAN_POINT ( 'NONE',  ( -107.6949999999999932, -8.437984349512085203, 5.166775262442717831E-16 ) ) ;
#18381=DIRECTION ( 'NONE',  ( -1.000000000000000000, -0.000000000000000000, -0.000000000000000000 ) ) ;
#18383=CARTESIAN_POINT ( 'NONE',  ( -19.33438955202580090, 11.73703352805583933, 2.513953393961228855 ) ) ;
#18385=CARTESIAN_POINT ( 'NONE',  ( -146.5429263765338135, 9.058813317711329915, 2.943386871421369566 ) ) ;
#18387=CARTESIAN_POINT ( 'NONE',  ( -169.9449999999999932, -9.827790563157499189E-16, -8.024999999999991473 ) ) ;
#18389=CARTESIAN_POINT ( 'NONE',  ( -195.0000000000000000, 0.000000000000000000, 9.524999999999991473 ) ) ;
#18398=CARTESIAN_POINT ( 'NONE',  ( -163.7049999999999841, 2.607480562269072433, 8.024999999999991473 ) ) ;
#18409=VERTEX_POINT ( 'NONE', #12354 ) ;
#18412=CARTESIAN_POINT ( 'NONE',  ( -84.05499999999999261, -9.827790563157499189E-16, -8.024999999999991473 ) ) ;
#18417=CARTESIAN_POINT ( 'NONE',  ( -100.9429263765338050, 0.000000000000000000, 9.524999999999991473 ) ) ;
#18420=ORIENTED_EDGE ( 'NONE', *, *, #56359, .F. ) ;
#18423=CARTESIAN_POINT ( 'NONE',  ( -50.84499999999997044, -7.632228543268599452, 2.479861379858951054 ) ) ;
#18432=CARTESIAN_POINT ( 'NONE',  ( -51.44499999999999318, 0.000000000000000000, 8.024999999999991473 ) ) ;
#18438=CARTESIAN_POINT ( 'NONE',  ( -100.1049999999999898, -6.826472737025115478, 4.959722759717900331 ) ) ;
#18443=CARTESIAN_POINT ( 'NONE',  ( -149.3070736234662093, -10.01517768586948698, 6.132527647946031529E-16 ) ) ;
#18446=CARTESIAN_POINT ( 'NONE',  ( -88.25707362346616947, 5.598654528085800663, -7.705886871421367523 ) ) ;
#18449=EDGE_CURVE ( 'NONE', #21270, #34770, #26027, .T. ) ;
#18454=CARTESIAN_POINT ( 'NONE',  ( -124.4049999999999869, -2.607480562269069768, 8.024999999999991473 ) ) ;
#18458=CARTESIAN_POINT ( 'NONE',  ( -134.8449999999999989, -7.632228543268599452, 2.479861379858951054 ) ) ;
#18461=CARTESIAN_POINT ( 'NONE',  ( -124.6449999999999960, 4.716976649647091513, -6.492361379858946790 ) ) ;
#18464=CARTESIAN_POINT ( 'NONE',  ( -146.1570736234662036, -9.058813317711329915, -2.943386871421370898 ) ) ;
#18467=CARTESIAN_POINT ( 'NONE',  ( -180.5929263765338249, -3.094860106618431139, -9.524999999999991473 ) ) ;
#18468=CARTESIAN_POINT ( 'NONE',  ( -52.34499999999997755, 7.632228543268599452, -2.479861379858951942 ) ) ;
#18475=CARTESIAN_POINT ( 'NONE',  ( -91.94292637653380496, 0.000000000000000000, 9.524999999999991473 ) ) ;
#18476=SHAPE_DEFINITION_REPRESENTATION ( #31602, #14155 ) ;
#18478=( BOUNDED_CURVE ( )  B_SPLINE_CURVE ( 2, ( #47956, #48270, #22195, #26076, #27098, #69354, #327, #21861, #16939, #43373, #47610 ),
 .UNSPECIFIED., .F., .F. ) 
 B_SPLINE_CURVE_WITH_KNOTS ( ( 3, 2, 2, 2, 2, 3 ),
 ( 0.3804347826086866280, 0.3826086956521648208, 0.3847826086956430136, 0.3869565217391212619, 0.3891304347825994547, 0.3913043478260777031 ),
 .UNSPECIFIED. ) 
 CURVE ( )  GEOMETRIC_REPRESENTATION_ITEM ( )  RATIONAL_B_SPLINE_CURVE ( ( 1.000000000000203615, 0.9510565162949498053, 1.000000000000000000, 0.9510565162951535312, 1.000000000000000000, 0.9510565162951535312, 1.000000000000000000, 0.9510565162951535312, 1.000000000000000000, 0.9510565162953622531, 0.9999999999997912781 ) ) 
 REPRESENTATION_ITEM ( '' )  );
#18483=AXIS2_PLACEMENT_3D ( 'NONE', #45762, #51355, #40475 ) ;
#18502=CARTESIAN_POINT ( 'NONE',  ( -73.55707362346616662, -1.166476076187852838E-15, -9.524999999999991473 ) ) ;
#18503=CARTESIAN_POINT ( 'NONE',  ( -82.34499999999998465, 7.632228543268599452, -2.479861379858951942 ) ) ;
#18507=CARTESIAN_POINT ( 'NONE',  ( -76.79292637653379927, -3.094860106618429807, 9.524999999999991473 ) ) ;
#18510=ADVANCED_FACE ( 'NONE', ( #30259 ), #8150, .T. ) ;
#18516=CARTESIAN_POINT ( 'NONE',  ( -137.9929263765338590, 8.102448949553172852, -5.886773742842744461 ) ) ;
#18520=CARTESIAN_POINT ( 'NONE',  ( -174.6570736234662036, 9.058813317711329915, 2.943386871421369566 ) ) ;
#18523=CARTESIAN_POINT ( 'NONE',  ( -117.8070736234661950, 10.01517768586948698, -1.839758294383808571E-15 ) ) ;
#18535=CARTESIAN_POINT ( 'NONE',  ( -163.4050000000000011, -2.607480562269069768, 8.024999999999991473 ) ) ;
#18538=CARTESIAN_POINT ( 'NONE',  ( -165.8949999999999818, 6.826472737025116366, 4.959722759717898555 ) ) ;
#18539=CARTESIAN_POINT ( 'NONE',  ( -159.1449999999999818, -4.716976649647092401, 6.492361379858946790 ) ) ;
#18544=FACE_OUTER_BOUND ( 'NONE', #17265, .T. ) ;
#18545=CARTESIAN_POINT ( 'NONE',  ( -122.8429263765338106, 9.058813317711329915, -2.943386871421373119 ) ) ;
#18546=CARTESIAN_POINT ( 'NONE',  ( -73.10499999999996135, -6.826472737025115478, 4.959722759717900331 ) ) ;
#18550=CARTESIAN_POINT ( 'NONE',  ( -68.54499999999998749, -7.632228543268600340, -2.479861379858950166 ) ) ;
#18556=CARTESIAN_POINT ( 'NONE',  ( -155.7570736234661979, -5.598654528085801552, 7.705886871421367523 ) ) ;
#18569=CARTESIAN_POINT ( 'NONE',  ( -155.0929263765342228, 3.094860106624684803, 9.524999999995451105 ) ) ;
#18579=CARTESIAN_POINT ( 'NONE',  ( -145.0429263765338135, -9.058813317711329915, -2.943386871421370898 ) ) ;
#18582=CARTESIAN_POINT ( 'NONE',  ( -115.3449999999999847, 7.632228543268599452, -2.479861379858951942 ) ) ;
#18589=CARTESIAN_POINT ( 'NONE',  ( -12.48200500612924024, -11.19251907289281966, 4.331800619050086176 ) ) ;
#18608=CARTESIAN_POINT ( 'NONE',  ( -136.5549999999999784, 0.000000000000000000, 8.024999999999991473 ) ) ;
#18613=CARTESIAN_POINT ( 'NONE',  ( -45.00000000000000000, 0.000000000000000000, 0.000000000000000000 ) ) ;
#18619=ADVANCED_FACE ( 'NONE', ( #58403 ), #21456, .T. ) ;
#18620=CARTESIAN_POINT ( 'NONE',  ( -48.35499999999998266, -4.716976649647093289, -6.492361379858945902 ) ) ;
#18623=CARTESIAN_POINT ( 'NONE',  ( -183.8050000000000068, -8.437984349512085203, 5.166775262442717831E-16 ) ) ;
#18625=CARTESIAN_POINT ( 'NONE',  ( -57.95707362346616520, 9.058813317711329915, -2.943386871421373119 ) ) ;
#18626=CARTESIAN_POINT ( 'NONE',  ( -183.1450000000000102, -4.716976649647092401, 6.492361379858946790 ) ) ;
#18630=CARTESIAN_POINT ( 'NONE',  ( -161.3070736234661808, -10.01517768586948698, 6.132527647946031529E-16 ) ) ;
#18632=CARTESIAN_POINT ( 'NONE',  ( -105.0549999999999926, -9.827790563157499189E-16, -8.024999999999991473 ) ) ;
#18636=CARTESIAN_POINT ( 'NONE',  ( -104.2449999999999903, -4.716976649647093289, -6.492361379858945902 ) ) ;
#18638=CARTESIAN_POINT ( 'NONE',  ( -79.04499999999998749, 7.632228543268600340, 2.479861379858949277 ) ) ;
#18645=CARTESIAN_POINT ( 'NONE',  ( -115.6429263765338078, -5.598654528085801552, 7.705886871421367523 ) ) ;
#18646=CARTESIAN_POINT ( 'NONE',  ( -141.1449999999999818, -4.716976649647092401, 6.492361379858946790 ) ) ;
#18661=CARTESIAN_POINT ( 'NONE',  ( -130.8549999999999898, 4.716976649647094177, 6.492361379858945902 ) ) ;
#18666=CARTESIAN_POINT ( 'NONE',  ( -83.39292637653379359, 8.102448949553176405, 5.886773742842740909 ) ) ;
#18668=ADVANCED_FACE ( 'NONE', ( #31304 ), #16004, .T. ) ;
#18673=VERTEX_POINT ( 'NONE', #57368 ) ;
#18676=CARTESIAN_POINT ( 'NONE',  ( -49.85499999999998266, 4.716976649647094177, 6.492361379858945902 ) ) ;
#18688=CARTESIAN_POINT ( 'NONE',  ( -117.4429263765338050, -1.166476076187852838E-15, -9.524999999999991473 ) ) ;
#18691=CARTESIAN_POINT ( 'NONE',  ( -159.3549999999999898, -4.716976649647093289, -6.492361379858945902 ) ) ;
#18703=CARTESIAN_POINT ( 'NONE',  ( -79.25499999999999545, -4.716976649647092401, 6.492361379858946790 ) ) ;
#18714=CARTESIAN_POINT ( 'NONE',  ( -105.8949999999999676, 6.826472737025116366, 4.959722759717898555 ) ) ;
#18717=CARTESIAN_POINT ( 'NONE',  ( -96.20707362346723812, 3.094860106636315056, 9.524999999987000976 ) ) ;
#18718=CARTESIAN_POINT ( 'NONE',  ( -147.5929263765338249, -3.094860106618431139, -9.524999999999991473 ) ) ;
#18719=CARTESIAN_POINT ( 'NONE',  ( -167.5449999999999875, -7.632228543268600340, -2.479861379858950166 ) ) ;
#18731=CARTESIAN_POINT ( 'NONE',  ( -160.4049999999999727, -2.607480562269069768, 8.024999999999991473 ) ) ;
#18736=ADVANCED_FACE ( 'NONE', ( #22153 ), #23199, .T. ) ;
#18745=CARTESIAN_POINT ( 'NONE',  ( -78.50499999999999545, -6.826472737025113702, -4.959722759717900331 ) ) ;
#18753=EDGE_CURVE ( 'NONE', #13980, #9643, #42989, .T. ) ;
#18757=CARTESIAN_POINT ( 'NONE',  ( -49.79499999999998039, 2.607480562269068880, -8.024999999999993250 ) ) ;
#18761=CARTESIAN_POINT ( 'NONE',  ( -85.94292637653380496, 0.000000000000000000, 9.524999999999991473 ) ) ;
#18766=CARTESIAN_POINT ( 'NONE',  ( -54.14499999999999602, -4.716976649647092401, 6.492361379858946790 ) ) ;
#18770=CARTESIAN_POINT ( 'NONE',  ( -103.7049999999999983, 2.607480562269073321, 8.024999999999991473 ) ) ;
#18772=DIRECTION ( 'NONE',  ( 0.000000000000000000, 0.000000000000000000, 1.000000000000000000 ) ) ;
#18774=CARTESIAN_POINT ( 'NONE',  ( -145.4070736234661467, 3.094860106618428031, -9.524999999999993250 ) ) ;
#18777=CARTESIAN_POINT ( 'NONE',  ( -88.85707362346617799, -5.598654528085803328, -7.705886871421366635 ) ) ;
#18782=CARTESIAN_POINT ( 'NONE',  ( -122.9049999999999727, 2.607480562269068880, -8.024999999999993250 ) ) ;
#18786=CARTESIAN_POINT ( 'NONE',  ( -131.2450000000000045, -4.716976649647093289, -6.492361379858945902 ) ) ;
#18787=CARTESIAN_POINT ( 'NONE',  ( -116.5450000000000017, -7.632228543268600340, -2.479861379858950166 ) ) ;
#18792=CARTESIAN_POINT ( 'NONE',  ( -120.5929263765346064, -3.094860106631942553, -9.524999999990175326 ) ) ;
#18793=CARTESIAN_POINT ( 'NONE',  ( -170.0929263765338249, 3.094860106618433360, 9.524999999999991473 ) ) ;
#18795=CARTESIAN_POINT ( 'NONE',  ( -49.49499999999997613, 6.826472737025113702, -4.959722759717902107 ) ) ;
#18801=CARTESIAN_POINT ( 'NONE',  ( -89.84292637653381064, 9.058813317711329915, -2.943386871421373119 ) ) ;
#18805=LINE ( 'NONE', #62745, #66269 ) ;
#18807=CARTESIAN_POINT ( 'NONE',  ( -78.20707362346617231, 3.094860106618433360, 9.524999999999991473 ) ) ;
#18822=ORIENTED_EDGE ( 'NONE', *, *, #48508, .T. ) ;
#18827=CARTESIAN_POINT ( 'NONE',  ( -15.00000000000000000, -12.00000000000000000, 5.000000000000000000 ) ) ;
#18828=CARTESIAN_POINT ( 'NONE',  ( -85.19500000000000739, 8.437984349512085203, -1.550032578732815448E-15 ) ) ;
#18839=CARTESIAN_POINT ( 'NONE',  ( -165.3570736234661922, 5.598654528085804216, 7.705886871421366635 ) ) ;
#18841=CARTESIAN_POINT ( 'NONE',  ( -115.2570736234661695, 5.598654528085800663, -7.705886871421367523 ) ) ;
#18847=CARTESIAN_POINT ( 'NONE',  ( -146.6049999999999329, 6.826472737025113702, -4.959722759717902107 ) ) ;
#18849=CARTESIAN_POINT ( 'NONE',  ( -162.1449999999999818, -4.716976649647092401, 6.492361379858946790 ) ) ;
#18850=CARTESIAN_POINT ( 'NONE',  ( -146.9949999999999761, -6.826472737025113702, 4.959722759717902107 ) ) ;
#18855=DIRECTION ( 'NONE',  ( -1.000000000000000000, -0.000000000000000000, -0.000000000000000000 ) ) ;
#18858=CARTESIAN_POINT ( 'NONE',  ( -65.30499999999999261, 8.437984349512085203, -1.550032578732815448E-15 ) ) ;
#18862=CARTESIAN_POINT ( 'NONE',  ( -69.89499999999998181, 6.826472737025115478, 4.959722759717899443 ) ) ;
#18867=CARTESIAN_POINT ( 'NONE',  ( -160.1070736234661922, 8.102448949553172852, -5.886773742842744461 ) ) ;
#18893=CARTESIAN_POINT ( 'NONE',  ( -83.15707362346617515, -9.058813317711329915, -2.943386871421370898 ) ) ;
#18894=CARTESIAN_POINT ( 'NONE',  ( -110.8449999999999847, -7.632228543268599452, 2.479861379858951054 ) ) ;
#18898=CARTESIAN_POINT ( 'NONE',  ( -10.75761710425530637, -11.70429995583328342, 2.651158507154013577 ) ) ;
#18914=CARTESIAN_POINT ( 'NONE',  ( -132.8050000000000068, -8.437984349512085203, 5.166775262442717831E-16 ) ) ;
#18928=CARTESIAN_POINT ( 'NONE',  ( -51.05499999999999261, -9.827790563157499189E-16, -8.024999999999991473 ) ) ;
#18930=CARTESIAN_POINT ( 'NONE',  ( -123.0570736234661808, 0.000000000000000000, 9.524999999999991473 ) ) ;
#18931=CARTESIAN_POINT ( 'NONE',  ( -182.0049999999999670, 6.826472737025116366, 4.959722759717898555 ) ) ;
#18934=CARTESIAN_POINT ( 'NONE',  ( -51.95707362346615810, 9.058813317711329915, -2.943386871421373119 ) ) ;
#18941=CARTESIAN_POINT ( 'NONE',  ( -100.8549999999999898, 4.716976649647094177, 6.492361379858945902 ) ) ;
#18945=CARTESIAN_POINT ( 'NONE',  ( -99.14499999999998181, -4.716976649647092401, 6.492361379858946790 ) ) ;
#18947=CARTESIAN_POINT ( 'NONE',  ( -70.94499999999997897, -9.827790563157499189E-16, -8.024999999999991473 ) ) ;
#18953=DIRECTION ( 'NONE',  ( -1.000000000000000000, -0.000000000000000000, -0.000000000000000000 ) ) ;
#18956=CARTESIAN_POINT ( 'NONE',  ( -111.7429263765338163, -5.598654528085803328, -7.705886871421366635 ) ) ;
#18957=CARTESIAN_POINT ( 'NONE',  ( -139.9449999999999932, -9.827790563157499189E-16, -8.024999999999991473 ) ) ;
#18966=CARTESIAN_POINT ( 'NONE',  ( -62.99292637653378080, 8.102448949553172852, -5.886773742842744461 ) ) ;
#18972=CARTESIAN_POINT ( 'NONE',  ( -133.1049999999999898, -6.826472737025113702, 4.959722759717902107 ) ) ;
#18975=CARTESIAN_POINT ( 'NONE',  ( -123.2070736234661581, 3.094860106618433360, 9.524999999999991473 ) ) ;
#18987=CARTESIAN_POINT ( 'NONE',  ( -49.70499999999996987, 2.607480562269072433, 8.024999999999991473 ) ) ;
#19003=CARTESIAN_POINT ( 'NONE',  ( -162.8050000000000068, -8.437984349512085203, 5.166775262442717831E-16 ) ) ;
#19012=ORIENTED_EDGE ( 'NONE', *, *, #52231, .F. ) ;
#19016=CARTESIAN_POINT ( 'NONE',  ( -80.00500000000000966, 6.826472737025116366, 4.959722759717898555 ) ) ;
#19020=CARTESIAN_POINT ( 'NONE',  ( -151.5570736234661808, -1.166476076187852838E-15, -9.524999999999991473 ) ) ;
#19028=CARTESIAN_POINT ( 'NONE',  ( -108.4449999999999790, 0.000000000000000000, 8.024999999999991473 ) ) ;
#19036=AXIS2_PLACEMENT_3D ( 'NONE', #59110, #53503, #15543 ) ;
#19037=CARTESIAN_POINT ( 'NONE',  ( -140.5429263765338135, 9.058813317711329915, 2.943386871421369566 ) ) ;
#19038=CARTESIAN_POINT ( 'NONE',  ( -166.3449999999999989, 7.632228543268599452, -2.479861379858951942 ) ) ;
#19043=FACE_OUTER_BOUND ( 'NONE', #33859, .T. ) ;
#19049=( BOUNDED_CURVE ( )  B_SPLINE_CURVE ( 2, ( #7540, #795, #60994, #1152, #65239, #22689, #17092, #28969, #12813, #6480, #27919 ),
 .UNSPECIFIED., .F., .F. ) 
 B_SPLINE_CURVE_WITH_KNOTS ( ( 3, 2, 2, 2, 2, 3 ),
 ( 0.2717391304347761549, 0.2739130434782543477, 0.2760869565217325960, 0.2782608695652108444, 0.2804347826086890372, 0.2826086956521672300 ),
 .UNSPECIFIED. ) 
 CURVE ( )  GEOMETRIC_REPRESENTATION_ITEM ( )  RATIONAL_B_SPLINE_CURVE ( ( 1.000000000000144995, 0.9510565162950085361, 1.000000000000000000, 0.9510565162951535312, 1.000000000000000000, 0.9510565162951535312, 1.000000000000000000, 0.9510565162951535312, 1.000000000000000000, 0.9510565162953035223, 0.9999999999998500089 ) ) 
 REPRESENTATION_ITEM ( '' )  );
#19053=CARTESIAN_POINT ( 'NONE',  ( -111.0570736234661808, 0.000000000000000000, 9.524999999999991473 ) ) ;
#19058=CARTESIAN_POINT ( 'NONE',  ( -162.6550000000000011, -7.632228543268600340, -2.479861379858950166 ) ) ;
#19059=ORIENTED_EDGE ( 'NONE', *, *, #31288, .T. ) ;
#19068=ORIENTED_EDGE ( 'NONE', *, *, #10415, .T. ) ;
#19071=CARTESIAN_POINT ( 'NONE',  ( -75.65499999999998693, -7.632228543268600340, -2.479861379858950166 ) ) ;
#19084=CARTESIAN_POINT ( 'NONE',  ( -48.89499999999999602, 6.826472737025116366, 4.959722759717898555 ) ) ;
#19085=VERTEX_POINT ( 'NONE', #46418 ) ;
#19086=LINE ( 'NONE', #40238, #19967 ) ;
#19091=CARTESIAN_POINT ( 'NONE',  ( -55.49499999999999034, 6.826472737025113702, -4.959722759717902107 ) ) ;
#19095=CARTESIAN_POINT ( 'NONE',  ( -101.7549999999999812, 4.716976649647091513, -6.492361379858946790 ) ) ;
#19101=CARTESIAN_POINT ( 'NONE',  ( -140.9070736234661183, -3.094860106618429807, 9.524999999999991473 ) ) ;
#19103=CARTESIAN_POINT ( 'NONE',  ( -79.10707362346616378, 8.102448949553171076, -5.886773742842744461 ) ) ;
#19109=CARTESIAN_POINT ( 'NONE',  ( -116.7549999999999812, 4.716976649647091513, -6.492361379858946790 ) ) ;
#19112=CARTESIAN_POINT ( 'NONE',  ( -139.3449999999999989, 7.632228543268599452, -2.479861379858951942 ) ) ;
#19116=CARTESIAN_POINT ( 'NONE',  ( -123.8949999999999818, 6.826472737025115478, 4.959722759717899443 ) ) ;
#19118=ORIENTED_EDGE ( 'NONE', *, *, #59734, .T. ) ;
#19124=CARTESIAN_POINT ( 'NONE',  ( -121.3429263765338106, -9.058813317711329915, 2.943386871421371787 ) ) ;
#19125=CARTESIAN_POINT ( 'NONE',  ( -168.7429263765338305, -5.598654528085803328, -7.705886871421366635 ) ) ;
#19130=EDGE_CURVE ( 'NONE', #11319, #56584, #9956, .T. ) ;
#19137=CARTESIAN_POINT ( 'NONE',  ( -89.99292637653380211, 8.102448949553171076, -5.886773742842744461 ) ) ;
#19140=EDGE_CURVE ( 'NONE', #12632, #42104, #7656, .T. ) ;
#19144=CARTESIAN_POINT ( 'NONE',  ( -162.7429263765338021, -5.598654528085803328, -7.705886871421366635 ) ) ;
#19147=CARTESIAN_POINT ( 'NONE',  ( -136.6429263765338078, -5.598654528085801552, 7.705886871421367523 ) ) ;
#19152=CARTESIAN_POINT ( 'NONE',  ( -64.94292637653380496, 0.000000000000000000, 9.524999999999991473 ) ) ;
#19162=CARTESIAN_POINT ( 'NONE',  ( -94.19292637653380496, -10.01517768586948698, 6.132527647946031529E-16 ) ) ;
#19165=CARTESIAN_POINT ( 'NONE',  ( -86.09499999999997044, -2.607480562269071545, -8.024999999999991473 ) ) ;
#19176=ORIENTED_EDGE ( 'NONE', *, *, #19704, .T. ) ;
#19180=CARTESIAN_POINT ( 'NONE',  ( -169.7070736234661581, -3.094860106618431139, -9.524999999999991473 ) ) ;
#19184=CARTESIAN_POINT ( 'NONE',  ( -115.8570736234661780, -5.598654528085803328, -7.705886871421366635 ) ) ;
#19193=CARTESIAN_POINT ( 'NONE',  ( -150.5049999999999955, -6.826472737025115478, -4.959722759717899443 ) ) ;
#19198=CARTESIAN_POINT ( 'NONE',  ( -165.5949999999999704, 2.607480562269073321, 8.024999999999991473 ) ) ;
#19199=CARTESIAN_POINT ( 'NONE',  ( -149.0949999999999704, -2.607480562269071545, -8.024999999999991473 ) ) ;
#19205=CARTESIAN_POINT ( 'NONE',  ( -64.10499999999997556, -6.826472737025115478, 4.959722759717900331 ) ) ;
#19209=CARTESIAN_POINT ( 'NONE',  ( -64.79499999999998749, 2.607480562269069324, -8.024999999999993250 ) ) ;
#19217=EDGE_CURVE ( 'NONE', #12224, #56168, #62110, .T. ) ;
#19222=ORIENTED_EDGE ( 'NONE', *, *, #30072, .T. ) ;
#19224=CARTESIAN_POINT ( 'NONE',  ( -61.55707362346617373, -1.166476076187852838E-15, -9.524999999999991473 ) ) ;
#19234=CARTESIAN_POINT ( 'NONE',  ( -195.0000000000000000, 6.735557395310425260E-16, -5.499999999999985789 ) ) ;
#19237=CARTESIAN_POINT ( 'NONE',  ( -65.84292637653379643, 9.058813317711329915, -2.943386871421373119 ) ) ;
#19238=CARTESIAN_POINT ( 'NONE',  ( -145.4929263765338021, -8.102448949553174629, 5.886773742842742685 ) ) ;
#19242=DIRECTION ( 'NONE',  ( 0.000000000000000000, 0.000000000000000000, 1.000000000000000000 ) ) ;
#19243=CARTESIAN_POINT ( 'NONE',  ( -110.2449999999999903, -4.716976649647093289, -6.492361379858945902 ) ) ;
#19249=CARTESIAN_POINT ( 'NONE',  ( -179.3070736234661524, -10.01517768586948698, 6.132527647946031529E-16 ) ) ;
#19263=CARTESIAN_POINT ( 'NONE',  ( -126.5049999999999528, -6.826472737025115478, -4.959722759717899443 ) ) ;
#19276=CARTESIAN_POINT ( 'NONE',  ( -49.85499999999998266, 4.716976649647094177, 6.492361379858945902 ) ) ;
#19279=CARTESIAN_POINT ( 'NONE',  ( -178.2549999999999955, -4.716976649647092401, 6.492361379858946790 ) ) ;
#19281=CARTESIAN_POINT ( 'NONE',  ( -90.59292637653381064, -3.094860106618431139, -9.524999999999991473 ) ) ;
#19283=CARTESIAN_POINT ( 'NONE',  ( -56.90707362346616804, -3.094860106618429807, 9.524999999999991473 ) ) ;
#19285=CARTESIAN_POINT ( 'NONE',  ( -178.6450000000000102, 4.716976649647091513, -6.492361379858946790 ) ) ;
#19288=LINE ( 'NONE', #14039, #12211 ) ;
#19294=CARTESIAN_POINT ( 'NONE',  ( -89.15499999999998693, 7.632228543268600340, 2.479861379858949277 ) ) ;
#19300=CARTESIAN_POINT ( 'NONE',  ( -89.09499999999998465, -2.607480562269071545, -8.024999999999991473 ) ) ;
#19302=CARTESIAN_POINT ( 'NONE',  ( -71.84499999999999886, -7.632228543268599452, 2.479861379858951054 ) ) ;
#19311=CARTESIAN_POINT ( 'NONE',  ( -111.5929263765337822, -3.094860106618431139, -9.524999999999991473 ) ) ;
#19313=CARTESIAN_POINT ( 'NONE',  ( -128.0949999999999704, -2.607480562269071545, -8.024999999999991473 ) ) ;
#19319=CARTESIAN_POINT ( 'NONE',  ( -131.3929263765338078, 8.102448949553176405, 5.886773742842740909 ) ) ;
#19327=CARTESIAN_POINT ( 'NONE',  ( -98.45707362346617231, -9.058813317711329915, 2.943386871421371787 ) ) ;
#19329=CARTESIAN_POINT ( 'NONE',  ( -45.99999999999998579, 0.000000000000000000, 0.000000000000000000 ) ) ;
#19332=CARTESIAN_POINT ( 'NONE',  ( -131.4549999999999841, 7.632228543268599452, -2.479861379858951942 ) ) ;
#19335=CARTESIAN_POINT ( 'NONE',  ( -119.0070736234661837, -8.102448949553172852, -5.886773742842741797 ) ) ;
#19344=CARTESIAN_POINT ( 'NONE',  ( -54.20707362346616520, 3.094860106618433360, 9.524999999999991473 ) ) ;
#19353=CARTESIAN_POINT ( 'NONE',  ( -97.94292637653380496, 0.000000000000000000, 9.524999999999991473 ) ) ;
#19358=VERTEX_POINT ( 'NONE', #34682 ) ;
#19362=CARTESIAN_POINT ( 'NONE',  ( -159.2050000000000125, -2.607480562269071545, -8.024999999999991473 ) ) ;
#19380=CARTESIAN_POINT ( 'NONE',  ( -71.30499999999997840, 8.437984349512085203, -1.550032578732815448E-15 ) ) ;
#19384=CARTESIAN_POINT ( 'NONE',  ( -150.5070736234661410, 8.102448949553176405, 5.886773742842740909 ) ) ;
#19385=ORIENTED_EDGE ( 'NONE', *, *, #48971, .F. ) ;
#19393=ADVANCED_FACE ( 'NONE', ( #19892 ), #47377, .T. ) ;
#19395=CARTESIAN_POINT ( 'NONE',  ( -101.2449999999999903, -4.716976649647093289, -6.492361379858945902 ) ) ;
#19403=CARTESIAN_POINT ( 'NONE',  ( -143.6929263765338192, 10.01517768586948698, -1.839758294383808571E-15 ) ) ;
#19406=CARTESIAN_POINT ( 'NONE',  ( -154.1949999999999648, 8.437984349512085203, -1.550032578732815448E-15 ) ) ;
#19419=CARTESIAN_POINT ( 'NONE',  ( -172.7070736234662718, -3.094860106620514362, -9.524999999998476241 ) ) ;
#19422=CARTESIAN_POINT ( 'NONE',  ( -156.6550000000000011, -7.632228543268600340, -2.479861379858950166 ) ) ;
#19435=CARTESIAN_POINT ( 'NONE',  ( -70.85499999999998977, 4.716976649647094177, 6.492361379858945902 ) ) ;
#19446=CARTESIAN_POINT ( 'NONE',  ( -53.99499999999998323, -6.826472737025115478, 4.959722759717900331 ) ) ;
#19452=EDGE_CURVE ( 'NONE', #59074, #9325, #14899, .T. ) ;
#19458=CARTESIAN_POINT ( 'NONE',  ( -100.8549999999999898, 4.716976649647094177, 6.492361379858945902 ) ) ;
#19460=FACE_OUTER_BOUND ( 'NONE', #41898, .T. ) ;
#19462=CARTESIAN_POINT ( 'NONE',  ( -140.6070736234661922, -8.102448949553172852, 5.886773742842742685 ) ) ;
#19466=CARTESIAN_POINT ( 'NONE',  ( -79.40707362346617515, 3.094860106618428031, -9.524999999999993250 ) ) ;
#19468=CARTESIAN_POINT ( 'NONE',  ( -92.69292637653379074, 10.01517768586948698, -1.839758294383808966E-15 ) ) ;
#19470=CARTESIAN_POINT ( 'NONE',  ( -19.48451829062191720, -11.79395247191043339, 2.235223184618424508 ) ) ;
#19472=CARTESIAN_POINT ( 'NONE',  ( -100.6429263765337936, -5.598654528085801552, 7.705886871421367523 ) ) ;
#19475=CARTESIAN_POINT ( 'NONE',  ( -121.2549999999999812, -4.716976649647092401, 6.492361379858946790 ) ) ;
#19476=CARTESIAN_POINT ( 'NONE',  ( -122.3949999999999818, -6.826472737025115478, -4.959722759717899443 ) ) ;
#19477=CARTESIAN_POINT ( 'NONE',  ( -119.8449999999999989, -7.632228543268599452, 2.479861379858951054 ) ) ;
#19479=( BOUNDED_CURVE ( )  B_SPLINE_CURVE ( 2, ( #9056, #14683, #47426, #52336, #36527, #51615, #67799, #36153, #58272, #68495, #57585 ),
 .UNSPECIFIED., .F., .F. ) 
 B_SPLINE_CURVE_WITH_KNOTS ( ( 3, 2, 2, 2, 2, 3 ),
 ( 0.7608695652173913526, 0.7630434782608696009, 0.7652173913043478493, 0.7673913043478260976, 0.7695652173913043459, 0.7717391304347825942 ),
 .UNSPECIFIED. ) 
 CURVE ( )  GEOMETRIC_REPRESENTATION_ITEM ( )  RATIONAL_B_SPLINE_CURVE ( ( 1.000000000000000000, 0.9510565162951535312, 1.000000000000000000, 0.9510565162951535312, 1.000000000000000000, 0.9510565162951535312, 1.000000000000000000, 0.9510565162951535312, 1.000000000000000000, 0.9510565162951535312, 1.000000000000000000 ) ) 
 REPRESENTATION_ITEM ( '' )  );
#19483=CARTESIAN_POINT ( 'NONE',  ( -169.1929263765338192, -10.01517768586948698, 6.132527647946031529E-16 ) ) ;
#19484=CARTESIAN_POINT ( 'NONE',  ( -48.44499999999998607, 0.000000000000000000, 8.024999999999991473 ) ) ;
#19485=AXIS2_PLACEMENT_3D ( 'NONE', #60595, #49384, #2520 ) ;
#19492=CARTESIAN_POINT ( 'NONE',  ( -87.74292637653380211, -5.598654528085803328, -7.705886871421366635 ) ) ;
#19514=CARTESIAN_POINT ( 'NONE',  ( -106.2549999999999955, -4.716976649647092401, 6.492361379858946790 ) ) ;
#19522=AXIS2_PLACEMENT_3D ( 'NONE', #65820, #33796, #39813 ) ;
#19523=CARTESIAN_POINT ( 'NONE',  ( -86.54499999999998749, -7.632228543268600340, -2.479861379858950166 ) ) ;
#19534=LINE ( 'NONE', #41729, #44760 ) ;
#19544=CARTESIAN_POINT ( 'NONE',  ( -171.8070736234661808, 10.01517768586948698, -1.839758294383808571E-15 ) ) ;
#19548=CARTESIAN_POINT ( 'NONE',  ( -107.4570736234661865, -9.058813317711329915, 2.943386871421371787 ) ) ;
#19552=DIRECTION ( 'NONE',  ( 0.000000000000000000, 0.000000000000000000, 1.000000000000000000 ) ) ;
#19553=CARTESIAN_POINT ( 'NONE',  ( -106.2570736234661695, 5.598654528085800663, -7.705886871421367523 ) ) ;
#19558=CARTESIAN_POINT ( 'NONE',  ( -152.3050000000000068, 8.437984349512085203, -1.550032578732815448E-15 ) ) ;
#19561=CARTESIAN_POINT ( 'NONE',  ( -153.8949999999999818, 6.826472737025116366, 4.959722759717898555 ) ) ;
#19563=CARTESIAN_POINT ( 'NONE',  ( -143.9949999999999761, -6.826472737025113702, 4.959722759717902107 ) ) ;
#19566=CARTESIAN_POINT ( 'NONE',  ( -181.4070736234661751, 3.094860106618131823, -9.525000000000206413 ) ) ;
#19570=CARTESIAN_POINT ( 'NONE',  ( -64.25499999999998124, -4.716976649647092401, 6.492361379858946790 ) ) ;
#19572=CARTESIAN_POINT ( 'NONE',  ( -154.2570736234661979, 5.598654528085800663, -7.705886871421367523 ) ) ;
#19574=CARTESIAN_POINT ( 'NONE',  ( -64.49499999999997613, 6.826472737025113702, -4.959722759717902107 ) ) ;
#19581=CARTESIAN_POINT ( 'NONE',  ( -159.6570736234661751, 9.058813317711329915, 2.943386871421369566 ) ) ;
#19596=ORIENTED_EDGE ( 'NONE', *, *, #41034, .T. ) ;
#19598=LINE ( 'NONE', #52340, #30888 ) ;
#19607=CARTESIAN_POINT ( 'NONE',  ( -106.6449999999999960, 4.716976649647091513, -6.492361379858946790 ) ) ;
#19611=PLANE ( 'NONE',  #27645 ) ;
#19619=VERTEX_POINT ( 'NONE', #39584 ) ;
#19624=DIRECTION ( 'NONE',  ( -1.000000000000000000, -0.000000000000000000, -0.000000000000000000 ) ) ;
#19627=CARTESIAN_POINT ( 'NONE',  ( -122.3050000000000068, 8.437984349512085203, -1.550032578732815448E-15 ) ) ;
#19643=CARTESIAN_POINT ( 'NONE',  ( -123.9570736234661723, 9.058813317711329915, -2.943386871421373119 ) ) ;
#19644=CARTESIAN_POINT ( 'NONE',  ( -180.2049999999999841, -2.607480562269071545, -8.024999999999991473 ) ) ;
#19647=CARTESIAN_POINT ( 'NONE',  ( -60.20707362346617231, 3.094860106618433360, 9.524999999999991473 ) ) ;
#19651=CARTESIAN_POINT ( 'NONE',  ( -181.6450000000000102, 4.716976649647091513, -6.492361379858946790 ) ) ;
#19656=CARTESIAN_POINT ( 'NONE',  ( -95.45499999999998408, 7.632228543268599452, -2.479861379858951942 ) ) ;
#19660=CARTESIAN_POINT ( 'NONE',  ( -87.29499999999998749, -2.607480562269069768, 8.024999999999991473 ) ) ;
#19662=CARTESIAN_POINT ( 'NONE',  ( -70.19499999999995055, 8.437984349512085203, -1.550032578732815448E-15 ) ) ;
#19665=CARTESIAN_POINT ( 'NONE',  ( -56.45707362346616520, -9.058813317711329915, 2.943386871421371787 ) ) ;
#19671=CARTESIAN_POINT ( 'NONE',  ( -115.7929263765337993, -3.094860106618429807, 9.524999999999991473 ) ) ;
#19672=CARTESIAN_POINT ( 'NONE',  ( -129.5949999999999989, 2.607480562269073321, 8.024999999999991473 ) ) ;
#19687=CARTESIAN_POINT ( 'NONE',  ( -127.2550000000000097, -4.716976649647092401, 6.492361379858946790 ) ) ;
#19691=CARTESIAN_POINT ( 'NONE',  ( -119.3070736234661808, -10.01517768586948698, 6.132527647946031529E-16 ) ) ;
#19704=EDGE_CURVE ( 'NONE', #51470, #48074, #28361, .T. ) ;
#19707=EDGE_LOOP ( 'NONE', ( #39635, #11222, #42520, #24545 ) ) ;
#19719=CARTESIAN_POINT ( 'NONE',  ( -56.39292637653378648, 8.102448949553176405, 5.886773742842740909 ) ) ;
#19722=CARTESIAN_POINT ( 'NONE',  ( -150.9550000000000125, -7.632228543268599452, 2.479861379858951054 ) ) ;
#19732=CARTESIAN_POINT ( 'NONE',  ( -64.40499999999998693, -2.607480562269069768, 8.024999999999991473 ) ) ;
#19735=CARTESIAN_POINT ( 'NONE',  ( -91.25707362346616947, 5.598654528085800663, -7.705886871421367523 ) ) ;
#19745=CARTESIAN_POINT ( 'NONE',  ( -94.04499999999998749, 7.632228543268600340, 2.479861379858949277 ) ) ;
#19752=CARTESIAN_POINT ( 'NONE',  ( -145.6429263765338078, -5.598654528085801552, 7.705886871421367523 ) ) ;
#19753=CARTESIAN_POINT ( 'NONE',  ( -160.9449999999999932, -9.827790563157499189E-16, -8.024999999999991473 ) ) ;
#19758=FACE_OUTER_BOUND ( 'NONE', #35879, .T. ) ;
#19762=ORIENTED_EDGE ( 'NONE', *, *, #65536, .T. ) ;
#19771=CARTESIAN_POINT ( 'NONE',  ( -159.0550000000000068, -9.827790563157499189E-16, -8.024999999999991473 ) ) ;
#19786=CARTESIAN_POINT ( 'NONE',  ( -76.85499999999998977, 4.716976649647094177, 6.492361379858945902 ) ) ;
#19800=CARTESIAN_POINT ( 'NONE',  ( -178.7050000000000125, 2.607480562269073321, 8.024999999999991473 ) ) ;
#19802=( BOUNDED_CURVE ( )  B_SPLINE_CURVE ( 2, ( #57993, #30882, #63596, #4478, #42889, #3778, #15440, #52380, #15102, #37258, #42528 ),
 .UNSPECIFIED., .F., .F. ) 
 B_SPLINE_CURVE_WITH_KNOTS ( ( 3, 2, 2, 2, 2, 3 ),
 ( 0.2173913043478209184, 0.2195652173912991389, 0.2217391304347773318, 0.2239130434782555801, 0.2260869565217337729, 0.2282608695652119657 ),
 .UNSPECIFIED. ) 
 CURVE ( )  GEOMETRIC_REPRESENTATION_ITEM ( )  RATIONAL_B_SPLINE_CURVE ( ( 1.000000000000116129, 0.9510565162950372908, 1.000000000000000000, 0.9510565162951535312, 1.000000000000000000, 0.9510565162951535312, 1.000000000000000000, 0.9510565162951535312, 1.000000000000000000, 0.9510565162952754337, 0.9999999999998780975 ) ) 
 REPRESENTATION_ITEM ( '' )  );
#19804=CARTESIAN_POINT ( 'NONE',  ( -86.84292637653381064, 9.058813317711329915, -2.943386871421373119 ) ) ;
#19807=DIRECTION ( 'NONE',  ( 0.000000000000000000, -1.000000000000000000, 0.000000000000000000 ) ) ;
#19812=CARTESIAN_POINT ( 'NONE',  ( -101.6049999999999898, 6.826472737025113702, -4.959722759717902107 ) ) ;
#19816=CARTESIAN_POINT ( 'NONE',  ( -141.6570736234662036, 9.058813317711329915, 2.943386871421369566 ) ) ;
#19819=CARTESIAN_POINT ( 'NONE',  ( -73.40707362346617515, 3.094860106618428031, -9.524999999999993250 ) ) ;
#19820=CARTESIAN_POINT ( 'NONE',  ( -92.84292637653379643, 9.058813317711329915, -2.943386871421373119 ) ) ;
#19823=CARTESIAN_POINT ( 'NONE',  ( -17.50859832773041447, -11.19035067480616874, 4.337450031442691589 ) ) ;
#19825=CARTESIAN_POINT ( 'NONE',  ( -100.3429263765337964, -9.058813317711329915, 2.943386871421371787 ) ) ;
#19826=CARTESIAN_POINT ( 'NONE',  ( -123.5049999999999955, -6.826472737025115478, -4.959722759717899443 ) ) ;
#19829=CARTESIAN_POINT ( 'NONE',  ( -125.9949999999999903, -6.826472737025115478, 4.959722759717900331 ) ) ;
#19830=CARTESIAN_POINT ( 'NONE',  ( -111.0570736234661808, 0.000000000000000000, 9.524999999999991473 ) ) ;
#19835=CARTESIAN_POINT ( 'NONE',  ( -170.3929263765337794, 8.102448949553176405, 5.886773742842740909 ) ) ;
#19843=CARTESIAN_POINT ( 'NONE',  ( -86.99292637653378790, 8.102448949553171076, -5.886773742842744461 ) ) ;
#19851=CARTESIAN_POINT ( 'NONE',  ( -156.2070736234664992, 3.094860106624047091, 9.524999999995914735 ) ) ;
#19856=CARTESIAN_POINT ( 'NONE',  ( -102.4429263765338050, -1.166476076187852838E-15, -9.524999999999991473 ) ) ;
#19862=CARTESIAN_POINT ( 'NONE',  ( -102.3549999999999898, -4.716976649647093289, -6.492361379858945902 ) ) ;
#19866=CARTESIAN_POINT ( 'NONE',  ( -103.8570736234661780, -5.598654528085803328, -7.705886871421366635 ) ) ;
#19870=CARTESIAN_POINT ( 'NONE',  ( -71.24499999999999034, -4.716976649647093289, -6.492361379858945902 ) ) ;
#19882=CARTESIAN_POINT ( 'NONE',  ( -138.4429263765337907, -1.166476076187852838E-15, -9.524999999999991473 ) ) ;
#19884=CARTESIAN_POINT ( 'NONE',  ( -168.0570736234661808, 0.000000000000000000, 9.524999999999991473 ) ) ;
#19887=( BOUNDED_CURVE ( )  B_SPLINE_CURVE ( 2, ( #10870, #58714, #58359, #41882, #47882, #10184, #48546, #63300, #48198, #15824, #4892 ),
 .UNSPECIFIED., .F., .F. ) 
 B_SPLINE_CURVE_WITH_KNOTS ( ( 3, 2, 2, 2, 2, 3 ),
 ( 0.3260869565217315302, 0.3282608695652097230, 0.3304347826086879159, 0.3326086956521662197, 0.3347826086956444125, 0.3369565217391226053 ),
 .UNSPECIFIED. ) 
 CURVE ( )  GEOMETRIC_REPRESENTATION_ITEM ( )  RATIONAL_B_SPLINE_CURVE ( ( 1.000000000000171196, 0.9510565162949823348, 1.000000000000000000, 0.9510565162951535312, 1.000000000000000000, 0.9510565162951535312, 1.000000000000000000, 0.9510565162951535312, 1.000000000000000000, 0.9510565162953297236, 0.9999999999998238076 ) ) 
 REPRESENTATION_ITEM ( '' )  );
#19888=CARTESIAN_POINT ( 'NONE',  ( -101.4570736234661723, -9.058813317711329915, 2.943386871421371787 ) ) ;
#19892=FACE_OUTER_BOUND ( 'NONE', #56235, .T. ) ;
#19893=CARTESIAN_POINT ( 'NONE',  ( -105.6570736234661751, 9.058813317711329915, 2.943386871421369566 ) ) ;
#19898=CARTESIAN_POINT ( 'NONE',  ( -147.0549999999999784, -9.827790563157499189E-16, -8.024999999999991473 ) ) ;
#19901=CARTESIAN_POINT ( 'NONE',  ( -157.6449999999999818, 4.716976649647091513, -6.492361379858946790 ) ) ;
#19902=CARTESIAN_POINT ( 'NONE',  ( -149.9949999999999193, -6.826472737025113702, 4.959722759717902107 ) ) ;
#19908=CARTESIAN_POINT ( 'NONE',  ( -60.05499999999998550, -9.827790563157499189E-16, -8.024999999999991473 ) ) ;
#19911=CARTESIAN_POINT ( 'NONE',  ( -60.44499999999998607, 0.000000000000000000, 8.024999999999991473 ) ) ;
#19914=EDGE_CURVE ( 'NONE', #63360, #42940, #48613, .T. ) ;
#19924=EDGE_CURVE ( 'NONE', #37240, #55900, #19288, .T. ) ;
#19932=EDGE_CURVE ( 'NONE', #44394, #42499, #36913, .T. ) ;
#19938=EDGE_LOOP ( 'NONE', ( #10895, #33215, #9178, #24433, #59255, #57963 ) ) ;
#19946=CARTESIAN_POINT ( 'NONE',  ( -106.0449999999999875, 7.632228543268600340, 2.479861379858949277 ) ) ;
#19961=CARTESIAN_POINT ( 'NONE',  ( -120.5049999999999812, -6.826472737025115478, -4.959722759717899443 ) ) ;
#19962=CARTESIAN_POINT ( 'NONE',  ( -51.05707362346617373, 0.000000000000000000, 9.524999999999991473 ) ) ;
#19967=VECTOR ( 'NONE', #8907, 1000.000000000000000 ) ;
#19973=CARTESIAN_POINT ( 'NONE',  ( -175.1050000000000182, -6.826472737025115478, 4.959722759717900331 ) ) ;
#19975=CARTESIAN_POINT ( 'NONE',  ( -50.75707362346618368, -5.598654528085801552, 7.705886871421367523 ) ) ;
#19977=CARTESIAN_POINT ( 'NONE',  ( -176.3949999999999818, -6.826472737025113702, -4.959722759717900331 ) ) ;
#19981=CARTESIAN_POINT ( 'NONE',  ( -11.02915983529077337, 11.60772081924744015, -3.055653888425151177 ) ) ;
#19982=CARTESIAN_POINT ( 'NONE',  ( -89.75499999999998124, 4.716976649647091513, -6.492361379858946790 ) ) ;
#19986=CARTESIAN_POINT ( 'NONE',  ( -86.69499999999999318, -8.437984349512086979, 5.166775262442717831E-16 ) ) ;
#19988=CARTESIAN_POINT ( 'NONE',  ( -65.99499999999996191, -6.826472737025115478, 4.959722759717900331 ) ) ;
#19998=CARTESIAN_POINT ( 'NONE',  ( -105.8929263765337794, -8.102448949553172852, -5.886773742842741797 ) ) ;
#19999=CARTESIAN_POINT ( 'NONE',  ( -125.3949999999999818, -6.826472737025115478, -4.959722759717899443 ) ) ;
#20004=ADVANCED_FACE ( 'NONE', ( #37961 ), #60386, .T. ) ;
#20006=DIRECTION ( 'NONE',  ( -0.000000000000000000, 1.000000000000000000, 1.224646799147353207E-16 ) ) ;
#20020=CARTESIAN_POINT ( 'NONE',  ( -119.7549999999999812, 4.716976649647091513, -6.492361379858946790 ) ) ;
#20023=CARTESIAN_POINT ( 'NONE',  ( -125.6070736234661922, -8.102448949553172852, 5.886773742842742685 ) ) ;
#20028=LINE ( 'NONE', #51721, #24174 ) ;
#20039=CARTESIAN_POINT ( 'NONE',  ( -98.09292637653487645, 3.094860106636583286, 9.524999999986803800 ) ) ;
#20045=CARTESIAN_POINT ( 'NONE',  ( -55.49292637653380211, -8.102448949553172852, 5.886773742842742685 ) ) ;
#20047=CARTESIAN_POINT ( 'NONE',  ( -155.4549999999999841, 7.632228543268599452, -2.479861379858951942 ) ) ;
#20055=CARTESIAN_POINT ( 'NONE',  ( -69.44292637653380496, -1.166476076187852838E-15, -9.524999999999991473 ) ) ;
#20062=CARTESIAN_POINT ( 'NONE',  ( -61.85499999999998266, 4.716976649647094177, 6.492361379858945902 ) ) ;
#20068=CARTESIAN_POINT ( 'NONE',  ( -124.7929263765345524, -3.094860106605926031, 9.525000000009075762 ) ) ;
#20071=ORIENTED_EDGE ( 'NONE', *, *, #60357, .T. ) ;
#20077=CARTESIAN_POINT ( 'NONE',  ( -92.84499999999998465, -7.632228543268599452, 2.479861379858951054 ) ) ;
#20080=EDGE_CURVE ( 'NONE', #59688, #52874, #22064, .T. ) ;
#20081=CARTESIAN_POINT ( 'NONE',  ( -71.99292637653380211, 8.102448949553172852, -5.886773742842744461 ) ) ;
#20083=CARTESIAN_POINT ( 'NONE',  ( -132.4429263765338192, -1.166476076187852838E-15, -9.524999999999991473 ) ) ;
#20086=CARTESIAN_POINT ( 'NONE',  ( -161.0949999999999420, -2.607480562269071545, -8.024999999999991473 ) ) ;
#20090=CARTESIAN_POINT ( 'NONE',  ( -132.7429263765338021, -5.598654528085803328, -7.705886871421366635 ) ) ;
#20095=FACE_OUTER_BOUND ( 'NONE', #69214, .T. ) ;
#20098=ORIENTED_EDGE ( 'NONE', *, *, #16824, .F. ) ;
#20099=CARTESIAN_POINT ( 'NONE',  ( -155.6049999999999329, 6.826472737025113702, -4.959722759717902107 ) ) ;
#20111=CARTESIAN_POINT ( 'NONE',  ( -66.05707362346618083, 0.000000000000000000, 9.524999999999991473 ) ) ;
#20113=CARTESIAN_POINT ( 'NONE',  ( -69.50499999999996703, -6.826472737025113702, -4.959722759717900331 ) ) ;
#20114=CARTESIAN_POINT ( 'NONE',  ( -81.05707362346618083, 0.000000000000000000, 9.524999999999991473 ) ) ;
#20127=CARTESIAN_POINT ( 'NONE',  ( -46.79499999999996618, 2.607480562269068880, -8.024999999999993250 ) ) ;
#20131=ADVANCED_FACE ( 'NONE', ( #28721 ), #29782, .T. ) ;
#20140=CARTESIAN_POINT ( 'NONE',  ( -94.25499999999999545, -4.716976649647092401, 6.492361379858946790 ) ) ;
#20144=CARTESIAN_POINT ( 'NONE',  ( -132.8070736234661808, 10.01517768586948698, -1.839758294383808571E-15 ) ) ;
#20148=CARTESIAN_POINT ( 'NONE',  ( -72.65707362346617515, 9.058813317711329915, 2.943386871421369566 ) ) ;
#20153=ORIENTED_EDGE ( 'NONE', *, *, #56873, .F. ) ;
#20155=CARTESIAN_POINT ( 'NONE',  ( -19.73763835060324823, -11.89250300617436551, 1.631536037870932043 ) ) ;
#20159=CARTESIAN_POINT ( 'NONE',  ( -107.6049999999999756, 6.826472737025113702, -4.959722759717902107 ) ) ;
#20160=EDGE_CURVE ( 'NONE', #58710, #51275, #29235, .T. ) ;
#20161=DIRECTION ( 'NONE',  ( -1.000000000000000000, -0.000000000000000000, -0.000000000000000000 ) ) ;
#20163=CARTESIAN_POINT ( 'NONE',  ( -126.2950000000000017, -2.607480562269069768, 8.024999999999991473 ) ) ;
#20164=AXIS2_PLACEMENT_3D ( 'NONE', #2765, #14061, #40129 ) ;
#20165=CARTESIAN_POINT ( 'NONE',  ( -111.6570736234661751, 9.058813317711329915, 2.943386871421369566 ) ) ;
#20173=CYLINDRICAL_SURFACE ( 'NONE', #67614, 9.524999999999991473 ) ;
#20175=CARTESIAN_POINT ( 'NONE',  ( -176.3929263765338078, 8.102448949553176405, 5.886773742842740909 ) ) ;
#20182=CARTESIAN_POINT ( 'NONE',  ( -81.14292637653380780, 5.598654528085800663, -7.705886871421367523 ) ) ;
#20190=CARTESIAN_POINT ( 'NONE',  ( -157.5570736234661808, -1.166476076187852838E-15, -9.524999999999991473 ) ) ;
#20192=CARTESIAN_POINT ( 'NONE',  ( -135.7429263765338021, -5.598654528085803328, -7.705886871421366635 ) ) ;
#20198=( BOUNDED_CURVE ( )  B_SPLINE_CURVE ( 2, ( #41340, #52242, #57486, #32138, #57851, #31785, #36431, #15994, #31086, #63794, #9315 ),
 .UNSPECIFIED., .F., .F. ) 
 B_SPLINE_CURVE_WITH_KNOTS ( ( 3, 2, 2, 2, 2, 3 ),
 ( 0.1304347826086926510, 0.1326086956521708715, 0.1347826086956490643, 0.1369565217391272849, 0.1391304347826055055, 0.1413043478260836983 ),
 .UNSPECIFIED. ) 
 CURVE ( )  GEOMETRIC_REPRESENTATION_ITEM ( )  RATIONAL_B_SPLINE_CURVE ( ( 1.000000000000067502, 0.9510565162950860296, 1.000000000000000000, 0.9510565162951535312, 1.000000000000000000, 0.9510565162951535312, 1.000000000000000000, 0.9510565162951535312, 1.000000000000000000, 0.9510565162952266949, 0.9999999999999268363 ) ) 
 REPRESENTATION_ITEM ( '' )  );
#20204=CARTESIAN_POINT ( 'NONE',  ( -99.95499999999998408, -7.632228543268599452, 2.479861379858951054 ) ) ;
#20215=CARTESIAN_POINT ( 'NONE',  ( -68.24499999999999034, -4.716976649647093289, -6.492361379858945902 ) ) ;
#20217=ORIENTED_EDGE ( 'NONE', *, *, #47839, .T. ) ;
#20228=ORIENTED_EDGE ( 'NONE', *, *, #12369, .F. ) ;
#20229=DIRECTION ( 'NONE',  ( 0.000000000000000000, 0.000000000000000000, 1.000000000000000000 ) ) ;
#20232=CARTESIAN_POINT ( 'NONE',  ( -195.0000000000000000, 1.166476076187852838E-15, -9.524999999999991473 ) ) ;
#20233=DIRECTION ( 'NONE',  ( -1.000000000000000000, -0.000000000000000000, -0.000000000000000000 ) ) ;
#20235=CARTESIAN_POINT ( 'NONE',  ( -171.5070736234661979, 8.102448949553176405, 5.886773742842740909 ) ) ;
#20238=CARTESIAN_POINT ( 'NONE',  ( -103.7070736234661865, -3.094860106618431139, -9.524999999999991473 ) ) ;
#20249=CARTESIAN_POINT ( 'NONE',  ( -152.1549999999999727, 7.632228543268600340, 2.479861379858949277 ) ) ;
#20251=CARTESIAN_POINT ( 'NONE',  ( -148.4929263765337737, -8.102448949553174629, 5.886773742842742685 ) ) ;
#20252=CARTESIAN_POINT ( 'NONE',  ( -158.6949999999999648, -8.437984349512085203, 5.166775262442717831E-16 ) ) ;
#20253=CARTESIAN_POINT ( 'NONE',  ( -149.8449999999999989, -7.632228543268599452, 2.479861379858951054 ) ) ;
#20257=FACE_OUTER_BOUND ( 'NONE', #12846, .T. ) ;
#20258=CARTESIAN_POINT ( 'NONE',  ( -65.90499999999998693, 2.607480562269068880, -8.024999999999993250 ) ) ;
#20260=EDGE_CURVE ( 'NONE', #30333, #23187, #25921, .T. ) ;
#20261=CARTESIAN_POINT ( 'NONE',  ( -59.09499999999997044, -2.607480562269071545, -8.024999999999991473 ) ) ;
#20272=CARTESIAN_POINT ( 'NONE',  ( -49.94292637653380496, 0.000000000000000000, 9.524999999999991473 ) ) ;
#20281=ORIENTED_EDGE ( 'NONE', *, *, #61298, .T. ) ;
#20292=ORIENTED_EDGE ( 'NONE', *, *, #69051, .T. ) ;
#20297=CARTESIAN_POINT ( 'NONE',  ( -103.7949999999999733, 2.607480562269068880, -8.024999999999993250 ) ) ;
#20299=( BOUNDED_CURVE ( )  B_SPLINE_CURVE ( 2, ( #45678, #55840, #50574, #39694, #16265, #56172, #11287, #37739, #45336, #18569, #40050 ),
 .UNSPECIFIED., .F., .F. ) 
 B_SPLINE_CURVE_WITH_KNOTS ( ( 3, 2, 2, 2, 2, 3 ),
 ( 0.2065217391304298156, 0.2086956521739080361, 0.2108695652173862567, 0.2130434782608644773, 0.2152173913043426978, 0.2173913043478209184 ),
 .UNSPECIFIED. ) 
 CURVE ( )  GEOMETRIC_REPRESENTATION_ITEM ( )  RATIONAL_B_SPLINE_CURVE ( ( 1.000000000000111910, 0.9510565162950417317, 1.000000000000000000, 0.9510565162951535312, 1.000000000000000000, 0.9510565162951535312, 1.000000000000000000, 0.9510565162951535312, 1.000000000000000000, 0.9510565162952697715, 0.9999999999998837596 ) ) 
 REPRESENTATION_ITEM ( '' )  );
#20312=CARTESIAN_POINT ( 'NONE',  ( -61.55707362346617373, -1.166476076187852838E-15, -9.524999999999991473 ) ) ;
#20315=DIRECTION ( 'NONE',  ( 0.000000000000000000, 0.000000000000000000, 1.000000000000000000 ) ) ;
#20318=CARTESIAN_POINT ( 'NONE',  ( -128.3050000000000068, 8.437984349512085203, -1.550032578732815448E-15 ) ) ;
#20325=CARTESIAN_POINT ( 'NONE',  ( -160.9429263765338192, 0.000000000000000000, 9.524999999999991473 ) ) ;
#20326=ORIENTED_EDGE ( 'NONE', *, *, #6583, .T. ) ;
#20336=CARTESIAN_POINT ( 'NONE',  ( -178.5549999999999784, 0.000000000000000000, 8.024999999999991473 ) ) ;
#20339=CARTESIAN_POINT ( 'NONE',  ( -182.5449999999999875, -7.632228543268600340, -2.479861379858950166 ) ) ;
#20340=CARTESIAN_POINT ( 'NONE',  ( -173.5450000000000159, -7.632228543268600340, -2.479861379858950166 ) ) ;
#20345=CARTESIAN_POINT ( 'NONE',  ( -96.80499999999999261, -8.437984349512085203, 5.166775262442717831E-16 ) ) ;
#20349=CARTESIAN_POINT ( 'NONE',  ( -86.09499999999995623, -2.607480562269071545, -8.024999999999991473 ) ) ;
#20351=CARTESIAN_POINT ( 'NONE',  ( -68.84499999999998465, -7.632228543268599452, 2.479861379858951054 ) ) ;
#20358=CARTESIAN_POINT ( 'NONE',  ( -109.7929263765338135, -3.094860106618429807, 9.524999999999991473 ) ) ;
#20360=CARTESIAN_POINT ( 'NONE',  ( -128.3949999999999534, -6.826472737025115478, -4.959722759717899443 ) ) ;
#20365=CARTESIAN_POINT ( 'NONE',  ( -131.2429263765338021, 5.598654528085804216, 7.705886871421366635 ) ) ;
#20371=CARTESIAN_POINT ( 'NONE',  ( -134.5429263765338135, 9.058813317711329915, 2.943386871421369566 ) ) ;
#20379=CARTESIAN_POINT ( 'NONE',  ( -125.7550000000000097, 4.716976649647091513, -6.492361379858946790 ) ) ;
#20382=CARTESIAN_POINT ( 'NONE',  ( -121.7070736234661581, -3.094860106618431139, -9.524999999999991473 ) ) ;
#20383=VERTEX_POINT ( 'NONE', #52308 ) ;
#20390=AXIS2_PLACEMENT_3D ( 'NONE', #1084, #53928, #5728 ) ;
#20399=CARTESIAN_POINT ( 'NONE',  ( -47.00707362346617657, -8.102448949553174629, -5.886773742842741797 ) ) ;
#20408=CARTESIAN_POINT ( 'NONE',  ( -56.84292637653378932, 9.058813317711329915, -2.943386871421373119 ) ) ;
#20410=CARTESIAN_POINT ( 'NONE',  ( -156.3549999999999898, -4.716976649647093289, -6.492361379858945902 ) ) ;
#20428=CARTESIAN_POINT ( 'NONE',  ( -63.95499999999998408, -7.632228543268599452, 2.479861379858951054 ) ) ;
#20435=CARTESIAN_POINT ( 'NONE',  ( -124.3429263765337964, -9.058813317711329915, 2.943386871421371787 ) ) ;
#20439=EDGE_CURVE ( 'NONE', #149, #17310, #16415, .T. ) ;
#20445=CARTESIAN_POINT ( 'NONE',  ( -97.19499999999997897, 8.437984349512085203, -1.550032578732815448E-15 ) ) ;
#20450=ORIENTED_EDGE ( 'NONE', *, *, #30460, .F. ) ;
#20451=CARTESIAN_POINT ( 'NONE',  ( -131.8429263765337964, 9.058813317711329915, -2.943386871421373119 ) ) ;
#20452=DIRECTION ( 'NONE',  ( -1.000000000000000000, -0.000000000000000000, -0.000000000000000000 ) ) ;
#20453=CARTESIAN_POINT ( 'NONE',  ( -159.5949999999999989, 2.607480562269073321, 8.024999999999991473 ) ) ;
#20457=CARTESIAN_POINT ( 'NONE',  ( -133.4929263765338021, -8.102448949553174629, 5.886773742842742685 ) ) ;
#20469=CARTESIAN_POINT ( 'NONE',  ( -146.4550000000000125, 7.632228543268599452, -2.479861379858951942 ) ) ;
#20483=CARTESIAN_POINT ( 'NONE',  ( -67.55499999999999261, 0.000000000000000000, 8.024999999999991473 ) ) ;
#20497=CARTESIAN_POINT ( 'NONE',  ( -179.9049999999999727, 2.607480562269068880, -8.024999999999993250 ) ) ;
#20500=EDGE_CURVE ( 'NONE', #61162, #8408, #56788, .T. ) ;
#20506=ORIENTED_EDGE ( 'NONE', *, *, #56629, .F. ) ;
#20509=CARTESIAN_POINT ( 'NONE',  ( -94.10499999999997556, -6.826472737025115478, 4.959722759717900331 ) ) ;
#20514=CARTESIAN_POINT ( 'NONE',  ( -135.5070736234661695, 8.102448949553176405, 5.886773742842740909 ) ) ;
#20518=CARTESIAN_POINT ( 'NONE',  ( -72.05707362346616662, 0.000000000000000000, 9.524999999999991473 ) ) ;
#20523=CARTESIAN_POINT ( 'NONE',  ( -18.30630105587923495, -11.39666211907883664, -3.764819142662532592 ) ) ;
#20526=CARTESIAN_POINT ( 'NONE',  ( -111.2049999999999983, -2.607480562269071545, -8.024999999999991473 ) ) ;
#20530=CARTESIAN_POINT ( 'NONE',  ( -124.1950000000000074, 8.437984349512085203, -1.550032578732815448E-15 ) ) ;
#20534=CARTESIAN_POINT ( 'NONE',  ( -158.9929263765338021, 8.102448949553171076, -5.886773742842744461 ) ) ;
#20535=CARTESIAN_POINT ( 'NONE',  ( -182.0949999999999989, -2.607480562269071545, -8.024999999999991473 ) ) ;
#20542=CARTESIAN_POINT ( 'NONE',  ( -78.29292637653378506, 3.094860106618428031, -9.524999999999993250 ) ) ;
#20545=EDGE_CURVE ( 'NONE', #63576, #53864, #59620, .T. ) ;
#20548=CARTESIAN_POINT ( 'NONE',  ( -181.2549999999999955, -4.716976649647092401, 6.492361379858946790 ) ) ;
#20563=CARTESIAN_POINT ( 'NONE',  ( -92.15499999999998693, 7.632228543268600340, 2.479861379858949277 ) ) ;
#20575=CARTESIAN_POINT ( 'NONE',  ( -70.94499999999997897, -9.827790563157499189E-16, -8.024999999999991473 ) ) ;
#20588=EDGE_LOOP ( 'NONE', ( #44055, #46909, #65570, #60092 ) ) ;
#20593=DIRECTION ( 'NONE',  ( 0.000000000000000000, 0.000000000000000000, 1.000000000000000000 ) ) ;
#20594=CARTESIAN_POINT ( 'NONE',  ( -158.9070736234661183, -3.094860106618429807, 9.524999999999991473 ) ) ;
#20596=CARTESIAN_POINT ( 'NONE',  ( -107.7570736234661695, -5.598654528085801552, 7.705886871421367523 ) ) ;
#20600=CARTESIAN_POINT ( 'NONE',  ( -65.45707362346617231, -9.058813317711329915, 2.943386871421371787 ) ) ;
#20603=CARTESIAN_POINT ( 'NONE',  ( -195.0000000000000000, 0.000000000000000000, 0.000000000000000000 ) ) ;
#20606=CARTESIAN_POINT ( 'NONE',  ( -141.8050000000000068, -8.437984349512085203, 5.166775262442717831E-16 ) ) ;
#20609=CARTESIAN_POINT ( 'NONE',  ( -156.7450000000000045, 4.716976649647094177, 6.492361379858945902 ) ) ;
#20612=CARTESIAN_POINT ( 'NONE',  ( -134.5449999999999875, -7.632228543268600340, -2.479861379858950166 ) ) ;
#20619=CARTESIAN_POINT ( 'NONE',  ( -56.30499999999999972, 8.437984349512085203, -1.550032578732815448E-15 ) ) ;
#20631=CARTESIAN_POINT ( 'NONE',  ( -81.65707362346617515, 9.058813317711329915, 2.943386871421369566 ) ) ;
#20661=CIRCLE ( 'NONE', #38628, 1.000000000000000888 ) ;
#20663=CARTESIAN_POINT ( 'NONE',  ( -100.6449999999999818, 4.716976649647091513, -6.492361379858946790 ) ) ;
#20665=AXIS2_PLACEMENT_3D ( 'NONE', #43409, #12348, #17340 ) ;
#20667=CARTESIAN_POINT ( 'NONE',  ( -53.09292637653378932, 3.094860106618433360, 9.524999999999991473 ) ) ;
#20673=DIRECTION ( 'NONE',  ( 0.000000000000000000, 0.000000000000000000, 1.000000000000000000 ) ) ;
#20678=CARTESIAN_POINT ( 'NONE',  ( -140.8429263765338249, 9.058813317711329915, -2.943386871421373119 ) ) ;
#20681=LINE ( 'NONE', #64953, #66798 ) ;
#20683=AXIS2_PLACEMENT_3D ( 'NONE', #40323, #9356, #20229 ) ;
#20695=CARTESIAN_POINT ( 'NONE',  ( -172.7049999999999841, 2.607480562269073321, 8.024999999999991473 ) ) ;
#20696=CARTESIAN_POINT ( 'NONE',  ( -90.74292637653380211, -5.598654528085803328, -7.705886871421366635 ) ) ;
#20699=CARTESIAN_POINT ( 'NONE',  ( -46.70707362346617231, -3.094860106618431139, -9.524999999999991473 ) ) ;
#20701=CARTESIAN_POINT ( 'NONE',  ( -179.2449999999999761, -4.716976649647093289, -6.492361379858945902 ) ) ;
#20706=CARTESIAN_POINT ( 'NONE',  ( -10.51151497852317718, 11.79546843913625231, 2.227144960977124999 ) ) ;
#20707=CARTESIAN_POINT ( 'NONE',  ( -90.95499999999999829, -7.632228543268599452, 2.479861379858951054 ) ) ;
#20710=CARTESIAN_POINT ( 'NONE',  ( -89.24499999999999034, -4.716976649647093289, -6.492361379858945902 ) ) ;
#20719=CARTESIAN_POINT ( 'NONE',  ( -48.29292637653378506, 3.094860106618428031, -9.524999999999993250 ) ) ;
#20729=EDGE_LOOP ( 'NONE', ( #55048, #49718, #3973, #41193 ) ) ;
#20738=DIRECTION ( 'NONE',  ( -1.000000000000000000, -0.000000000000000000, -0.000000000000000000 ) ) ;
#20741=CARTESIAN_POINT ( 'NONE',  ( -125.4549999999999841, 7.632228543268599452, -2.479861379858951942 ) ) ;
#20756=CARTESIAN_POINT ( 'NONE',  ( -55.25707362346615525, 5.598654528085800663, -7.705886871421367523 ) ) ;
#20758=CARTESIAN_POINT ( 'NONE',  ( -135.0570736234661808, 0.000000000000000000, 9.524999999999991473 ) ) ;
#20762=CARTESIAN_POINT ( 'NONE',  ( -195.0000000000000000, 0.000000000000000000, 9.524999999999991473 ) ) ;
#20766=EDGE_CURVE ( 'NONE', #44158, #69107, #55959, .T. ) ;
#20770=CARTESIAN_POINT ( 'NONE',  ( -55.34292637653378932, -9.058813317711329915, 2.943386871421371787 ) ) ;
#20774=CARTESIAN_POINT ( 'NONE',  ( -156.8050000000000068, -8.437984349512085203, 5.166775262442717831E-16 ) ) ;
#20781=VERTEX_POINT ( 'NONE', #18688 ) ;
#20785=CARTESIAN_POINT ( 'NONE',  ( -1.000000000000028644, 0.000000000000000000, 11.99999999999999645 ) ) ;
#20786=CARTESIAN_POINT ( 'NONE',  ( -70.55499999999999261, 0.000000000000000000, 8.024999999999991473 ) ) ;
#20788=ORIENTED_EDGE ( 'NONE', *, *, #40060, .F. ) ;
#20800=CARTESIAN_POINT ( 'NONE',  ( -119.3949999999999676, -6.826472737025113702, -4.959722759717900331 ) ) ;
#20802=CARTESIAN_POINT ( 'NONE',  ( -86.69499999999999318, -8.437984349512085203, 5.166775262442717831E-16 ) ) ;
#20809=CARTESIAN_POINT ( 'NONE',  ( -129.4429263765338192, -1.166476076187852838E-15, -9.524999999999991473 ) ) ;
#20811=LINE ( 'NONE', #52830, #34356 ) ;
#20812=CARTESIAN_POINT ( 'NONE',  ( -157.7950000000000159, 2.607480562269068880, -8.024999999999993250 ) ) ;
#20816=DIRECTION ( 'NONE',  ( -1.000000000000000000, -0.000000000000000000, -0.000000000000000000 ) ) ;
#20819=EDGE_LOOP ( 'NONE', ( #49510, #25854, #9611, #51129, #1396 ) ) ;
#20822=CARTESIAN_POINT ( 'NONE',  ( -143.2429263765338021, 5.598654528085804216, 7.705886871421366635 ) ) ;
#20826=CARTESIAN_POINT ( 'NONE',  ( -148.8549999999999898, 4.716976649647094177, 6.492361379858945902 ) ) ;
#20831=ADVANCED_FACE ( 'NONE', ( #40863 ), #24254, .T. ) ;
#20843=CARTESIAN_POINT ( 'NONE',  ( -67.85499999999998977, 4.716976649647094177, 6.492361379858945902 ) ) ;
#20845=CARTESIAN_POINT ( 'NONE',  ( -157.9429263765338192, 0.000000000000000000, 9.524999999999991473 ) ) ;
#20854=LINE ( 'NONE', #52872, #66496 ) ;
#20855=CARTESIAN_POINT ( 'NONE',  ( -183.8050000000000068, -8.437984349512085203, 5.166775262442717831E-16 ) ) ;
#20860=EDGE_LOOP ( 'NONE', ( #42481, #42232, #14027, #30313 ) ) ;
#20861=CARTESIAN_POINT ( 'NONE',  ( -121.5570736234661808, -1.166476076187852838E-15, -9.524999999999991473 ) ) ;
#20866=CARTESIAN_POINT ( 'NONE',  ( -91.70499999999998408, 2.607480562269073321, 8.024999999999991473 ) ) ;
#20870=CARTESIAN_POINT ( 'NONE',  ( -133.5570736234661808, -1.166476076187852838E-15, -9.524999999999991473 ) ) ;
#20873=CARTESIAN_POINT ( 'NONE',  ( -65.30707362346618083, -10.01517768586948698, 6.132527647946031529E-16 ) ) ;
#20874=CARTESIAN_POINT ( 'NONE',  ( -81.14292637653380780, 5.598654528085800663, -7.705886871421367523 ) ) ;
#20878=CARTESIAN_POINT ( 'NONE',  ( -111.8049999999999784, -8.437984349512085203, 5.166775262442717831E-16 ) ) ;
#20880=CARTESIAN_POINT ( 'NONE',  ( -125.2449999999999903, -4.716976649647093289, -6.492361379858945902 ) ) ;
#20888=CARTESIAN_POINT ( 'NONE',  ( -165.8929263765338078, -8.102448949553172852, -5.886773742842741797 ) ) ;
#20891=LINE ( 'NONE', #68747, #23662 ) ;
#20895=CARTESIAN_POINT ( 'NONE',  ( -71.99292637653381632, 8.102448949553171076, -5.886773742842744461 ) ) ;
#20897=LINE ( 'NONE', #52581, #50948 ) ;
#20904=AXIS2_PLACEMENT_3D ( 'NONE', #24535, #41125, #46049 ) ;
#20905=CARTESIAN_POINT ( 'NONE',  ( -182.9049999999999727, 2.607480562269069324, -8.024999999999993250 ) ) ;
#20914=CARTESIAN_POINT ( 'NONE',  ( -110.5429263765337993, 9.058813317711329915, 2.943386871421369566 ) ) ;
#20919=CARTESIAN_POINT ( 'NONE',  ( -100.8570736234661780, -5.598654528085803328, -7.705886871421366635 ) ) ;
#20921=CARTESIAN_POINT ( 'NONE',  ( -95.60499999999997556, 6.826472737025113702, -4.959722759717902107 ) ) ;
#20931=ORIENTED_EDGE ( 'NONE', *, *, #60425, .T. ) ;
#20932=CARTESIAN_POINT ( 'NONE',  ( -76.94499999999997897, -9.827790563157499189E-16, -8.024999999999991473 ) ) ;
#20936=CARTESIAN_POINT ( 'NONE',  ( -120.9570736234661865, 9.058813317711329915, -2.943386871421373119 ) ) ;
#20938=PLANE ( 'NONE',  #958 ) ;
#20942=EDGE_LOOP ( 'NONE', ( #37427, #62579, #4032, #48731 ) ) ;
#20947=CARTESIAN_POINT ( 'NONE',  ( -156.5070736234661126, 8.102448949553176405, 5.886773742842740909 ) ) ;
#20949=CARTESIAN_POINT ( 'NONE',  ( -107.1570736234661751, -9.058813317711329915, -2.943386871421370898 ) ) ;
#20959=CARTESIAN_POINT ( 'NONE',  ( -144.0549999999999784, -9.827790563157499189E-16, -8.024999999999991473 ) ) ;
#20963=CARTESIAN_POINT ( 'NONE',  ( -157.3449999999999989, 7.632228543268599452, -2.479861379858951942 ) ) ;
#20964=CARTESIAN_POINT ( 'NONE',  ( -140.5450000000000159, -7.632228543268600340, -2.479861379858950166 ) ) ;
#20968=CARTESIAN_POINT ( 'NONE',  ( -57.80499999999998550, -8.437984349512085203, 5.166775262442717831E-16 ) ) ;
#20978=CARTESIAN_POINT ( 'NONE',  ( -89.90707362346732623, -3.094860106599338412, 9.525000000013864820 ) ) ;
#20982=CARTESIAN_POINT ( 'NONE',  ( -78.44292637653380496, -1.166476076187852838E-15, -9.524999999999991473 ) ) ;
#21003=CARTESIAN_POINT ( 'NONE',  ( -105.5949999999999989, 2.607480562269073321, 8.024999999999991473 ) ) ;
#21015=ORIENTED_EDGE ( 'NONE', *, *, #6120, .F. ) ;
#21031=CARTESIAN_POINT ( 'NONE',  ( -166.7049999999999557, 2.607480562269073321, 8.024999999999991473 ) ) ;
#21034=CARTESIAN_POINT ( 'NONE',  ( -180.2949999999999591, -2.607480562269069768, 8.024999999999991473 ) ) ;
#21035=CARTESIAN_POINT ( 'NONE',  ( -166.6449999999999818, 4.716976649647091513, -6.492361379858946790 ) ) ;
#21042=CARTESIAN_POINT ( 'NONE',  ( -80.30499999999999261, 8.437984349512085203, -1.550032578732815448E-15 ) ) ;
#21048=CARTESIAN_POINT ( 'NONE',  ( -80.84499999999998465, -7.632228543268599452, 2.479861379858951054 ) ) ;
#21064=ORIENTED_EDGE ( 'NONE', *, *, #10238, .F. ) ;
#21072=CARTESIAN_POINT ( 'NONE',  ( -125.9049999999999869, 2.607480562269069324, -8.024999999999993250 ) ) ;
#21075=FACE_OUTER_BOUND ( 'NONE', #916, .T. ) ;
#21098=CARTESIAN_POINT ( 'NONE',  ( -61.49292637653379501, -8.102448949553172852, 5.886773742842742685 ) ) ;
#21102=CARTESIAN_POINT ( 'NONE',  ( -144.9550000000000125, -7.632228543268599452, 2.479861379858951054 ) ) ;
#21114=CARTESIAN_POINT ( 'NONE',  ( -68.30499999999997840, 8.437984349512085203, -1.550032578732815448E-15 ) ) ;
#21118=CARTESIAN_POINT ( 'NONE',  ( -1.000000000000028644, 0.000000000000000000, 0.000000000000000000 ) ) ;
#21127=CARTESIAN_POINT ( 'NONE',  ( -119.2449999999999903, -4.716976649647093289, -6.492361379858945902 ) ) ;
#21129=CARTESIAN_POINT ( 'NONE',  ( -90.44499999999997897, 0.000000000000000000, 8.024999999999991473 ) ) ;
#21134=CARTESIAN_POINT ( 'NONE',  ( -137.9929263765338305, 8.102448949553171076, -5.886773742842744461 ) ) ;
#21136=CARTESIAN_POINT ( 'NONE',  ( -146.5449999999999875, -7.632228543268600340, -2.479861379858950166 ) ) ;
#21145=CARTESIAN_POINT ( 'NONE',  ( -143.6929263765337907, 10.01517768586948698, -1.839758294383808966E-15 ) ) ;
#21151=CARTESIAN_POINT ( 'NONE',  ( -149.3049999999999784, 8.437984349512086979, -1.550032578732815448E-15 ) ) ;
#21163=CARTESIAN_POINT ( 'NONE',  ( -68.60499999999997556, 6.826472737025113702, -4.959722759717902107 ) ) ;
#21165=CARTESIAN_POINT ( 'NONE',  ( -117.7449999999999903, 4.716976649647094177, 6.492361379858945902 ) ) ;
#21167=ORIENTED_EDGE ( 'NONE', *, *, #18449, .T. ) ;
#21169=CARTESIAN_POINT ( 'NONE',  ( -183.0000000000000284, -1.154738647139537111, 9.454745033939424559 ) ) ;
#21176=CARTESIAN_POINT ( 'NONE',  ( -178.1049999999999329, -6.826472737025115478, 4.959722759717900331 ) ) ;
#21179=CARTESIAN_POINT ( 'NONE',  ( -45.00000000000000000, 0.000000000000000000, 9.525000000000000355 ) ) ;
#21185=CARTESIAN_POINT ( 'NONE',  ( -90.35499999999998977, -4.716976649647093289, -6.492361379858945902 ) ) ;
#21190=CARTESIAN_POINT ( 'NONE',  ( -128.0070736234661979, -8.102448949553172852, -5.886773742842741797 ) ) ;
#21192=CARTESIAN_POINT ( 'NONE',  ( -70.25707362346616947, 5.598654528085800663, -7.705886871421367523 ) ) ;
#21199=CARTESIAN_POINT ( 'NONE',  ( -114.8049999999999926, -8.437984349512085203, 5.166775262442717831E-16 ) ) ;
#21202=CARTESIAN_POINT ( 'NONE',  ( -116.5450000000000017, -7.632228543268600340, -2.479861379858950166 ) ) ;
#21204=CARTESIAN_POINT ( 'NONE',  ( -118.4929263765338021, -8.102448949553174629, 5.886773742842742685 ) ) ;
#21209=CARTESIAN_POINT ( 'NONE',  ( -159.1429263765338078, 5.598654528085800663, -7.705886871421367523 ) ) ;
#21210=CARTESIAN_POINT ( 'NONE',  ( -183.1450000000000102, -4.716976649647092401, 6.492361379858946790 ) ) ;
#21219=CARTESIAN_POINT ( 'NONE',  ( -80.84292637653379643, 9.058813317711329915, -2.943386871421373119 ) ) ;
#21225=CARTESIAN_POINT ( 'NONE',  ( -178.2549999999999955, -4.716976649647092401, 6.492361379858946790 ) ) ;
#21235=CARTESIAN_POINT ( 'NONE',  ( -93.05499999999997840, -9.827790563157499189E-16, -8.024999999999991473 ) ) ;
#21245=CARTESIAN_POINT ( 'NONE',  ( -69.59499999999999886, 2.607480562269073321, 8.024999999999991473 ) ) ;
#21248=CARTESIAN_POINT ( 'NONE',  ( -125.6070736234661780, -8.102448949553174629, 5.886773742842742685 ) ) ;
#21258=CARTESIAN_POINT ( 'NONE',  ( -159.5929263765341659, -3.094860106623775753, -9.524999999996111910 ) ) ;
#21261=CARTESIAN_POINT ( 'NONE',  ( -155.7570736234661979, -5.598654528085801552, 7.705886871421367523 ) ) ;
#21265=CARTESIAN_POINT ( 'NONE',  ( -89.90707362346616094, -3.094860106618429807, 9.524999999999991473 ) ) ;
#21268=CIRCLE ( 'NONE', #22441, 5.499999999999984901 ) ;
#21270=VERTEX_POINT ( 'NONE', #42748 ) ;
#21277=CARTESIAN_POINT ( 'NONE',  ( -136.8550000000000182, 4.716976649647094177, 6.492361379858945902 ) ) ;
#21279=CARTESIAN_POINT ( 'NONE',  ( -86.00707362346616947, -8.102448949553174629, -5.886773742842741797 ) ) ;
#21281=CARTESIAN_POINT ( 'NONE',  ( -147.5949999999999704, 2.607480562269073321, 8.024999999999991473 ) ) ;
#21283=CARTESIAN_POINT ( 'NONE',  ( -138.8949999999999250, 6.826472737025115478, 4.959722759717899443 ) ) ;
#21293=CARTESIAN_POINT ( 'NONE',  ( -58.40499999999997982, -2.607480562269069768, 8.024999999999991473 ) ) ;
#21324=CARTESIAN_POINT ( 'NONE',  ( -46.25707362346617657, 5.598654528085800663, -7.705886871421367523 ) ) ;
#21331=CARTESIAN_POINT ( 'NONE',  ( -97.79500000000000171, 2.607480562269068880, -8.024999999999993250 ) ) ;
#21363=CARTESIAN_POINT ( 'NONE',  ( -169.8550000000000182, 4.716976649647094177, 6.492361379858945902 ) ) ;
#21367=CARTESIAN_POINT ( 'NONE',  ( -50.90707362346616094, -3.094860106618429807, 9.524999999999991473 ) ) ;
#21369=CARTESIAN_POINT ( 'NONE',  ( -168.7450000000000045, 4.716976649647094177, 6.492361379858945902 ) ) ;
#21375=CARTESIAN_POINT ( 'NONE',  ( -11.69477403538655480, 11.39635258918007210, 3.765737026947071353 ) ) ;
#21376=CARTESIAN_POINT ( 'NONE',  ( -85.25499999999998124, -4.716976649647092401, 6.492361379858946790 ) ) ;
#21377=DIRECTION ( 'NONE',  ( 0.000000000000000000, 0.000000000000000000, 1.000000000000000000 ) ) ;
#21381=CARTESIAN_POINT ( 'NONE',  ( -77.24499999999997613, -4.716976649647093289, -6.492361379858945902 ) ) ;
#21400=ORIENTED_EDGE ( 'NONE', *, *, #33524, .F. ) ;
#21403=EDGE_CURVE ( 'NONE', #48545, #45861, #16523, .T. ) ;
#21411=CARTESIAN_POINT ( 'NONE',  ( -123.6549999999999869, -7.632228543268600340, -2.479861379858950166 ) ) ;
#21439=CARTESIAN_POINT ( 'NONE',  ( -50.09292637653377511, 3.094860106618433360, 9.524999999999991473 ) ) ;
#21441=CARTESIAN_POINT ( 'NONE',  ( -144.2050000000000125, -2.607480562269071545, -8.024999999999991473 ) ) ;
#21443=( BOUNDED_CURVE ( )  B_SPLINE_CURVE ( 2, ( #31273, #4546, #20756, #42264, #63653, #15494, #36961, #24607, #67547, #19344, #40847 ),
 .UNSPECIFIED., .F., .F. ) 
 B_SPLINE_CURVE_WITH_KNOTS ( ( 3, 2, 2, 2, 2, 3 ),
 ( 0.9239130434782608647, 0.9260869565217391131, 0.9282608695652173614, 0.9304347826086956097, 0.9326086956521738580, 0.9347826086956522174 ),
 .UNSPECIFIED. ) 
 CURVE ( )  GEOMETRIC_REPRESENTATION_ITEM ( )  RATIONAL_B_SPLINE_CURVE ( ( 1.000000000000000000, 0.9510565162951535312, 1.000000000000000000, 0.9510565162951535312, 1.000000000000000000, 0.9510565162951535312, 1.000000000000000000, 0.9510565162951535312, 1.000000000000000000, 0.9510565162951535312, 1.000000000000000000 ) ) 
 REPRESENTATION_ITEM ( '' )  );
#21448=ADVANCED_FACE ( 'NONE', ( #20095 ), #45835, .T. ) ;
#21454=EDGE_LOOP ( 'NONE', ( #45677, #51999, #34341, #20281 ) ) ;
#21456=CYLINDRICAL_SURFACE ( 'NONE', #27182, 9.524999999999991473 ) ;
#21458=CARTESIAN_POINT ( 'NONE',  ( -59.15499999999998693, 7.632228543268600340, 2.479861379858949277 ) ) ;
#21467=CARTESIAN_POINT ( 'NONE',  ( -96.89292637653379359, -8.102448949553174629, -5.886773742842741797 ) ) ;
#21476=CARTESIAN_POINT ( 'NONE',  ( -107.3949999999999960, -6.826472737025113702, -4.959722759717900331 ) ) ;
#21478=CARTESIAN_POINT ( 'NONE',  ( -91.49499999999997613, 6.826472737025113702, -4.959722759717902107 ) ) ;
#21485=CARTESIAN_POINT ( 'NONE',  ( -136.4929263765338305, -8.102448949553172852, 5.886773742842742685 ) ) ;
#21486=CARTESIAN_POINT ( 'NONE',  ( -145.6450000000000102, 4.716976649647091513, -6.492361379858946790 ) ) ;
#21501=CARTESIAN_POINT ( 'NONE',  ( -147.6549999999999727, -7.632228543268600340, -2.479861379858950166 ) ) ;
#21515=CARTESIAN_POINT ( 'NONE',  ( -68.45499999999998408, 7.632228543268599452, -2.479861379858951942 ) ) ;
#21516=CARTESIAN_POINT ( 'NONE',  ( -124.6449999999999960, 4.716976649647091513, -6.492361379858946790 ) ) ;
#21534=CARTESIAN_POINT ( 'NONE',  ( -175.5549999999999784, 0.000000000000000000, 8.024999999999991473 ) ) ;
#21547=CARTESIAN_POINT ( 'NONE',  ( -96.95499999999998408, -7.632228543268599452, 2.479861379858951054 ) ) ;
#21551=CARTESIAN_POINT ( 'NONE',  ( -135.6570736234661751, 9.058813317711329915, 2.943386871421369566 ) ) ;
#21553=CARTESIAN_POINT ( 'NONE',  ( -68.30707362346616662, -10.01517768586948698, 6.132527647946031529E-16 ) ) ;
#21561=CARTESIAN_POINT ( 'NONE',  ( -116.4549999999999841, 7.632228543268599452, -2.479861379858951942 ) ) ;
#21564=CARTESIAN_POINT ( 'NONE',  ( -112.7949999999999733, 2.607480562269068880, -8.024999999999993250 ) ) ;
#21568=DIRECTION ( 'NONE',  ( 0.000000000000000000, 0.000000000000000000, 1.000000000000000000 ) ) ;
#21570=CARTESIAN_POINT ( 'NONE',  ( -160.1929263765337907, -10.01517768586948698, 6.132527647946031529E-16 ) ) ;
#21571=CARTESIAN_POINT ( 'NONE',  ( -175.1949999999999932, 8.437984349512085203, -1.550032578732815448E-15 ) ) ;
#21576=ORIENTED_EDGE ( 'NONE', *, *, #25782, .T. ) ;
#21578=CARTESIAN_POINT ( 'NONE',  ( -79.04292637653379927, -9.058813317711329915, -2.943386871421370898 ) ) ;
#21580=DIRECTION ( 'NONE',  ( -1.000000000000000000, -0.000000000000000000, -0.000000000000000000 ) ) ;
#21586=CARTESIAN_POINT ( 'NONE',  ( -180.0550000000000068, -9.827790563157499189E-16, -8.024999999999991473 ) ) ;
#21589=DIRECTION ( 'NONE',  ( 0.000000000000000000, 0.000000000000000000, 1.000000000000000000 ) ) ;
#21595=EDGE_LOOP ( 'NONE', ( #58148, #43700, #65472, #9186 ) ) ;
#21598=CARTESIAN_POINT ( 'NONE',  ( -93.95499999999998408, -7.632228543268599452, 2.479861379858951054 ) ) ;
#21608=CARTESIAN_POINT ( 'NONE',  ( -65.39499999999998181, -6.826472737025115478, -4.959722759717899443 ) ) ;
#21618=CARTESIAN_POINT ( 'NONE',  ( -125.3049999999999926, 8.437984349512085203, -1.550032578732815448E-15 ) ) ;
#21623=CARTESIAN_POINT ( 'NONE',  ( -159.4429263765338192, -1.166476076187852838E-15, -9.524999999999991473 ) ) ;
#21625=CARTESIAN_POINT ( 'NONE',  ( -164.3070736234662093, -10.01517768586948698, 6.132527647946031529E-16 ) ) ;
#21629=CARTESIAN_POINT ( 'NONE',  ( -90.80707362346613820, 10.01517768586948698, -1.839758294383808571E-15 ) ) ;
#21638=CARTESIAN_POINT ( 'NONE',  ( -136.5549999999999784, 0.000000000000000000, 8.024999999999991473 ) ) ;
#21639=CARTESIAN_POINT ( 'NONE',  ( -85.85707362346617799, -5.598654528085803328, -7.705886871421366635 ) ) ;
#21643=CARTESIAN_POINT ( 'NONE',  ( -147.8949999999999818, 6.826472737025116366, 4.959722759717898555 ) ) ;
#21644=CARTESIAN_POINT ( 'NONE',  ( -140.3949999999999818, -6.826472737025113702, -4.959722759717900331 ) ) ;
#21650=CARTESIAN_POINT ( 'NONE',  ( -52.70499999999996277, 2.607480562269073321, 8.024999999999991473 ) ) ;
#21653=CARTESIAN_POINT ( 'NONE',  ( -55.64499999999997470, 4.716976649647091513, -6.492361379858946790 ) ) ;
#21657=CARTESIAN_POINT ( 'NONE',  ( -154.7070736234665276, -3.094860106624346408, -9.524999999995696243 ) ) ;
#21658=CARTESIAN_POINT ( 'NONE',  ( -102.4429263765338050, -1.166476076187852838E-15, -9.524999999999991473 ) ) ;
#21663=CARTESIAN_POINT ( 'NONE',  ( -99.80707362346616662, 10.01517768586948698, -1.839758294383808966E-15 ) ) ;
#21678=ORIENTED_EDGE ( 'NONE', *, *, #14636, .F. ) ;
#21683=AXIS2_PLACEMENT_3D ( 'NONE', #65768, #54836, #56232 ) ;
#21693=CARTESIAN_POINT ( 'NONE',  ( -104.8449999999999989, -7.632228543268599452, 2.479861379858951054 ) ) ;
#21704=CARTESIAN_POINT ( 'NONE',  ( -165.6570736234661751, 9.058813317711329915, 2.943386871421369566 ) ) ;
#21705=CARTESIAN_POINT ( 'NONE',  ( -45.00000000000000000, 0.000000000000000000, 8.525000000000000355 ) ) ;
#21715=CARTESIAN_POINT ( 'NONE',  ( -115.3429263765337964, -9.058813317711329915, 2.943386871421371787 ) ) ;
#21719=CARTESIAN_POINT ( 'NONE',  ( -58.55707362346616662, -1.166476076187852838E-15, -9.524999999999991473 ) ) ;
#21724=CARTESIAN_POINT ( 'NONE',  ( -170.4549999999999841, 7.632228543268599452, -2.479861379858951942 ) ) ;
#21727=CARTESIAN_POINT ( 'NONE',  ( -178.1949999999999648, 8.437984349512085203, -1.550032578732815448E-15 ) ) ;
#21729=CARTESIAN_POINT ( 'NONE',  ( -164.5449999999999875, -7.632228543268600340, -2.479861379858950166 ) ) ;
#21736=CARTESIAN_POINT ( 'NONE',  ( -87.35499999999998977, -4.716976649647093289, -6.492361379858945902 ) ) ;
#21742=CARTESIAN_POINT ( 'NONE',  ( -76.79499999999998749, 2.607480562269069324, -8.024999999999993250 ) ) ;
#21745=CARTESIAN_POINT ( 'NONE',  ( -172.2570736234661695, 5.598654528085800663, -7.705886871421367523 ) ) ;
#21746=FACE_OUTER_BOUND ( 'NONE', #27048, .T. ) ;
#21748=AXIS2_PLACEMENT_3D ( 'NONE', #10829, #873, #43576 ) ;
#21761=ORIENTED_EDGE ( 'NONE', *, *, #68917, .F. ) ;
#21772=CARTESIAN_POINT ( 'NONE',  ( -108.8049999999999784, -8.437984349512086979, 5.166775262442717831E-16 ) ) ;
#21790=CARTESIAN_POINT ( 'NONE',  ( -181.3429263765338249, -9.058813317711329915, 2.943386871421371787 ) ) ;
#21800=ORIENTED_EDGE ( 'NONE', *, *, #5570, .F. ) ;
#21805=CARTESIAN_POINT ( 'NONE',  ( -139.8550000000000182, 4.716976649647094177, 6.492361379858945902 ) ) ;
#21810=CARTESIAN_POINT ( 'NONE',  ( -106.1929263765338050, -10.01517768586948698, 6.132527647946031529E-16 ) ) ;
#21817=CARTESIAN_POINT ( 'NONE',  ( -55.40499999999997982, -2.607480562269069768, 8.024999999999991473 ) ) ;
#21826=CARTESIAN_POINT ( 'NONE',  ( -96.74292637653380211, -5.598654528085803328, -7.705886871421366635 ) ) ;
#21829=CARTESIAN_POINT ( 'NONE',  ( -195.0000000000000000, 9.184850993605132167E-16, -7.499999999999985789 ) ) ;
#21834=CARTESIAN_POINT ( 'NONE',  ( -110.2449999999999903, -4.716976649647093289, -6.492361379858945902 ) ) ;
#21836=CARTESIAN_POINT ( 'NONE',  ( -89.54499999999998749, -7.632228543268600340, -2.479861379858950166 ) ) ;
#21844=CARTESIAN_POINT ( 'NONE',  ( -123.4429263765338192, -1.166476076187852838E-15, -9.524999999999991473 ) ) ;
#21847=CARTESIAN_POINT ( 'NONE',  ( -143.6949999999999932, -8.437984349512085203, 5.166775262442717831E-16 ) ) ;
#21861=CARTESIAN_POINT ( 'NONE',  ( -129.5070736234661695, 8.102448949553176405, 5.886773742842740909 ) ) ;
#21862=CARTESIAN_POINT ( 'NONE',  ( -51.05707362346617373, 0.000000000000000000, 9.524999999999991473 ) ) ;
#21865=CARTESIAN_POINT ( 'NONE',  ( -138.0549999999999784, -9.827790563157499189E-16, -8.024999999999991473 ) ) ;
#21880=CARTESIAN_POINT ( 'NONE',  ( -67.10499999999998977, -6.826472737025113702, 4.959722759717902107 ) ) ;
#21881=CARTESIAN_POINT ( 'NONE',  ( -119.0949999999999847, -2.607480562269071545, -8.024999999999991473 ) ) ;
#21890=PLANE ( 'NONE',  #44470 ) ;
#21895=CARTESIAN_POINT ( 'NONE',  ( -173.0049999999999670, 6.826472737025116366, 4.959722759717898555 ) ) ;
#21896=ORIENTED_EDGE ( 'NONE', *, *, #69308, .T. ) ;
#21900=CARTESIAN_POINT ( 'NONE',  ( -76.94292637653380496, 0.000000000000000000, 9.524999999999991473 ) ) ;
#21904=CARTESIAN_POINT ( 'NONE',  ( -87.65499999999998693, -7.632228543268600340, -2.479861379858950166 ) ) ;
#21910=CARTESIAN_POINT ( 'NONE',  ( -63.35707362346617089, 5.598654528085804216, 7.705886871421366635 ) ) ;
#21921=CARTESIAN_POINT ( 'NONE',  ( -105.3549999999999898, -4.716976649647093289, -6.492361379858945902 ) ) ;
#21923=CARTESIAN_POINT ( 'NONE',  ( -120.4449999999999932, 0.000000000000000000, 8.024999999999991473 ) ) ;
#21927=CARTESIAN_POINT ( 'NONE',  ( -160.7929263765338135, -3.094860106618429807, 9.524999999999991473 ) ) ;
#21928=CARTESIAN_POINT ( 'NONE',  ( -180.2949999999999591, -2.607480562269069768, 8.024999999999991473 ) ) ;
#21939=CARTESIAN_POINT ( 'NONE',  ( -80.24292637653380211, 5.598654528085804216, 7.705886871421366635 ) ) ;
#21951=CARTESIAN_POINT ( 'NONE',  ( -176.9050000000000011, 2.607480562269069324, -8.024999999999993250 ) ) ;
#21962=CARTESIAN_POINT ( 'NONE',  ( -90.95499999999999829, -7.632228543268599452, 2.479861379858951054 ) ) ;
#21964=ORIENTED_EDGE ( 'NONE', *, *, #31608, .F. ) ;
#21966=CARTESIAN_POINT ( 'NONE',  ( -72.65707362346617515, 9.058813317711329915, 2.943386871421369566 ) ) ;
#21970=VERTEX_POINT ( 'NONE', #26665 ) ;
#21974=CARTESIAN_POINT ( 'NONE',  ( -65.69499999999999318, -8.437984349512085203, 5.166775262442717831E-16 ) ) ;
#21978=CARTESIAN_POINT ( 'NONE',  ( -138.0570736234661808, 0.000000000000000000, 9.524999999999991473 ) ) ;
#21981=ORIENTED_EDGE ( 'NONE', *, *, #61722, .T. ) ;
#21985=CARTESIAN_POINT ( 'NONE',  ( -112.1049999999999756, -6.826472737025115478, 4.959722759717900331 ) ) ;
#21991=CARTESIAN_POINT ( 'NONE',  ( -159.0570736234661808, 0.000000000000000000, 9.524999999999991473 ) ) ;
#21994=CARTESIAN_POINT ( 'NONE',  ( -92.60707362346619220, -8.102448949553172852, 5.886773742842742685 ) ) ;
#22001=CARTESIAN_POINT ( 'NONE',  ( -144.6549999999999727, -7.632228543268600340, -2.479861379858950166 ) ) ;
#22002=CARTESIAN_POINT ( 'NONE',  ( -86.90707362346618936, -3.094860106618429807, 9.524999999999991473 ) ) ;
#22004=CARTESIAN_POINT ( 'NONE',  ( -146.2449999999999761, -4.716976649647093289, -6.492361379858945902 ) ) ;
#22005=CARTESIAN_POINT ( 'NONE',  ( -136.4949999999999477, 6.826472737025113702, -4.959722759717902107 ) ) ;
#22011=CARTESIAN_POINT ( 'NONE',  ( -54.65499999999997982, -7.632228543268600340, -2.479861379858950166 ) ) ;
#22013=CARTESIAN_POINT ( 'NONE',  ( -56.69499999999998607, -8.437984349512085203, 5.166775262442717831E-16 ) ) ;
#22016=CARTESIAN_POINT ( 'NONE',  ( -103.5570736234661808, -1.166476076187852838E-15, -9.524999999999991473 ) ) ;
#22019=CARTESIAN_POINT ( 'NONE',  ( -109.3429263765338106, -9.058813317711329915, 2.943386871421371787 ) ) ;
#22035=EDGE_LOOP ( 'NONE', ( #49864, #11746, #65479, #507 ) ) ;
#22041=CARTESIAN_POINT ( 'NONE',  ( -120.0570736234661808, 0.000000000000000000, 9.524999999999991473 ) ) ;
#22044=CARTESIAN_POINT ( 'NONE',  ( -95.24499999999997613, -4.716976649647093289, -6.492361379858945902 ) ) ;
#22048=DIRECTION ( 'NONE',  ( -1.000000000000000000, -0.000000000000000000, -0.000000000000000000 ) ) ;
#22064=( BOUNDED_CURVE ( )  B_SPLINE_CURVE ( 2, ( #27669, #880, #49866, #22420, #65334, #66018, #32278, #6564, #53729, #26972, #17178 ),
 .UNSPECIFIED., .F., .F. ) 
 B_SPLINE_CURVE_WITH_KNOTS ( ( 3, 2, 2, 2, 2, 3 ),
 ( 0.6847826086956522174, 0.6869565217391304657, 0.6891304347826087140, 0.6913043478260869623, 0.6934782608695652106, 0.6956521739130434590 ),
 .UNSPECIFIED. ) 
 CURVE ( )  GEOMETRIC_REPRESENTATION_ITEM ( )  RATIONAL_B_SPLINE_CURVE ( ( 1.000000000000000000, 0.9510565162951535312, 1.000000000000000000, 0.9510565162951535312, 1.000000000000000000, 0.9510565162951535312, 1.000000000000000000, 0.9510565162951535312, 1.000000000000000000, 0.9510565162951535312, 1.000000000000000000 ) ) 
 REPRESENTATION_ITEM ( '' )  );
#22066=CARTESIAN_POINT ( 'NONE',  ( -68.99292637653380211, 8.102448949553172852, -5.886773742842744461 ) ) ;
#22074=CARTESIAN_POINT ( 'NONE',  ( -170.3049999999999784, 8.437984349512085203, -1.550032578732815448E-15 ) ) ;
#22078=CARTESIAN_POINT ( 'NONE',  ( -170.8449999999999989, -7.632228543268599452, 2.479861379858951054 ) ) ;
#22079=CARTESIAN_POINT ( 'NONE',  ( -167.6949999999999648, -8.437984349512086979, 5.166775262442717831E-16 ) ) ;
#22084=CARTESIAN_POINT ( 'NONE',  ( -78.95499999999998408, -7.632228543268599452, 2.479861379858951054 ) ) ;
#22087=CYLINDRICAL_SURFACE ( 'NONE', #57351, 9.524999999999991473 ) ;
#22089=CARTESIAN_POINT ( 'NONE',  ( -83.84499999999998465, -7.632228543268599452, 2.479861379858951054 ) ) ;
#22093=CARTESIAN_POINT ( 'NONE',  ( -176.8429263765338249, 9.058813317711329915, -2.943386871421373119 ) ) ;
#22115=CARTESIAN_POINT ( 'NONE',  ( -112.5549999999999926, 0.000000000000000000, 8.024999999999991473 ) ) ;
#22121=CARTESIAN_POINT ( 'NONE',  ( -56.09292637653378222, 3.094860106618433360, 9.524999999999991473 ) ) ;
#22135=FACE_OUTER_BOUND ( 'NONE', #37888, .T. ) ;
#22136=CARTESIAN_POINT ( 'NONE',  ( -104.8429263765338106, 9.058813317711329915, -2.943386871421373119 ) ) ;
#22140=CARTESIAN_POINT ( 'NONE',  ( -48.59292637653380353, -3.094860106618431139, -9.524999999999991473 ) ) ;
#22143=CARTESIAN_POINT ( 'NONE',  ( -145.7050000000000125, 2.607480562269073321, 8.024999999999991473 ) ) ;
#22151=ORIENTED_EDGE ( 'NONE', *, *, #47294, .F. ) ;
#22153=FACE_OUTER_BOUND ( 'NONE', #9463, .T. ) ;
#22156=CARTESIAN_POINT ( 'NONE',  ( -53.15499999999997982, 7.632228543268600340, 2.479861379858949277 ) ) ;
#22164=ORIENTED_EDGE ( 'NONE', *, *, #157, .F. ) ;
#22175=CARTESIAN_POINT ( 'NONE',  ( -106.1949999999999932, 8.437984349512086979, -1.550032578732815448E-15 ) ) ;
#22177=CARTESIAN_POINT ( 'NONE',  ( -90.14499999999999602, -4.716976649647092401, 6.492361379858946790 ) ) ;
#22186=CARTESIAN_POINT ( 'NONE',  ( -127.6429263765337936, -5.598654528085801552, 7.705886871421367523 ) ) ;
#22187=CARTESIAN_POINT ( 'NONE',  ( -145.9449999999999932, -9.827790563157499189E-16, -8.024999999999991473 ) ) ;
#22195=CARTESIAN_POINT ( 'NONE',  ( -130.2570736234661695, 5.598654528085800663, -7.705886871421367523 ) ) ;
#22197=CARTESIAN_POINT ( 'NONE',  ( -117.2929263765346519, 3.094860106604310879, -9.525000000010253487 ) ) ;
#22201=CARTESIAN_POINT ( 'NONE',  ( -138.5049999999999955, -6.826472737025113702, -4.959722759717900331 ) ) ;
#22214=CARTESIAN_POINT ( 'NONE',  ( -95.30707362346615241, -10.01517768586948698, 6.132527647946031529E-16 ) ) ;
#22216=CARTESIAN_POINT ( 'NONE',  ( -54.05499999999999261, -9.827790563157499189E-16, -8.024999999999991473 ) ) ;
#22217=CARTESIAN_POINT ( 'NONE',  ( -120.8949999999999960, 6.826472737025116366, 4.959722759717898555 ) ) ;
#22218=DIRECTION ( 'NONE',  ( 0.000000000000000000, 0.000000000000000000, 1.000000000000000000 ) ) ;
#22228=CARTESIAN_POINT ( 'NONE',  ( -170.0049999999999955, 6.826472737025116366, 4.959722759717898555 ) ) ;
#22230=CARTESIAN_POINT ( 'NONE',  ( -87.65707362346617515, 9.058813317711329915, 2.943386871421369566 ) ) ;
#22232=CARTESIAN_POINT ( 'NONE',  ( -52.94292637653380496, 0.000000000000000000, 9.524999999999991473 ) ) ;
#22239=CARTESIAN_POINT ( 'NONE',  ( -82.70499999999999829, 2.607480562269073321, 8.024999999999991473 ) ) ;
#22245=CARTESIAN_POINT ( 'NONE',  ( -61.55707362346617373, -1.166476076187852838E-15, -9.524999999999991473 ) ) ;
#22248=CARTESIAN_POINT ( 'NONE',  ( -81.44292637653380496, -1.166476076187852838E-15, -9.524999999999991473 ) ) ;
#22254=CARTESIAN_POINT ( 'NONE',  ( -100.2549999999999812, -4.716976649647092401, 6.492361379858946790 ) ) ;
#22256=CARTESIAN_POINT ( 'NONE',  ( -119.5449999999999875, -7.632228543268600340, -2.479861379858950166 ) ) ;
#22262=CARTESIAN_POINT ( 'NONE',  ( -150.1429263765338078, 5.598654528085800663, -7.705886871421367523 ) ) ;
#22263=CARTESIAN_POINT ( 'NONE',  ( -172.0450000000000159, 7.632228543268600340, 2.479861379858949277 ) ) ;
#22270=CARTESIAN_POINT ( 'NONE',  ( -64.79292637653381348, -3.094860106618429807, 9.524999999999991473 ) ) ;
#22276=ORIENTED_EDGE ( 'NONE', *, *, #13911, .F. ) ;
#22277=CARTESIAN_POINT ( 'NONE',  ( -171.5049999999999670, -6.826472737025113702, -4.959722759717900331 ) ) ;
#22281=CARTESIAN_POINT ( 'NONE',  ( -195.0000000000000000, 0.000000000000000000, 0.000000000000000000 ) ) ;
#22289=CARTESIAN_POINT ( 'NONE',  ( -81.35499999999998977, -4.716976649647093289, -6.492361379858945902 ) ) ;
#22295=CARTESIAN_POINT ( 'NONE',  ( -114.0570736234661808, 0.000000000000000000, 9.524999999999991473 ) ) ;
#22299=CARTESIAN_POINT ( 'NONE',  ( -60.29499999999999460, -2.607480562269069768, 8.024999999999991473 ) ) ;
#22300=EDGE_LOOP ( 'NONE', ( #69370, #45172, #1840, #4013 ) ) ;
#22307=ORIENTED_EDGE ( 'NONE', *, *, #54623, .T. ) ;
#22309=DIRECTION ( 'NONE',  ( 0.000000000000000000, 0.000000000000000000, 1.000000000000000000 ) ) ;
#22315=CARTESIAN_POINT ( 'NONE',  ( -116.0049999999999955, 6.826472737025116366, 4.959722759717898555 ) ) ;
#22323=CARTESIAN_POINT ( 'NONE',  ( -151.8570736234661638, -5.598654528085803328, -7.705886871421366635 ) ) ;
#22326=CARTESIAN_POINT ( 'NONE',  ( -97.70707362346617231, -3.094860106618431139, -9.524999999999991473 ) ) ;
#22336=CARTESIAN_POINT ( 'NONE',  ( -133.2549999999999955, -4.716976649647092401, 6.492361379858946790 ) ) ;
#22339=CARTESIAN_POINT ( 'NONE',  ( -145.3449999999999989, 7.632228543268599452, -2.479861379858951942 ) ) ;
#22342=CARTESIAN_POINT ( 'NONE',  ( -132.8949999999999818, 6.826472737025115478, 4.959722759717899443 ) ) ;
#22348=CARTESIAN_POINT ( 'NONE',  ( -47.90499999999997272, 2.607480562269068880, -8.024999999999993250 ) ) ;
#22349=CARTESIAN_POINT ( 'NONE',  ( -59.39499999999998892, -6.826472737025115478, -4.959722759717899443 ) ) ;
#22355=CARTESIAN_POINT ( 'NONE',  ( -76.10707362346617799, 8.102448949553172852, -5.886773742842744461 ) ) ;
#22356=CARTESIAN_POINT ( 'NONE',  ( -103.7929263765337851, -3.094860106618429807, 9.524999999999991473 ) ) ;
#22360=CARTESIAN_POINT ( 'NONE',  ( -163.1070736234661354, 8.102448949553172852, -5.886773742842744461 ) ) ;
#22375=CARTESIAN_POINT ( 'NONE',  ( -116.6070736234661780, -8.102448949553174629, 5.886773742842742685 ) ) ;
#22381=CARTESIAN_POINT ( 'NONE',  ( -86.84499999999998465, -7.632228543268599452, 2.479861379858951054 ) ) ;
#22393=EDGE_CURVE ( 'NONE', #35268, #30333, #8291, .T. ) ;
#22400=CARTESIAN_POINT ( 'NONE',  ( -177.9570736234661865, 9.058813317711329915, -2.943386871421373119 ) ) ;
#22412=CARTESIAN_POINT ( 'NONE',  ( -158.4549999999999841, 7.632228543268599452, -2.479861379858951942 ) ) ;
#22415=CARTESIAN_POINT ( 'NONE',  ( -172.1949999999999648, 8.437984349512085203, -1.550032578732815448E-15 ) ) ;
#22416=CARTESIAN_POINT ( 'NONE',  ( -159.2949999999999875, -2.607480562269069768, 8.024999999999991473 ) ) ;
#22420=CARTESIAN_POINT ( 'NONE',  ( -89.99292637653380211, 8.102448949553172852, -5.886773742842744461 ) ) ;
#22424=CARTESIAN_POINT ( 'NONE',  ( -86.45499999999998408, 7.632228543268599452, -2.479861379858951942 ) ) ;
#22425=CARTESIAN_POINT ( 'NONE',  ( -168.5070736234661695, 8.102448949553176405, 5.886773742842740909 ) ) ;
#22428=CARTESIAN_POINT ( 'NONE',  ( -80.24499999999997613, -4.716976649647093289, -6.492361379858945902 ) ) ;
#22441=AXIS2_PLACEMENT_3D ( 'NONE', #59160, #374, #16644 ) ;
#22443=CARTESIAN_POINT ( 'NONE',  ( -135.0570736234661808, 0.000000000000000000, 9.524999999999991473 ) ) ;
#22455=VECTOR ( 'NONE', #20161, 1000.000000000000000 ) ;
#22459=CARTESIAN_POINT ( 'NONE',  ( -114.6549999999999869, -7.632228543268600340, -2.479861379858950166 ) ) ;
#22469=( BOUNDED_CURVE ( )  B_SPLINE_CURVE ( 2, ( #32925, #1879, #59986, #22360, #44892, #38231, #33267, #39262, #23389, #27609, #50152 ),
 .UNSPECIFIED., .F., .F. ) 
 B_SPLINE_CURVE_WITH_KNOTS ( ( 3, 2, 2, 2, 2, 3 ),
 ( 0.1413043478260837538, 0.1434782608695619466, 0.1456521739130400839, 0.1478260869565182767, 0.1499999999999964140, 0.1521739130434746068 ),
 .UNSPECIFIED. ) 
 CURVE ( )  GEOMETRIC_REPRESENTATION_ITEM ( )  RATIONAL_B_SPLINE_CURVE ( ( 1.000000000000071720, 0.9510565162950815887, 1.000000000000000000, 0.9510565162951535312, 1.000000000000000000, 0.9510565162951535312, 1.000000000000000000, 0.9510565162951535312, 1.000000000000000000, 0.9510565162952360208, 0.9999999999999175104 ) ) 
 REPRESENTATION_ITEM ( '' )  );
#22479=DIRECTION ( 'NONE',  ( 0.000000000000000000, 0.000000000000000000, 1.000000000000000000 ) ) ;
#22487=CARTESIAN_POINT ( 'NONE',  ( -51.89292637653380069, -8.102448949553172852, -5.886773742842741797 ) ) ;
#22491=CARTESIAN_POINT ( 'NONE',  ( -158.7570736234661979, -5.598654528085801552, 7.705886871421367523 ) ) ;
#22492=CARTESIAN_POINT ( 'NONE',  ( -142.5549999999999784, 0.000000000000000000, 8.024999999999991473 ) ) ;
#22504=CARTESIAN_POINT ( 'NONE',  ( -51.35707362346617089, 5.598654528085804216, 7.705886871421366635 ) ) ;
#22505=CARTESIAN_POINT ( 'NONE',  ( -52.55499999999999261, 0.000000000000000000, 8.024999999999991473 ) ) ;
#22513=CARTESIAN_POINT ( 'NONE',  ( -128.5429263765338135, 9.058813317711329915, 2.943386871421369566 ) ) ;
#22522=CARTESIAN_POINT ( 'NONE',  ( -105.4449999999999790, 0.000000000000000000, 8.024999999999991473 ) ) ;
#22524=CARTESIAN_POINT ( 'NONE',  ( -79.49499999999999034, 6.826472737025113702, -4.959722759717902107 ) ) ;
#22531=CARTESIAN_POINT ( 'NONE',  ( -124.7929263765337851, -3.094860106618429807, 9.524999999999991473 ) ) ;
#22532=CARTESIAN_POINT ( 'NONE',  ( -142.7949999999999875, 2.607480562269068880, -8.024999999999993250 ) ) ;
#22542=CARTESIAN_POINT ( 'NONE',  ( -172.5570736234661808, -1.166476076187852838E-15, -9.524999999999991473 ) ) ;
#22544=CARTESIAN_POINT ( 'NONE',  ( -50.15707362346616094, -9.058813317711329915, -2.943386871421370898 ) ) ;
#22547=CARTESIAN_POINT ( 'NONE',  ( -142.8550000000000182, 4.716976649647094177, 6.492361379858945902 ) ) ;
#22549=ORIENTED_EDGE ( 'NONE', *, *, #52281, .F. ) ;
#22563=CARTESIAN_POINT ( 'NONE',  ( -50.45499999999996987, 7.632228543268599452, -2.479861379858951942 ) ) ;
#22564=CARTESIAN_POINT ( 'NONE',  ( -120.2949999999999733, -2.607480562269069768, 8.024999999999991473 ) ) ;
#22577=CARTESIAN_POINT ( 'NONE',  ( -171.6550000000000011, -7.632228543268600340, -2.479861379858950166 ) ) ;
#22581=( BOUNDED_CURVE ( )  B_SPLINE_CURVE ( 2, ( #54712, #59286, #6886, #22375, #17135, #27963, #38252, #37915, #1559, #50169, #7246 ),
 .UNSPECIFIED., .F., .F. ) 
 B_SPLINE_CURVE_WITH_KNOTS ( ( 3, 2, 2, 2, 2, 3 ),
 ( 0.4782608695652061370, 0.4804347826086843298, 0.4826086956521625226, 0.4847826086956407710, 0.4869565217391190193, 0.4891304347825972121 ),
 .UNSPECIFIED. ) 
 CURVE ( )  GEOMETRIC_REPRESENTATION_ITEM ( )  RATIONAL_B_SPLINE_CURVE ( ( 1.000000000000253797, 0.9510565162948998452, 1.000000000000000000, 0.9510565162951535312, 1.000000000000000000, 0.9510565162951535312, 1.000000000000000000, 0.9510565162951535312, 1.000000000000000000, 0.9510565162954122131, 0.9999999999997413180 ) ) 
 REPRESENTATION_ITEM ( '' )  );
#22588=CARTESIAN_POINT ( 'NONE',  ( -78.44292637653380496, -1.166476076187852838E-15, -9.524999999999991473 ) ) ;
#22593=CARTESIAN_POINT ( 'NONE',  ( -82.40500000000000114, -2.607480562269069768, 8.024999999999991473 ) ) ;
#22599=CARTESIAN_POINT ( 'NONE',  ( -55.85707362346617799, -5.598654528085803328, -7.705886871421366635 ) ) ;
#22606=CARTESIAN_POINT ( 'NONE',  ( -104.6050000000000040, 6.826472737025113702, -4.959722759717902107 ) ) ;
#22608=CARTESIAN_POINT ( 'NONE',  ( -116.6949999999999790, -8.437984349512085203, 5.166775262442717831E-16 ) ) ;
#22611=CARTESIAN_POINT ( 'NONE',  ( -18.05403742664741529, 11.32513715180358993, -3.972212260121688931 ) ) ;
#22612=CARTESIAN_POINT ( 'NONE',  ( -156.8929263765338362, -8.102448949553172852, -5.886773742842741797 ) ) ;
#22613=CARTESIAN_POINT ( 'NONE',  ( -180.7449999999999761, 4.716976649647094177, 6.492361379858945902 ) ) ;
#22621=CARTESIAN_POINT ( 'NONE',  ( -67.64292637653379359, -5.598654528085801552, 7.705886871421367523 ) ) ;
#22623=LINE ( 'NONE', #65173, #52076 ) ;
#22631=VECTOR ( 'NONE', #11340, 1000.000000000000000 ) ;
#22633=CARTESIAN_POINT ( 'NONE',  ( -169.5549999999999784, 0.000000000000000000, 8.024999999999991473 ) ) ;
#22644=CARTESIAN_POINT ( 'NONE',  ( -80.90499999999998693, 2.607480562269069324, -8.024999999999993250 ) ) ;
#22655=CARTESIAN_POINT ( 'NONE',  ( -63.14499999999998181, -4.716976649647092401, 6.492361379858946790 ) ) ;
#22668=CARTESIAN_POINT ( 'NONE',  ( -112.4050000000000011, -2.607480562269069768, 8.024999999999991473 ) ) ;
#22669=ORIENTED_EDGE ( 'NONE', *, *, #52775, .T. ) ;
#22675=CARTESIAN_POINT ( 'NONE',  ( -146.3070736234662093, -10.01517768586948698, 6.132527647946031529E-16 ) ) ;
#22677=CARTESIAN_POINT ( 'NONE',  ( -98.75707362346616947, -5.598654528085801552, 7.705886871421367523 ) ) ;
#22687=CARTESIAN_POINT ( 'NONE',  ( -126.9549999999999841, -7.632228543268599452, 2.479861379858951054 ) ) ;
#22689=CARTESIAN_POINT ( 'NONE',  ( -146.6929263765337623, 10.01517768586948698, -1.839758294383808966E-15 ) ) ;
#22691=CARTESIAN_POINT ( 'NONE',  ( -148.7950000000000159, 2.607480562269068880, -8.024999999999993250 ) ) ;
#22692=CARTESIAN_POINT ( 'NONE',  ( -124.4949999999999761, 6.826472737025113702, -4.959722759717902107 ) ) ;
#22696=DIRECTION ( 'NONE',  ( -0.7071067811865425767, -0.000000000000000000, -0.7071067811865525687 ) ) ;
#22697=CARTESIAN_POINT ( 'NONE',  ( -195.0000000000000000, 0.000000000000000000, 9.524999999999991473 ) ) ;
#22699=CARTESIAN_POINT ( 'NONE',  ( -183.8929263765337794, -8.102448949553172852, -5.886773742842741797 ) ) ;
#22701=CARTESIAN_POINT ( 'NONE',  ( -57.74499999999999034, 4.716976649647094177, 6.492361379858945902 ) ) ;
#22705=CARTESIAN_POINT ( 'NONE',  ( -195.0000000000000000, 1.166476076187852838E-15, -9.524999999999991473 ) ) ;
#22708=CARTESIAN_POINT ( 'NONE',  ( -95.24292637653381632, 5.598654528085804216, 7.705886871421366635 ) ) ;
#22714=CARTESIAN_POINT ( 'NONE',  ( -99.35707362346617799, 5.598654528085804216, 7.705886871421366635 ) ) ;
#22739=CARTESIAN_POINT ( 'NONE',  ( -87.89499999999998181, 6.826472737025116366, 4.959722759717898555 ) ) ;
#22740=ORIENTED_EDGE ( 'NONE', *, *, #50219, .T. ) ;
#22749=CARTESIAN_POINT ( 'NONE',  ( -67.94292637653380496, 0.000000000000000000, 9.524999999999991473 ) ) ;
#22757=CARTESIAN_POINT ( 'NONE',  ( -182.1570736234661751, -9.058813317711329915, -2.943386871421370898 ) ) ;
#22761=CARTESIAN_POINT ( 'NONE',  ( -68.09292637653378222, 3.094860106618433360, 9.524999999999991473 ) ) ;
#22770=CARTESIAN_POINT ( 'NONE',  ( -161.6050000000000182, 6.826472737025113702, -4.959722759717902107 ) ) ;
#22773=CARTESIAN_POINT ( 'NONE',  ( -176.2449999999999761, -4.716976649647093289, -6.492361379858945902 ) ) ;
#22776=CARTESIAN_POINT ( 'NONE',  ( -160.0449999999999875, 7.632228543268600340, 2.479861379858949277 ) ) ;
#22782=CARTESIAN_POINT ( 'NONE',  ( -77.00499999999999545, 6.826472737025116366, 4.959722759717898555 ) ) ;
#22786=CARTESIAN_POINT ( 'NONE',  ( -67.49499999999999034, 6.826472737025113702, -4.959722759717902107 ) ) ;
#22815=CARTESIAN_POINT ( 'NONE',  ( -111.9549999999999841, -7.632228543268599452, 2.479861379858951054 ) ) ;
#22842=CARTESIAN_POINT ( 'NONE',  ( -50.39292637653380780, 8.102448949553176405, 5.886773742842740909 ) ) ;
#22845=CYLINDRICAL_SURFACE ( 'NONE', #69165, 9.524999999999991473 ) ;
#22846=CARTESIAN_POINT ( 'NONE',  ( -132.5049999999999670, -6.826472737025115478, -4.959722759717899443 ) ) ;
#22853=CARTESIAN_POINT ( 'NONE',  ( -107.7570736234661695, -5.598654528085801552, 7.705886871421367523 ) ) ;
#22860=CARTESIAN_POINT ( 'NONE',  ( -56.00499999999996703, 6.826472737025116366, 4.959722759717898555 ) ) ;
#22873=CARTESIAN_POINT ( 'NONE',  ( -109.0449999999999875, 7.632228543268600340, 2.479861379858949277 ) ) ;
#22875=CARTESIAN_POINT ( 'NONE',  ( -80.54499999999998749, -7.632228543268600340, -2.479861379858950166 ) ) ;
#22889=CARTESIAN_POINT ( 'NONE',  ( -123.8929263765337794, -8.102448949553172852, -5.886773742842741797 ) ) ;
#22891=CARTESIAN_POINT ( 'NONE',  ( -134.2450000000000045, -4.716976649647093289, -6.492361379858945902 ) ) ;
#22895=CARTESIAN_POINT ( 'NONE',  ( -48.29499999999997328, -2.607480562269069768, 8.024999999999991473 ) ) ;
#22896=DIRECTION ( 'NONE',  ( -1.000000000000000000, -0.000000000000000000, -0.000000000000000000 ) ) ;
#22909=CARTESIAN_POINT ( 'NONE',  ( -143.7549999999999955, 4.716976649647091513, -6.492361379858946790 ) ) ;
#22922=CARTESIAN_POINT ( 'NONE',  ( -58.40499999999997982, -2.607480562269069768, 8.024999999999991473 ) ) ;
#22924=ORIENTED_EDGE ( 'NONE', *, *, #177, .T. ) ;
#22936=CARTESIAN_POINT ( 'NONE',  ( -176.6049999999999898, 6.826472737025113702, -4.959722759717902107 ) ) ;
#22945=CARTESIAN_POINT ( 'NONE',  ( -83.60499999999998977, 6.826472737025113702, -4.959722759717902107 ) ) ;
#22958=CARTESIAN_POINT ( 'NONE',  ( -102.5949999999999704, 2.607480562269073321, 8.024999999999991473 ) ) ;
#22964=CARTESIAN_POINT ( 'NONE',  ( -150.4429263765338192, -1.166476076187852838E-15, -9.524999999999991473 ) ) ;
#22966=CARTESIAN_POINT ( 'NONE',  ( -169.4949999999999761, 6.826472737025113702, -4.959722759717902107 ) ) ;
#22969=LINE ( 'NONE', #18389, #48994 ) ;
#22971=CIRCLE ( 'NONE', #31947, 8.524999999999977263 ) ;
#22976=CARTESIAN_POINT ( 'NONE',  ( -66.14292637653379359, 5.598654528085800663, -7.705886871421367523 ) ) ;
#22986=CARTESIAN_POINT ( 'NONE',  ( -173.9049999999999443, 2.607480562269069324, -8.024999999999993250 ) ) ;
#22989=EDGE_LOOP ( 'NONE', ( #22549, #35054, #61533, #67211 ) ) ;
#22997=( BOUNDED_CURVE ( )  B_SPLINE_CURVE ( 2, ( #49091, #32883, #32503, #64547, #59232, #26860, #54319, #16726, #17072, #1135, #11761 ),
 .UNSPECIFIED., .F., .F. ) 
 B_SPLINE_CURVE_WITH_KNOTS ( ( 3, 2, 2, 2, 2, 3 ),
 ( 0.8043478260869565410, 0.8065217391304347894, 0.8086956521739130377, 0.8108695652173912860, 0.8130434782608695343, 0.8152173913043477826 ),
 .UNSPECIFIED. ) 
 CURVE ( )  GEOMETRIC_REPRESENTATION_ITEM ( )  RATIONAL_B_SPLINE_CURVE ( ( 1.000000000000000000, 0.9510565162951535312, 1.000000000000000000, 0.9510565162951535312, 1.000000000000000000, 0.9510565162951535312, 1.000000000000000000, 0.9510565162951535312, 1.000000000000000000, 0.9510565162951535312, 1.000000000000000000 ) ) 
 REPRESENTATION_ITEM ( '' )  );
#22999=CARTESIAN_POINT ( 'NONE',  ( -87.35499999999998977, -4.716976649647093289, -6.492361379858945902 ) ) ;
#23003=CARTESIAN_POINT ( 'NONE',  ( -92.60707362346617799, -8.102448949553174629, 5.886773742842742685 ) ) ;
#23009=CARTESIAN_POINT ( 'NONE',  ( -66.59499999999999886, 2.607480562269073321, 8.024999999999991473 ) ) ;
#23012=CARTESIAN_POINT ( 'NONE',  ( -49.49292637653378790, -8.102448949553174629, 5.886773742842742685 ) ) ;
#23016=CARTESIAN_POINT ( 'NONE',  ( -52.04499999999998039, 7.632228543268600340, 2.479861379858949277 ) ) ;
#23021=CARTESIAN_POINT ( 'NONE',  ( -116.1550000000000011, 7.632228543268600340, 2.479861379858949277 ) ) ;
#23027=CARTESIAN_POINT ( 'NONE',  ( -146.1570736234662036, -9.058813317711329915, -2.943386871421370898 ) ) ;
#23031=CARTESIAN_POINT ( 'NONE',  ( -86.60707362346619220, -8.102448949553172852, 5.886773742842742685 ) ) ;
#23039=CARTESIAN_POINT ( 'NONE',  ( -127.2550000000000097, -4.716976649647092401, 6.492361379858946790 ) ) ;
#23042=CARTESIAN_POINT ( 'NONE',  ( -133.7949999999999875, 2.607480562269068880, -8.024999999999993250 ) ) ;
#23045=CARTESIAN_POINT ( 'NONE',  ( -130.6449999999999818, 4.716976649647091513, -6.492361379858946790 ) ) ;
#23048=CARTESIAN_POINT ( 'NONE',  ( -146.3070736234662093, -10.01517768586948698, 6.132527647946031529E-16 ) ) ;
#23052=CARTESIAN_POINT ( 'NONE',  ( -178.6429263765338078, -5.598654528085801552, 7.705886871421367523 ) ) ;
#23053=CARTESIAN_POINT ( 'NONE',  ( -58.79499999999998749, 2.607480562269068880, -8.024999999999993250 ) ) ;
#23060=CARTESIAN_POINT ( 'NONE',  ( -95.54292637653379927, 9.058813317711329915, 2.943386871421369566 ) ) ;
#23072=VECTOR ( 'NONE', #51273, 1000.000000000000000 ) ;
#23081=DIRECTION ( 'NONE',  ( -1.000000000000000000, -0.000000000000000000, -0.000000000000000000 ) ) ;
#23089=CARTESIAN_POINT ( 'NONE',  ( -95.99499999999996191, -6.826472737025115478, 4.959722759717900331 ) ) ;
#23103=ORIENTED_EDGE ( 'NONE', *, *, #1612, .T. ) ;
#23104=CARTESIAN_POINT ( 'NONE',  ( -195.0000000000000000, 0.000000000000000000, 0.000000000000000000 ) ) ;
#23108=CARTESIAN_POINT ( 'NONE',  ( -177.2070736234661581, 3.094860106618433360, 9.524999999999991473 ) ) ;
#23111=CARTESIAN_POINT ( 'NONE',  ( -110.9070736234661609, -3.094860106618429807, 9.524999999999991473 ) ) ;
#23123=CARTESIAN_POINT ( 'NONE',  ( -159.9549999999999841, -7.632228543268599452, 2.479861379858951054 ) ) ;
#23126=CARTESIAN_POINT ( 'NONE',  ( -184.0000000000000000, -8.446573402700972011, 1.153699593821606140 ) ) ;
#23127=CARTESIAN_POINT ( 'NONE',  ( -175.6449999999999818, 4.716976649647091513, -6.492361379858946790 ) ) ;
#23130=CARTESIAN_POINT ( 'NONE',  ( -161.6949999999999932, -8.437984349512086979, 5.166775262442717831E-16 ) ) ;
#23135=CARTESIAN_POINT ( 'NONE',  ( -75.05499999999997840, -9.827790563157499189E-16, -8.024999999999991473 ) ) ;
#23138=CARTESIAN_POINT ( 'NONE',  ( -72.89499999999998181, 6.826472737025115478, 4.959722759717899443 ) ) ;
#23144=CARTESIAN_POINT ( 'NONE',  ( -176.0929263765339385, 3.094860106620248352, 9.524999999998673417 ) ) ;
#23160=CARTESIAN_POINT ( 'NONE',  ( -111.0549999999999926, -9.827790563157499189E-16, -8.024999999999991473 ) ) ;
#23166=CARTESIAN_POINT ( 'NONE',  ( -67.85707362346617799, -5.598654528085803328, -7.705886871421366635 ) ) ;
#23173=ADVANCED_FACE ( 'NONE', ( #34729 ), #35092, .T. ) ;
#23176=CARTESIAN_POINT ( 'NONE',  ( -152.3070736234661524, -10.01517768586948698, 6.132527647946031529E-16 ) ) ;
#23187=VERTEX_POINT ( 'NONE', #51625 ) ;
#23190=CARTESIAN_POINT ( 'NONE',  ( -129.6550000000000011, -7.632228543268600340, -2.479861379858950166 ) ) ;
#23199=CYLINDRICAL_SURFACE ( 'NONE', #11492, 9.524999999999991473 ) ;
#23200=B_SPLINE_CURVE_WITH_KNOTS ( 'NONE', 3,
 ( #12039, #23636, #66559, #60556, #61596, #28896, #33838, #55300, #50055, #60916, #13081, #18383, #1788, #34890, #50384, #34535, #55993, #29251, #6413, #28189, #50734, #2478, #23988, #45502, #27845, #49347, #1433, #1069, #22611, #44115, #33501, #65514, #17364, #38830, #60244, #49697, #54932, #6760 ),
 .UNSPECIFIED., .F., .F.,
 ( 4, 2, 2, 2, 2, 2, 2, 2, 2, 2, 2, 2, 2, 2, 2, 2, 2, 2, 4 ),
 ( 3.576224061345498009E-18, 0.0009883658144282647922, 0.001976731628856526115, 0.002965097443284787221, 0.003953463257713048760, 0.004941829072141310300, 0.005930194886569570972, 0.006424377793783702176, 0.006918560700997832512, 0.007906926515426092317, 0.008895292329854354724, 0.009883658144282615396, 0.01087202395871087780, 0.01186038977313913674, 0.01284875558756739915, 0.01334293849478152862, 0.01383712140199565982, 0.01482548721642392743, 0.01581385303085219851 ),
 .UNSPECIFIED. ) ;
#23218=CARTESIAN_POINT ( 'NONE',  ( -95.69499999999997897, -8.437984349512086979, 5.166775262442717831E-16 ) ) ;
#23221=CARTESIAN_POINT ( 'NONE',  ( -77.99499999999997613, -6.826472737025115478, 4.959722759717900331 ) ) ;
#23223=CARTESIAN_POINT ( 'NONE',  ( -147.4429263765338192, -1.166476076187852838E-15, -9.524999999999991473 ) ) ;
#23229=CARTESIAN_POINT ( 'NONE',  ( -124.1929263765338192, -10.01517768586948698, 6.132527647946031529E-16 ) ) ;
#23230=CARTESIAN_POINT ( 'NONE',  ( -140.3950000000000102, -6.826472737025115478, -4.959722759717899443 ) ) ;
#23235=VERTEX_POINT ( 'NONE', #52677 ) ;
#23244=CARTESIAN_POINT ( 'NONE',  ( -144.0549999999999784, -9.827790563157499189E-16, -8.024999999999991473 ) ) ;
#23256=CARTESIAN_POINT ( 'NONE',  ( -53.30499999999998550, 8.437984349512086979, -1.550032578732815448E-15 ) ) ;
#23267=ORIENTED_EDGE ( 'NONE', *, *, #1609, .T. ) ;
#23271=CARTESIAN_POINT ( 'NONE',  ( -159.0550000000000068, -9.827790563157499189E-16, -8.024999999999991473 ) ) ;
#23272=ORIENTED_EDGE ( 'NONE', *, *, #44790, .T. ) ;
#23283=CARTESIAN_POINT ( 'NONE',  ( -75.80499999999997840, -8.437984349512085203, 5.166775262442717831E-16 ) ) ;
#23291=CARTESIAN_POINT ( 'NONE',  ( -52.85707362346617089, -5.598654528085803328, -7.705886871421366635 ) ) ;
#23295=CARTESIAN_POINT ( 'NONE',  ( -104.5449999999999875, -7.632228543268600340, -2.479861379858950166 ) ) ;
#23298=LINE ( 'NONE', #34205, #37068 ) ;
#23299=CARTESIAN_POINT ( 'NONE',  ( -151.0429263765337851, -9.058813317711329915, -2.943386871421370898 ) ) ;
#23301=CARTESIAN_POINT ( 'NONE',  ( -167.3949999999999534, -6.826472737025115478, -4.959722759717899443 ) ) ;
#23309=CARTESIAN_POINT ( 'NONE',  ( -63.59292637653378932, -3.094860106618431139, -9.524999999999991473 ) ) ;
#23318=CARTESIAN_POINT ( 'NONE',  ( -170.7549999999999955, 4.716976649647091513, -6.492361379858946790 ) ) ;
#23328=CARTESIAN_POINT ( 'NONE',  ( -85.25499999999998124, -4.716976649647092401, 6.492361379858946790 ) ) ;
#23331=CARTESIAN_POINT ( 'NONE',  ( -127.1929263765338192, -10.01517768586948698, 6.132527647946031529E-16 ) ) ;
#23337=CARTESIAN_POINT ( 'NONE',  ( -52.49499999999999034, 6.826472737025113702, -4.959722759717902107 ) ) ;
#23344=CARTESIAN_POINT ( 'NONE',  ( -57.44499999999999318, 0.000000000000000000, 8.024999999999991473 ) ) ;
#23349=ADVANCED_FACE ( 'NONE', ( #17808 ), #43208, .T. ) ;
#23350=CARTESIAN_POINT ( 'NONE',  ( -113.1549999999999869, 7.632228543268600340, 2.479861379858949277 ) ) ;
#23355=CARTESIAN_POINT ( 'NONE',  ( -152.6070736234661354, -8.102448949553172852, 5.886773742842742685 ) ) ;
#23359=CARTESIAN_POINT ( 'NONE',  ( -85.55707362346618083, -1.166476076187852838E-15, -9.524999999999991473 ) ) ;
#23368=CARTESIAN_POINT ( 'NONE',  ( -126.3549999999999898, -4.716976649647093289, -6.492361379858945902 ) ) ;
#23371=CARTESIAN_POINT ( 'NONE',  ( -137.2450000000000045, -4.716976649647093289, -6.492361379858945902 ) ) ;
#23372=CARTESIAN_POINT ( 'NONE',  ( -126.2949999999999875, -2.607480562269069768, 8.024999999999991473 ) ) ;
#23375=CARTESIAN_POINT ( 'NONE',  ( -145.7070736234666413, -3.094860106626094787, -9.524999999994424371 ) ) ;
#23378=CARTESIAN_POINT ( 'NONE',  ( -182.0929263765337964, 3.094860106618433360, 9.524999999999991473 ) ) ;
#23379=CARTESIAN_POINT ( 'NONE',  ( -46.94499999999998607, -9.827790563157499189E-16, -8.024999999999991473 ) ) ;
#23385=CARTESIAN_POINT ( 'NONE',  ( -98.99292637653378790, 8.102448949553171076, -5.886773742842744461 ) ) ;
#23388=( BOUNDED_CURVE ( )  B_SPLINE_CURVE ( 2, ( #5311, #43380, #58803, #59129, #26757, #63386, #26430, #47962, #67545, #53855, #27103 ),
 .UNSPECIFIED., .F., .F. ) 
 B_SPLINE_CURVE_WITH_KNOTS ( ( 3, 2, 2, 2, 2, 3 ),
 ( 0.2934782608695583606, 0.2956521739130365534, 0.2978260869565147462, 0.2999999999999929945, 0.3021739130434711873, 0.3043478260869494356 ),
 .UNSPECIFIED. ) 
 CURVE ( )  GEOMETRIC_REPRESENTATION_ITEM ( )  RATIONAL_B_SPLINE_CURVE ( ( 1.000000000000154987, 0.9510565162949985440, 1.000000000000000000, 0.9510565162951535312, 1.000000000000000000, 0.9510565162951535312, 1.000000000000000000, 0.9510565162951535312, 1.000000000000000000, 0.9510565162953135143, 0.9999999999998400169 ) ) 
 REPRESENTATION_ITEM ( '' )  );
#23389=CARTESIAN_POINT ( 'NONE',  ( -162.3570736234661922, 5.598654528085804216, 7.705886871421366635 ) ) ;
#23408=CARTESIAN_POINT ( 'NONE',  ( -90.59499999999999886, 2.607480562269073321, 8.024999999999991473 ) ) ;
#23424=ORIENTED_EDGE ( 'NONE', *, *, #50588, .T. ) ;
#23425=CARTESIAN_POINT ( 'NONE',  ( -15.00000000000000000, -12.00000000000000000, 0.000000000000000000 ) ) ;
#23427=CARTESIAN_POINT ( 'NONE',  ( -176.6070736234661354, -8.102448949553172852, 5.886773742842742685 ) ) ;
#23432=CARTESIAN_POINT ( 'NONE',  ( -116.7570736234661695, -5.598654528085801552, 7.705886871421367523 ) ) ;
#23442=ORIENTED_EDGE ( 'NONE', *, *, #49174, .F. ) ;
#23443=CARTESIAN_POINT ( 'NONE',  ( -163.8549999999999898, 4.716976649647094177, 6.492361379858945902 ) ) ;
#23445=CARTESIAN_POINT ( 'NONE',  ( -160.1950000000000216, 8.437984349512085203, -1.550032578732815448E-15 ) ) ;
#23447=CARTESIAN_POINT ( 'NONE',  ( -153.7450000000000045, 4.716976649647094177, 6.492361379858945902 ) ) ;
#23452=CARTESIAN_POINT ( 'NONE',  ( -72.95499999999999829, -7.632228543268599452, 2.479861379858951054 ) ) ;
#23456=CARTESIAN_POINT ( 'NONE',  ( -69.44499999999999318, 0.000000000000000000, 8.024999999999991473 ) ) ;
#23474=CARTESIAN_POINT ( 'NONE',  ( -132.0570736234661808, 0.000000000000000000, 9.524999999999991473 ) ) ;
#23482=CARTESIAN_POINT ( 'NONE',  ( -98.75499999999999545, 4.716976649647091513, -6.492361379858946790 ) ) ;
#23485=EDGE_CURVE ( 'NONE', #7596, #69443, #18358, .T. ) ;
#23509=CARTESIAN_POINT ( 'NONE',  ( -133.4049999999999443, -2.607480562269069768, 8.024999999999991473 ) ) ;
#23513=AXIS2_PLACEMENT_3D ( 'NONE', #51082, #18381, #55298 ) ;
#23523=CARTESIAN_POINT ( 'NONE',  ( -52.40707362346616804, 3.094860106618428031, -9.524999999999993250 ) ) ;
#23530=CARTESIAN_POINT ( 'NONE',  ( -181.9449999999999932, -9.827790563157499189E-16, -8.024999999999991473 ) ) ;
#23535=CARTESIAN_POINT ( 'NONE',  ( -144.3570736234661638, 5.598654528085804216, 7.705886871421366635 ) ) ;
#23541=FACE_OUTER_BOUND ( 'NONE', #67174, .T. ) ;
#23542=CARTESIAN_POINT ( 'NONE',  ( -98.84499999999998465, -7.632228543268599452, 2.479861379858951054 ) ) ;
#23544=CARTESIAN_POINT ( 'NONE',  ( -76.04499999999998749, 7.632228543268600340, 2.479861379858949277 ) ) ;
#23548=DIRECTION ( 'NONE',  ( 0.000000000000000000, 0.000000000000000000, 1.000000000000000000 ) ) ;
#23553=CARTESIAN_POINT ( 'NONE',  ( -111.8929263765338078, -8.102448949553172852, -5.886773742842741797 ) ) ;
#23554=CARTESIAN_POINT ( 'NONE',  ( -142.0449999999999875, 7.632228543268600340, 2.479861379858949277 ) ) ;
#23561=VERTEX_POINT ( 'NONE', #18502 ) ;
#23572=CARTESIAN_POINT ( 'NONE',  ( -130.5549999999999784, 0.000000000000000000, 8.024999999999991473 ) ) ;
#23578=ORIENTED_EDGE ( 'NONE', *, *, #67628, .F. ) ;
#23585=ORIENTED_EDGE ( 'NONE', *, *, #35279, .F. ) ;
#23588=EDGE_CURVE ( 'NONE', #48074, #37145, #50855, .T. ) ;
#23589=CARTESIAN_POINT ( 'NONE',  ( -57.95499999999997698, -7.632228543268599452, 2.479861379858951054 ) ) ;
#23607=CARTESIAN_POINT ( 'NONE',  ( -122.0070736234661553, -8.102448949553174629, -5.886773742842741797 ) ) ;
#23609=CARTESIAN_POINT ( 'NONE',  ( -161.4549999999999841, 7.632228543268599452, -2.479861379858951942 ) ) ;
#23619=CARTESIAN_POINT ( 'NONE',  ( -79.85499999999997556, 4.716976649647094177, 6.492361379858945902 ) ) ;
#23625=ORIENTED_EDGE ( 'NONE', *, *, #47750, .F. ) ;
#23629=CARTESIAN_POINT ( 'NONE',  ( -107.3949999999999960, -6.826472737025115478, -4.959722759717899443 ) ) ;
#23633=AXIS2_PLACEMENT_3D ( 'NONE', #8785, #67178, #9504 ) ;
#23636=CARTESIAN_POINT ( 'NONE',  ( -15.33454427322983626, 10.90871211463571555, 5.000000000000000888 ) ) ;
#23638=CARTESIAN_POINT ( 'NONE',  ( -150.2929263765338135, 3.094860106618428031, -9.524999999999993250 ) ) ;
#23639=CARTESIAN_POINT ( 'NONE',  ( -170.3950000000000102, -6.826472737025115478, -4.959722759717899443 ) ) ;
#23657=CARTESIAN_POINT ( 'NONE',  ( -166.7049999999999557, 2.607480562269072433, 8.024999999999991473 ) ) ;
#23662=VECTOR ( 'NONE', #5049, 1000.000000000000000 ) ;
#23670=CARTESIAN_POINT ( 'NONE',  ( -83.60499999999998977, 6.826472737025113702, -4.959722759717902107 ) ) ;
#23671=( BOUNDED_CURVE ( )  B_SPLINE_CURVE ( 2, ( #24643, #20068, #10235, #9560, #20435, #47212, #57024, #15530, #40885, #3881, #25358 ),
 .UNSPECIFIED., .F., .F. ) 
 B_SPLINE_CURVE_WITH_KNOTS ( ( 3, 2, 2, 2, 2, 3 ),
 ( 0.4347826086956418368, 0.4369565217391200296, 0.4391304347825982779, 0.4413043478260764707, 0.4434782608695546635, 0.4456521739130328563 ),
 .UNSPECIFIED. ) 
 CURVE ( )  GEOMETRIC_REPRESENTATION_ITEM ( )  RATIONAL_B_SPLINE_CURVE ( ( 1.000000000000232481, 0.9510565162949210505, 1.000000000000000000, 0.9510565162951535312, 1.000000000000000000, 0.9510565162951535312, 1.000000000000000000, 0.9510565162951535312, 1.000000000000000000, 0.9510565162953922291, 0.9999999999997613020 ) ) 
 REPRESENTATION_ITEM ( '' )  );
#23682=DIRECTION ( 'NONE',  ( -1.000000000000000000, -0.000000000000000000, -0.000000000000000000 ) ) ;
#23684=CARTESIAN_POINT ( 'NONE',  ( -55.34499999999997755, 7.632228543268599452, -2.479861379858951942 ) ) ;
#23694=CARTESIAN_POINT ( 'NONE',  ( -52.19499999999999318, 8.437984349512086979, -1.550032578732815448E-15 ) ) ;
#23696=VERTEX_POINT ( 'NONE', #58209 ) ;
#23698=CARTESIAN_POINT ( 'NONE',  ( -101.4549999999999841, 7.632228543268599452, -2.479861379858951942 ) ) ;
#23704=CARTESIAN_POINT ( 'NONE',  ( -148.7070736234662149, -3.094860106618431139, -9.524999999999991473 ) ) ;
#23709=CARTESIAN_POINT ( 'NONE',  ( -87.65707362346617515, 9.058813317711329915, 2.943386871421369566 ) ) ;
#23716=CARTESIAN_POINT ( 'NONE',  ( -118.5549999999999926, 0.000000000000000000, 8.024999999999991473 ) ) ;
#23717=CARTESIAN_POINT ( 'NONE',  ( -164.8429263765337964, 9.058813317711329915, -2.943386871421373119 ) ) ;
#23719=CARTESIAN_POINT ( 'NONE',  ( -131.9949999999999477, -6.826472737025115478, 4.959722759717900331 ) ) ;
#23720=CARTESIAN_POINT ( 'NONE',  ( -131.5449999999999875, -7.632228543268600340, -2.479861379858950166 ) ) ;
#23727=CARTESIAN_POINT ( 'NONE',  ( -183.7429263765338021, -5.598654528085803328, -7.705886871421366635 ) ) ;
#23734=CARTESIAN_POINT ( 'NONE',  ( -93.59292637653378222, -3.094860106618431139, -9.524999999999991473 ) ) ;
#23763=CARTESIAN_POINT ( 'NONE',  ( -83.24499999999999034, -4.716976649647093289, -6.492361379858945902 ) ) ;
#23769=ORIENTED_EDGE ( 'NONE', *, *, #44790, .F. ) ;
#23771=CARTESIAN_POINT ( 'NONE',  ( -75.44292637653379074, -1.166476076187852838E-15, -9.524999999999991473 ) ) ;
#23774=ORIENTED_EDGE ( 'NONE', *, *, #38570, .F. ) ;
#23781=CARTESIAN_POINT ( 'NONE',  ( -175.1070736234661922, 8.102448949553171076, -5.886773742842744461 ) ) ;
#23785=CARTESIAN_POINT ( 'NONE',  ( -116.9070736234661894, -3.094860106618429807, 9.524999999999991473 ) ) ;
#23797=CARTESIAN_POINT ( 'NONE',  ( -160.8549999999999898, 4.716976649647094177, 6.492361379858945902 ) ) ;
#23801=CARTESIAN_POINT ( 'NONE',  ( -164.0949999999999989, -2.607480562269071545, -8.024999999999991473 ) ) ;
#23802=CARTESIAN_POINT ( 'NONE',  ( -160.6449999999999818, 4.716976649647091513, -6.492361379858946790 ) ) ;
#23804=( BOUNDED_CURVE ( )  B_SPLINE_CURVE ( 2, ( #50675, #2417, #61906, #5148, #42494, #63559, #16453, #37216, #31178, #64929, #26594 ),
 .UNSPECIFIED., .F., .F. ) 
 B_SPLINE_CURVE_WITH_KNOTS ( ( 3, 2, 2, 2, 2, 3 ),
 ( 0.5978260869565075186, 0.5999999999999856559, 0.6021739130434639042, 0.6043478260869420415, 0.6065217391304204009, 0.6086956521738985382 ),
 .UNSPECIFIED. ) 
 CURVE ( )  GEOMETRIC_REPRESENTATION_ITEM ( )  RATIONAL_B_SPLINE_CURVE ( ( 1.000000000000319966, 0.9510565162948335649, 1.000000000000000000, 0.9510565162951535312, 1.000000000000000000, 0.9510565162951535312, 1.000000000000000000, 0.9510565162951535312, 1.000000000000000000, 0.9510565162954809360, 0.9999999999996725952 ) ) 
 REPRESENTATION_ITEM ( '' )  );
#23807=CARTESIAN_POINT ( 'NONE',  ( -72.20499999999998408, -2.607480562269071545, -8.024999999999991473 ) ) ;
#23811=CARTESIAN_POINT ( 'NONE',  ( -72.44499999999997897, 0.000000000000000000, 8.024999999999991473 ) ) ;
#23844=CARTESIAN_POINT ( 'NONE',  ( -195.0000000000000000, 0.000000000000000000, 0.000000000000000000 ) ) ;
#23845=CARTESIAN_POINT ( 'NONE',  ( -113.8449999999999847, -7.632228543268599452, 2.479861379858951054 ) ) ;
#23846=VERTEX_POINT ( 'NONE', #46588 ) ;
#23849=CARTESIAN_POINT ( 'NONE',  ( -9.999969304761462396, -12.00001278968254148, -0.1637141617949805783 ) ) ;
#23865=CARTESIAN_POINT ( 'NONE',  ( -130.5549999999999784, 0.000000000000000000, 8.024999999999991473 ) ) ;
#23870=FACE_OUTER_BOUND ( 'NONE', #44591, .T. ) ;
#23871=CARTESIAN_POINT ( 'NONE',  ( -106.5570736234661666, -1.166476076187852838E-15, -9.524999999999991473 ) ) ;
#23874=VERTEX_POINT ( 'NONE', #63741 ) ;
#23882=DIRECTION ( 'NONE',  ( -1.000000000000000000, -0.000000000000000000, -0.000000000000000000 ) ) ;
#23883=CARTESIAN_POINT ( 'NONE',  ( -59.90707362346616094, -3.094860106618429807, 9.524999999999991473 ) ) ;
#23885=CARTESIAN_POINT ( 'NONE',  ( -177.9570736234661865, 9.058813317711329915, -2.943386871421373119 ) ) ;
#23888=CARTESIAN_POINT ( 'NONE',  ( -161.9070736234664594, -3.094860106613992912, 9.525000000003217338 ) ) ;
#23889=CARTESIAN_POINT ( 'NONE',  ( -94.94292637653380496, 0.000000000000000000, 9.524999999999991473 ) ) ;
#23891=CARTESIAN_POINT ( 'NONE',  ( -98.30499999999997840, 8.437984349512085203, -1.550032578732815448E-15 ) ) ;
#23895=CARTESIAN_POINT ( 'NONE',  ( -100.7950000000000017, 2.607480562269069324, -8.024999999999993250 ) ) ;
#23897=CARTESIAN_POINT ( 'NONE',  ( -77.09499999999997044, -2.607480562269071545, -8.024999999999991473 ) ) ;
#23901=DIRECTION ( 'NONE',  ( 0.000000000000000000, 0.000000000000000000, -1.000000000000000000 ) ) ;
#23908=CARTESIAN_POINT ( 'NONE',  ( -116.6929263765337907, 10.01517768586948698, -1.839758294383808571E-15 ) ) ;
#23910=CARTESIAN_POINT ( 'NONE',  ( -139.3449999999999989, 7.632228543268599452, -2.479861379858951942 ) ) ;
#23920=EDGE_CURVE ( 'NONE', #3684, #27751, #20854, .T. ) ;
#23923=CARTESIAN_POINT ( 'NONE',  ( -135.0549999999999784, -9.827790563157499189E-16, -8.024999999999991473 ) ) ;
#23927=CARTESIAN_POINT ( 'NONE',  ( -83.69292637653379074, 10.01517768586948698, -1.839758294383808966E-15 ) ) ;
#23937=CARTESIAN_POINT ( 'NONE',  ( -47.90499999999997272, 2.607480562269069324, -8.024999999999993250 ) ) ;
#23954=CARTESIAN_POINT ( 'NONE',  ( -164.3049999999999784, 8.437984349512085203, -1.550032578732815448E-15 ) ) ;
#23962=ORIENTED_EDGE ( 'NONE', *, *, #11768, .F. ) ;
#23966=CARTESIAN_POINT ( 'NONE',  ( -73.40500000000000114, -2.607480562269069768, 8.024999999999991473 ) ) ;
#23971=CARTESIAN_POINT ( 'NONE',  ( -151.2570736234661979, 5.598654528085800663, -7.705886871421367523 ) ) ;
#23982=CARTESIAN_POINT ( 'NONE',  ( -104.3949999999999960, -6.826472737025115478, -4.959722759717899443 ) ) ;
#23988=CARTESIAN_POINT ( 'NONE',  ( -19.74070358558185490, 11.89371749334803141, -1.623204134912098917 ) ) ;
#23989=EDGE_CURVE ( 'NONE', #55259, #63576, #8901, .T. ) ;
#23990=CARTESIAN_POINT ( 'NONE',  ( -138.8929263765338078, -8.102448949553172852, -5.886773742842741797 ) ) ;
#23992=CARTESIAN_POINT ( 'NONE',  ( -171.2949999999999875, -2.607480562269069768, 8.024999999999991473 ) ) ;
#24003=( BOUNDED_CURVE ( )  B_SPLINE_CURVE ( 2, ( #59325, #28349, #33320, #64964, #49855, #54743, #59686, #6551, #1236, #55095, #17511 ),
 .UNSPECIFIED., .F., .F. ) 
 B_SPLINE_CURVE_WITH_KNOTS ( ( 3, 2, 2, 2, 2, 3 ),
 ( 0.2391304347826030685, 0.2413043478260812613, 0.2434782608695594819, 0.2456521739130377024, 0.2478260869565159230, 0.2499999999999941158 ),
 .UNSPECIFIED. ) 
 CURVE ( )  GEOMETRIC_REPRESENTATION_ITEM ( )  RATIONAL_B_SPLINE_CURVE ( ( 1.000000000000127010, 0.9510565162950267437, 1.000000000000000000, 0.9510565162951535312, 1.000000000000000000, 0.9510565162951535312, 1.000000000000000000, 0.9510565162951535312, 1.000000000000000000, 0.9510565162952859808, 0.9999999999998675504 ) ) 
 REPRESENTATION_ITEM ( '' )  );
#24005=EDGE_CURVE ( 'NONE', #50943, #65527, #12287, .T. ) ;
#24011=CARTESIAN_POINT ( 'NONE',  ( -159.6550000000000011, -7.632228543268600340, -2.479861379858950166 ) ) ;
#24024=CARTESIAN_POINT ( 'NONE',  ( -74.45499999999999829, 7.632228543268599452, -2.479861379858951942 ) ) ;
#24029=CARTESIAN_POINT ( 'NONE',  ( -85.94292637653380496, 0.000000000000000000, 9.524999999999991473 ) ) ;
#24034=CARTESIAN_POINT ( 'NONE',  ( -56.09499999999997044, -2.607480562269071545, -8.024999999999991473 ) ) ;
#24045=CARTESIAN_POINT ( 'NONE',  ( -52.49499999999999034, 6.826472737025113702, -4.959722759717902107 ) ) ;
#24049=CARTESIAN_POINT ( 'NONE',  ( -103.5549999999999926, 0.000000000000000000, 8.024999999999991473 ) ) ;
#24052=CARTESIAN_POINT ( 'NONE',  ( -195.0000000000000000, 0.000000000000000000, 0.000000000000000000 ) ) ;
#24053=CARTESIAN_POINT ( 'NONE',  ( -143.7570736234661695, -5.598654528085801552, 7.705886871421367523 ) ) ;
#24057=CARTESIAN_POINT ( 'NONE',  ( -81.50707362346615525, 8.102448949553176405, 5.886773742842740909 ) ) ;
#24066=CARTESIAN_POINT ( 'NONE',  ( -117.9549999999999841, -7.632228543268599452, 2.479861379858951054 ) ) ;
#24069=CARTESIAN_POINT ( 'NONE',  ( -136.9449999999999932, -9.827790563157499189E-16, -8.024999999999991473 ) ) ;
#24072=CARTESIAN_POINT ( 'NONE',  ( -120.8949999999999818, 6.826472737025115478, 4.959722759717899443 ) ) ;
#24074=EDGE_LOOP ( 'NONE', ( #59925, #17922, #11560, #22276 ) ) ;
#24075=CARTESIAN_POINT ( 'NONE',  ( -195.0000000000000000, 1.469576158976823553E-15, -11.99999999999999645 ) ) ;
#24078=CARTESIAN_POINT ( 'NONE',  ( -121.6429263765338078, -5.598654528085801552, 7.705886871421367523 ) ) ;
#24079=CARTESIAN_POINT ( 'NONE',  ( -171.2929263765338135, 3.094860106618428031, -9.524999999999993250 ) ) ;
#24080=CARTESIAN_POINT ( 'NONE',  ( -52.04499999999998039, 7.632228543268600340, 2.479861379858949277 ) ) ;
#24088=CARTESIAN_POINT ( 'NONE',  ( -93.29292637653379927, 3.094860106618428031, -9.524999999999993250 ) ) ;
#24094=CARTESIAN_POINT ( 'NONE',  ( -156.9570736234661581, 9.058813317711329915, -2.943386871421373119 ) ) ;
#24099=ORIENTED_EDGE ( 'NONE', *, *, #65617, .F. ) ;
#24100=CARTESIAN_POINT ( 'NONE',  ( -64.64292637653379359, -5.598654528085801552, 7.705886871421367523 ) ) ;
#24108=VERTEX_POINT ( 'NONE', #23223 ) ;
#24111=CARTESIAN_POINT ( 'NONE',  ( -104.0070736234661553, -8.102448949553174629, -5.886773742842741797 ) ) ;
#24115=CARTESIAN_POINT ( 'NONE',  ( -84.89499999999996760, 6.826472737025116366, 4.959722759717898555 ) ) ;
#24116=VERTEX_POINT ( 'NONE', #11618 ) ;
#24129=CARTESIAN_POINT ( 'NONE',  ( -167.7570736234661695, -5.598654528085801552, 7.705886871421367523 ) ) ;
#24133=CARTESIAN_POINT ( 'NONE',  ( -116.1570736234661751, -9.058813317711329915, -2.943386871421370898 ) ) ;
#24135=CARTESIAN_POINT ( 'NONE',  ( -183.2329476844139720, 2.873132234127047102, -8.866736753779713709 ) ) ;
#24143=CARTESIAN_POINT ( 'NONE',  ( -149.1549999999999727, 7.632228543268600340, 2.479861379858949277 ) ) ;
#24144=CARTESIAN_POINT ( 'NONE',  ( -165.7450000000000045, 4.716976649647094177, 6.492361379858945902 ) ) ;
#24145=CARTESIAN_POINT ( 'NONE',  ( -147.4449999999999932, 0.000000000000000000, 8.024999999999991473 ) ) ;
#24147=AXIS2_PLACEMENT_3D ( 'NONE', #10839, #48164, #48511 ) ;
#24148=CARTESIAN_POINT ( 'NONE',  ( -67.04292637653381348, -9.058813317711329915, -2.943386871421370898 ) ) ;
#24151=CARTESIAN_POINT ( 'NONE',  ( -72.05499999999997840, -9.827790563157499189E-16, -8.024999999999991473 ) ) ;
#24156=CARTESIAN_POINT ( 'NONE',  ( -72.29499999999998749, -2.607480562269069768, 8.024999999999991473 ) ) ;
#24158=CARTESIAN_POINT ( 'NONE',  ( -195.0000000000000000, 0.000000000000000000, 0.000000000000000000 ) ) ;
#24168=CARTESIAN_POINT ( 'NONE',  ( -195.0000000000000000, 0.000000000000000000, 0.000000000000000000 ) ) ;
#24174=VECTOR ( 'NONE', #62940, 1000.000000000000000 ) ;
#24186=CARTESIAN_POINT ( 'NONE',  ( -114.2950000000000017, -2.607480562269069768, 8.024999999999991473 ) ) ;
#24191=CARTESIAN_POINT ( 'NONE',  ( -54.14292637653381490, 5.598654528085800663, -7.705886871421367523 ) ) ;
#24192=CARTESIAN_POINT ( 'NONE',  ( -11.23428045036074252, -11.53834988893305713, 3.305092309263673034 ) ) ;
#24193=CARTESIAN_POINT ( 'NONE',  ( -179.9070736234662604, -3.094860106617838280, 9.525000000000423128 ) ) ;
#24207=CARTESIAN_POINT ( 'NONE',  ( -134.7549999999999955, 4.716976649647091513, -6.492361379858946790 ) ) ;
#24219=CARTESIAN_POINT ( 'NONE',  ( -49.25499999999999545, -4.716976649647092401, 6.492361379858946790 ) ) ;
#24224=CARTESIAN_POINT ( 'NONE',  ( -182.1549999999999727, 7.632228543268600340, 2.479861379858949277 ) ) ;
#24227=CARTESIAN_POINT ( 'NONE',  ( -58.25707362346617657, 5.598654528085800663, -7.705886871421367523 ) ) ;
#24235=AXIS2_PLACEMENT_3D ( 'NONE', #37109, #58515, #10345 ) ;
#24237=CARTESIAN_POINT ( 'NONE',  ( -101.6049999999999898, 6.826472737025113702, -4.959722759717902107 ) ) ;
#24241=CARTESIAN_POINT ( 'NONE',  ( -104.6949999999999790, -8.437984349512086979, 5.166775262442717831E-16 ) ) ;
#24243=CARTESIAN_POINT ( 'NONE',  ( -69.14499999999998181, -4.716976649647092401, 6.492361379858946790 ) ) ;
#24251=CARTESIAN_POINT ( 'NONE',  ( -112.6429263765338078, -5.598654528085801552, 7.705886871421367523 ) ) ;
#24252=CARTESIAN_POINT ( 'NONE',  ( -135.1449999999999818, -4.716976649647092401, 6.492361379858946790 ) ) ;
#24254=CYLINDRICAL_SURFACE ( 'NONE', #20164, 9.524999999999991473 ) ;
#24255=CARTESIAN_POINT ( 'NONE',  ( -45.00000000000000000, 1.166476076187854022E-15, -9.525000000000000355 ) ) ;
#24258=EDGE_LOOP ( 'NONE', ( #26357, #52465, #49956, #50667 ) ) ;
#24267=CARTESIAN_POINT ( 'NONE',  ( -128.1550000000000011, 7.632228543268600340, 2.479861379858949277 ) ) ;
#24271=CARTESIAN_POINT ( 'NONE',  ( -123.9570736234661723, 9.058813317711329915, -2.943386871421373119 ) ) ;
#24287=FACE_OUTER_BOUND ( 'NONE', #19707, .T. ) ;
#24297=CARTESIAN_POINT ( 'NONE',  ( -161.6050000000000182, 6.826472737025113702, -4.959722759717902107 ) ) ;
#24311=CARTESIAN_POINT ( 'NONE',  ( -79.55499999999999261, 0.000000000000000000, 8.024999999999991473 ) ) ;
#24326=CARTESIAN_POINT ( 'NONE',  ( -109.6449999999999960, 4.716976649647091513, -6.492361379858946790 ) ) ;
#24331=CARTESIAN_POINT ( 'NONE',  ( -145.7929263765337851, -3.094860106618429807, 9.524999999999991473 ) ) ;
#24332=CARTESIAN_POINT ( 'NONE',  ( -169.0449999999999875, 7.632228543268600340, 2.479861379858949277 ) ) ;
#24342=AXIS2_PLACEMENT_3D ( 'NONE', #47023, #20233, #20593 ) ;
#24344=CARTESIAN_POINT ( 'NONE',  ( -163.4050000000000011, -2.607480562269069768, 8.024999999999991473 ) ) ;
#24356=CARTESIAN_POINT ( 'NONE',  ( -77.45499999999998408, 7.632228543268599452, -2.479861379858951942 ) ) ;
#24369=CARTESIAN_POINT ( 'NONE',  ( -49.34499999999997044, 7.632228543268599452, -2.479861379858951942 ) ) ;
#24372=ADVANCED_FACE ( 'NONE', ( #11747 ), #33216, .T. ) ;
#24377=CARTESIAN_POINT ( 'NONE',  ( -58.34499999999997755, 7.632228543268599452, -2.479861379858951942 ) ) ;
#24380=CARTESIAN_POINT ( 'NONE',  ( -108.8049999999999784, -8.437984349512085203, 5.166775262442717831E-16 ) ) ;
#24385=CARTESIAN_POINT ( 'NONE',  ( -138.6570736234661751, 9.058813317711329915, 2.943386871421369566 ) ) ;
#24388=CARTESIAN_POINT ( 'NONE',  ( -84.95707362346617231, 9.058813317711329915, -2.943386871421373119 ) ) ;
#24397=CARTESIAN_POINT ( 'NONE',  ( -119.9049999999999869, 2.607480562269068880, -8.024999999999993250 ) ) ;
#24399=CARTESIAN_POINT ( 'NONE',  ( -157.9429263765338192, 0.000000000000000000, 9.524999999999991473 ) ) ;
#24401=CARTESIAN_POINT ( 'NONE',  ( -136.3449999999999989, 7.632228543268599452, -2.479861379858951942 ) ) ;
#24402=CARTESIAN_POINT ( 'NONE',  ( -118.4949999999999903, 6.826472737025113702, -4.959722759717902107 ) ) ;
#24407=CARTESIAN_POINT ( 'NONE',  ( -170.6929263765337623, 10.01517768586948698, -1.839758294383808571E-15 ) ) ;
#24408=CARTESIAN_POINT ( 'NONE',  ( -47.69499999999999318, -8.437984349512085203, 5.166775262442717831E-16 ) ) ;
#24415=CARTESIAN_POINT ( 'NONE',  ( -88.04292637653379927, -9.058813317711329915, -2.943386871421370898 ) ) ;
#24433=ORIENTED_EDGE ( 'NONE', *, *, #47966, .T. ) ;
#24441=CARTESIAN_POINT ( 'NONE',  ( -82.04499999999998749, 7.632228543268600340, 2.479861379858949277 ) ) ;
#24458=CARTESIAN_POINT ( 'NONE',  ( -170.4570736234661865, -9.058813317711329915, 2.943386871421371787 ) ) ;
#24461=CARTESIAN_POINT ( 'NONE',  ( -113.9070736234661751, -3.094860106618429807, 9.524999999999991473 ) ) ;
#24471=CARTESIAN_POINT ( 'NONE',  ( -145.5549999999999784, 0.000000000000000000, 8.024999999999991473 ) ) ;
#24474=CARTESIAN_POINT ( 'NONE',  ( -168.4449999999999932, 0.000000000000000000, 8.024999999999991473 ) ) ;
#24475=CARTESIAN_POINT ( 'NONE',  ( -144.4449999999999932, 0.000000000000000000, 8.024999999999991473 ) ) ;
#24478=CARTESIAN_POINT ( 'NONE',  ( -68.15499999999997272, 7.632228543268600340, 2.479861379858949277 ) ) ;
#24482=CARTESIAN_POINT ( 'NONE',  ( -63.14499999999998181, -4.716976649647092401, 6.492361379858946790 ) ) ;
#24497=CARTESIAN_POINT ( 'NONE',  ( -61.10707362346615668, 8.102448949553172852, -5.886773742842744461 ) ) ;
#24512=CARTESIAN_POINT ( 'NONE',  ( -145.3429263765338249, -9.058813317711329915, 2.943386871421371787 ) ) ;
#24516=CARTESIAN_POINT ( 'NONE',  ( -114.1449999999999960, -4.716976649647092401, 6.492361379858946790 ) ) ;
#24521=CARTESIAN_POINT ( 'NONE',  ( -11.94707626989746529, -11.32487227758645432, -3.972914747560817972 ) ) ;
#24535=CARTESIAN_POINT ( 'NONE',  ( -195.0000000000000000, 0.000000000000000000, 0.000000000000000000 ) ) ;
#24536=CARTESIAN_POINT ( 'NONE',  ( -124.8549999999999898, 4.716976649647094177, 6.492361379858945902 ) ) ;
#24537=CARTESIAN_POINT ( 'NONE',  ( -184.0000000000000000, -4.077197870136868296, 6.923068838537520975 ) ) ;
#24539=ORIENTED_EDGE ( 'NONE', *, *, #32461, .F. ) ;
#24544=CIRCLE ( 'NONE', #39169, 11.99999999999999645 ) ;
#24545=ORIENTED_EDGE ( 'NONE', *, *, #53832, .F. ) ;
#24550=ORIENTED_EDGE ( 'NONE', *, *, #16824, .T. ) ;
#24551=CARTESIAN_POINT ( 'NONE',  ( -180.6550000000000011, -7.632228543268600340, -2.479861379858950166 ) ) ;
#24555=CARTESIAN_POINT ( 'NONE',  ( -51.50707362346617657, 8.102448949553176405, 5.886773742842740909 ) ) ;
#24556=CARTESIAN_POINT ( 'NONE',  ( -172.9449999999999932, -9.827790563157499189E-16, -8.024999999999991473 ) ) ;
#24564=CARTESIAN_POINT ( 'NONE',  ( -94.10499999999997556, -6.826472737025115478, 4.959722759717900331 ) ) ;
#24565=DIRECTION ( 'NONE',  ( 0.000000000000000000, 0.000000000000000000, 1.000000000000000000 ) ) ;
#24568=CARTESIAN_POINT ( 'NONE',  ( -90.29499999999997328, -2.607480562269069768, 8.024999999999991473 ) ) ;
#24570=CARTESIAN_POINT ( 'NONE',  ( -72.59499999999998465, 2.607480562269073321, 8.024999999999991473 ) ) ;
#24578=CARTESIAN_POINT ( 'NONE',  ( -113.5429263765338135, 9.058813317711329915, 2.943386871421369566 ) ) ;
#24579=CARTESIAN_POINT ( 'NONE',  ( -130.1950000000000216, 8.437984349512085203, -1.550032578732815448E-15 ) ) ;
#24595=CARTESIAN_POINT ( 'NONE',  ( -128.6049999999999898, 6.826472737025113702, -4.959722759717902107 ) ) ;
#24598=CARTESIAN_POINT ( 'NONE',  ( -119.6070736234661638, -8.102448949553172852, 5.886773742842742685 ) ) ;
#24601=CARTESIAN_POINT ( 'NONE',  ( -172.1929263765337907, -10.01517768586948698, 6.132527647946031529E-16 ) ) ;
#24607=CARTESIAN_POINT ( 'NONE',  ( -54.50707362346614104, 8.102448949553176405, 5.886773742842740909 ) ) ;
#24624=FACE_BOUND ( 'NONE', #11211, .T. ) ;
#24626=CARTESIAN_POINT ( 'NONE',  ( -163.1050000000000182, -6.826472737025115478, 4.959722759717900331 ) ) ;
#24627=VERTEX_POINT ( 'NONE', #16302 ) ;
#24639=CARTESIAN_POINT ( 'NONE',  ( -76.55499999999997840, 0.000000000000000000, 8.024999999999991473 ) ) ;
#24643=CARTESIAN_POINT ( 'NONE',  ( -124.9429263765338192, 0.000000000000000000, 9.524999999999991473 ) ) ;
#24653=CARTESIAN_POINT ( 'NONE',  ( -94.79499999999997328, 2.607480562269068880, -8.024999999999993250 ) ) ;
#24657=CARTESIAN_POINT ( 'NONE',  ( -96.50707362346616947, 8.102448949553176405, 5.886773742842740909 ) ) ;
#24660=CARTESIAN_POINT ( 'NONE',  ( -146.0929263765337964, 3.094860106618433360, 9.524999999999991473 ) ) ;
#24662=CARTESIAN_POINT ( 'NONE',  ( -155.8449999999999704, -7.632228543268599452, 2.479861379858951054 ) ) ;
#24665=EDGE_CURVE ( 'NONE', #12387, #47261, #3938, .T. ) ;
#24678=CARTESIAN_POINT ( 'NONE',  ( -161.1550000000000011, 7.632228543268600340, 2.479861379858949277 ) ) ;
#24695=CARTESIAN_POINT ( 'NONE',  ( -76.70499999999999829, 2.607480562269072433, 8.024999999999991473 ) ) ;
#24707=CARTESIAN_POINT ( 'NONE',  ( -52.19499999999999318, 8.437984349512085203, -1.550032578732815448E-15 ) ) ;
#24709=( BOUNDED_CURVE ( )  B_SPLINE_CURVE ( 2, ( #20114, #26095, #3565, #69034, #36365, #25408, #62678, #56744, #41991, #8556, #8886 ),
 .UNSPECIFIED., .F., .F. ) 
 B_SPLINE_CURVE_WITH_KNOTS ( ( 3, 2, 2, 2, 2, 3 ),
 ( 0.7391304347826086474, 0.7413043478260870067, 0.7434782608695652550, 0.7456521739130435034, 0.7478260869565217517, 0.7500000000000000000 ),
 .UNSPECIFIED. ) 
 CURVE ( )  GEOMETRIC_REPRESENTATION_ITEM ( )  RATIONAL_B_SPLINE_CURVE ( ( 1.000000000000000000, 0.9510565162951535312, 1.000000000000000000, 0.9510565162951535312, 1.000000000000000000, 0.9510565162951535312, 1.000000000000000000, 0.9510565162951535312, 1.000000000000000000, 0.9510565162951535312, 1.000000000000000000 ) ) 
 REPRESENTATION_ITEM ( '' )  );
#24719=CARTESIAN_POINT ( 'NONE',  ( -106.1049999999999756, -6.826472737025115478, 4.959722759717900331 ) ) ;
#24725=CARTESIAN_POINT ( 'NONE',  ( -145.1070736234661638, 8.102448949553171076, -5.886773742842744461 ) ) ;
#24728=CARTESIAN_POINT ( 'NONE',  ( -70.70707362346615810, -3.094860106618431139, -9.524999999999991473 ) ) ;
#24734=CARTESIAN_POINT ( 'NONE',  ( -169.5570736234661808, -1.166476076187852838E-15, -9.524999999999991473 ) ) ;
#24736=CARTESIAN_POINT ( 'NONE',  ( -117.3549999999999898, -4.716976649647093289, -6.492361379858945902 ) ) ;
#24737=CARTESIAN_POINT ( 'NONE',  ( -158.0929263765341375, 3.094860106624147011, 9.524999999995840128 ) ) ;
#24739=CARTESIAN_POINT ( 'NONE',  ( -126.1450000000000102, -4.716976649647092401, 6.492361379858946790 ) ) ;
#24741=CARTESIAN_POINT ( 'NONE',  ( -116.8449999999999847, -7.632228543268599452, 2.479861379858951054 ) ) ;
#24747=CARTESIAN_POINT ( 'NONE',  ( -173.3929263765337510, 8.102448949553176405, 5.886773742842740909 ) ) ;
#24750=CARTESIAN_POINT ( 'NONE',  ( -51.74499999999998323, 4.716976649647094177, 6.492361379858945902 ) ) ;
#24756=CARTESIAN_POINT ( 'NONE',  ( -83.84292637653379643, 9.058813317711329915, -2.943386871421373119 ) ) ;
#24765=CARTESIAN_POINT ( 'NONE',  ( -157.1070736234661922, 8.102448949553172852, -5.886773742842744461 ) ) ;
#24780=CARTESIAN_POINT ( 'NONE',  ( -103.2549999999999812, -4.716976649647092401, 6.492361379858946790 ) ) ;
#24786=CARTESIAN_POINT ( 'NONE',  ( -104.1570736234661751, -9.058813317711329915, -2.943386871421370898 ) ) ;
#24791=CARTESIAN_POINT ( 'NONE',  ( -83.09499999999999886, -2.607480562269071545, -8.024999999999991473 ) ) ;
#24797=CARTESIAN_POINT ( 'NONE',  ( -76.94292637653380496, 0.000000000000000000, 9.524999999999991473 ) ) ;
#24804=CARTESIAN_POINT ( 'NONE',  ( -150.1429263765338078, 5.598654528085800663, -7.705886871421367523 ) ) ;
#24805=CARTESIAN_POINT ( 'NONE',  ( -167.9070736234661751, -3.094860106618429807, 9.524999999999991473 ) ) ;
#24810=CARTESIAN_POINT ( 'NONE',  ( -108.0570736234661666, 0.000000000000000000, 9.524999999999991473 ) ) ;
#24814=CARTESIAN_POINT ( 'NONE',  ( -65.30707362346618083, -10.01517768586948698, 6.132527647946031529E-16 ) ) ;
#24822=CARTESIAN_POINT ( 'NONE',  ( -153.0550000000000068, -9.827790563157499189E-16, -8.024999999999991473 ) ) ;
#24825=CARTESIAN_POINT ( 'NONE',  ( -167.2450000000000045, -4.716976649647093289, -6.492361379858945902 ) ) ;
#24826=CARTESIAN_POINT ( 'NONE',  ( -148.6450000000000102, 4.716976649647091513, -6.492361379858946790 ) ) ;
#24833=CARTESIAN_POINT ( 'NONE',  ( -63.65499999999998693, -7.632228543268600340, -2.479861379858950166 ) ) ;
#24838=CARTESIAN_POINT ( 'NONE',  ( -66.14499999999998181, -4.716976649647092401, 6.492361379858946790 ) ) ;
#24850=DIRECTION ( 'NONE',  ( 0.000000000000000000, 0.000000000000000000, 1.000000000000000000 ) ) ;
#24863=ORIENTED_EDGE ( 'NONE', *, *, #59801, .T. ) ;
#24875=CARTESIAN_POINT ( 'NONE',  ( -114.4449999999999932, 0.000000000000000000, 8.024999999999991473 ) ) ;
#24880=CARTESIAN_POINT ( 'NONE',  ( -53.39292637653380780, 8.102448949553176405, 5.886773742842740909 ) ) ;
#24888=VERTEX_POINT ( 'NONE', #30605 ) ;
#24890=ORIENTED_EDGE ( 'NONE', *, *, #45943, .F. ) ;
#24894=CARTESIAN_POINT ( 'NONE',  ( -122.7549999999999955, 4.716976649647091513, -6.492361379858946790 ) ) ;
#24906=CARTESIAN_POINT ( 'NONE',  ( -103.9429263765338050, 0.000000000000000000, 9.524999999999991473 ) ) ;
#24910=CARTESIAN_POINT ( 'NONE',  ( -176.1550000000000011, 7.632228543268600340, 2.479861379858949277 ) ) ;
#24912=CARTESIAN_POINT ( 'NONE',  ( -60.65707362346617515, 9.058813317711329915, 2.943386871421369566 ) ) ;
#24914=CARTESIAN_POINT ( 'NONE',  ( -175.1949999999999932, 8.437984349512086979, -1.550032578732815448E-15 ) ) ;
#24923=CARTESIAN_POINT ( 'NONE',  ( -88.55499999999999261, 0.000000000000000000, 8.024999999999991473 ) ) ;
#24929=CARTESIAN_POINT ( 'NONE',  ( -88.19499999999996476, 8.437984349512086979, -1.550032578732815448E-15 ) ) ;
#24932=CARTESIAN_POINT ( 'NONE',  ( -66.59499999999999886, 2.607480562269073321, 8.024999999999991473 ) ) ;
#24940=ORIENTED_EDGE ( 'NONE', *, *, #8132, .T. ) ;
#24942=CARTESIAN_POINT ( 'NONE',  ( -115.1929263765338050, -10.01517768586948698, 6.132527647946031529E-16 ) ) ;
#24943=CARTESIAN_POINT ( 'NONE',  ( -131.5449999999999875, -7.632228543268600340, -2.479861379858950166 ) ) ;
#24959=CARTESIAN_POINT ( 'NONE',  ( -127.4049999999999869, -2.607480562269069768, 8.024999999999991473 ) ) ;
#24961=DIRECTION ( 'NONE',  ( 1.000000000000000000, 0.000000000000000000, 0.000000000000000000 ) ) ;
#24962=CARTESIAN_POINT ( 'NONE',  ( -119.9070736234661609, -3.094860106618429807, 9.524999999999991473 ) ) ;
#24984=CARTESIAN_POINT ( 'NONE',  ( -98.24292637653380211, 5.598654528085804216, 7.705886871421366635 ) ) ;
#24987=EDGE_LOOP ( 'NONE', ( #23442, #63750, #62211, #8622 ) ) ;
#24990=CARTESIAN_POINT ( 'NONE',  ( -56.24292637653380211, 5.598654528085804216, 7.705886871421366635 ) ) ;
#24993=CARTESIAN_POINT ( 'NONE',  ( -155.7549999999999955, 4.716976649647091513, -6.492361379858946790 ) ) ;
#25008=CARTESIAN_POINT ( 'NONE',  ( -68.45499999999998408, 7.632228543268599452, -2.479861379858951942 ) ) ;
#25025=CARTESIAN_POINT ( 'NONE',  ( -100.3449999999999847, 7.632228543268599452, -2.479861379858951942 ) ) ;
#25030=CARTESIAN_POINT ( 'NONE',  ( -72.14292637653379359, 5.598654528085800663, -7.705886871421367523 ) ) ;
#25033=CARTESIAN_POINT ( 'NONE',  ( -139.3429263765337964, -9.058813317711329915, 2.943386871421371787 ) ) ;
#25036=CARTESIAN_POINT ( 'NONE',  ( -156.1450000000000102, -4.716976649647092401, 6.492361379858946790 ) ) ;
#25041=CARTESIAN_POINT ( 'NONE',  ( -133.0429263765338135, -9.058813317711329915, -2.943386871421370898 ) ) ;
#25052=CARTESIAN_POINT ( 'NONE',  ( -161.9050000000000011, 2.607480562269069324, -8.024999999999993250 ) ) ;
#25056=CARTESIAN_POINT ( 'NONE',  ( -47.51430879217793546, 5.598654528085803328, -7.705886871421366635 ) ) ;
#25066=CARTESIAN_POINT ( 'NONE',  ( -78.35499999999997556, -4.716976649647093289, -6.492361379858945902 ) ) ;
#25081=CARTESIAN_POINT ( 'NONE',  ( -178.5549999999999784, 0.000000000000000000, 8.024999999999991473 ) ) ;
#25091=CARTESIAN_POINT ( 'NONE',  ( -105.8050000000000068, -8.437984349512085203, 5.166775262442717831E-16 ) ) ;
#25097=CARTESIAN_POINT ( 'NONE',  ( -143.9070736234661751, -3.094860106618429807, 9.524999999999991473 ) ) ;
#25100=CARTESIAN_POINT ( 'NONE',  ( -74.45707362346617231, -9.058813317711329915, 2.943386871421371787 ) ) ;
#25106=CARTESIAN_POINT ( 'NONE',  ( -125.9049999999999869, 2.607480562269068880, -8.024999999999993250 ) ) ;
#25109=CARTESIAN_POINT ( 'NONE',  ( -130.3449999999999989, 7.632228543268599452, -2.479861379858951942 ) ) ;
#25117=CARTESIAN_POINT ( 'NONE',  ( -172.0429263765338135, -9.058813317711329915, -2.943386871421370898 ) ) ;
#25126=CARTESIAN_POINT ( 'NONE',  ( -83.69292637653379074, 10.01517768586948698, -1.839758294383808571E-15 ) ) ;
#25133=CARTESIAN_POINT ( 'NONE',  ( -162.8929263765338078, -8.102448949553174629, -5.886773742842741797 ) ) ;
#25138=EDGE_LOOP ( 'NONE', ( #50063, #13191, #15225, #14767 ) ) ;
#25141=( BOUNDED_CURVE ( )  B_SPLINE_CURVE ( 2, ( #43088, #16341, #37814, #32453, #25185, #15008, #40700, #62800, #3688, #46702, #67757 ),
 .UNSPECIFIED., .F., .F. ) 
 B_SPLINE_CURVE_WITH_KNOTS ( ( 3, 2, 2, 2, 2, 3 ),
 ( 0.8913043478260869179, 0.8934782608695651662, 0.8956521739130435256, 0.8978260869565217739, 0.9000000000000000222, 0.9021739130434782705 ),
 .UNSPECIFIED. ) 
 CURVE ( )  GEOMETRIC_REPRESENTATION_ITEM ( )  RATIONAL_B_SPLINE_CURVE ( ( 1.000000000000000000, 0.9510565162951535312, 1.000000000000000000, 0.9510565162951535312, 1.000000000000000000, 0.9510565162951535312, 1.000000000000000000, 0.9510565162951535312, 1.000000000000000000, 0.9510565162951535312, 1.000000000000000000 ) ) 
 REPRESENTATION_ITEM ( '' )  );
#25146=CARTESIAN_POINT ( 'NONE',  ( -106.1049999999999756, -6.826472737025113702, 4.959722759717902107 ) ) ;
#25157=CARTESIAN_POINT ( 'NONE',  ( -81.74499999999999034, 4.716976649647094177, 6.492361379858945902 ) ) ;
#25168=CARTESIAN_POINT ( 'NONE',  ( -154.9429263765338192, 0.000000000000000000, 9.524999999999991473 ) ) ;
#25175=CARTESIAN_POINT ( 'NONE',  ( -168.2070736234661297, 3.094860106618433360, 9.524999999999991473 ) ) ;
#25178=CARTESIAN_POINT ( 'NONE',  ( -103.8570736234661780, -5.598654528085803328, -7.705886871421366635 ) ) ;
#25183=CARTESIAN_POINT ( 'NONE',  ( -106.4070736234671131, 3.094860106602697503, -9.525000000011422330 ) ) ;
#25185=CARTESIAN_POINT ( 'NONE',  ( -61.34292637653379643, -9.058813317711329915, 2.943386871421371787 ) ) ;
#25187=CARTESIAN_POINT ( 'NONE',  ( -147.2050000000000125, -2.607480562269071545, -8.024999999999991473 ) ) ;
#25188=CARTESIAN_POINT ( 'NONE',  ( -147.7429263765338021, -5.598654528085803328, -7.705886871421366635 ) ) ;
#25189=CARTESIAN_POINT ( 'NONE',  ( -155.0949999999999989, -2.607480562269071545, -8.024999999999991473 ) ) ;
#25191=CARTESIAN_POINT ( 'NONE',  ( -151.7949999999999591, 2.607480562269069324, -8.024999999999993250 ) ) ;
#25198=DIRECTION ( 'NONE',  ( 0.000000000000000000, 0.000000000000000000, 1.000000000000000000 ) ) ;
#25200=CARTESIAN_POINT ( 'NONE',  ( -60.20499999999998408, -2.607480562269071545, -8.024999999999991473 ) ) ;
#25202=CARTESIAN_POINT ( 'NONE',  ( -62.24499999999998323, -4.716976649647093289, -6.492361379858945902 ) ) ;
#25233=CARTESIAN_POINT ( 'NONE',  ( -113.5449999999999875, -7.632228543268600340, -2.479861379858950166 ) ) ;
#25252=CARTESIAN_POINT ( 'NONE',  ( -126.0550000000000068, -9.827790563157499189E-16, -8.024999999999991473 ) ) ;
#25258=CARTESIAN_POINT ( 'NONE',  ( -125.8429263765337964, 9.058813317711329915, -2.943386871421373119 ) ) ;
#25267=CARTESIAN_POINT ( 'NONE',  ( -181.2549999999999955, -4.716976649647092401, 6.492361379858946790 ) ) ;
#25270=CARTESIAN_POINT ( 'NONE',  ( -179.3950000000000102, -6.826472737025115478, -4.959722759717899443 ) ) ;
#25274=CARTESIAN_POINT ( 'NONE',  ( -176.5450000000000159, -7.632228543268600340, -2.479861379858950166 ) ) ;
#25280=CARTESIAN_POINT ( 'NONE',  ( -91.55499999999997840, 0.000000000000000000, 8.024999999999991473 ) ) ;
#25283=CARTESIAN_POINT ( 'NONE',  ( -88.79499999999998749, 2.607480562269069324, -8.024999999999993250 ) ) ;
#25285=CARTESIAN_POINT ( 'NONE',  ( -72.29499999999998749, -2.607480562269069768, 8.024999999999991473 ) ) ;
#25293=CARTESIAN_POINT ( 'NONE',  ( -104.0929263765338106, 3.094860106618433360, 9.524999999999991473 ) ) ;
#25295=CARTESIAN_POINT ( 'NONE',  ( -130.9449999999999648, -9.827790563157499189E-16, -8.024999999999991473 ) ) ;
#25302=CARTESIAN_POINT ( 'NONE',  ( -174.8070736234661524, 10.01517768586948698, -1.839758294383808966E-15 ) ) ;
#25304=APPLICATION_CONTEXT ( 'automotive_design' ) ;
#25310=ORIENTED_EDGE ( 'NONE', *, *, #68859, .F. ) ;
#25311=CARTESIAN_POINT ( 'NONE',  ( -119.0049999999999812, 6.826472737025115478, 4.959722759717899443 ) ) ;
#25314=CARTESIAN_POINT ( 'NONE',  ( -126.9570736234661723, 9.058813317711329915, -2.943386871421373119 ) ) ;
#25315=ORIENTED_EDGE ( 'NONE', *, *, #29632, .T. ) ;
#25339=VERTEX_POINT ( 'NONE', #19962 ) ;
#25340=CARTESIAN_POINT ( 'NONE',  ( -61.94292637653379785, 0.000000000000000000, 9.524999999999991473 ) ) ;
#25342=CARTESIAN_POINT ( 'NONE',  ( -154.4050000000000011, -2.607480562269069768, 8.024999999999991473 ) ) ;
#25355=CARTESIAN_POINT ( 'NONE',  ( -62.30499999999997840, 8.437984349512085203, -1.550032578732815448E-15 ) ) ;
#25358=CARTESIAN_POINT ( 'NONE',  ( -123.4429263765338192, -1.166476076187852838E-15, -9.524999999999991473 ) ) ;
#25368=CARTESIAN_POINT ( 'NONE',  ( -93.89499999999998181, 6.826472737025116366, 4.959722759717898555 ) ) ;
#25373=CARTESIAN_POINT ( 'NONE',  ( -71.09292637653381064, 3.094860106618433360, 9.524999999999991473 ) ) ;
#25375=CARTESIAN_POINT ( 'NONE',  ( -145.3429263765338249, -9.058813317711329915, 2.943386871421371787 ) ) ;
#25378=CARTESIAN_POINT ( 'NONE',  ( -158.8449999999999989, -7.632228543268599452, 2.479861379858951054 ) ) ;
#25384=CARTESIAN_POINT ( 'NONE',  ( -133.9429263765338192, 0.000000000000000000, 9.524999999999991473 ) ) ;
#25392=CARTESIAN_POINT ( 'NONE',  ( -109.8570736234661780, -5.598654528085803328, -7.705886871421366635 ) ) ;
#25394=CARTESIAN_POINT ( 'NONE',  ( -161.7549999999999955, 4.716976649647091513, -6.492361379858946790 ) ) ;
#25395=ORIENTED_EDGE ( 'NONE', *, *, #50273, .T. ) ;
#25407=CARTESIAN_POINT ( 'NONE',  ( -69.65499999999998693, -7.632228543268600340, -2.479861379858950166 ) ) ;
#25408=CARTESIAN_POINT ( 'NONE',  ( -80.30707362346618083, -10.01517768586948698, 6.132527647946031529E-16 ) ) ;
#25410=ORIENTED_EDGE ( 'NONE', *, *, #34166, .F. ) ;
#25422=CARTESIAN_POINT ( 'NONE',  ( -177.8049999999999784, -8.437984349512085203, 5.166775262442717831E-16 ) ) ;
#25429=CARTESIAN_POINT ( 'NONE',  ( -45.00000000000000000, 0.000000000000000000, 9.525000000000000355 ) ) ;
#25435=CARTESIAN_POINT ( 'NONE',  ( -92.90499999999997272, 2.607480562269068880, -8.024999999999993250 ) ) ;
#25439=CARTESIAN_POINT ( 'NONE',  ( -140.1570736234661751, -9.058813317711329915, -2.943386871421370898 ) ) ;
#25442=CARTESIAN_POINT ( 'NONE',  ( -77.00707362346616947, -8.102448949553172852, -5.886773742842741797 ) ) ;
#25444=CARTESIAN_POINT ( 'NONE',  ( -16.14263016465302414, -10.96720793458296939, 4.870483257825171997 ) ) ;
#25447=CARTESIAN_POINT ( 'NONE',  ( -115.7049999999999983, 2.607480562269073321, 8.024999999999991473 ) ) ;
#25451=CARTESIAN_POINT ( 'NONE',  ( -127.9449999999999790, -9.827790563157499189E-16, -8.024999999999991473 ) ) ;
#25458=CARTESIAN_POINT ( 'NONE',  ( -173.8429263765338249, 9.058813317711329915, -2.943386871421373119 ) ) ;
#25466=CARTESIAN_POINT ( 'NONE',  ( -81.59292637653378222, -3.094860106618431139, -9.524999999999991473 ) ) ;
#25482=CARTESIAN_POINT ( 'NONE',  ( -101.3070736234661808, -10.01517768586948698, 6.132527647946031529E-16 ) ) ;
#25483=CARTESIAN_POINT ( 'NONE',  ( -101.6049999999999898, 6.826472737025113702, -4.959722759717902107 ) ) ;
#25493=CARTESIAN_POINT ( 'NONE',  ( -74.24499999999999034, -4.716976649647093289, -6.492361379858945902 ) ) ;
#25511=CARTESIAN_POINT ( 'NONE',  ( -165.9570736234661865, 9.058813317711329915, -2.943386871421373119 ) ) ;
#25513=CARTESIAN_POINT ( 'NONE',  ( -101.9070736234661609, -3.094860106618429807, 9.524999999999991473 ) ) ;
#25517=( BOUNDED_CURVE ( )  B_SPLINE_CURVE ( 2, ( #44688, #66800, #22853, #39741, #17593, #44349, #61480, #65409, #17909, #39058, #23871 ),
 .UNSPECIFIED., .F., .F. ) 
 B_SPLINE_CURVE_WITH_KNOTS ( ( 3, 2, 2, 2, 2, 3 ),
 ( 0.5434782608695525319, 0.5456521739130306692, 0.5478260869565089175, 0.5499999999999871658, 0.5521739130434654141, 0.5543478260869435514 ),
 .UNSPECIFIED. ) 
 CURVE ( )  GEOMETRIC_REPRESENTATION_ITEM ( )  RATIONAL_B_SPLINE_CURVE ( ( 1.000000000000284883, 0.9510565162948685369, 1.000000000000000000, 0.9510565162951535312, 1.000000000000000000, 0.9510565162951535312, 1.000000000000000000, 0.9510565162951535312, 1.000000000000000000, 0.9510565162954459639, 0.9999999999997075673 ) ) 
 REPRESENTATION_ITEM ( '' )  );
#25522=CARTESIAN_POINT ( 'NONE',  ( -149.3049999999999500, 8.437984349512085203, -1.550032578732815448E-15 ) ) ;
#25525=CARTESIAN_POINT ( 'NONE',  ( -154.0449999999999875, 7.632228543268600340, 2.479861379858949277 ) ) ;
#25526=CARTESIAN_POINT ( 'NONE',  ( -150.8950000000000102, 6.826472737025115478, 4.959722759717899443 ) ) ;
#25531=CARTESIAN_POINT ( 'NONE',  ( -59.15499999999998693, 7.632228543268600340, 2.479861379858949277 ) ) ;
#25532=CARTESIAN_POINT ( 'NONE',  ( -60.14499999999998892, -4.716976649647092401, 6.492361379858946790 ) ) ;
#25544=ADVANCED_FACE ( 'NONE', ( #19460 ), #28951, .T. ) ;
#25546=ORIENTED_EDGE ( 'NONE', *, *, #15888, .F. ) ;
#25554=CARTESIAN_POINT ( 'NONE',  ( -108.0570736234661666, 0.000000000000000000, 9.524999999999991473 ) ) ;
#25565=CARTESIAN_POINT ( 'NONE',  ( -96.89499999999998181, 6.826472737025116366, 4.959722759717898555 ) ) ;
#25568=CARTESIAN_POINT ( 'NONE',  ( -164.4570736234661865, -9.058813317711329915, 2.943386871421371787 ) ) ;
#25570=CARTESIAN_POINT ( 'NONE',  ( -178.8570736234661638, -5.598654528085803328, -7.705886871421366635 ) ) ;
#25575=ORIENTED_EDGE ( 'NONE', *, *, #52985, .T. ) ;
#25576=CARTESIAN_POINT ( 'NONE',  ( -62.15707362346617515, -9.058813317711329915, -2.943386871421370898 ) ) ;
#25580=CARTESIAN_POINT ( 'NONE',  ( -120.2049999999999983, -2.607480562269071545, -8.024999999999991473 ) ) ;
#25581=CARTESIAN_POINT ( 'NONE',  ( -184.0000000000000568, -7.022622464067349135, 3.903023461144195405 ) ) ;
#25596=ORIENTED_EDGE ( 'NONE', *, *, #54386, .F. ) ;
#25598=CARTESIAN_POINT ( 'NONE',  ( -181.7050000000000125, 2.607480562269073321, 8.024999999999991473 ) ) ;
#25601=CARTESIAN_POINT ( 'NONE',  ( -183.4449999999999932, 0.000000000000000000, 8.024999999999991473 ) ) ;
#25602=CARTESIAN_POINT ( 'NONE',  ( -177.7449999999999761, 4.716976649647094177, 6.492361379858945902 ) ) ;
#25607=CARTESIAN_POINT ( 'NONE',  ( -13.37809012747797865, 11.02455069633067275, 4.741122039576717739 ) ) ;
#25608=CARTESIAN_POINT ( 'NONE',  ( -95.60499999999998977, 6.826472737025113702, -4.959722759717902107 ) ) ;
#25613=CARTESIAN_POINT ( 'NONE',  ( -89.69499999999997897, -8.437984349512086979, 5.166775262442717831E-16 ) ) ;
#25615=CARTESIAN_POINT ( 'NONE',  ( -71.69499999999999318, -8.437984349512085203, 5.166775262442717831E-16 ) ) ;
#25617=CARTESIAN_POINT ( 'NONE',  ( -56.15707362346616804, -9.058813317711329915, -2.943386871421370898 ) ) ;
#25623=CARTESIAN_POINT ( 'NONE',  ( -100.4929263765337879, -8.102448949553172852, 5.886773742842742685 ) ) ;
#25624=CARTESIAN_POINT ( 'NONE',  ( -131.2450000000000045, -4.716976649647093289, -6.492361379858945902 ) ) ;
#25628=CARTESIAN_POINT ( 'NONE',  ( -132.4429263765338192, -1.166476076187852838E-15, -9.524999999999991473 ) ) ;
#25642=EDGE_LOOP ( 'NONE', ( #49640, #4566, #12613, #2366 ) ) ;
#25643=CARTESIAN_POINT ( 'NONE',  ( -123.3549999999999898, -4.716976649647093289, -6.492361379858945902 ) ) ;
#25646=CARTESIAN_POINT ( 'NONE',  ( -124.1070736234661638, 8.102448949553171076, -5.886773742842744461 ) ) ;
#25665=CARTESIAN_POINT ( 'NONE',  ( -47.45707362346615810, -9.058813317711329915, 2.943386871421371787 ) ) ;
#25671=CARTESIAN_POINT ( 'NONE',  ( -59.69292637653379785, 10.01517768586948698, -1.839758294383808571E-15 ) ) ;
#25673=CARTESIAN_POINT ( 'NONE',  ( -148.7049999999999841, 2.607480562269073321, 8.024999999999991473 ) ) ;
#25684=CARTESIAN_POINT ( 'NONE',  ( -68.00499999999998124, 6.826472737025116366, 4.959722759717898555 ) ) ;
#25701=CARTESIAN_POINT ( 'NONE',  ( -95.69499999999997897, -8.437984349512085203, 5.166775262442717831E-16 ) ) ;
#25707=CARTESIAN_POINT ( 'NONE',  ( -137.6929263765337623, 10.01517768586948698, -1.839758294383808571E-15 ) ) ;
#25710=CARTESIAN_POINT ( 'NONE',  ( -155.3950000000000102, -6.826472737025115478, -4.959722759717899443 ) ) ;
#25713=ADVANCED_FACE ( 'NONE', ( #9276 ), #36247, .F. ) ;
#25716=CARTESIAN_POINT ( 'NONE',  ( -133.7929263765344956, -3.094860106607741468, 9.525000000007759482 ) ) ;
#25725=CARTESIAN_POINT ( 'NONE',  ( -109.7070736234670534, -3.094860106633489316, -9.524999999989050892 ) ) ;
#25730=CARTESIAN_POINT ( 'NONE',  ( -147.2050000000000125, -2.607480562269071545, -8.024999999999991473 ) ) ;
#25739=CARTESIAN_POINT ( 'NONE',  ( -121.9429263765338050, 0.000000000000000000, 9.524999999999991473 ) ) ;
#25743=CARTESIAN_POINT ( 'NONE',  ( -58.64292637653378648, -5.598654528085801552, 7.705886871421367523 ) ) ;
#25745=CARTESIAN_POINT ( 'NONE',  ( -67.70499999999999829, 2.607480562269072433, 8.024999999999991473 ) ) ;
#25748=ORIENTED_EDGE ( 'NONE', *, *, #65861, .F. ) ;
#25752=DIRECTION ( 'NONE',  ( -1.000000000000000000, -0.000000000000000000, -0.000000000000000000 ) ) ;
#25760=CARTESIAN_POINT ( 'NONE',  ( -47.09499999999999886, -2.607480562269071545, -8.024999999999991473 ) ) ;
#25769=EDGE_LOOP ( 'NONE', ( #53856, #52328, #2454, #44755, #43377, #2127, #66863, #4714, #33031, #20931, #57460, #9888, #40479, #14512, #59875, #9235, #67306, #56124, #28841, #10757, #42850, #22669, #26662, #43636, #14150, #58245, #67886, #63566, #64169, #8090, #28055, #29312, #53101, #3852, #54291, #49329, #58290, #25315, #20326, #56893, #5918, #50349, #52859, #35125, #26920, #62069, #6605, #28794, #6212, #43698, #64448, #45109, #19762, #66757, #17774, #57719, #53524, #39631, #33472, #25395, #33663, #10906, #34822, #10273, #5936, #39707, #22740, #8048, #37736, #14291, #47654, #17260, #35206, #31568, #54966, #3030, #68664, #52200, #49705, #20217, #49138, #19068, #18822, #50927, #46938, #40267, #9083, #31114, #40955, #10544, #54811, #66249, #23424, #48814, #8548, #55181 ) ) ;
#25771=CARTESIAN_POINT ( 'NONE',  ( -128.4570736234661865, -9.058813317711329915, 2.943386871421371787 ) ) ;
#25772=CARTESIAN_POINT ( 'NONE',  ( -98.45499999999998408, 7.632228543268599452, -2.479861379858951942 ) ) ;
#25776=CARTESIAN_POINT ( 'NONE',  ( -128.6070736234661638, -8.102448949553172852, 5.886773742842742685 ) ) ;
#25781=CARTESIAN_POINT ( 'NONE',  ( -75.20707362346614389, 3.094860106618433360, 9.524999999999991473 ) ) ;
#25782=EDGE_CURVE ( 'NONE', #20781, #6242, #11685, .T. ) ;
#25784=CARTESIAN_POINT ( 'NONE',  ( -92.54292637653379927, 9.058813317711329915, 2.943386871421369566 ) ) ;
#25787=CARTESIAN_POINT ( 'NONE',  ( -19.33312911335796969, -11.73659741771296794, -2.515642419290914145 ) ) ;
#25788=CARTESIAN_POINT ( 'NONE',  ( -99.44292637653380496, -1.166476076187852838E-15, -9.524999999999991473 ) ) ;
#25790=CARTESIAN_POINT ( 'NONE',  ( -112.2549999999999955, -4.716976649647092401, 6.492361379858946790 ) ) ;
#25792=CARTESIAN_POINT ( 'NONE',  ( -130.4950000000000045, 6.826472737025113702, -4.959722759717902107 ) ) ;
#25793=VECTOR ( 'NONE', #13052, 1000.000000000000000 ) ;
#25800=CARTESIAN_POINT ( 'NONE',  ( -164.5429263765338135, 9.058813317711329915, 2.943386871421369566 ) ) ;
#25803=EDGE_CURVE ( 'NONE', #34770, #49320, #32991, .T. ) ;
#25809=CARTESIAN_POINT ( 'NONE',  ( -90.59292637653381064, -3.094860106618431139, -9.524999999999991473 ) ) ;
#25811=FACE_OUTER_BOUND ( 'NONE', #14340, .T. ) ;
#25817=CARTESIAN_POINT ( 'NONE',  ( -181.4049999999999727, -2.607480562269069768, 8.024999999999991473 ) ) ;
#25820=CARTESIAN_POINT ( 'NONE',  ( -74.15707362346617515, -9.058813317711329915, -2.943386871421370898 ) ) ;
#25822=CARTESIAN_POINT ( 'NONE',  ( -110.2429263765338021, 5.598654528085804216, 7.705886871421366635 ) ) ;
#25829=CARTESIAN_POINT ( 'NONE',  ( -104.6049999999999898, 6.826472737025113702, -4.959722759717902107 ) ) ;
#25836=CARTESIAN_POINT ( 'NONE',  ( -83.90707362346614673, -3.094860106618429807, 9.524999999999991473 ) ) ;
#25842=CARTESIAN_POINT ( 'NONE',  ( -72.59499999999998465, 2.607480562269073321, 8.024999999999991473 ) ) ;
#25854=ORIENTED_EDGE ( 'NONE', *, *, #67014, .T. ) ;
#25855=FACE_OUTER_BOUND ( 'NONE', #62255, .T. ) ;
#25858=CARTESIAN_POINT ( 'NONE',  ( -160.7070736234661865, -3.094860106618431139, -9.524999999999991473 ) ) ;
#25861=CARTESIAN_POINT ( 'NONE',  ( -104.7570736234661695, -5.598654528085801552, 7.705886871421367523 ) ) ;
#25866=CARTESIAN_POINT ( 'NONE',  ( -135.9549999999999841, -7.632228543268599452, 2.479861379858951054 ) ) ;
#25870=CARTESIAN_POINT ( 'NONE',  ( -156.1450000000000102, -4.716976649647092401, 6.492361379858946790 ) ) ;
#25871=CARTESIAN_POINT ( 'NONE',  ( -136.9449999999999932, -9.827790563157499189E-16, -8.024999999999991473 ) ) ;
#25879=CARTESIAN_POINT ( 'NONE',  ( -50.15499999999997982, 7.632228543268600340, 2.479861379858949277 ) ) ;
#25883=CARTESIAN_POINT ( 'NONE',  ( -52.34292637653378932, -9.058813317711329915, 2.943386871421371787 ) ) ;
#25889=CARTESIAN_POINT ( 'NONE',  ( -81.80707362346616662, 10.01517768586948698, -1.839758294383808966E-15 ) ) ;
#25913=CARTESIAN_POINT ( 'NONE',  ( -102.8949999999999960, 6.826472737025116366, 4.959722759717898555 ) ) ;
#25915=DIRECTION ( 'NONE',  ( 0.000000000000000000, 0.5877852522924733591, -0.8090169943749472292 ) ) ;
#25921=( BOUNDED_CURVE ( )  B_SPLINE_CURVE ( 2, ( #35757, #19566, #57554, #4772, #31847, #36493, #3699, #63518, #58247, #9382, #53335 ),
 .UNSPECIFIED., .F., .F. ) 
 B_SPLINE_CURVE_WITH_KNOTS ( ( 3, 2, 2, 2, 2, 3 ),
 ( 0.01086956521739105945, 0.01304347826086927134, 0.01521739130434748496, 0.01739130434782569512, 0.01956521739130390874, 0.02173913043478211890 ),
 .UNSPECIFIED. ) 
 CURVE ( )  GEOMETRIC_REPRESENTATION_ITEM ( )  RATIONAL_B_SPLINE_CURVE ( ( 1.000000000000005551, 0.9510565162951480911, 1.000000000000000000, 0.9510565162951535312, 1.000000000000000000, 0.9510565162951535312, 1.000000000000000000, 0.9510565162951535312, 1.000000000000000000, 0.9510565162951645224, 0.9999999999999890088 ) ) 
 REPRESENTATION_ITEM ( '' )  );
#25932=CARTESIAN_POINT ( 'NONE',  ( -184.0000000000000853, -6.613845720572140152, 4.561563678776720643 ) ) ;
#25942=CARTESIAN_POINT ( 'NONE',  ( -181.9429263765338192, 0.000000000000000000, 9.524999999999991473 ) ) ;
#25946=CARTESIAN_POINT ( 'NONE',  ( -167.7549999999999955, 4.716976649647091513, -6.492361379858946790 ) ) ;
#25948=CARTESIAN_POINT ( 'NONE',  ( -147.2070736234666697, 3.094860106625827445, 9.524999999994619770 ) ) ;
#25951=CARTESIAN_POINT ( 'NONE',  ( -183.2949999999999307, -2.607480562269069768, 8.024999999999991473 ) ) ;
#25952=CARTESIAN_POINT ( 'NONE',  ( -178.9449999999999932, -9.827790563157499189E-16, -8.024999999999991473 ) ) ;
#25953=VERTEX_POINT ( 'NONE', #29593 ) ;
#25956=CARTESIAN_POINT ( 'NONE',  ( -92.75499999999999545, 4.716976649647091513, -6.492361379858946790 ) ) ;
#25960=CARTESIAN_POINT ( 'NONE',  ( -87.74499999999999034, 4.716976649647094177, 6.492361379858945902 ) ) ;
#25962=CARTESIAN_POINT ( 'NONE',  ( -59.69499999999997897, -8.437984349512085203, 5.166775262442717831E-16 ) ) ;
#25965=CARTESIAN_POINT ( 'NONE',  ( -170.2429263765338305, 5.598654528085804216, 7.705886871421366635 ) ) ;
#25985=CARTESIAN_POINT ( 'NONE',  ( -134.2429263765338305, 5.598654528085804216, 7.705886871421366635 ) ) ;
#25992=CARTESIAN_POINT ( 'NONE',  ( -117.6550000000000011, -7.632228543268600340, -2.479861379858950166 ) ) ;
#26011=CIRCLE ( 'NONE', #37363, 8.525000000000000355 ) ;
#26017=CARTESIAN_POINT ( 'NONE',  ( -54.29292637653379927, 3.094860106618428031, -9.524999999999993250 ) ) ;
#26020=CARTESIAN_POINT ( 'NONE',  ( -154.8549999999999898, 4.716976649647094177, 6.492361379858945902 ) ) ;
#26023=VECTOR ( 'NONE', #33589, 1000.000000000000000 ) ;
#26027=B_SPLINE_CURVE_WITH_KNOTS ( 'NONE', 1,
 ( #13402, #57018 ),
 .UNSPECIFIED., .F., .F.,
 ( 2, 2 ),
 ( 0.000000000000000000, 1.000000000000000000 ),
 .UNSPECIFIED. ) ;
#26029=AXIS2_PLACEMENT_3D ( 'NONE', #43547, #39286, #16457 ) ;
#26032=VECTOR ( 'NONE', #15877, 1000.000000000000000 ) ;
#26034=CARTESIAN_POINT ( 'NONE',  ( -64.55499999999999261, 0.000000000000000000, 8.024999999999991473 ) ) ;
#26040=CARTESIAN_POINT ( 'NONE',  ( -91.10707362346617799, 8.102448949553172852, -5.886773742842744461 ) ) ;
#26053=CARTESIAN_POINT ( 'NONE',  ( -124.0449999999999875, 7.632228543268600340, 2.479861379858949277 ) ) ;
#26055=CARTESIAN_POINT ( 'NONE',  ( -92.69499999999996476, -8.437984349512085203, 5.166775262442717831E-16 ) ) ;
#26059=( BOUNDED_CURVE ( )  B_SPLINE_CURVE ( 2, ( #39103, #49989, #28482, #61210, #65803, #45081, #34131, #27782, #60172, #34476, #60850 ),
 .UNSPECIFIED., .F., .F. ) 
 B_SPLINE_CURVE_WITH_KNOTS ( ( 3, 2, 2, 2, 2, 3 ),
 ( 0.3695652173912956084, 0.3717391304347738568, 0.3739130434782520496, 0.3760869565217301869, 0.3782608695652083797, 0.3804347826086866280 ),
 .UNSPECIFIED. ) 
 CURVE ( )  GEOMETRIC_REPRESENTATION_ITEM ( )  RATIONAL_B_SPLINE_CURVE ( ( 1.000000000000196287, 0.9510565162949573548, 1.000000000000000000, 0.9510565162951535312, 1.000000000000000000, 0.9510565162951535312, 1.000000000000000000, 0.9510565162951535312, 1.000000000000000000, 0.9510565162953572571, 0.9999999999997962741 ) ) 
 REPRESENTATION_ITEM ( '' )  );
#26061=VERTEX_POINT ( 'NONE', #35583 ) ;
#26063=CARTESIAN_POINT ( 'NONE',  ( -132.5929263765337964, -3.094860106618431139, -9.524999999999991473 ) ) ;
#26064=CARTESIAN_POINT ( 'NONE',  ( -195.0000000000000000, 0.000000000000000000, 0.000000000000000000 ) ) ;
#26065=CARTESIAN_POINT ( 'NONE',  ( -157.0449999999999875, 7.632228543268600340, 2.479861379858949277 ) ) ;
#26076=CARTESIAN_POINT ( 'NONE',  ( -130.1070736234661922, 8.102448949553172852, -5.886773742842744461 ) ) ;
#26080=CARTESIAN_POINT ( 'NONE',  ( -150.3549999999999898, -4.716976649647093289, -6.492361379858945902 ) ) ;
#26092=CARTESIAN_POINT ( 'NONE',  ( -58.94292637653381206, 0.000000000000000000, 9.524999999999991473 ) ) ;
#26094=CARTESIAN_POINT ( 'NONE',  ( -63.50499999999998124, -6.826472737025113702, -4.959722759717900331 ) ) ;
#26095=CARTESIAN_POINT ( 'NONE',  ( -80.90707362346616094, -3.094860106618429807, 9.524999999999991473 ) ) ;
#26105=CARTESIAN_POINT ( 'NONE',  ( -176.7549999999999955, 4.716976649647091513, -6.492361379858946790 ) ) ;
#26114=CARTESIAN_POINT ( 'NONE',  ( -127.5570736234661950, -1.166476076187852838E-15, -9.524999999999991473 ) ) ;
#26117=CARTESIAN_POINT ( 'NONE',  ( -92.45499999999998408, 7.632228543268599452, -2.479861379858951942 ) ) ;
#26122=CARTESIAN_POINT ( 'NONE',  ( -134.6070736234661638, -8.102448949553172852, 5.886773742842742685 ) ) ;
#26126=CARTESIAN_POINT ( 'NONE',  ( -74.30707362346615241, -10.01517768586948698, 6.132527647946031529E-16 ) ) ;
#26134=CARTESIAN_POINT ( 'NONE',  ( -111.0549999999999926, -9.827790563157499189E-16, -8.024999999999991473 ) ) ;
#26137=CARTESIAN_POINT ( 'NONE',  ( -129.5949999999999989, 2.607480562269073321, 8.024999999999991473 ) ) ;
#26139=VECTOR ( 'NONE', #12698, 1000.000000000000000 ) ;
#26145=CARTESIAN_POINT ( 'NONE',  ( -159.5929263765337680, -3.094860106618431139, -9.524999999999991473 ) ) ;
#26153=CARTESIAN_POINT ( 'NONE',  ( -74.69292637653379074, 10.01517768586948698, -1.839758294383808571E-15 ) ) ;
#26160=CARTESIAN_POINT ( 'NONE',  ( -175.5549999999999784, 0.000000000000000000, 8.024999999999991473 ) ) ;
#26164=CARTESIAN_POINT ( 'NONE',  ( -74.90707362346617515, -3.094860106618429807, 9.524999999999991473 ) ) ;
#26174=CARTESIAN_POINT ( 'NONE',  ( -90.50499999999998124, -6.826472737025113702, -4.959722759717900331 ) ) ;
#26181=ORIENTED_EDGE ( 'NONE', *, *, #31787, .F. ) ;
#26183=CARTESIAN_POINT ( 'NONE',  ( -73.04499999999998749, 7.632228543268600340, 2.479861379858949277 ) ) ;
#26197=CARTESIAN_POINT ( 'NONE',  ( -175.5570736234661808, -1.166476076187852838E-15, -9.524999999999991473 ) ) ;
#26203=CARTESIAN_POINT ( 'NONE',  ( -149.0929263765342228, 3.094860106625894947, 9.524999999994570032 ) ) ;
#26205=CARTESIAN_POINT ( 'NONE',  ( -163.1070736234661354, 8.102448949553171076, -5.886773742842744461 ) ) ;
#26207=CARTESIAN_POINT ( 'NONE',  ( -99.20707362346618652, 3.094860106618433360, 9.524999999999991473 ) ) ;
#26216=CARTESIAN_POINT ( 'NONE',  ( -140.7549999999999955, 4.716976649647091513, -6.492361379858946790 ) ) ;
#26219=CARTESIAN_POINT ( 'NONE',  ( -150.2949999999999875, -2.607480562269069768, 8.024999999999991473 ) ) ;
#26223=CARTESIAN_POINT ( 'NONE',  ( -134.2450000000000045, -4.716976649647093289, -6.492361379858945902 ) ) ;
#26231=CARTESIAN_POINT ( 'NONE',  ( -55.40499999999997982, -2.607480562269069768, 8.024999999999991473 ) ) ;
#26234=CARTESIAN_POINT ( 'NONE',  ( -139.9429263765337907, 0.000000000000000000, 9.524999999999991473 ) ) ;
#26245=CARTESIAN_POINT ( 'NONE',  ( -178.7929263765338703, -3.094860106617228102, 9.525000000000863665 ) ) ;
#26253=( BOUNDED_CURVE ( )  B_SPLINE_CURVE ( 2, ( #60142, #15873, #32027, #64730, #27415, #11603, #69654, #21467, #21826, #54837, #641 ),
 .UNSPECIFIED., .F., .F. ) 
 B_SPLINE_CURVE_WITH_KNOTS ( ( 3, 2, 2, 2, 2, 3 ),
 ( 0.6304347826086806883, 0.6326086956521589366, 0.6347826086956371849, 0.6369565217391153222, 0.6391304347825935706, 0.6413043478260718189 ),
 .UNSPECIFIED. ) 
 CURVE ( )  GEOMETRIC_REPRESENTATION_ITEM ( )  RATIONAL_B_SPLINE_CURVE ( ( 1.000000000000337508, 0.9510565162948161344, 1.000000000000000000, 0.9510565162951535312, 1.000000000000000000, 0.9510565162951535312, 1.000000000000000000, 0.9510565162951535312, 1.000000000000000000, 0.9510565162954934815, 0.9999999999996600497 ) ) 
 REPRESENTATION_ITEM ( '' )  );
#26268=CARTESIAN_POINT ( 'NONE',  ( -97.94499999999999318, -9.827790563157499189E-16, -8.024999999999991473 ) ) ;
#26277=CARTESIAN_POINT ( 'NONE',  ( -61.85707362346616378, -5.598654528085803328, -7.705886871421366635 ) ) ;
#26293=CARTESIAN_POINT ( 'NONE',  ( -170.6070736234661922, -8.102448949553174629, 5.886773742842742685 ) ) ;
#26296=CARTESIAN_POINT ( 'NONE',  ( -167.1550000000000011, 7.632228543268600340, 2.479861379858949277 ) ) ;
#26299=CARTESIAN_POINT ( 'NONE',  ( -179.9950000000000045, -6.826472737025115478, 4.959722759717900331 ) ) ;
#26300=CARTESIAN_POINT ( 'NONE',  ( -167.9949999999999761, -6.826472737025113702, 4.959722759717902107 ) ) ;
#26305=CARTESIAN_POINT ( 'NONE',  ( -81.50499999999999545, -6.826472737025115478, -4.959722759717899443 ) ) ;
#26306=CARTESIAN_POINT ( 'NONE',  ( -195.0000000000000000, 1.166476076187852838E-15, -9.524999999999991473 ) ) ;
#26307=DIRECTION ( 'NONE',  ( -1.000000000000000000, -0.000000000000000000, -0.000000000000000000 ) ) ;
#26309=CARTESIAN_POINT ( 'NONE',  ( -85.34499999999998465, 7.632228543268599452, -2.479861379858951942 ) ) ;
#26313=CARTESIAN_POINT ( 'NONE',  ( -171.8070736234661808, 10.01517768586948698, -1.839758294383808966E-15 ) ) ;
#26325=ORIENTED_EDGE ( 'NONE', *, *, #19130, .F. ) ;
#26328=CARTESIAN_POINT ( 'NONE',  ( -174.0570736234661808, 0.000000000000000000, 9.524999999999991473 ) ) ;
#26338=CARTESIAN_POINT ( 'NONE',  ( -120.5049999999999670, -6.826472737025113702, -4.959722759717900331 ) ) ;
#26355=CARTESIAN_POINT ( 'NONE',  ( -135.6570736234661751, 9.058813317711329915, 2.943386871421369566 ) ) ;
#26356=CARTESIAN_POINT ( 'NONE',  ( -195.0000000000000000, 0.000000000000000000, 0.000000000000000000 ) ) ;
#26357=ORIENTED_EDGE ( 'NONE', *, *, #45497, .F. ) ;
#26368=CARTESIAN_POINT ( 'NONE',  ( -58.79292637653379927, -3.094860106618429807, 9.524999999999991473 ) ) ;
#26373=CARTESIAN_POINT ( 'NONE',  ( -156.9549999999999841, -7.632228543268599452, 2.479861379858951054 ) ) ;
#26378=EDGE_CURVE ( 'NONE', #30878, #59688, #47142, .T. ) ;
#26387=CARTESIAN_POINT ( 'NONE',  ( -65.15499999999998693, 7.632228543268600340, 2.479861379858949277 ) ) ;
#26401=CARTESIAN_POINT ( 'NONE',  ( -122.2449999999999903, -4.716976649647093289, -6.492361379858945902 ) ) ;
#26403=CARTESIAN_POINT ( 'NONE',  ( -87.89499999999998181, 6.826472737025116366, 4.959722759717898555 ) ) ;
#26410=CARTESIAN_POINT ( 'NONE',  ( -131.9929263765338305, 8.102448949553171076, -5.886773742842744461 ) ) ;
#26412=CARTESIAN_POINT ( 'NONE',  ( -147.5949999999999704, 2.607480562269073321, 8.024999999999991473 ) ) ;
#26423=CARTESIAN_POINT ( 'NONE',  ( -59.24292637653380211, 5.598654528085804216, 7.705886871421366635 ) ) ;
#26426=CARTESIAN_POINT ( 'NONE',  ( -151.1049999999999613, -6.826472737025113702, 4.959722759717902107 ) ) ;
#26430=CARTESIAN_POINT ( 'NONE',  ( -141.6570736234662036, 9.058813317711329915, 2.943386871421369566 ) ) ;
#26438=EDGE_CURVE ( 'NONE', #65525, #8699, #57996, .T. ) ;
#26443=CARTESIAN_POINT ( 'NONE',  ( -63.20499999999998408, -2.607480562269071545, -8.024999999999991473 ) ) ;
#26444=DIRECTION ( 'NONE',  ( -1.000000000000000000, -0.000000000000000000, -0.000000000000000000 ) ) ;
#26458=CARTESIAN_POINT ( 'NONE',  ( -182.4550000000000125, 7.632228543268599452, -2.479861379858951942 ) ) ;
#26461=CARTESIAN_POINT ( 'NONE',  ( -88.10707362346616378, 8.102448949553172852, -5.886773742842744461 ) ) ;
#26470=CARTESIAN_POINT ( 'NONE',  ( -90.95499999999999829, -7.632228543268599452, 2.479861379858951054 ) ) ;
#26474=CARTESIAN_POINT ( 'NONE',  ( -128.1570736234661751, -9.058813317711329915, -2.943386871421370898 ) ) ;
#26477=CARTESIAN_POINT ( 'NONE',  ( -63.65707362346617515, 9.058813317711329915, 2.943386871421369566 ) ) ;
#26480=DIRECTION ( 'NONE',  ( -1.000000000000000000, -0.000000000000000000, -0.000000000000000000 ) ) ;
#26484=CARTESIAN_POINT ( 'NONE',  ( -110.3049999999999926, 8.437984349512085203, -1.550032578732815448E-15 ) ) ;
#26486=CARTESIAN_POINT ( 'NONE',  ( -118.3449999999999989, 7.632228543268599452, -2.479861379858951942 ) ) ;
#26490=CARTESIAN_POINT ( 'NONE',  ( -45.00000000000000000, 0.000000000000000000, 0.000000000000000000 ) ) ;
#26492=CARTESIAN_POINT ( 'NONE',  ( -161.9929263765337737, 8.102448949553171076, -5.886773742842744461 ) ) ;
#26493=CARTESIAN_POINT ( 'NONE',  ( -182.9949999999999761, -6.826472737025115478, 4.959722759717900331 ) ) ;
#26498=ORIENTED_EDGE ( 'NONE', *, *, #33973, .T. ) ;
#26499=CARTESIAN_POINT ( 'NONE',  ( -74.09292637653381064, 3.094860106618433360, 9.524999999999991473 ) ) ;
#26507=CARTESIAN_POINT ( 'NONE',  ( -177.8049999999999500, -8.437984349512086979, 5.166775262442717831E-16 ) ) ;
#26521=CARTESIAN_POINT ( 'NONE',  ( -97.85499999999998977, 4.716976649647094177, 6.492361379858945902 ) ) ;
#26534=CARTESIAN_POINT ( 'NONE',  ( -73.49499999999999034, 6.826472737025113702, -4.959722759717902107 ) ) ;
#26538=CARTESIAN_POINT ( 'NONE',  ( -125.4570736234661723, -9.058813317711329915, 2.943386871421371787 ) ) ;
#26542=CARTESIAN_POINT ( 'NONE',  ( -195.0000000000000000, 1.166476076187852838E-15, -9.524999999999991473 ) ) ;
#26548=CARTESIAN_POINT ( 'NONE',  ( -157.7070736234661865, -3.094860106618431139, -9.524999999999991473 ) ) ;
#26550=CARTESIAN_POINT ( 'NONE',  ( -95.60707362346617799, -8.102448949553172852, 5.886773742842742685 ) ) ;
#26557=CARTESIAN_POINT ( 'NONE',  ( -137.0049999999999670, 6.826472737025116366, 4.959722759717898555 ) ) ;
#26560=CARTESIAN_POINT ( 'NONE',  ( -158.5449999999999875, -7.632228543268600340, -2.479861379858950166 ) ) ;
#26562=CARTESIAN_POINT ( 'NONE',  ( -137.3949999999999818, -6.826472737025113702, -4.959722759717900331 ) ) ;
#26567=CARTESIAN_POINT ( 'NONE',  ( -57.05499999999999261, -9.827790563157499189E-16, -8.024999999999991473 ) ) ;
#26572=CARTESIAN_POINT ( 'NONE',  ( -155.3070736234661524, -10.01517768586948698, 6.132527647946031529E-16 ) ) ;
#26573=CARTESIAN_POINT ( 'NONE',  ( -168.0570736234661808, 0.000000000000000000, 9.524999999999991473 ) ) ;
#26584=EDGE_CURVE ( 'NONE', #57697, #27775, #42891, .T. ) ;
#26585=LINE ( 'NONE', #15728, #6807 ) ;
#26588=ADVANCED_FACE ( 'NONE', ( #38292 ), #69236, .T. ) ;
#26592=CARTESIAN_POINT ( 'NONE',  ( -108.5070736234661695, 8.102448949553176405, 5.886773742842740909 ) ) ;
#26593=FACE_OUTER_BOUND ( 'NONE', #39885, .T. ) ;
#26594=CARTESIAN_POINT ( 'NONE',  ( -100.9429263765338050, 0.000000000000000000, 9.524999999999991473 ) ) ;
#26602=CARTESIAN_POINT ( 'NONE',  ( -99.74499999999999034, 4.716976649647094177, 6.492361379858945902 ) ) ;
#26628=ORIENTED_EDGE ( 'NONE', *, *, #41034, .F. ) ;
#26629=CARTESIAN_POINT ( 'NONE',  ( -165.5049999999999955, -6.826472737025115478, -4.959722759717899443 ) ) ;
#26632=CARTESIAN_POINT ( 'NONE',  ( -180.4449999999999932, 0.000000000000000000, 8.024999999999991473 ) ) ;
#26633=CARTESIAN_POINT ( 'NONE',  ( -165.2949999999999591, -2.607480562269069768, 8.024999999999991473 ) ) ;
#26639=CARTESIAN_POINT ( 'NONE',  ( -87.50499999999995282, -6.826472737025115478, -4.959722759717899443 ) ) ;
#26644=CARTESIAN_POINT ( 'NONE',  ( -77.39499999999999602, -6.826472737025113702, -4.959722759717900331 ) ) ;
#26649=CARTESIAN_POINT ( 'NONE',  ( -74.99292637653380211, 8.102448949553172852, -5.886773742842744461 ) ) ;
#26662=ORIENTED_EDGE ( 'NONE', *, *, #11446, .T. ) ;
#26664=CARTESIAN_POINT ( 'NONE',  ( -134.9929263765338021, 8.102448949553172852, -5.886773742842744461 ) ) ;
#26665=CARTESIAN_POINT ( 'NONE',  ( -120.0570736234661808, 0.000000000000000000, 9.524999999999991473 ) ) ;
#26670=CARTESIAN_POINT ( 'NONE',  ( -124.2549999999999955, -4.716976649647092401, 6.492361379858946790 ) ) ;
#26677=ORIENTED_EDGE ( 'NONE', *, *, #42934, .F. ) ;
#26685=CYLINDRICAL_SURFACE ( 'NONE', #67844, 9.524999999999991473 ) ;
#26697=CARTESIAN_POINT ( 'NONE',  ( -51.44292637653380496, -1.166476076187852838E-15, -9.524999999999991473 ) ) ;
#26701=CARTESIAN_POINT ( 'NONE',  ( -143.9050000000000011, 2.607480562269068880, -8.024999999999993250 ) ) ;
#26714=CARTESIAN_POINT ( 'NONE',  ( -59.00499999999998124, 6.826472737025116366, 4.959722759717898555 ) ) ;
#26720=CARTESIAN_POINT ( 'NONE',  ( -128.0929263765345070, 3.094860106630465957, 9.524999999991248245 ) ) ;
#26725=CARTESIAN_POINT ( 'NONE',  ( -111.5949999999999704, 2.607480562269072433, 8.024999999999991473 ) ) ;
#26727=CARTESIAN_POINT ( 'NONE',  ( -86.84499999999998465, -7.632228543268599452, 2.479861379858951054 ) ) ;
#26728=ADVANCED_FACE ( 'NONE', ( #49859 ), #35256, .T. ) ;
#26730=CYLINDRICAL_SURFACE ( 'NONE', #19036, 9.524999999999991473 ) ;
#26731=CARTESIAN_POINT ( 'NONE',  ( -190.0000000000000000, 0.000000000000000000, 5.499999999999984901 ) ) ;
#26734=CARTESIAN_POINT ( 'NONE',  ( -135.2929263765337851, 3.094860106618428031, -9.524999999999993250 ) ) ;
#26736=CARTESIAN_POINT ( 'NONE',  ( -148.3449999999999989, 7.632228543268599452, -2.479861379858951942 ) ) ;
#26737=CARTESIAN_POINT ( 'NONE',  ( -195.0000000000000000, 0.000000000000000000, 0.000000000000000000 ) ) ;
#26741=CARTESIAN_POINT ( 'NONE',  ( -48.59499999999997044, 2.607480562269072433, 8.024999999999991473 ) ) ;
#26754=CARTESIAN_POINT ( 'NONE',  ( -148.1049999999999898, -6.826472737025113702, 4.959722759717902107 ) ) ;
#26757=CARTESIAN_POINT ( 'NONE',  ( -141.9570736234661865, 9.058813317711329915, -2.943386871421373119 ) ) ;
#26764=CARTESIAN_POINT ( 'NONE',  ( -68.00499999999998124, 6.826472737025115478, 4.959722759717899443 ) ) ;
#26766=CARTESIAN_POINT ( 'NONE',  ( -118.3449999999999989, 7.632228543268599452, -2.479861379858951942 ) ) ;
#26779=CARTESIAN_POINT ( 'NONE',  ( -169.8550000000000182, 4.716976649647094177, 6.492361379858945902 ) ) ;
#26788=CARTESIAN_POINT ( 'NONE',  ( -97.25499999999999545, -4.716976649647092401, 6.492361379858946790 ) ) ;
#26792=CARTESIAN_POINT ( 'NONE',  ( -129.3570736234661922, 5.598654528085804216, 7.705886871421366635 ) ) ;
#26794=CARTESIAN_POINT ( 'NONE',  ( -65.90707362346617515, -3.094860106618429807, 9.524999999999991473 ) ) ;
#26801=CARTESIAN_POINT ( 'NONE',  ( -108.8049999999999784, -8.437984349512085203, 5.166775262442717831E-16 ) ) ;
#26803=CARTESIAN_POINT ( 'NONE',  ( -113.2449999999999903, -4.716976649647093289, -6.492361379858945902 ) ) ;
#26807=CARTESIAN_POINT ( 'NONE',  ( -166.0429263765338135, -9.058813317711329915, -2.943386871421370898 ) ) ;
#26808=CARTESIAN_POINT ( 'NONE',  ( -171.7450000000000045, 4.716976649647094177, 6.492361379858945902 ) ) ;
#26811=ADVANCED_FACE ( 'NONE', ( #44270 ), #29414, .T. ) ;
#26812=CARTESIAN_POINT ( 'NONE',  ( -151.9429263765338192, 0.000000000000000000, 9.524999999999991473 ) ) ;
#26820=CARTESIAN_POINT ( 'NONE',  ( -76.94292637653380496, 0.000000000000000000, 9.524999999999991473 ) ) ;
#26831=CARTESIAN_POINT ( 'NONE',  ( -74.75707362346616947, -5.598654528085801552, 7.705886871421367523 ) ) ;
#26836=CARTESIAN_POINT ( 'NONE',  ( -93.50499999999999545, -6.826472737025113702, -4.959722759717900331 ) ) ;
#26849=CARTESIAN_POINT ( 'NONE',  ( -76.49500000000000455, 6.826472737025113702, -4.959722759717902107 ) ) ;
#26858=CARTESIAN_POINT ( 'NONE',  ( -123.3549999999999898, -4.716976649647093289, -6.492361379858945902 ) ) ;
#26860=CARTESIAN_POINT ( 'NONE',  ( -73.19292637653379074, -10.01517768586948698, 6.132527647946031529E-16 ) ) ;
#26867=CARTESIAN_POINT ( 'NONE',  ( -163.4070736234661467, 3.094860106618428031, -9.524999999999993250 ) ) ;
#26871=CARTESIAN_POINT ( 'NONE',  ( -92.15707362346617515, -9.058813317711329915, -2.943386871421370898 ) ) ;
#26874=ORIENTED_EDGE ( 'NONE', *, *, #728, .T. ) ;
#26879=CARTESIAN_POINT ( 'NONE',  ( -141.2050000000000125, -2.607480562269071545, -8.024999999999991473 ) ) ;
#26883=CARTESIAN_POINT ( 'NONE',  ( -141.7450000000000045, 4.716976649647094177, 6.492361379858945902 ) ) ;
#26886=CARTESIAN_POINT ( 'NONE',  ( -139.6449999999999818, 4.716976649647091513, -6.492361379858946790 ) ) ;
#26893=CARTESIAN_POINT ( 'NONE',  ( -53.00500000000000256, 6.826472737025116366, 4.959722759717898555 ) ) ;
#26896=LINE ( 'NONE', #38582, #51121 ) ;
#26900=CARTESIAN_POINT ( 'NONE',  ( -108.4429263765338050, -1.166476076187852838E-15, -9.524999999999991473 ) ) ;
#26902=CARTESIAN_POINT ( 'NONE',  ( -152.2429263765338021, 5.598654528085804216, 7.705886871421366635 ) ) ;
#26906=CARTESIAN_POINT ( 'NONE',  ( -99.65707362346617515, 9.058813317711329915, 2.943386871421369566 ) ) ;
#26920=ORIENTED_EDGE ( 'NONE', *, *, #13085, .T. ) ;
#26922=CARTESIAN_POINT ( 'NONE',  ( -195.0000000000000000, 0.000000000000000000, 0.000000000000000000 ) ) ;
#26924=ORIENTED_EDGE ( 'NONE', *, *, #47656, .T. ) ;
#26929=CARTESIAN_POINT ( 'NONE',  ( -97.04499999999998749, 7.632228543268600340, 2.479861379858949277 ) ) ;
#26944=FACE_OUTER_BOUND ( 'NONE', #35970, .T. ) ;
#26946=( BOUNDED_CURVE ( )  B_SPLINE_CURVE ( 2, ( #6945, #55482, #6576, #5896, #22093, #28021, #55117, #17194, #12555, #23144, #34023 ),
 .UNSPECIFIED., .F., .F. ) 
 B_SPLINE_CURVE_WITH_KNOTS ( ( 3, 2, 2, 2, 2, 3 ),
 ( 0.05434782608695527817, 0.05652173913043349179, 0.05869565217391169848, 0.06086956521738991210, 0.06304347826086811879, 0.06521739130434632548 ),
 .UNSPECIFIED. ) 
 CURVE ( )  GEOMETRIC_REPRESENTATION_ITEM ( )  RATIONAL_B_SPLINE_CURVE ( ( 1.000000000000027978, 0.9510565162951255536, 1.000000000000000000, 0.9510565162951535312, 1.000000000000000000, 0.9510565162951535312, 1.000000000000000000, 0.9510565162951535312, 1.000000000000000000, 0.9510565162951872820, 0.9999999999999662492 ) ) 
 REPRESENTATION_ITEM ( '' )  );
#26955=CARTESIAN_POINT ( 'NONE',  ( -48.80707362346616662, 10.01517768586948698, -1.839758294383808966E-15 ) ) ;
#26962=CARTESIAN_POINT ( 'NONE',  ( -173.3049999999999500, 8.437984349512085203, -1.550032578732815448E-15 ) ) ;
#26967=CARTESIAN_POINT ( 'NONE',  ( -176.5450000000000159, -7.632228543268600340, -2.479861379858950166 ) ) ;
#26969=CARTESIAN_POINT ( 'NONE',  ( -163.3449999999999989, 7.632228543268599452, -2.479861379858951942 ) ) ;
#26972=CARTESIAN_POINT ( 'NONE',  ( -89.09292637653379643, 3.094860106618433360, 9.524999999999991473 ) ) ;
#26976=CARTESIAN_POINT ( 'NONE',  ( -10.16381930648914711, 11.93252338341607910, -1.311443076476738856 ) ) ;
#26977=CARTESIAN_POINT ( 'NONE',  ( -80.15499999999998693, 7.632228543268600340, 2.479861379858949277 ) ) ;
#26981=CARTESIAN_POINT ( 'NONE',  ( -77.69499999999999318, -8.437984349512086979, 5.166775262442717831E-16 ) ) ;
#26984=EDGE_CURVE ( 'NONE', #47261, #8699, #40336, .T. ) ;
#27008=CARTESIAN_POINT ( 'NONE',  ( -112.7049999999999699, 2.607480562269072433, 8.024999999999991473 ) ) ;
#27011=CARTESIAN_POINT ( 'NONE',  ( -195.0000000000000000, 0.000000000000000000, 0.000000000000000000 ) ) ;
#27025=CARTESIAN_POINT ( 'NONE',  ( -136.5570736234661808, -1.166476076187852838E-15, -9.524999999999991473 ) ) ;
#27026=CARTESIAN_POINT ( 'NONE',  ( -181.4929263765337737, -8.102448949553174629, 5.886773742842742685 ) ) ;
#27030=CARTESIAN_POINT ( 'NONE',  ( -48.05707362346617373, 0.000000000000000000, 9.524999999999991473 ) ) ;
#27037=CARTESIAN_POINT ( 'NONE',  ( -52.94292637653380496, 0.000000000000000000, 9.524999999999991473 ) ) ;
#27040=CARTESIAN_POINT ( 'NONE',  ( -144.6549999999999727, -7.632228543268600340, -2.479861379858950166 ) ) ;
#27041=CARTESIAN_POINT ( 'NONE',  ( -175.5570736234661808, -1.166476076187852838E-15, -9.524999999999991473 ) ) ;
#27044=EDGE_CURVE ( 'NONE', #3787, #68105, #40757, .T. ) ;
#27048=EDGE_LOOP ( 'NONE', ( #47345, #20788, #19118, #40151 ) ) ;
#27049=DIRECTION ( 'NONE',  ( -1.000000000000000000, -0.000000000000000000, -0.000000000000000000 ) ) ;
#27052=CARTESIAN_POINT ( 'NONE',  ( -56.30499999999999972, 8.437984349512085203, -1.550032578732815448E-15 ) ) ;
#27061=CARTESIAN_POINT ( 'NONE',  ( -128.2429263765338021, 5.598654528085804216, 7.705886871421366635 ) ) ;
#27063=( BOUNDED_CURVE ( )  B_SPLINE_CURVE ( 2, ( #36057, #57137, #62429, #10015, #14958, #41699, #57499, #36782, #63121, #57863, #19856 ),
 .UNSPECIFIED., .F., .F. ) 
 B_SPLINE_CURVE_WITH_KNOTS ( ( 3, 2, 2, 2, 2, 3 ),
 ( 0.5869565217391164991, 0.5891304347825947474, 0.5913043478260728847, 0.5934782608695511330, 0.5956521739130292703, 0.5978260869565075186 ),
 .UNSPECIFIED. ) 
 CURVE ( )  GEOMETRIC_REPRESENTATION_ITEM ( )  RATIONAL_B_SPLINE_CURVE ( ( 1.000000000000314859, 0.9510565162948385609, 1.000000000000000000, 0.9510565162951535312, 1.000000000000000000, 0.9510565162951535312, 1.000000000000000000, 0.9510565162951535312, 1.000000000000000000, 0.9510565162954734975, 0.9999999999996800337 ) ) 
 REPRESENTATION_ITEM ( '' )  );
#27072=CARTESIAN_POINT ( 'NONE',  ( -112.4949999999999761, 6.826472737025113702, -4.959722759717902107 ) ) ;
#27074=CARTESIAN_POINT ( 'NONE',  ( -88.94499999999997897, -9.827790563157499189E-16, -8.024999999999991473 ) ) ;
#27082=CARTESIAN_POINT ( 'NONE',  ( -124.4929263765337879, -8.102448949553172852, 5.886773742842742685 ) ) ;
#27084=CARTESIAN_POINT ( 'NONE',  ( -150.5949999999999989, 2.607480562269073321, 8.024999999999991473 ) ) ;
#27098=CARTESIAN_POINT ( 'NONE',  ( -129.9570736234661865, 9.058813317711329915, -2.943386871421373119 ) ) ;
#27100=CARTESIAN_POINT ( 'NONE',  ( -152.6049999999999898, 6.826472737025113702, -4.959722759717902107 ) ) ;
#27103=CARTESIAN_POINT ( 'NONE',  ( -141.0570736234661808, 0.000000000000000000, 9.524999999999991473 ) ) ;
#27110=CARTESIAN_POINT ( 'NONE',  ( -95.45707362346617231, -9.058813317711329915, 2.943386871421371787 ) ) ;
#27113=CARTESIAN_POINT ( 'NONE',  ( -60.95499999999998408, -7.632228543268599452, 2.479861379858951054 ) ) ;
#27114=CARTESIAN_POINT ( 'NONE',  ( -122.2449999999999903, -4.716976649647093289, -6.492361379858945902 ) ) ;
#27129=CARTESIAN_POINT ( 'NONE',  ( -174.6550000000000011, -7.632228543268600340, -2.479861379858950166 ) ) ;
#27144=CARTESIAN_POINT ( 'NONE',  ( -81.95499999999998408, -7.632228543268599452, 2.479861379858951054 ) ) ;
#27149=CARTESIAN_POINT ( 'NONE',  ( -65.75707362346616947, -5.598654528085801552, 7.705886871421367523 ) ) ;
#27156=CARTESIAN_POINT ( 'NONE',  ( -102.6549999999999869, -7.632228543268600340, -2.479861379858950166 ) ) ;
#27158=CARTESIAN_POINT ( 'NONE',  ( -115.3449999999999847, 7.632228543268599452, -2.479861379858951942 ) ) ;
#27161=CARTESIAN_POINT ( 'NONE',  ( -162.8929263765338078, -8.102448949553172852, -5.886773742842741797 ) ) ;
#27163=CARTESIAN_POINT ( 'NONE',  ( -179.9950000000000045, -6.826472737025115478, 4.959722759717900331 ) ) ;
#27172=CARTESIAN_POINT ( 'NONE',  ( -72.74292637653380211, -5.598654528085803328, -7.705886871421366635 ) ) ;
#27180=CARTESIAN_POINT ( 'NONE',  ( -180.5049999999999670, -6.826472737025113702, -4.959722759717900331 ) ) ;
#27182=AXIS2_PLACEMENT_3D ( 'NONE', #68624, #41561, #36656 ) ;
#27189=CARTESIAN_POINT ( 'NONE',  ( -92.30499999999997840, 8.437984349512086979, -1.550032578732815448E-15 ) ) ;
#27202=CARTESIAN_POINT ( 'NONE',  ( -58.79499999999998749, 2.607480562269068880, -8.024999999999993250 ) ) ;
#27208=ORIENTED_EDGE ( 'NONE', *, *, #56521, .F. ) ;
#27213=CARTESIAN_POINT ( 'NONE',  ( -113.9049999999999869, 2.607480562269068880, -8.024999999999993250 ) ) ;
#27219=CARTESIAN_POINT ( 'NONE',  ( -164.6070736234661922, -8.102448949553172852, 5.886773742842742685 ) ) ;
#27223=CARTESIAN_POINT ( 'NONE',  ( -93.20707362346615810, 3.094860106618433360, 9.524999999999991473 ) ) ;
#27232=ADVANCED_FACE ( 'NONE', ( #34605 ), #47583, .T. ) ;
#27234=CARTESIAN_POINT ( 'NONE',  ( -142.2549999999999955, -4.716976649647092401, 6.492361379858946790 ) ) ;
#27238=CARTESIAN_POINT ( 'NONE',  ( -143.2449999999999761, -4.716976649647093289, -6.492361379858945902 ) ) ;
#27239=CARTESIAN_POINT ( 'NONE',  ( -137.8449999999999989, -7.632228543268599452, 2.479861379858951054 ) ) ;
#27245=CARTESIAN_POINT ( 'NONE',  ( -51.35499999999998266, -4.716976649647093289, -6.492361379858945902 ) ) ;
#27247=CARTESIAN_POINT ( 'NONE',  ( -59.54499999999998749, -7.632228543268600340, -2.479861379858950166 ) ) ;
#27248=CARTESIAN_POINT ( 'NONE',  ( -139.3429263765337964, -9.058813317711329915, 2.943386871421371787 ) ) ;
#27254=CARTESIAN_POINT ( 'NONE',  ( -106.9429263765337907, 0.000000000000000000, 9.524999999999991473 ) ) ;
#27277=DIRECTION ( 'NONE',  ( -1.000000000000000000, -0.000000000000000000, -0.000000000000000000 ) ) ;
#27281=CARTESIAN_POINT ( 'NONE',  ( -88.94499999999997897, -9.827790563157499189E-16, -8.024999999999991473 ) ) ;
#27299=CARTESIAN_POINT ( 'NONE',  ( -165.5070736234661695, 8.102448949553176405, 5.886773742842740909 ) ) ;
#27317=CARTESIAN_POINT ( 'NONE',  ( -171.8050000000000068, -8.437984349512085203, 5.166775262442717831E-16 ) ) ;
#27321=CARTESIAN_POINT ( 'NONE',  ( -172.3449999999999989, 7.632228543268599452, -2.479861379858951942 ) ) ;
#27323=CARTESIAN_POINT ( 'NONE',  ( -168.5949999999999989, 2.607480562269072433, 8.024999999999991473 ) ) ;
#27325=AXIS2_PLACEMENT_3D ( 'NONE', #33307, #6535, #66336 ) ;
#27331=CARTESIAN_POINT ( 'NONE',  ( -85.55499999999999261, 0.000000000000000000, 8.024999999999991473 ) ) ;
#27335=CARTESIAN_POINT ( 'NONE',  ( -81.74499999999999034, 4.716976649647094177, 6.492361379858945902 ) ) ;
#27360=CARTESIAN_POINT ( 'NONE',  ( -112.8550000000000040, 4.716976649647094177, 6.492361379858945902 ) ) ;
#27362=DIRECTION ( 'NONE',  ( 0.000000000000000000, 0.000000000000000000, 1.000000000000000000 ) ) ;
#27370=( BOUNDED_SURFACE ( )  B_SPLINE_SURFACE ( 1, 2, ( 
 ( #50622, #66812, #18264, #12978, #2361, #18623, #68536, #62544, #51316, #57275, #9106, #36206, #67849, #67484, #8415, #35132, #24224, #18931, #8750, #25598, #9808, #31218, #25267, #47114, #3061, #2731, #24551, #45729, #41839, #19644, #56586, #30176, #67141, #30523, #46424, #46066, #62205, #29848, #51662, #3417, #20336, #63254, #19279, #36576, #3779, #40430, #40786, #61843, #15103, #14029, #57634, #35489, #57994, #56936, #68195, #13672, #24910, #41139, #14359, #9456, #35829, #52023, #46790, #19973, #62885, #41472, #14732, #30883, #52381, #4131, #15777, #54067, #16491, #58660, #37955, #26962, #4479, #31573, #64967, #20695, #5874, #47473, #43238, #37259, #64283, #27317, #59015, #48850, #63597, #64642, #547, #47837, #42207, #32602, #21724, #22074, #69235, #10489, #21363, #63928, #58319, #43575, #48500, #16819, #31928, #4850, #59690, #15441, #69560, #42890, #10828, #53406, #25946, #38291, #68896, #32270, #26296, #5185, #11508, #21031, #52712, #37612, #59329, #199, #53055, #36905, #16135, #26629, #53721, #42529, #10140, #5512, #48152, #11158, #66719, #50545, #44269, #39317, #23443, #55808, #54415, #18535, #33656, #40022, #28001, #61411, #55099, #17514, #32980, #44948, #11859, #38989, #65667, #22770, #45298, #6554, #6926, #2267, #23797, #50202, #7611, #1596, #17839, #28351, #23123, #6235, #27663, #29047, #55463, #28713, #1924, #60380, #49171, #872, #22412, #43914, #65326, #17170, #49511, #1239, #7286, #66354, #60720, #38643, #60045, #44615, #49858, #18175, #33324, #66012, #12538, #34002, #12185, #39659, #54745, #61080, #12895, #34359, #8331, #45976, #7967, #40703, #46704, #67758, #35752, #56859, #13579, #4057, #51575, #2644, #24822, #9374, #35409, #56496, #36109, #19558, #20249, #41052, #51936, #13941, #3690, #41753, #62469, #57188, #9018, #45649, #67401, #19193, #67068, #14286, #62115, #40341, #30798, #8674, #61751, #25522, #24143, #50885, #34685, #68117, #57546, #47035, #3332, #13228, #30100, #52299, #46337, #35048, #30435, #25187, #19898, #41395, #29774, #18847, #51236, #56141, #29413, #62803, #68450, #2982, #24471, #14645, #16407, #63513, #471, #15368, #22001, #32521, #58582, #47384, #20959, #63174, #48080, #37174, #36823, #52971, #68816, #42453, #63846, #37881, #53985, #10063, #27234, #64197, #15010, #20606, #52635, #5786, #4764, #26879, #58240, #11071, #26216, #58939, #4392, #31140, #36485, #47757, #109, #48770, #31839, #42120, #10751, #53645, #69152, #57908, #42810, #15692, #10411, #69482, #48418, #32198, #53328, #9732, #5110, #5432, #31487, #26557, #21277, #16053, #21638, #37533, #43155, #64562, #25866, #59249, #7537, #60992, #54678, #49773, #33916, #66274, #64890, #28966, #44188, #50457, #38565, #2185, #65587, #27917, #43502, #55382, #22336, #49429, #6478, #33242, #55733, #17090, #17438, #12811, #34277, #60638, #18098, #12114, #28265, #38904, #33577, #16738, #38205, #39588, #65937, #39238, #12453, #1150, #59609, #11425, #32901, #54337, #6155, #27587, #59963, #11780, #17767, #7204, #1512, #49105, #792, #55013, #60307, #28634, #43831, #6842, #23039, #44534, #22687, #50126, #65237, #1854, #23368, #44867, #56415, #25106, #57107, #29692, #8931, #67673, #45214, #2557, #36023, #61339, #46622, #18454, #14212, #8250, #35325, #68040, #30027, #19826, #34604, #35674, #41315, #18782, #13149, #3603, #62395, #62718, #40261, #51162, #62031, #34967, #29327, #14548, #19475, #57465, #2907, #45570, #30710, #56063, #40615, #13860, #51489, #24397, #66638, #9289, #39938, #3248, #66990, #45892, #52215, #61663, #23716, #8593, #30352, #40976, #24066, #7879, #56779, #67321, #24736, #13494, #50806, #46253, #19109, #51856, #21561, #36750, #69411, #14922, #41666, #25447, #63440, #10666, #37800, #42382, #9649, #21199, #64120, #15287, #64480, #53248, #31402, #52896, #58505, #58858, #42723, #9982, #16323, #69076, #15973, #31065, #58167, #68730, #25790, #32120, #5034, #20878, #4681, #59175, #37455, #20526, #26134, #68369, #47671, #53573, #10329, #26484, #63771, #4306, #11002, #15620, #63084, #37094, #27, #31757, #47303, #26801, #48009, #32440, #5360, #48334, #43074, #3977, #46961, #20159, #36409, #57823, #52560, #42036, #59879, #16663, #61180, #16996, #11343, #50980, #11698, #32811, #67153, #64816, #21921, #5706, #18632, #8063, #45738, #22606, #13685, #27839, #2742, #44109, #54251, #39765, #12991, #40111, #49342, #49033, #59523, #38128, #27156, #392, #33167, #29516, #61858, #53901, #7707, #24237, #6071, #48685, #27506, #43431, #18941, #1062, #721, #54603, #22254, #34446, #66457, #43750, #65151, #38488, #6408, #18278, #40442, #55905, #29147, #50633, #2371, #23891, #45402, #66823, #61499, #13325, #34787, #56239, #36587, #68548, #41152, #20345, #9469, #56599, #14041, #47483, #3072, #58007, #29862, #25608, #19656, #46801, #9818, #41482, #31228, #46076, #47122, #52722, #30185, #24564, #15114, #4140, #4491, #51677, #62552, #3791, #46437, #40800, #25956, #30895, #68907, #67863, #56945, #42218, #67494, #52036, #25280, #62898, #14370, #8428, #20707, #51326, #14743, #8762, #35842, #63608, #3426, #35144, #19982, #41849, #52394, #35502, #19294, #68205, #57285, #36219, #24923, #62216, #57643, #9118, #30535, #63267, #32992, #26639, #21736, #5888, #38303, #36916, #49180, #16144, #22424, #10501, #882, #37623, #69571, #43925, #27331, #63940, #21376, #48163, #5197, #27672, #58670, #59026, #54425, #6245, #32617, #59704, #53732, #206, #10838, #5525, #15451, #58327, #11519, #37964, #11172, #54080, #42899, #10153, #31584, #53067, #4860, #26305, #47849, #31938, #53416, #59340, #48860, #43248, #69246, #21042, #26977, #32280, #559, #42541, #48510, #64653, #16499, #64293, #22084, #15788, #37270, #43585, #64976, #16831, #50214, #50556, #12904, #1607, #7979, #60728, #34369, #22782, #28360, #60390, #17527, #2279, #44959, #12547, #66021, #29423, #55817, #12194, #49869, #60056, #23135, #29058, #1935, #18185, #39328, #65679, #56154, #34013, #54755, #7296, #61421, #17848, #38997, #18546, #23452, #2656, #66365, #7623, #55474, #23807, #24151, #39671, #61093, #45309, #28012, #44625, #28723, #49523, #66730, #40033, #44280, #13238, #34696, #33667, #50895, #6567, #33333, #17182, #65337, #38657, #11870, #1251, #55109, #6936, #41764, #35759, #24478, #30447, #51946, #9387, #41063, #40715, #51246, #8342, #67075, #61762, #51586, #68462, #52645, #4404, #68128, #20258, #45986, #45658, #67409, #18858, #15024, #62477, #29786, #3342, #40350, #3704, #19570, #19205, #35420, #2990, #24833, #46350, #63184, #36497, #62126, #9745, #46715, #13591, #13952, #35058, #57922, #56869, #30812, #8682, #31151, #30108, #41408, #56505, #67772, #14297, #57198, #52312, #9029, #25200, #19908, #62812, #36123, #14655, #57558, #4065, #25531, #47045, #43169, #31852, #38218, #21293, #64576, #52982, #58595, #20968, #47767, #11084, #5442, #42820, #26567, #59619, #16420, #42465, #10424, #20619, #53339, #59259, #10761, #48434, #69494, #26231, #16749, #64209, #15381, #37549, #22011, #48089, #69163, #48780, #32209, #32915, #53657, #37891, #16065, #32534, #54348, #26893, #121, #21650, #58249, #5119, #58949, #10074, #54000, #5802, #4776, #43514, #27245, #63861, #11437, #36836, #63523, #47396, #481, #64902, #25879, #68824, #42131, #31498, #15703, #37185, #54687, #60650, #12467, #39602, #1524, #1164, #11790, #38576, #27597, #22348, #12125 ),
 ( #7216, #6166, #59976, #65251, #45226, #65601, #61007, #22699, #23727, #38915, #1870, #17102, #43842, #49118, #17451, #12823, #39951, #44549, #33254, #23378, #66286, #60319, #66652, #55394, #33590, #55029, #33929, #34290, #804, #18467, #6488, #28645, #49444, #6855, #55745, #44197, #13160, #50139, #44879, #18112, #27931, #28279, #23052, #49784, #7551, #65949, #61352, #28982, #34617, #17778, #39250, #50470, #2199, #62405, #46631, #9300, #7893, #20175, #56792, #63094, #51173, #41681, #8604, #40629, #14936, #68052, #34978, #62041, #67334, #45904, #68379, #29703, #30039, #3989, #25458, #3616, #30724, #24747, #40989, #51499, #46267, #46970, #56082, #52229, #8945, #51867, #25117, #13871, #50816, #29340, #2569, #24079, #45583, #67000, #2918, #24407, #30363, #19835, #14222, #18793, #40272, #67689, #3261, #41327, #61680, #19483, #35685, #57119, #19125, #62730, #56428, #13508, #35336, #8260, #14564, #57475, #36035, #42391, #36, #10676, #57835, #15299, #48696, #4314, #59180, #31074, #26807, #20888, #48015, #11008, #42733, #32446, #47315, #48345, #53912, #31412, #25800, #16333, #5367, #37810, #52904, #63782, #5043, #47680, #42045, #5715, #32129, #27161, #69085, #58175, #43440, #68742, #53259, #26492, #64132, #15627, #9665, #400, #37105, #64823, #4692, #21927, #58511, #10339, #36419, #21570, #36760, #31770, #69420, #26145, #52570, #9991, #21209, #20534, #63447, #53581, #15982, #37466, #58869, #43083, #64490, #55658, #16669, #39510, #39167, #12378, #55302, #22612, #11352, #38134, #12734, #59533, #28897, #7473, #59889, #11707, #60559, #33840, #44464, #6081, #49040, #28190, #38831, #28551, #54260, #6762, #17366, #60245, #33175, #49699, #17005, #50385, #49350, #43756, #1070, #18021, #50056, #44116, #1789, #7124, #32821, #65161, #2110, #27514, #60918, #729, #23299, #65515, #1434, #34207, #22964, #23638, #22262, #44799, #45143, #54609, #38495, #66195, #6415, #27847, #12040, #33503, #54935, #65868, #17698, #46541, #40900, #67969, #8173, #18718, #3900, #7804, #13789, #35244, #3169, #45824, #18385, #57394, #13082, #24660, #40191, #24331, #19752, #13424, #25375, #51422, #35603, #14143, #66919, #34536, #56705, #51089, #67601, #61597, #9218, #19403, #66562, #61960, #30637, #14470, #29614, #46179, #57042, #41248, #62645, #39870, #52144, #61274, #34892, #56338, #62321, #8858, #30279, #55994, #29253, #8526, #19037, #51779, #50735, #29961, #67249, #40548, #2840, #3528, #25033, #2481, #35947, #23990, #45505, #48258, #10599, #52828, #32045, #21134, #68299, #25707, #59114, #14846, #69672, #41586, #37373, #31330, #58431, #21485, #53171, #42997, #57747, #58781, #64402, #41955, #36323, #26734, #15892, #16251, #63361, #4606, #15546, #58102, #52494, #37728, #42639, #10934, #9913, #68651, #53833, #9578, #63703, #37022, #4961, #26063, #20083, #32369, #63005, #26410, #20451, #47597, #5630, #15216, #46896, #31692, #53508, #64045, #47230, #30996, #10257, #69002, #47942, #36682, #4232, #69342, #20809, #42316, #5289, #44722, #38413, #33427, #17625, #49976, #48617, #60836, #27770, #34118, #22186, #12652, #49274, #11626, #55575, #39092, #5994, #33091, #59812, #16927, #39434, #658, #982, #66115, #17943, #44385, #1711, #65440, #11970, #22531, #17289, #27082, #313, #23229, #49620, #22889, #65790, #54530, #21844, #43359, #64752, #60482, #16593, #38049, #38752, #59443, #44032, #11275, #60161, #27432, #54858, #6678, #12295, #28112, #43682, #32728, #54181, #48959, #65072, #6338, #1356, #33766, #55215, #7037, #28469, #7724, #14386, #29161, #35856, #46453, #2761, #61197, #34800, #7397, #61875, #50997, #50649, #66840, #13005, #56255, #8082, #30200, #67878, #23908, #41166, #8446, #28827, #34462, #66477, #19671, #18645, #40815, #2388, #24942, #40125, #3086, #18299, #45063, #50309, #61515, #14056, #62569, #45751, #55919, #24578, #67511, #13342, #2027, #56615, #29527, #24251, #13700, #62232, #46092, #67168, #23553, #18956, #19311, #45421, #40459, #35160, #29880, #35518, #51343, #56963, #8777, #39782, #51693, #3439, #20358, #52053, #16073, #22019, #43177, #11094, #32215, #57661, #49125, #26900, #46817, #131, #54356, #10769, #30911, #11449, #64585, #65259, #16432, #27254, #58955, #48786, #17113, #37899, #32544, #54008, #19998, #41862, #63280, #41503, #59266, #37557, #14757, #6174, #53663, #36234, #812, #68220, #25293, #64907, #22356, #48441, #62913, #5810, #486, #47141, #43851, #43522, #5451, #21658, #16757, #38228, #59629, #32923, #57303, #27607, #9132, #9489, #30551, #52407, #4153, #3808, #25623, #68567, #39259, #50826, #7560, #33598, #1534, #33264, #65955, #2207, #23385, #61016, #12476, #38925, #29347, #7225, #27940, #50149, #34629, #60658, #12131, #61361, #44889, #45591, #66296, #28989, #33938, #50478, #67010, #18122, #12832, #34297, #1173, #23060, #44557, #22708, #39610, #17785, #65612, #56089, #55400, #17457, #2581, #49452, #6497, #59982, #23734, #13170, #24088, #28652, #38588, #1877, #7903, #55757, #60326, #45233, #66660, #18475, #39956, #55040, #44205, #6864, #11795, #54695, #28289, #49792, #25809, #47323, #41338, #41688, #19137, #18801, #40638, #40282, #57849, #14232, #2926, #46280, #61691, #3628, #62414, #62048, #8614, #24415, #67698, #19492, #63105, #9671, #35345, #52579, #19843, #13518, #45913, #8270, #31083, #30047, #52238, #13879, #36429, #51507, #14574, #29714, #56438, #34989, #3268, #4325, #62741, #51179, #35694, #67342, #56800, #24756, #25126, #9311, #14946, #40996, #57126, #8954, #30370, #51875, #46639, #68058, #36043, #57484, #30735, #3995, #25466, #46979, #68389, #20182, #42402, #21219, #16679, #38143, #16344, #21939, #37477, #53592, #69429, #58879, #59544, #68751, #43449, #21578, #64499, #37817, #5052, #63458, #20542, #64833, #42054, #11364, #32830, #63791, #15635, #43091, #59189, #26820, #58183, #31419, #10685, #42741, #11015, #36770, #32136, #64138, #15992, #37115, #5375, #69094, #54270, #31782, #26153, #53268, #409, #32456, #26499, #53925, #5725, #15310, #47689, #6092, #10001, #27524, #52913, #27172, #48024, #48355, #4704, #45, #20895, #58521, #48707, #10351, #49362, #65171, #66204, #7133, #18032, #1081, #17377, #49708, #44125, #11717, #39517, #33848, #60928, #65529, #27857, #50393, #38506, #28200, #1445, #65877, #12050, #739, #55667, #43768, #17709, #22621, #60252, #12744, #38840, #2118, #44475, #28562, #55310, #54617, #17018, #22976, #33516, #60569, #6429, #54946, #33184, #7481, #59899, #6773, #22270, #1797, #34216, #28907, #39175, #49050, #12388, #50066, #23309, #44806, #15471, #67927, #63324, #63665, #30599, #57707, #62961, #41543, #64004, #25340, #4198, #69304, #21098, #68964, #4916, #42597, #35901, #15508, #9537, #47190, #57350, #30955, #10558, #36643, #25671, #52105, #14803, #9181, #52454, #68611, #26368, #15852, #68265, #37332, #52788, #51743, #3855, #41213, #58741, #36285, #36978, #46860, #3489, #20408, #47550, #62612, #19719, #24990, #41911, #58387, #46499, #15176, #20045, #20770, #42280, #58064, #14428, #31290, #9874, #4563, #26017, #10213, #31649, #53130, #47906, #27390, #935, #59079, #64713, #27037, #53789, #17246, #11575, #48920, #32680, #44340, #22487, #48571, #16552, #26697, #59400, #65398, #16888, #54483, #5947, #32337, #22842, #619, #21439, #43637, #28066, #54133, #5590, #54814, #38366, #39048, #59767, #43984, #22140, #38711, #60445, #33050 ) ),
 .UNSPECIFIED., .F., .F., .F. ) 
 B_SPLINE_SURFACE_WITH_KNOTS ( ( 2, 2 ),
 ( 3, 2, 2, 2, 2, 2, 2, 2, 2, 2, 2, 2, 2, 2, 2, 2, 2, 2, 2, 2, 2, 2, 2, 2, 2, 2, 2, 2, 2, 2, 2, 2, 2, 2, 2, 2, 2, 2, 2, 2, 2, 2, 2, 2, 2, 2, 2, 2, 2, 2, 2, 2, 2, 2, 2, 2, 2, 2, 2, 2, 2, 2, 2, 2, 2, 2, 2, 2, 2, 2, 2, 2, 2, 2, 2, 2, 2, 2, 2, 2, 2, 2, 2, 2, 2, 2, 2, 2, 2, 2, 2, 2, 2, 2, 2, 2, 2, 2, 2, 2, 2, 2, 2, 2, 2, 2, 2, 2, 2, 2, 2, 2, 2, 2, 2, 2, 2, 2, 2, 2, 2, 2, 2, 2, 2, 2, 2, 2, 2, 2, 2, 2, 2, 2, 2, 2, 2, 2, 2, 2, 2, 2, 2, 2, 2, 2, 2, 2, 2, 2, 2, 2, 2, 2, 2, 2, 2, 2, 2, 2, 2, 2, 2, 2, 2, 2, 2, 2, 2, 2, 2, 2, 2, 2, 2, 2, 2, 2, 2, 2, 2, 2, 2, 2, 2, 2, 2, 2, 2, 2, 2, 2, 2, 2, 2, 2, 2, 2, 2, 2, 2, 2, 2, 2, 2, 2, 2, 2, 2, 2, 2, 2, 2, 2, 2, 2, 2, 2, 2, 2, 2, 2, 2, 2, 2, 2, 2, 2, 2, 2, 2, 2, 2, 2, 2, 2, 2, 2, 2, 2, 2, 2, 2, 2, 2, 2, 2, 2, 2, 2, 2, 2, 2, 2, 2, 2, 2, 2, 2, 2, 2, 2, 2, 2, 2, 2, 2, 2, 2, 2, 2, 2, 2, 2, 2, 2, 2, 2, 2, 2, 2, 2, 2, 2, 2, 2, 2, 2, 2, 2, 2, 2, 2, 2, 2, 2, 2, 2, 2, 2, 2, 2, 2, 2, 2, 2, 2, 2, 2, 2, 2, 2, 2, 2, 2, 2, 2, 2, 2, 2, 2, 2, 2, 2, 2, 2, 2, 2, 2, 2, 2, 2, 2, 2, 2, 2, 2, 2, 2, 2, 2, 2, 2, 2, 2, 2, 2, 2, 2, 2, 2, 2, 2, 2, 2, 2, 2, 2, 2, 2, 2, 2, 2, 2, 2, 2, 2, 2, 2, 2, 2, 2, 2, 2, 2, 2, 2, 2, 2, 2, 2, 2, 2, 2, 2, 2, 2, 2, 2, 2, 2, 2, 2, 2, 2, 2, 2, 2, 2, 2, 2, 2, 2, 2, 2, 2, 2, 2, 2, 2, 2, 2, 2, 2, 2, 2, 2, 2, 2, 2, 2, 2, 2, 2, 2, 2, 2, 2, 2, 2, 2, 2, 2, 2, 2, 2, 2, 2, 2, 2, 2, 2, 2, 2, 2, 2, 2, 2, 2, 2, 2, 2, 2, 2, 2, 2, 3 ),
 ( 0.000000000000000000, 1.000000000000000000 ),
 ( 0.000000000000000000, 0.002173913043478260896, 0.004347826086956521792, 0.006521739130434782254, 0.008695652173913043584, 0.01086956521739130405, 0.01304347826086956451, 0.01521739130434782671, 0.01739130434782608717, 0.01956521739130434936, 0.02173913043478260809, 0.02391304347826087029, 0.02608695652173912902, 0.02826086956521739121, 0.03043478260869565341, 0.03260869565217391214, 0.03478260869565217434, 0.03695652173913043653, 0.03913043478260869873, 0.04130434782608695399, 0.04347826086956521618, 0.04565217391304347838, 0.04782608695652174058, 0.05000000000000000278, 0.05217391304347825803, 0.05434782608695652023, 0.05652173913043478243, 0.05869565217391304462, 0.06086956521739130682, 0.06304347826086956208, 0.06521739130434782428, 0.06739130434782608647, 0.06956521739130434867, 0.07173913043478261087, 0.07391304347826087306, 0.07608695652173913526, 0.07826086956521739746, 0.08043478260869564578, 0.08260869565217390798, 0.08478260869565217017, 0.08695652173913043237, 0.08913043478260869457, 0.09130434782608695676, 0.09347826086956521896, 0.09565217391304348116, 0.09782608695652174335, 0.1000000000000000056, 0.1021739130434782677, 0.1043478260869565161, 0.1065217391304347783, 0.1086956521739130405, 0.1108695652173913027, 0.1130434782608695649, 0.1152173913043478271, 0.1173913043478260892, 0.1195652173913043514, 0.1217391304347826136, 0.1239130434782608758, 0.1260869565217391242, 0.1282608695652174002, 0.1304347826086956486, 0.1326086956521739246, 0.1347826086956521729, 0.1369565217391304213, 0.1391304347826086973, 0.1413043478260869457, 0.1434782608695652217, 0.1456521739130434701, 0.1478260869565217461, 0.1499999999999999944, 0.1521739130434782705, 0.1543478260869565188, 0.1565217391304347949, 0.1586956521739130432, 0.1608695652173912916, 0.1630434782608695676, 0.1652173913043478160, 0.1673913043478260920, 0.1695652173913043403, 0.1717391304347826164, 0.1739130434782608647, 0.1760869565217391408, 0.1782608695652173891, 0.1804347826086956652, 0.1826086956521739135, 0.1847826086956521618, 0.1869565217391304379, 0.1891304347826086862, 0.1913043478260869623, 0.1934782608695652106, 0.1956521739130434867, 0.1978260869565217350, 0.2000000000000000111, 0.2021739130434782594, 0.2043478260869565355, 0.2065217391304347838, 0.2086956521739130321, 0.2108695652173913082, 0.2130434782608695565, 0.2152173913043478326, 0.2173913043478260809, 0.2195652173913043570, 0.2217391304347826053, 0.2239130434782608814, 0.2260869565217391297, 0.2282608695652173780, 0.2304347826086956541, 0.2326086956521739024, 0.2347826086956521785, 0.2369565217391304268, 0.2391304347826087029, 0.2413043478260869512, 0.2434782608695652273, 0.2456521739130434756, 0.2478260869565217517, 0.2500000000000000000, 0.2521739130434782483, 0.2543478260869564966, 0.2565217391304348005, 0.2586956521739130488, 0.2608695652173912971, 0.2630434782608695454, 0.2652173913043478493, 0.2673913043478260976, 0.2695652173913043459, 0.2717391304347825942, 0.2739130434782608425, 0.2760869565217391464, 0.2782608695652173947, 0.2804347826086956430, 0.2826086956521738913, 0.2847826086956521952, 0.2869565217391304435, 0.2891304347826086918, 0.2913043478260869401, 0.2934782608695652439, 0.2956521739130434923, 0.2978260869565217406, 0.2999999999999999889, 0.3021739130434782372, 0.3043478260869565410, 0.3065217391304347894, 0.3086956521739130377, 0.3108695652173912860, 0.3130434782608695898, 0.3152173913043478382, 0.3173913043478260865, 0.3195652173913043348, 0.3217391304347825831, 0.3239130434782608869, 0.3260869565217391353, 0.3282608695652173836, 0.3304347826086956319, 0.3326086956521739357, 0.3347826086956521840, 0.3369565217391304324, 0.3391304347826086807, 0.3413043478260869290, 0.3434782608695652328, 0.3456521739130434812, 0.3478260869565217295, 0.3499999999999999778, 0.3521739130434782816, 0.3543478260869565299, 0.3565217391304347783, 0.3586956521739130266, 0.3608695652173913304, 0.3630434782608695787, 0.3652173913043478271, 0.3673913043478260754, 0.3695652173913043237, 0.3717391304347826275, 0.3739130434782608758, 0.3760869565217391242, 0.3782608695652173725, 0.3804347826086956763, 0.3826086956521739246, 0.3847826086956521729, 0.3869565217391304213, 0.3891304347826086696, 0.3913043478260869734, 0.3934782608695652217, 0.3956521739130434701, 0.3978260869565217184, 0.4000000000000000222, 0.4021739130434782705, 0.4043478260869565188, 0.4065217391304347672, 0.4086956521739130710, 0.4108695652173913193, 0.4130434782608695676, 0.4152173913043478160, 0.4173913043478260643, 0.4195652173913043681, 0.4217391304347826164, 0.4239130434782608647, 0.4260869565217391131, 0.4282608695652174169, 0.4304347826086956652, 0.4326086956521739135, 0.4347826086956521618, 0.4369565217391304102, 0.4391304347826087140, 0.4413043478260869623, 0.4434782608695652106, 0.4456521739130434590, 0.4478260869565217628, 0.4500000000000000111, 0.4521739130434782594, 0.4543478260869565077, 0.4565217391304347561, 0.4586956521739130599, 0.4608695652173913082, 0.4630434782608695565, 0.4652173913043478048, 0.4673913043478261087, 0.4695652173913043570, 0.4717391304347826053, 0.4739130434782608536, 0.4760869565217391575, 0.4782608695652174058, 0.4804347826086956541, 0.4826086956521739024, 0.4847826086956521507, 0.4869565217391304546, 0.4891304347826087029, 0.4913043478260869512, 0.4934782608695651995, 0.4956521739130435034, 0.4978260869565217517, 0.5000000000000000000, 0.5021739130434782483, 0.5043478260869564966, 0.5065217391304347450, 0.5086956521739129933, 0.5108695652173913526, 0.5130434782608696009, 0.5152173913043478493, 0.5173913043478260976, 0.5195652173913043459, 0.5217391304347825942, 0.5239130434782608425, 0.5260869565217390909, 0.5282608695652173392, 0.5304347826086956985, 0.5326086956521739468, 0.5347826086956521952, 0.5369565217391304435, 0.5391304347826086918, 0.5413043478260869401, 0.5434782608695651884, 0.5456521739130434367, 0.5478260869565216851, 0.5500000000000000444, 0.5521739130434782927, 0.5543478260869565410, 0.5565217391304347894, 0.5586956521739130377, 0.5608695652173912860, 0.5630434782608695343, 0.5652173913043477826, 0.5673913043478261420, 0.5695652173913043903, 0.5717391304347826386, 0.5739130434782608869, 0.5760869565217391353, 0.5782608695652173836, 0.5804347826086956319, 0.5826086956521738802, 0.5847826086956521285, 0.5869565217391304879, 0.5891304347826087362, 0.5913043478260869845, 0.5934782608695652328, 0.5956521739130434812, 0.5978260869565217295, 0.5999999999999999778, 0.6021739130434782261, 0.6043478260869564744, 0.6065217391304348338, 0.6086956521739130821, 0.6108695652173913304, 0.6130434782608695787, 0.6152173913043478271, 0.6173913043478260754, 0.6195652173913043237, 0.6217391304347825720, 0.6239130434782608203, 0.6260869565217391797, 0.6282608695652174280, 0.6304347826086956763, 0.6326086956521739246, 0.6347826086956521729, 0.6369565217391304213, 0.6391304347826086696, 0.6413043478260869179, 0.6434782608695651662, 0.6456521739130435256, 0.6478260869565217739, 0.6500000000000000222, 0.6521739130434782705, 0.6543478260869565188, 0.6565217391304347672, 0.6586956521739130155, 0.6608695652173912638, 0.6630434782608695121, 0.6652173913043478715, 0.6673913043478261198, 0.6695652173913043681, 0.6717391304347826164, 0.6739130434782608647, 0.6760869565217391131, 0.6782608695652173614, 0.6804347826086956097, 0.6826086956521738580, 0.6847826086956522174, 0.6869565217391304657, 0.6891304347826087140, 0.6913043478260869623, 0.6934782608695652106, 0.6956521739130434590, 0.6978260869565217073, 0.6999999999999999556, 0.7021739130434783149, 0.7043478260869565633, 0.7065217391304348116, 0.7086956521739130599, 0.7108695652173913082, 0.7130434782608695565, 0.7152173913043478048, 0.7173913043478260532, 0.7195652173913043015, 0.7217391304347826608, 0.7239130434782609091, 0.7260869565217391575, 0.7282608695652174058, 0.7304347826086956541, 0.7326086956521739024, 0.7347826086956521507, 0.7369565217391303991, 0.7391304347826086474, 0.7413043478260870067, 0.7434782608695652550, 0.7456521739130435034, 0.7478260869565217517, 0.7500000000000000000, 0.7521739130434782483, 0.7543478260869564966, 0.7565217391304347450, 0.7586956521739129933, 0.7608695652173913526, 0.7630434782608696009, 0.7652173913043478493, 0.7673913043478260976, 0.7695652173913043459, 0.7717391304347825942, 0.7739130434782608425, 0.7760869565217390909, 0.7782608695652173392, 0.7804347826086956985, 0.7826086956521739468, 0.7847826086956521952, 0.7869565217391304435, 0.7891304347826086918, 0.7913043478260869401, 0.7934782608695651884, 0.7956521739130434367, 0.7978260869565216851, 0.8000000000000000444, 0.8021739130434782927, 0.8043478260869565410, 0.8065217391304347894, 0.8086956521739130377, 0.8108695652173912860, 0.8130434782608695343, 0.8152173913043477826, 0.8173913043478261420, 0.8195652173913043903, 0.8217391304347826386, 0.8239130434782608869, 0.8260869565217391353, 0.8282608695652173836, 0.8304347826086956319, 0.8326086956521738802, 0.8347826086956521285, 0.8369565217391304879, 0.8391304347826087362, 0.8413043478260869845, 0.8434782608695652328, 0.8456521739130434812, 0.8478260869565217295, 0.8499999999999999778, 0.8521739130434782261, 0.8543478260869564744, 0.8565217391304348338, 0.8586956521739130821, 0.8608695652173913304, 0.8630434782608695787, 0.8652173913043478271, 0.8673913043478260754, 0.8695652173913043237, 0.8717391304347825720, 0.8739130434782608203, 0.8760869565217391797, 0.8782608695652174280, 0.8804347826086956763, 0.8826086956521739246, 0.8847826086956521729, 0.8869565217391304213, 0.8891304347826086696, 0.8913043478260869179, 0.8934782608695651662, 0.8956521739130435256, 0.8978260869565217739, 0.9000000000000000222, 0.9021739130434782705, 0.9043478260869565188, 0.9065217391304347672, 0.9086956521739130155, 0.9108695652173912638, 0.9130434782608695121, 0.9152173913043478715, 0.9173913043478261198, 0.9195652173913043681, 0.9217391304347826164, 0.9239130434782608647, 0.9260869565217391131, 0.9282608695652173614, 0.9304347826086956097, 0.9326086956521738580, 0.9347826086956522174, 0.9369565217391304657, 0.9391304347826087140, 0.9413043478260869623, 0.9434782608695652106, 0.9456521739130434590, 0.9478260869565217073, 0.9499999999999999556, 0.9521739130434783149, 0.9543478260869565633, 0.9565217391304348116, 0.9586956521739130599, 0.9608695652173913082, 0.9630434782608695565, 0.9652173913043478048, 0.9673913043478260532, 0.9695652173913043015, 0.9717391304347826608, 0.9739130434782609091, 0.9760869565217391575, 0.9782608695652174058, 0.9804347826086956541, 0.9826086956521739024, 0.9847826086956521507, 0.9869565217391303991, 0.9891304347826086474, 0.9913043478260870067 ),
 .UNSPECIFIED. ) 
 GEOMETRIC_REPRESENTATION_ITEM ( )  RATIONAL_B_SPLINE_SURFACE ( (
 ( 1.000000000000000000, 0.9510565162951535312, 1.000000000000000000, 0.9510565162951535312, 1.000000000000000000, 0.9510565162951535312, 1.000000000000000000, 0.9510565162951535312, 1.000000000000000000, 0.9510565162951535312, 1.000000000000000000, 0.9510565162951535312, 1.000000000000000000, 0.9510565162951535312, 1.000000000000000000, 0.9510565162951535312, 1.000000000000000000, 0.9510565162951535312, 1.000000000000000000, 0.9510565162951535312, 1.000000000000000000, 0.9510565162951535312, 1.000000000000000000, 0.9510565162951535312, 1.000000000000000000, 0.9510565162951535312, 1.000000000000000000, 0.9510565162951535312, 1.000000000000000000, 0.9510565162951535312, 1.000000000000000000, 0.9510565162951535312, 1.000000000000000000, 0.9510565162951535312, 1.000000000000000000, 0.9510565162951535312, 1.000000000000000000, 0.9510565162951535312, 1.000000000000000000, 0.9510565162951535312, 1.000000000000000000, 0.9510565162951535312, 1.000000000000000000, 0.9510565162951535312, 1.000000000000000000, 0.9510565162951535312, 1.000000000000000000, 0.9510565162951535312, 1.000000000000000000, 0.9510565162951535312, 1.000000000000000000, 0.9510565162951535312, 1.000000000000000000, 0.9510565162951535312, 1.000000000000000000, 0.9510565162951535312, 1.000000000000000000, 0.9510565162951535312, 1.000000000000000000, 0.9510565162951535312, 1.000000000000000000, 0.9510565162951535312, 1.000000000000000000, 0.9510565162951535312, 1.000000000000000000, 0.9510565162951535312, 1.000000000000000000, 0.9510565162951535312, 1.000000000000000000, 0.9510565162951535312, 1.000000000000000000, 0.9510565162951535312, 1.000000000000000000, 0.9510565162951535312, 1.000000000000000000, 0.9510565162951535312, 1.000000000000000000, 0.9510565162951535312, 1.000000000000000000, 0.9510565162951535312, 1.000000000000000000, 0.9510565162951535312, 1.000000000000000000, 0.9510565162951535312, 1.000000000000000000, 0.9510565162951535312, 1.000000000000000000, 0.9510565162951535312, 1.000000000000000000, 0.9510565162951535312, 1.000000000000000000, 0.9510565162951535312, 1.000000000000000000, 0.9510565162951535312, 1.000000000000000000, 0.9510565162951535312, 1.000000000000000000, 0.9510565162951535312, 1.000000000000000000, 0.9510565162951535312, 1.000000000000000000, 0.9510565162951535312, 1.000000000000000000, 0.9510565162951535312, 1.000000000000000000, 0.9510565162951535312, 1.000000000000000000, 0.9510565162951535312, 1.000000000000000000, 0.9510565162951535312, 1.000000000000000000, 0.9510565162951535312, 1.000000000000000000, 0.9510565162951535312, 1.000000000000000000, 0.9510565162951535312, 1.000000000000000000, 0.9510565162951535312, 1.000000000000000000, 0.9510565162951535312, 1.000000000000000000, 0.9510565162951535312, 1.000000000000000000, 0.9510565162951535312, 1.000000000000000000, 0.9510565162951535312, 1.000000000000000000, 0.9510565162951535312, 1.000000000000000000, 0.9510565162951535312, 1.000000000000000000, 0.9510565162951535312, 1.000000000000000000, 0.9510565162951535312, 1.000000000000000000, 0.9510565162951535312, 1.000000000000000000, 0.9510565162951535312, 1.000000000000000000, 0.9510565162951535312, 1.000000000000000000, 0.9510565162951535312, 1.000000000000000000, 0.9510565162951535312, 1.000000000000000000, 0.9510565162951535312, 1.000000000000000000, 0.9510565162951535312, 1.000000000000000000, 0.9510565162951535312, 1.000000000000000000, 0.9510565162951535312, 1.000000000000000000, 0.9510565162951535312, 1.000000000000000000, 0.9510565162951535312, 1.000000000000000000, 0.9510565162951535312, 1.000000000000000000, 0.9510565162951535312, 1.000000000000000000, 0.9510565162951535312, 1.000000000000000000, 0.9510565162951535312, 1.000000000000000000, 0.9510565162951535312, 1.000000000000000000, 0.9510565162951535312, 1.000000000000000000, 0.9510565162951535312, 1.000000000000000000, 0.9510565162951535312, 1.000000000000000000, 0.9510565162951535312, 1.000000000000000000, 0.9510565162951535312, 1.000000000000000000, 0.9510565162951535312, 1.000000000000000000, 0.9510565162951535312, 1.000000000000000000, 0.9510565162951535312, 1.000000000000000000, 0.9510565162951535312, 1.000000000000000000, 0.9510565162951535312, 1.000000000000000000, 0.9510565162951535312, 1.000000000000000000, 0.9510565162951535312, 1.000000000000000000, 0.9510565162951535312, 1.000000000000000000, 0.9510565162951535312, 1.000000000000000000, 0.9510565162951535312, 1.000000000000000000, 0.9510565162951535312, 1.000000000000000000, 0.9510565162951535312, 1.000000000000000000, 0.9510565162951535312, 1.000000000000000000, 0.9510565162951535312, 1.000000000000000000, 0.9510565162951535312, 1.000000000000000000, 0.9510565162951535312, 1.000000000000000000, 0.9510565162951535312, 1.000000000000000000, 0.9510565162951535312, 1.000000000000000000, 0.9510565162951535312, 1.000000000000000000, 0.9510565162951535312, 1.000000000000000000, 0.9510565162951535312, 1.000000000000000000, 0.9510565162951535312, 1.000000000000000000, 0.9510565162951535312, 1.000000000000000000, 0.9510565162951535312, 1.000000000000000000, 0.9510565162951535312, 1.000000000000000000, 0.9510565162951535312, 1.000000000000000000, 0.9510565162951535312, 1.000000000000000000, 0.9510565162951535312, 1.000000000000000000, 0.9510565162951535312, 1.000000000000000000, 0.9510565162951535312, 1.000000000000000000, 0.9510565162951535312, 1.000000000000000000, 0.9510565162951535312, 1.000000000000000000, 0.9510565162951535312, 1.000000000000000000, 0.9510565162951535312, 1.000000000000000000, 0.9510565162951535312, 1.000000000000000000, 0.9510565162951535312, 1.000000000000000000, 0.9510565162951535312, 1.000000000000000000, 0.9510565162951535312, 1.000000000000000000, 0.9510565162951535312, 1.000000000000000000, 0.9510565162951535312, 1.000000000000000000, 0.9510565162951535312, 1.000000000000000000, 0.9510565162951535312, 1.000000000000000000, 0.9510565162951535312, 1.000000000000000000, 0.9510565162951535312, 1.000000000000000000, 0.9510565162951535312, 1.000000000000000000, 0.9510565162951535312, 1.000000000000000000, 0.9510565162951535312, 1.000000000000000000, 0.9510565162951535312, 1.000000000000000000, 0.9510565162951535312, 1.000000000000000000, 0.9510565162951535312, 1.000000000000000000, 0.9510565162951535312, 1.000000000000000000, 0.9510565162951535312, 1.000000000000000000, 0.9510565162951535312, 1.000000000000000000, 0.9510565162951535312, 1.000000000000000000, 0.9510565162951535312, 1.000000000000000000, 0.9510565162951535312, 1.000000000000000000, 0.9510565162951535312, 1.000000000000000000, 0.9510565162951535312, 1.000000000000000000, 0.9510565162951535312, 1.000000000000000000, 0.9510565162951535312, 1.000000000000000000, 0.9510565162951535312, 1.000000000000000000, 0.9510565162951535312, 1.000000000000000000, 0.9510565162951535312, 1.000000000000000000, 0.9510565162951535312, 1.000000000000000000, 0.9510565162951535312, 1.000000000000000000, 0.9510565162951535312, 1.000000000000000000, 0.9510565162951535312, 1.000000000000000000, 0.9510565162951535312, 1.000000000000000000, 0.9510565162951535312, 1.000000000000000000, 0.9510565162951535312, 1.000000000000000000, 0.9510565162951535312, 1.000000000000000000, 0.9510565162951535312, 1.000000000000000000, 0.9510565162951535312, 1.000000000000000000, 0.9510565162951535312, 1.000000000000000000, 0.9510565162951535312, 1.000000000000000000, 0.9510565162951535312, 1.000000000000000000, 0.9510565162951535312, 1.000000000000000000, 0.9510565162951535312, 1.000000000000000000, 0.9510565162951535312, 1.000000000000000000, 0.9510565162951535312, 1.000000000000000000, 0.9510565162951535312, 1.000000000000000000, 0.9510565162951535312, 1.000000000000000000, 0.9510565162951535312, 1.000000000000000000, 0.9510565162951535312, 1.000000000000000000, 0.9510565162951535312, 1.000000000000000000, 0.9510565162951535312, 1.000000000000000000, 0.9510565162951535312, 1.000000000000000000, 0.9510565162951535312, 1.000000000000000000, 0.9510565162951535312, 1.000000000000000000, 0.9510565162951535312, 1.000000000000000000, 0.9510565162951535312, 1.000000000000000000, 0.9510565162951535312, 1.000000000000000000, 0.9510565162951535312, 1.000000000000000000, 0.9510565162951535312, 1.000000000000000000, 0.9510565162951535312, 1.000000000000000000, 0.9510565162951535312, 1.000000000000000000, 0.9510565162951535312, 1.000000000000000000, 0.9510565162951535312, 1.000000000000000000, 0.9510565162951535312, 1.000000000000000000, 0.9510565162951535312, 1.000000000000000000, 0.9510565162951535312, 1.000000000000000000, 0.9510565162951535312, 1.000000000000000000, 0.9510565162951535312, 1.000000000000000000, 0.9510565162951535312, 1.000000000000000000, 0.9510565162951535312, 1.000000000000000000, 0.9510565162951535312, 1.000000000000000000, 0.9510565162951535312, 1.000000000000000000, 0.9510565162951535312, 1.000000000000000000, 0.9510565162951535312, 1.000000000000000000, 0.9510565162951535312, 1.000000000000000000, 0.9510565162951535312, 1.000000000000000000, 0.9510565162951535312, 1.000000000000000000, 0.9510565162951535312, 1.000000000000000000, 0.9510565162951535312, 1.000000000000000000, 0.9510565162951535312, 1.000000000000000000, 0.9510565162951535312, 1.000000000000000000, 0.9510565162951535312, 1.000000000000000000, 0.9510565162951535312, 1.000000000000000000, 0.9510565162951535312, 1.000000000000000000, 0.9510565162951535312, 1.000000000000000000, 0.9510565162951535312, 1.000000000000000000, 0.9510565162951535312, 1.000000000000000000, 0.9510565162951535312, 1.000000000000000000, 0.9510565162951535312, 1.000000000000000000, 0.9510565162951535312, 1.000000000000000000, 0.9510565162951535312, 1.000000000000000000, 0.9510565162951535312, 1.000000000000000000, 0.9510565162951535312, 1.000000000000000000, 0.9510565162951535312, 1.000000000000000000, 0.9510565162951535312, 1.000000000000000000, 0.9510565162951535312, 1.000000000000000000, 0.9510565162951535312, 1.000000000000000000, 0.9510565162951535312, 1.000000000000000000, 0.9510565162951535312, 1.000000000000000000, 0.9510565162951535312, 1.000000000000000000, 0.9510565162951535312, 1.000000000000000000, 0.9510565162951535312, 1.000000000000000000, 0.9510565162951535312, 1.000000000000000000, 0.9510565162951535312, 1.000000000000000000, 0.9510565162951535312, 1.000000000000000000, 0.9510565162951535312, 1.000000000000000000, 0.9510565162951535312, 1.000000000000000000, 0.9510565162951535312, 1.000000000000000000, 0.9510565162951535312, 1.000000000000000000, 0.9510565162951535312, 1.000000000000000000, 0.9510565162951535312, 1.000000000000000000, 0.9510565162951535312, 1.000000000000000000, 0.9510565162951535312, 1.000000000000000000, 0.9510565162951535312, 1.000000000000000000, 0.9510565162951535312, 1.000000000000000000, 0.9510565162951535312, 1.000000000000000000, 0.9510565162951535312, 1.000000000000000000, 0.9510565162951535312, 1.000000000000000000, 0.9510565162951535312, 1.000000000000000000, 0.9510565162951535312, 1.000000000000000000, 0.9510565162951535312, 1.000000000000000000, 0.9510565162951535312, 1.000000000000000000, 0.9510565162951535312, 1.000000000000000000, 0.9510565162951535312, 1.000000000000000000, 0.9510565162951535312, 1.000000000000000000, 0.9510565162951535312, 1.000000000000000000, 0.9510565162951535312, 1.000000000000000000, 0.9510565162951535312, 1.000000000000000000, 0.9510565162951535312, 1.000000000000000000, 0.9510565162951535312, 1.000000000000000000, 0.9510565162951535312, 1.000000000000000000, 0.9510565162951535312, 1.000000000000000000, 0.9510565162951535312, 1.000000000000000000, 0.9510565162951535312, 1.000000000000000000, 0.9510565162951535312, 1.000000000000000000, 0.9510565162951535312, 1.000000000000000000, 0.9510565162951535312, 1.000000000000000000, 0.9510565162951535312, 1.000000000000000000, 0.9510565162951535312, 1.000000000000000000, 0.9510565162951535312, 1.000000000000000000, 0.9510565162951535312, 1.000000000000000000, 0.9510565162951535312, 1.000000000000000000, 0.9510565162951535312, 1.000000000000000000, 0.9510565162951535312, 1.000000000000000000, 0.9510565162951535312, 1.000000000000000000, 0.9510565162951535312, 1.000000000000000000, 0.9510565162951535312, 1.000000000000000000, 0.9510565162951535312, 1.000000000000000000, 0.9510565162951535312, 1.000000000000000000, 0.9510565162951535312, 1.000000000000000000, 0.9510565162951535312, 1.000000000000000000, 0.9510565162951535312, 1.000000000000000000, 0.9510565162951535312, 1.000000000000000000, 0.9510565162951535312, 1.000000000000000000, 0.9510565162951535312, 1.000000000000000000, 0.9510565162951535312, 1.000000000000000000, 0.9510565162951535312, 1.000000000000000000, 0.9510565162951535312, 1.000000000000000000, 0.9510565162951535312, 1.000000000000000000, 0.9510565162951535312, 1.000000000000000000, 0.9510565162951535312, 1.000000000000000000, 0.9510565162951535312, 1.000000000000000000, 0.9510565162951535312, 1.000000000000000000, 0.9510565162951535312, 1.000000000000000000, 0.9510565162951535312, 1.000000000000000000, 0.9510565162951535312, 1.000000000000000000, 0.9510565162951535312, 1.000000000000000000, 0.9510565162951535312, 1.000000000000000000, 0.9510565162951535312, 1.000000000000000000, 0.9510565162951535312, 1.000000000000000000, 0.9510565162951535312, 1.000000000000000000, 0.9510565162951535312, 1.000000000000000000, 0.9510565162951535312, 1.000000000000000000, 0.9510565162951535312, 1.000000000000000000, 0.9510565162951535312, 1.000000000000000000, 0.9510565162951535312, 1.000000000000000000, 0.9510565162951535312, 1.000000000000000000, 0.9510565162951535312, 1.000000000000000000, 0.9510565162951535312, 1.000000000000000000, 0.9510565162951535312, 1.000000000000000000, 0.9510565162951535312, 1.000000000000000000, 0.9510565162951535312, 1.000000000000000000, 0.9510565162951535312, 1.000000000000000000, 0.9510565162951535312, 1.000000000000000000, 0.9510565162951535312, 1.000000000000000000, 0.9510565162951535312, 1.000000000000000000, 0.9510565162951535312, 1.000000000000000000, 0.9510565162951535312, 1.000000000000000000, 0.9510565162951535312, 1.000000000000000000, 0.9510565162951535312, 1.000000000000000000, 0.9510565162951535312, 1.000000000000000000, 0.9510565162951535312, 1.000000000000000000, 0.9510565162951535312, 1.000000000000000000, 0.9510565162951535312, 1.000000000000000000, 0.9510565162951535312, 1.000000000000000000, 0.9510565162951535312, 1.000000000000000000, 0.9510565162951535312, 1.000000000000000000, 0.9510565162951535312, 1.000000000000000000, 0.9510565162951535312, 1.000000000000000000, 0.9510565162951535312, 1.000000000000000000, 0.9510565162951535312, 1.000000000000000000, 0.9510565162951535312, 1.000000000000000000, 0.9510565162951535312, 1.000000000000000000, 0.9510565162951535312, 1.000000000000000000, 0.9510565162951535312, 1.000000000000000000, 0.9510565162951535312, 1.000000000000000000, 0.9510565162951535312, 1.000000000000000000, 0.9510565162951535312, 1.000000000000000000, 0.9510565162951535312, 1.000000000000000000, 0.9510565162951535312, 1.000000000000000000, 0.9510565162951535312, 1.000000000000000000, 0.9510565162951535312, 1.000000000000000000, 0.9510565162951535312, 1.000000000000000000, 0.9510565162951535312, 1.000000000000000000, 0.9510565162951535312, 1.000000000000000000, 0.9510565162951535312, 1.000000000000000000, 0.9510565162951535312, 1.000000000000000000, 0.9510565162951535312, 1.000000000000000000, 0.9510565162951535312, 1.000000000000000000, 0.9510565162951535312, 1.000000000000000000, 0.9510565162951535312, 1.000000000000000000, 0.9510565162951535312, 1.000000000000000000, 0.9510565162951535312, 1.000000000000000000, 0.9510565162951535312, 1.000000000000000000, 0.9510565162951535312, 1.000000000000000000, 0.9510565162951535312, 1.000000000000000000, 0.9510565162951535312, 1.000000000000000000, 0.9510565162951535312, 1.000000000000000000, 0.9510565162951535312, 1.000000000000000000, 0.9510565162951535312, 1.000000000000000000, 0.9510565162951535312, 1.000000000000000000, 0.9510565162951535312, 1.000000000000000000, 0.9510565162951535312, 1.000000000000000000, 0.9510565162951535312, 1.000000000000000000, 0.9510565162951535312, 1.000000000000000000, 0.9510565162951535312, 1.000000000000000000, 0.9510565162951535312, 1.000000000000000000, 0.9510565162951535312, 1.000000000000000000, 0.9510565162951535312, 1.000000000000000000, 0.9510565162951535312, 1.000000000000000000, 0.9510565162951535312, 1.000000000000000000, 0.9510565162951535312, 1.000000000000000000, 0.9510565162951535312, 1.000000000000000000, 0.9510565162951535312, 1.000000000000000000, 0.9510565162951535312, 1.000000000000000000, 0.9510565162951535312, 1.000000000000000000, 0.9510565162951535312, 1.000000000000000000, 0.9510565162951535312, 1.000000000000000000, 0.9510565162951535312, 1.000000000000000000, 0.9510565162951535312, 1.000000000000000000, 0.9510565162951535312, 1.000000000000000000, 0.9510565162951535312, 1.000000000000000000, 0.9510565162951535312, 1.000000000000000000, 0.9510565162951535312, 1.000000000000000000, 0.9510565162951535312, 1.000000000000000000, 0.9510565162951535312, 1.000000000000000000, 0.9510565162951535312, 1.000000000000000000, 0.9510565162951535312, 1.000000000000000000, 0.9510565162951535312, 1.000000000000000000, 0.9510565162951535312, 1.000000000000000000, 0.9510565162951535312, 1.000000000000000000, 0.9510565162951535312, 1.000000000000000000, 0.9510565162951535312, 1.000000000000000000, 0.9510565162951535312, 1.000000000000000000, 0.9510565162951535312, 1.000000000000000000, 0.9510565162951535312, 1.000000000000000000, 0.9510565162951535312, 1.000000000000000000, 0.9510565162951535312, 1.000000000000000000, 0.9510565162951535312, 1.000000000000000000, 0.9510565162951535312, 1.000000000000000000, 0.9510565162951535312, 1.000000000000000000, 0.9510565162951535312, 1.000000000000000000, 0.9510565162951535312, 1.000000000000000000, 0.9510565162951535312, 1.000000000000000000, 0.9510565162951535312, 1.000000000000000000, 0.9510565162951535312, 1.000000000000000000, 0.9510565162951535312, 1.000000000000000000, 0.9510565162951535312, 1.000000000000000000, 0.9510565162951535312, 1.000000000000000000, 0.9510565162951535312, 1.000000000000000000, 0.9510565162951535312, 1.000000000000000000, 0.9510565162951535312, 1.000000000000000000, 0.9510565162951535312, 1.000000000000000000, 0.9510565162951535312, 1.000000000000000000, 0.9510565162951535312, 1.000000000000000000, 0.9510565162951535312, 1.000000000000000000, 0.9510565162951535312, 1.000000000000000000, 0.9510565162951535312, 1.000000000000000000, 0.9510565162951535312, 1.000000000000000000, 0.9510565162951535312, 1.000000000000000000, 0.9510565162951535312, 1.000000000000000000, 0.9510565162951535312, 1.000000000000000000, 0.9510565162951535312, 1.000000000000000000, 0.9510565162951535312, 1.000000000000000000, 0.9510565162951535312, 1.000000000000000000, 0.9510565162951535312, 1.000000000000000000, 0.9510565162951535312, 1.000000000000000000, 0.9510565162951535312, 1.000000000000000000, 0.9510565162951535312, 1.000000000000000000, 0.9510565162951535312, 1.000000000000000000, 0.9510565162951535312, 1.000000000000000000, 0.9510565162951535312, 1.000000000000000000, 0.9510565162951535312, 1.000000000000000000, 0.9510565162951535312, 1.000000000000000000, 0.9510565162951535312, 1.000000000000000000, 0.9510565162951535312, 1.000000000000000000, 0.9510565162951535312, 1.000000000000000000, 0.9510565162951535312, 1.000000000000000000, 0.9510565162951535312, 1.000000000000000000, 0.9510565162951535312, 1.000000000000000000, 0.9510565162951535312, 1.000000000000000000, 0.9510565162951535312, 1.000000000000000000, 0.9510565162951535312, 1.000000000000000000, 0.9510565162951535312, 1.000000000000000000, 0.9510565162951535312, 1.000000000000000000, 0.9510565162951535312, 1.000000000000000000, 0.9510565162951535312, 1.000000000000000000, 0.9510565162951535312, 1.000000000000000000, 0.9510565162951535312, 1.000000000000000000, 0.9510565162951535312, 1.000000000000000000, 0.9510565162951535312, 1.000000000000000000, 0.9510565162951535312, 1.000000000000000000, 0.9510565162951535312, 1.000000000000000000, 0.9510565162951535312, 1.000000000000000000, 0.9510565162951535312, 1.000000000000000000, 0.9510565162951535312, 1.000000000000000000, 0.9510565162951535312, 1.000000000000000000, 0.9510565162951535312, 1.000000000000000000, 0.9510565162951535312, 1.000000000000000000, 0.9510565162951535312, 1.000000000000000000, 0.9510565162951535312, 1.000000000000000000, 0.9510565162951535312, 1.000000000000000000, 0.9510565162951535312, 1.000000000000000000),
 ( 1.000000000000000000, 0.9510565162951535312, 1.000000000000000000, 0.9510565162951535312, 1.000000000000000000, 0.9510565162951535312, 1.000000000000000000, 0.9510565162951535312, 1.000000000000000000, 0.9510565162951535312, 1.000000000000000000, 0.9510565162951535312, 1.000000000000000000, 0.9510565162951535312, 1.000000000000000000, 0.9510565162951535312, 1.000000000000000000, 0.9510565162951535312, 1.000000000000000000, 0.9510565162951535312, 1.000000000000000000, 0.9510565162951535312, 1.000000000000000000, 0.9510565162951535312, 1.000000000000000000, 0.9510565162951535312, 1.000000000000000000, 0.9510565162951535312, 1.000000000000000000, 0.9510565162951535312, 1.000000000000000000, 0.9510565162951535312, 1.000000000000000000, 0.9510565162951535312, 1.000000000000000000, 0.9510565162951535312, 1.000000000000000000, 0.9510565162951535312, 1.000000000000000000, 0.9510565162951535312, 1.000000000000000000, 0.9510565162951535312, 1.000000000000000000, 0.9510565162951535312, 1.000000000000000000, 0.9510565162951535312, 1.000000000000000000, 0.9510565162951535312, 1.000000000000000000, 0.9510565162951535312, 1.000000000000000000, 0.9510565162951535312, 1.000000000000000000, 0.9510565162951535312, 1.000000000000000000, 0.9510565162951535312, 1.000000000000000000, 0.9510565162951535312, 1.000000000000000000, 0.9510565162951535312, 1.000000000000000000, 0.9510565162951535312, 1.000000000000000000, 0.9510565162951535312, 1.000000000000000000, 0.9510565162951535312, 1.000000000000000000, 0.9510565162951535312, 1.000000000000000000, 0.9510565162951535312, 1.000000000000000000, 0.9510565162951535312, 1.000000000000000000, 0.9510565162951535312, 1.000000000000000000, 0.9510565162951535312, 1.000000000000000000, 0.9510565162951535312, 1.000000000000000000, 0.9510565162951535312, 1.000000000000000000, 0.9510565162951535312, 1.000000000000000000, 0.9510565162951535312, 1.000000000000000000, 0.9510565162951535312, 1.000000000000000000, 0.9510565162951535312, 1.000000000000000000, 0.9510565162951535312, 1.000000000000000000, 0.9510565162951535312, 1.000000000000000000, 0.9510565162951535312, 1.000000000000000000, 0.9510565162951535312, 1.000000000000000000, 0.9510565162951535312, 1.000000000000000000, 0.9510565162951535312, 1.000000000000000000, 0.9510565162951535312, 1.000000000000000000, 0.9510565162951535312, 1.000000000000000000, 0.9510565162951535312, 1.000000000000000000, 0.9510565162951535312, 1.000000000000000000, 0.9510565162951535312, 1.000000000000000000, 0.9510565162951535312, 1.000000000000000000, 0.9510565162951535312, 1.000000000000000000, 0.9510565162951535312, 1.000000000000000000, 0.9510565162951535312, 1.000000000000000000, 0.9510565162951535312, 1.000000000000000000, 0.9510565162951535312, 1.000000000000000000, 0.9510565162951535312, 1.000000000000000000, 0.9510565162951535312, 1.000000000000000000, 0.9510565162951535312, 1.000000000000000000, 0.9510565162951535312, 1.000000000000000000, 0.9510565162951535312, 1.000000000000000000, 0.9510565162951535312, 1.000000000000000000, 0.9510565162951535312, 1.000000000000000000, 0.9510565162951535312, 1.000000000000000000, 0.9510565162951535312, 1.000000000000000000, 0.9510565162951535312, 1.000000000000000000, 0.9510565162951535312, 1.000000000000000000, 0.9510565162951535312, 1.000000000000000000, 0.9510565162951535312, 1.000000000000000000, 0.9510565162951535312, 1.000000000000000000, 0.9510565162951535312, 1.000000000000000000, 0.9510565162951535312, 1.000000000000000000, 0.9510565162951535312, 1.000000000000000000, 0.9510565162951535312, 1.000000000000000000, 0.9510565162951535312, 1.000000000000000000, 0.9510565162951535312, 1.000000000000000000, 0.9510565162951535312, 1.000000000000000000, 0.9510565162951535312, 1.000000000000000000, 0.9510565162951535312, 1.000000000000000000, 0.9510565162951535312, 1.000000000000000000, 0.9510565162951535312, 1.000000000000000000, 0.9510565162951535312, 1.000000000000000000, 0.9510565162951535312, 1.000000000000000000, 0.9510565162951535312, 1.000000000000000000, 0.9510565162951535312, 1.000000000000000000, 0.9510565162951535312, 1.000000000000000000, 0.9510565162951535312, 1.000000000000000000, 0.9510565162951535312, 1.000000000000000000, 0.9510565162951535312, 1.000000000000000000, 0.9510565162951535312, 1.000000000000000000, 0.9510565162951535312, 1.000000000000000000, 0.9510565162951535312, 1.000000000000000000, 0.9510565162951535312, 1.000000000000000000, 0.9510565162951535312, 1.000000000000000000, 0.9510565162951535312, 1.000000000000000000, 0.9510565162951535312, 1.000000000000000000, 0.9510565162951535312, 1.000000000000000000, 0.9510565162951535312, 1.000000000000000000, 0.9510565162951535312, 1.000000000000000000, 0.9510565162951535312, 1.000000000000000000, 0.9510565162951535312, 1.000000000000000000, 0.9510565162951535312, 1.000000000000000000, 0.9510565162951535312, 1.000000000000000000, 0.9510565162951535312, 1.000000000000000000, 0.9510565162951535312, 1.000000000000000000, 0.9510565162951535312, 1.000000000000000000, 0.9510565162951535312, 1.000000000000000000, 0.9510565162951535312, 1.000000000000000000, 0.9510565162951535312, 1.000000000000000000, 0.9510565162951535312, 1.000000000000000000, 0.9510565162951535312, 1.000000000000000000, 0.9510565162951535312, 1.000000000000000000, 0.9510565162951535312, 1.000000000000000000, 0.9510565162951535312, 1.000000000000000000, 0.9510565162951535312, 1.000000000000000000, 0.9510565162951535312, 1.000000000000000000, 0.9510565162951535312, 1.000000000000000000, 0.9510565162951535312, 1.000000000000000000, 0.9510565162951535312, 1.000000000000000000, 0.9510565162951535312, 1.000000000000000000, 0.9510565162951535312, 1.000000000000000000, 0.9510565162951535312, 1.000000000000000000, 0.9510565162951535312, 1.000000000000000000, 0.9510565162951535312, 1.000000000000000000, 0.9510565162951535312, 1.000000000000000000, 0.9510565162951535312, 1.000000000000000000, 0.9510565162951535312, 1.000000000000000000, 0.9510565162951535312, 1.000000000000000000, 0.9510565162951535312, 1.000000000000000000, 0.9510565162951535312, 1.000000000000000000, 0.9510565162951535312, 1.000000000000000000, 0.9510565162951535312, 1.000000000000000000, 0.9510565162951535312, 1.000000000000000000, 0.9510565162951535312, 1.000000000000000000, 0.9510565162951535312, 1.000000000000000000, 0.9510565162951535312, 1.000000000000000000, 0.9510565162951535312, 1.000000000000000000, 0.9510565162951535312, 1.000000000000000000, 0.9510565162951535312, 1.000000000000000000, 0.9510565162951535312, 1.000000000000000000, 0.9510565162951535312, 1.000000000000000000, 0.9510565162951535312, 1.000000000000000000, 0.9510565162951535312, 1.000000000000000000, 0.9510565162951535312, 1.000000000000000000, 0.9510565162951535312, 1.000000000000000000, 0.9510565162951535312, 1.000000000000000000, 0.9510565162951535312, 1.000000000000000000, 0.9510565162951535312, 1.000000000000000000, 0.9510565162951535312, 1.000000000000000000, 0.9510565162951535312, 1.000000000000000000, 0.9510565162951535312, 1.000000000000000000, 0.9510565162951535312, 1.000000000000000000, 0.9510565162951535312, 1.000000000000000000, 0.9510565162951535312, 1.000000000000000000, 0.9510565162951535312, 1.000000000000000000, 0.9510565162951535312, 1.000000000000000000, 0.9510565162951535312, 1.000000000000000000, 0.9510565162951535312, 1.000000000000000000, 0.9510565162951535312, 1.000000000000000000, 0.9510565162951535312, 1.000000000000000000, 0.9510565162951535312, 1.000000000000000000, 0.9510565162951535312, 1.000000000000000000, 0.9510565162951535312, 1.000000000000000000, 0.9510565162951535312, 1.000000000000000000, 0.9510565162951535312, 1.000000000000000000, 0.9510565162951535312, 1.000000000000000000, 0.9510565162951535312, 1.000000000000000000, 0.9510565162951535312, 1.000000000000000000, 0.9510565162951535312, 1.000000000000000000, 0.9510565162951535312, 1.000000000000000000, 0.9510565162951535312, 1.000000000000000000, 0.9510565162951535312, 1.000000000000000000, 0.9510565162951535312, 1.000000000000000000, 0.9510565162951535312, 1.000000000000000000, 0.9510565162951535312, 1.000000000000000000, 0.9510565162951535312, 1.000000000000000000, 0.9510565162951535312, 1.000000000000000000, 0.9510565162951535312, 1.000000000000000000, 0.9510565162951535312, 1.000000000000000000, 0.9510565162951535312, 1.000000000000000000, 0.9510565162951535312, 1.000000000000000000, 0.9510565162951535312, 1.000000000000000000, 0.9510565162951535312, 1.000000000000000000, 0.9510565162951535312, 1.000000000000000000, 0.9510565162951535312, 1.000000000000000000, 0.9510565162951535312, 1.000000000000000000, 0.9510565162951535312, 1.000000000000000000, 0.9510565162951535312, 1.000000000000000000, 0.9510565162951535312, 1.000000000000000000, 0.9510565162951535312, 1.000000000000000000, 0.9510565162951535312, 1.000000000000000000, 0.9510565162951535312, 1.000000000000000000, 0.9510565162951535312, 1.000000000000000000, 0.9510565162951535312, 1.000000000000000000, 0.9510565162951535312, 1.000000000000000000, 0.9510565162951535312, 1.000000000000000000, 0.9510565162951535312, 1.000000000000000000, 0.9510565162951535312, 1.000000000000000000, 0.9510565162951535312, 1.000000000000000000, 0.9510565162951535312, 1.000000000000000000, 0.9510565162951535312, 1.000000000000000000, 0.9510565162951535312, 1.000000000000000000, 0.9510565162951535312, 1.000000000000000000, 0.9510565162951535312, 1.000000000000000000, 0.9510565162951535312, 1.000000000000000000, 0.9510565162951535312, 1.000000000000000000, 0.9510565162951535312, 1.000000000000000000, 0.9510565162951535312, 1.000000000000000000, 0.9510565162951535312, 1.000000000000000000, 0.9510565162951535312, 1.000000000000000000, 0.9510565162951535312, 1.000000000000000000, 0.9510565162951535312, 1.000000000000000000, 0.9510565162951535312, 1.000000000000000000, 0.9510565162951535312, 1.000000000000000000, 0.9510565162951535312, 1.000000000000000000, 0.9510565162951535312, 1.000000000000000000, 0.9510565162951535312, 1.000000000000000000, 0.9510565162951535312, 1.000000000000000000, 0.9510565162951535312, 1.000000000000000000, 0.9510565162951535312, 1.000000000000000000, 0.9510565162951535312, 1.000000000000000000, 0.9510565162951535312, 1.000000000000000000, 0.9510565162951535312, 1.000000000000000000, 0.9510565162951535312, 1.000000000000000000, 0.9510565162951535312, 1.000000000000000000, 0.9510565162951535312, 1.000000000000000000, 0.9510565162951535312, 1.000000000000000000, 0.9510565162951535312, 1.000000000000000000, 0.9510565162951535312, 1.000000000000000000, 0.9510565162951535312, 1.000000000000000000, 0.9510565162951535312, 1.000000000000000000, 0.9510565162951535312, 1.000000000000000000, 0.9510565162951535312, 1.000000000000000000, 0.9510565162951535312, 1.000000000000000000, 0.9510565162951535312, 1.000000000000000000, 0.9510565162951535312, 1.000000000000000000, 0.9510565162951535312, 1.000000000000000000, 0.9510565162951535312, 1.000000000000000000, 0.9510565162951535312, 1.000000000000000000, 0.9510565162951535312, 1.000000000000000000, 0.9510565162951535312, 1.000000000000000000, 0.9510565162951535312, 1.000000000000000000, 0.9510565162951535312, 1.000000000000000000, 0.9510565162951535312, 1.000000000000000000, 0.9510565162951535312, 1.000000000000000000, 0.9510565162951535312, 1.000000000000000000, 0.9510565162951535312, 1.000000000000000000, 0.9510565162951535312, 1.000000000000000000, 0.9510565162951535312, 1.000000000000000000, 0.9510565162951535312, 1.000000000000000000, 0.9510565162951535312, 1.000000000000000000, 0.9510565162951535312, 1.000000000000000000, 0.9510565162951535312, 1.000000000000000000, 0.9510565162951535312, 1.000000000000000000, 0.9510565162951535312, 1.000000000000000000, 0.9510565162951535312, 1.000000000000000000, 0.9510565162951535312, 1.000000000000000000, 0.9510565162951535312, 1.000000000000000000, 0.9510565162951535312, 1.000000000000000000, 0.9510565162951535312, 1.000000000000000000, 0.9510565162951535312, 1.000000000000000000, 0.9510565162951535312, 1.000000000000000000, 0.9510565162951535312, 1.000000000000000000, 0.9510565162951535312, 1.000000000000000000, 0.9510565162951535312, 1.000000000000000000, 0.9510565162951535312, 1.000000000000000000, 0.9510565162951535312, 1.000000000000000000, 0.9510565162951535312, 1.000000000000000000, 0.9510565162951535312, 1.000000000000000000, 0.9510565162951535312, 1.000000000000000000, 0.9510565162951535312, 1.000000000000000000, 0.9510565162951535312, 1.000000000000000000, 0.9510565162951535312, 1.000000000000000000, 0.9510565162951535312, 1.000000000000000000, 0.9510565162951535312, 1.000000000000000000, 0.9510565162951535312, 1.000000000000000000, 0.9510565162951535312, 1.000000000000000000, 0.9510565162951535312, 1.000000000000000000, 0.9510565162951535312, 1.000000000000000000, 0.9510565162951535312, 1.000000000000000000, 0.9510565162951535312, 1.000000000000000000, 0.9510565162951535312, 1.000000000000000000, 0.9510565162951535312, 1.000000000000000000, 0.9510565162951535312, 1.000000000000000000, 0.9510565162951535312, 1.000000000000000000, 0.9510565162951535312, 1.000000000000000000, 0.9510565162951535312, 1.000000000000000000, 0.9510565162951535312, 1.000000000000000000, 0.9510565162951535312, 1.000000000000000000, 0.9510565162951535312, 1.000000000000000000, 0.9510565162951535312, 1.000000000000000000, 0.9510565162951535312, 1.000000000000000000, 0.9510565162951535312, 1.000000000000000000, 0.9510565162951535312, 1.000000000000000000, 0.9510565162951535312, 1.000000000000000000, 0.9510565162951535312, 1.000000000000000000, 0.9510565162951535312, 1.000000000000000000, 0.9510565162951535312, 1.000000000000000000, 0.9510565162951535312, 1.000000000000000000, 0.9510565162951535312, 1.000000000000000000, 0.9510565162951535312, 1.000000000000000000, 0.9510565162951535312, 1.000000000000000000, 0.9510565162951535312, 1.000000000000000000, 0.9510565162951535312, 1.000000000000000000, 0.9510565162951535312, 1.000000000000000000, 0.9510565162951535312, 1.000000000000000000, 0.9510565162951535312, 1.000000000000000000, 0.9510565162951535312, 1.000000000000000000, 0.9510565162951535312, 1.000000000000000000, 0.9510565162951535312, 1.000000000000000000, 0.9510565162951535312, 1.000000000000000000, 0.9510565162951535312, 1.000000000000000000, 0.9510565162951535312, 1.000000000000000000, 0.9510565162951535312, 1.000000000000000000, 0.9510565162951535312, 1.000000000000000000, 0.9510565162951535312, 1.000000000000000000, 0.9510565162951535312, 1.000000000000000000, 0.9510565162951535312, 1.000000000000000000, 0.9510565162951535312, 1.000000000000000000, 0.9510565162951535312, 1.000000000000000000, 0.9510565162951535312, 1.000000000000000000, 0.9510565162951535312, 1.000000000000000000, 0.9510565162951535312, 1.000000000000000000, 0.9510565162951535312, 1.000000000000000000, 0.9510565162951535312, 1.000000000000000000, 0.9510565162951535312, 1.000000000000000000, 0.9510565162951535312, 1.000000000000000000, 0.9510565162951535312, 1.000000000000000000, 0.9510565162951535312, 1.000000000000000000, 0.9510565162951535312, 1.000000000000000000, 0.9510565162951535312, 1.000000000000000000, 0.9510565162951535312, 1.000000000000000000, 0.9510565162951535312, 1.000000000000000000, 0.9510565162951535312, 1.000000000000000000, 0.9510565162951535312, 1.000000000000000000, 0.9510565162951535312, 1.000000000000000000, 0.9510565162951535312, 1.000000000000000000, 0.9510565162951535312, 1.000000000000000000, 0.9510565162951535312, 1.000000000000000000, 0.9510565162951535312, 1.000000000000000000, 0.9510565162951535312, 1.000000000000000000, 0.9510565162951535312, 1.000000000000000000, 0.9510565162951535312, 1.000000000000000000, 0.9510565162951535312, 1.000000000000000000, 0.9510565162951535312, 1.000000000000000000, 0.9510565162951535312, 1.000000000000000000, 0.9510565162951535312, 1.000000000000000000, 0.9510565162951535312, 1.000000000000000000, 0.9510565162951535312, 1.000000000000000000, 0.9510565162951535312, 1.000000000000000000, 0.9510565162951535312, 1.000000000000000000, 0.9510565162951535312, 1.000000000000000000, 0.9510565162951535312, 1.000000000000000000, 0.9510565162951535312, 1.000000000000000000, 0.9510565162951535312, 1.000000000000000000, 0.9510565162951535312, 1.000000000000000000, 0.9510565162951535312, 1.000000000000000000, 0.9510565162951535312, 1.000000000000000000, 0.9510565162951535312, 1.000000000000000000, 0.9510565162951535312, 1.000000000000000000, 0.9510565162951535312, 1.000000000000000000, 0.9510565162951535312, 1.000000000000000000, 0.9510565162951535312, 1.000000000000000000, 0.9510565162951535312, 1.000000000000000000, 0.9510565162951535312, 1.000000000000000000, 0.9510565162951535312, 1.000000000000000000, 0.9510565162951535312, 1.000000000000000000, 0.9510565162951535312, 1.000000000000000000, 0.9510565162951535312, 1.000000000000000000, 0.9510565162951535312, 1.000000000000000000, 0.9510565162951535312, 1.000000000000000000, 0.9510565162951535312, 1.000000000000000000, 0.9510565162951535312, 1.000000000000000000, 0.9510565162951535312, 1.000000000000000000, 0.9510565162951535312, 1.000000000000000000, 0.9510565162951535312, 1.000000000000000000, 0.9510565162951535312, 1.000000000000000000, 0.9510565162951535312, 1.000000000000000000, 0.9510565162951535312, 1.000000000000000000, 0.9510565162951535312, 1.000000000000000000, 0.9510565162951535312, 1.000000000000000000, 0.9510565162951535312, 1.000000000000000000, 0.9510565162951535312, 1.000000000000000000, 0.9510565162951535312, 1.000000000000000000, 0.9510565162951535312, 1.000000000000000000, 0.9510565162951535312, 1.000000000000000000, 0.9510565162951535312, 1.000000000000000000, 0.9510565162951535312, 1.000000000000000000, 0.9510565162951535312, 1.000000000000000000, 0.9510565162951535312, 1.000000000000000000, 0.9510565162951535312, 1.000000000000000000, 0.9510565162951535312, 1.000000000000000000, 0.9510565162951535312, 1.000000000000000000, 0.9510565162951535312, 1.000000000000000000, 0.9510565162951535312, 1.000000000000000000, 0.9510565162951535312, 1.000000000000000000, 0.9510565162951535312, 1.000000000000000000, 0.9510565162951535312, 1.000000000000000000, 0.9510565162951535312, 1.000000000000000000, 0.9510565162951535312, 1.000000000000000000, 0.9510565162951535312, 1.000000000000000000, 0.9510565162951535312, 1.000000000000000000, 0.9510565162951535312, 1.000000000000000000, 0.9510565162951535312, 1.000000000000000000, 0.9510565162951535312, 1.000000000000000000, 0.9510565162951535312, 1.000000000000000000, 0.9510565162951535312, 1.000000000000000000, 0.9510565162951535312, 1.000000000000000000, 0.9510565162951535312, 1.000000000000000000, 0.9510565162951535312, 1.000000000000000000, 0.9510565162951535312, 1.000000000000000000, 0.9510565162951535312, 1.000000000000000000, 0.9510565162951535312, 1.000000000000000000, 0.9510565162951535312, 1.000000000000000000, 0.9510565162951535312, 1.000000000000000000, 0.9510565162951535312, 1.000000000000000000, 0.9510565162951535312, 1.000000000000000000, 0.9510565162951535312, 1.000000000000000000, 0.9510565162951535312, 1.000000000000000000, 0.9510565162951535312, 1.000000000000000000, 0.9510565162951535312, 1.000000000000000000, 0.9510565162951535312, 1.000000000000000000, 0.9510565162951535312, 1.000000000000000000, 0.9510565162951535312, 1.000000000000000000, 0.9510565162951535312, 1.000000000000000000, 0.9510565162951535312, 1.000000000000000000, 0.9510565162951535312, 1.000000000000000000, 0.9510565162951535312, 1.000000000000000000, 0.9510565162951535312, 1.000000000000000000, 0.9510565162951535312, 1.000000000000000000, 0.9510565162951535312, 1.000000000000000000, 0.9510565162951535312, 1.000000000000000000, 0.9510565162951535312, 1.000000000000000000, 0.9510565162951535312, 1.000000000000000000, 0.9510565162951535312, 1.000000000000000000, 0.9510565162951535312, 1.000000000000000000, 0.9510565162951535312, 1.000000000000000000, 0.9510565162951535312, 1.000000000000000000, 0.9510565162951535312, 1.000000000000000000, 0.9510565162951535312, 1.000000000000000000, 0.9510565162951535312, 1.000000000000000000, 0.9510565162951535312, 1.000000000000000000, 0.9510565162951535312, 1.000000000000000000, 0.9510565162951535312, 1.000000000000000000, 0.9510565162951535312, 1.000000000000000000, 0.9510565162951535312, 1.000000000000000000, 0.9510565162951535312, 1.000000000000000000, 0.9510565162951535312, 1.000000000000000000, 0.9510565162951535312, 1.000000000000000000, 0.9510565162951535312, 1.000000000000000000, 0.9510565162951535312, 1.000000000000000000) ) ) 
 REPRESENTATION_ITEM ( '' )  SURFACE ( )  );
#27373=VERTEX_POINT ( 'NONE', #48603 ) ;
#27376=DIRECTION ( 'NONE',  ( -1.000000000000000000, -0.000000000000000000, -0.000000000000000000 ) ) ;
#27390=CARTESIAN_POINT ( 'NONE',  ( -53.54292637653379217, 9.058813317711329915, 2.943386871421369566 ) ) ;
#27392=CYLINDRICAL_SURFACE ( 'NONE', #64412, 9.524999999999991473 ) ;
#27395=CARTESIAN_POINT ( 'NONE',  ( -143.1549999999999727, 7.632228543268600340, 2.479861379858949277 ) ) ;
#27401=EDGE_CURVE ( 'NONE', #618, #48114, #42193, .T. ) ;
#27408=CARTESIAN_POINT ( 'NONE',  ( -61.40499999999999403, -2.607480562269069768, 8.024999999999991473 ) ) ;
#27415=CARTESIAN_POINT ( 'NONE',  ( -97.34292637653379643, -9.058813317711329915, 2.943386871421371787 ) ) ;
#27419=CARTESIAN_POINT ( 'NONE',  ( -195.0000000000000000, 0.000000000000000000, 0.000000000000000000 ) ) ;
#27421=CARTESIAN_POINT ( 'NONE',  ( -106.7949999999999733, 2.607480562269069324, -8.024999999999993250 ) ) ;
#27423=CARTESIAN_POINT ( 'NONE',  ( -83.09499999999999886, -2.607480562269071545, -8.024999999999991473 ) ) ;
#27432=CARTESIAN_POINT ( 'NONE',  ( -121.7929263765337993, -3.094860106618429807, 9.524999999999991473 ) ) ;
#27434=CARTESIAN_POINT ( 'NONE',  ( -143.3949999999999818, -6.826472737025115478, -4.959722759717899443 ) ) ;
#27438=CARTESIAN_POINT ( 'NONE',  ( -195.0000000000000000, 1.166476076187852838E-15, -9.524999999999991473 ) ) ;
#27446=CARTESIAN_POINT ( 'NONE',  ( -58.94292637653381206, 0.000000000000000000, 9.524999999999991473 ) ) ;
#27450=CARTESIAN_POINT ( 'NONE',  ( -144.5049999999999670, -6.826472737025113702, -4.959722759717900331 ) ) ;
#27468=CARTESIAN_POINT ( 'NONE',  ( -58.70499999999996987, 2.607480562269072433, 8.024999999999991473 ) ) ;
#27469=CARTESIAN_POINT ( 'NONE',  ( -116.0949999999999704, -2.607480562269071545, -8.024999999999991473 ) ) ;
#27482=CARTESIAN_POINT ( 'NONE',  ( -170.9049999999999727, 2.607480562269068880, -8.024999999999993250 ) ) ;
#27484=CARTESIAN_POINT ( 'NONE',  ( -88.25707362346616947, 5.598654528085800663, -7.705886871421367523 ) ) ;
#27493=EDGE_LOOP ( 'NONE', ( #1737, #65747, #11952, #17177 ) ) ;
#27496=CARTESIAN_POINT ( 'NONE',  ( -86.75499999999998124, 4.716976649647091513, -6.492361379858946790 ) ) ;
#27500=CARTESIAN_POINT ( 'NONE',  ( -69.05707362346618083, 0.000000000000000000, 9.524999999999991473 ) ) ;
#27506=CARTESIAN_POINT ( 'NONE',  ( -101.1550000000000011, 7.632228543268600340, 2.479861379858949277 ) ) ;
#27508=CARTESIAN_POINT ( 'NONE',  ( -121.0449999999999875, 7.632228543268600340, 2.479861379858949277 ) ) ;
#27510=AXIS2_PLACEMENT_3D ( 'NONE', #26922, #64605, #32566 ) ;
#27514=CARTESIAN_POINT ( 'NONE',  ( -151.4929263765338305, -8.102448949553172852, 5.886773742842742685 ) ) ;
#27515=CARTESIAN_POINT ( 'NONE',  ( -174.1449999999999818, -4.716976649647092401, 6.492361379858946790 ) ) ;
#27524=CARTESIAN_POINT ( 'NONE',  ( -73.04292637653379927, -9.058813317711329915, -2.943386871421370898 ) ) ;
#27533=ADVANCED_FACE ( 'NONE', ( #32281 ), #63941, .T. ) ;
#27536=CARTESIAN_POINT ( 'NONE',  ( -168.0550000000000068, -9.827790563157499189E-16, -8.024999999999991473 ) ) ;
#27540=CARTESIAN_POINT ( 'NONE',  ( -126.3570736234661780, 5.598654528085804216, 7.705886871421366635 ) ) ;
#27546=CARTESIAN_POINT ( 'NONE',  ( -95.75499999999999545, 4.716976649647091513, -6.492361379858946790 ) ) ;
#27551=CARTESIAN_POINT ( 'NONE',  ( -168.5929263765339954, -3.094860106621758700, -9.524999999997572075 ) ) ;
#27559=CARTESIAN_POINT ( 'NONE',  ( -61.04499999999998749, 7.632228543268600340, 2.479861379858949277 ) ) ;
#27563=CARTESIAN_POINT ( 'NONE',  ( -138.6570736234661751, 9.058813317711329915, 2.943386871421369566 ) ) ;
#27566=CYLINDRICAL_SURFACE ( 'NONE', #52824, 9.524999999999991473 ) ;
#27570=CARTESIAN_POINT ( 'NONE',  ( -119.0049999999999955, 6.826472737025116366, 4.959722759717898555 ) ) ;
#27575=CARTESIAN_POINT ( 'NONE',  ( -160.3429263765337964, -9.058813317711329915, 2.943386871421371787 ) ) ;
#27577=CARTESIAN_POINT ( 'NONE',  ( -148.1070736234661354, 8.102448949553171076, -5.886773742842744461 ) ) ;
#27578=ADVANCED_FACE ( 'NONE', ( #37965 ), #54081, .T. ) ;
#27581=CARTESIAN_POINT ( 'NONE',  ( -98.15707362346617515, -9.058813317711329915, -2.943386871421370898 ) ) ;
#27587=CARTESIAN_POINT ( 'NONE',  ( -129.2049999999999841, -2.607480562269071545, -8.024999999999991473 ) ) ;
#27588=CARTESIAN_POINT ( 'NONE',  ( -165.1429263765338078, 5.598654528085800663, -7.705886871421367523 ) ) ;
#27590=CARTESIAN_POINT ( 'NONE',  ( -140.9949999999999193, -6.826472737025115478, 4.959722759717900331 ) ) ;
#27591=CARTESIAN_POINT ( 'NONE',  ( -125.6950000000000074, -8.437984349512086979, 5.166775262442717831E-16 ) ) ;
#27597=CARTESIAN_POINT ( 'NONE',  ( -48.05499999999998550, -9.827790563157499189E-16, -8.024999999999991473 ) ) ;
#27599=CARTESIAN_POINT ( 'NONE',  ( -61.49499999999998323, 6.826472737025113702, -4.959722759717902107 ) ) ;
#27607=CARTESIAN_POINT ( 'NONE',  ( -101.5429263765338135, 9.058813317711329915, 2.943386871421369566 ) ) ;
#27609=CARTESIAN_POINT ( 'NONE',  ( -162.2070736234664423, 3.094860106622869811, 9.524999999996769162 ) ) ;
#27611=CARTESIAN_POINT ( 'NONE',  ( -100.1070736234661780, 8.102448949553172852, -5.886773742842744461 ) ) ;
#27614=EDGE_CURVE ( 'NONE', #11014, #52425, #48861, .T. ) ;
#27634=CARTESIAN_POINT ( 'NONE',  ( -87.14499999999998181, -4.716976649647092401, 6.492361379858946790 ) ) ;
#27645=AXIS2_PLACEMENT_3D ( 'NONE', #30854, #35462, #25915 ) ;
#27648=CARTESIAN_POINT ( 'NONE',  ( -165.3570736234661922, 5.598654528085804216, 7.705886871421366635 ) ) ;
#27663=CARTESIAN_POINT ( 'NONE',  ( -159.6550000000000011, -7.632228543268600340, -2.479861379858950166 ) ) ;
#27666=CARTESIAN_POINT ( 'NONE',  ( -170.3950000000000102, -6.826472737025115478, -4.959722759717899443 ) ) ;
#27667=CARTESIAN_POINT ( 'NONE',  ( -165.1449999999999818, -4.716976649647092401, 6.492361379858946790 ) ) ;
#27669=CARTESIAN_POINT ( 'NONE',  ( -90.44292637653379074, -1.166476076187852838E-15, -9.524999999999991473 ) ) ;
#27672=CARTESIAN_POINT ( 'NONE',  ( -84.80499999999999261, -8.437984349512085203, 5.166775262442717831E-16 ) ) ;
#27674=CARTESIAN_POINT ( 'NONE',  ( -84.59499999999997044, 2.607480562269072433, 8.024999999999991473 ) ) ;
#27704=CARTESIAN_POINT ( 'NONE',  ( -107.9049999999999869, 2.607480562269069324, -8.024999999999993250 ) ) ;
#27716=CARTESIAN_POINT ( 'NONE',  ( -117.2070736234669965, 3.094860106632079777, 9.524999999990075850 ) ) ;
#27719=CARTESIAN_POINT ( 'NONE',  ( -180.7429263765338021, -5.598654528085803328, -7.705886871421366635 ) ) ;
#27730=CARTESIAN_POINT ( 'NONE',  ( -165.0570736234661524, 0.000000000000000000, 9.524999999999991473 ) ) ;
#27731=CARTESIAN_POINT ( 'NONE',  ( -143.6049999999999613, 6.826472737025113702, -4.959722759717902107 ) ) ;
#27734=CARTESIAN_POINT ( 'NONE',  ( -105.7429263765338021, -5.598654528085803328, -7.705886871421366635 ) ) ;
#27742=CARTESIAN_POINT ( 'NONE',  ( -53.00500000000000256, 6.826472737025116366, 4.959722759717898555 ) ) ;
#27743=ORIENTED_EDGE ( 'NONE', *, *, #39509, .F. ) ;
#27744=CARTESIAN_POINT ( 'NONE',  ( -15.00000000000000000, 10.90871211463571200, -5.000000000000000000 ) ) ;
#27751=VERTEX_POINT ( 'NONE', #20861 ) ;
#27754=( BOUNDED_CURVE ( )  B_SPLINE_CURVE ( 2, ( #36923, #69252, #43257, #48172, #52732, #10510, #42907, #64663, #25965, #47494, #68915 ),
 .UNSPECIFIED., .F., .F. ) 
 B_SPLINE_CURVE_WITH_KNOTS ( ( 3, 2, 2, 2, 2, 3 ),
 ( 0.09782608695651948127, 0.09999999999999770184, 0.1021739130434759224, 0.1043478260869541152, 0.1065217391304323358, 0.1086956521739105563 ),
 .UNSPECIFIED. ) 
 CURVE ( )  GEOMETRIC_REPRESENTATION_ITEM ( )  RATIONAL_B_SPLINE_CURVE ( ( 1.000000000000050848, 0.9510565162951025719, 1.000000000000000000, 0.9510565162951535312, 1.000000000000000000, 0.9510565162951535312, 1.000000000000000000, 0.9510565162951535312, 1.000000000000000000, 0.9510565162952094864, 0.9999999999999440448 ) ) 
 REPRESENTATION_ITEM ( '' )  );
#27759=CARTESIAN_POINT ( 'NONE',  ( -107.8449999999999989, -7.632228543268599452, 2.479861379858951054 ) ) ;
#27761=CARTESIAN_POINT ( 'NONE',  ( -91.34499999999998465, 7.632228543268599452, -2.479861379858951942 ) ) ;
#27770=CARTESIAN_POINT ( 'NONE',  ( -127.9429263765338192, 0.000000000000000000, 9.524999999999991473 ) ) ;
#27771=CARTESIAN_POINT ( 'NONE',  ( -143.0949999999999704, -2.607480562269071545, -8.024999999999991473 ) ) ;
#27773=CARTESIAN_POINT ( 'NONE',  ( -66.20707362346615810, 3.094860106618433360, 9.524999999999991473 ) ) ;
#27774=DIRECTION ( 'NONE',  ( -1.000000000000000000, -0.000000000000000000, -0.000000000000000000 ) ) ;
#27775=VERTEX_POINT ( 'NONE', #44089 ) ;
#27777=( BOUNDED_CURVE ( )  B_SPLINE_CURVE ( 2, ( #48898, #33366, #914, #34049, #60422, #12582, #39025, #6276, #55143, #22121, #5566 ),
 .UNSPECIFIED., .F., .F. ) 
 B_SPLINE_CURVE_WITH_KNOTS ( ( 3, 2, 2, 2, 2, 3 ),
 ( 0.9239130434782608647, 0.9260869565217391131, 0.9282608695652173614, 0.9304347826086956097, 0.9326086956521738580, 0.9347826086956522174 ),
 .UNSPECIFIED. ) 
 CURVE ( )  GEOMETRIC_REPRESENTATION_ITEM ( )  RATIONAL_B_SPLINE_CURVE ( ( 1.000000000000000000, 0.9510565162951535312, 1.000000000000000000, 0.9510565162951535312, 1.000000000000000000, 0.9510565162951535312, 1.000000000000000000, 0.9510565162951535312, 1.000000000000000000, 0.9510565162951535312, 1.000000000000000000 ) ) 
 REPRESENTATION_ITEM ( '' )  );
#27782=CARTESIAN_POINT ( 'NONE',  ( -131.0070736234661410, -8.102448949553174629, -5.886773742842741797 ) ) ;
#27784=DIRECTION ( 'NONE',  ( 0.000000000000000000, 0.000000000000000000, 1.000000000000000000 ) ) ;
#27788=CARTESIAN_POINT ( 'NONE',  ( -145.2549999999999955, -4.716976649647092401, 6.492361379858946790 ) ) ;
#27792=DIRECTION ( 'NONE',  ( -1.000000000000000000, -0.000000000000000000, -0.000000000000000000 ) ) ;
#27793=ORIENTED_EDGE ( 'NONE', *, *, #34179, .T. ) ;
#27799=CARTESIAN_POINT ( 'NONE',  ( -57.65499999999998693, -7.632228543268600340, -2.479861379858950166 ) ) ;
#27800=CARTESIAN_POINT ( 'NONE',  ( -122.6949999999999790, -8.437984349512085203, 5.166775262442717831E-16 ) ) ;
#27811=CARTESIAN_POINT ( 'NONE',  ( -105.0570736234661666, 0.000000000000000000, 9.524999999999991473 ) ) ;
#27815=CARTESIAN_POINT ( 'NONE',  ( -174.2050000000000125, -2.607480562269071545, -8.024999999999991473 ) ) ;
#27817=CARTESIAN_POINT ( 'NONE',  ( -87.05707362346618083, 0.000000000000000000, 9.524999999999991473 ) ) ;
#27823=CARTESIAN_POINT ( 'NONE',  ( -77.09292637653378222, 3.094860106618433360, 9.524999999999991473 ) ) ;
#27827=CARTESIAN_POINT ( 'NONE',  ( -83.00499999999995282, 6.826472737025116366, 4.959722759717898555 ) ) ;
#27831=CARTESIAN_POINT ( 'NONE',  ( -57.20707362346615099, 3.094860106618433360, 9.524999999999991473 ) ) ;
#27839=CARTESIAN_POINT ( 'NONE',  ( -104.3049999999999784, 8.437984349512085203, -1.550032578732815448E-15 ) ) ;
#27842=CARTESIAN_POINT ( 'NONE',  ( -117.5949999999999989, 2.607480562269073321, 8.024999999999991473 ) ) ;
#27845=CARTESIAN_POINT ( 'NONE',  ( -19.33136078104492483, 11.73593362212572622, -2.518815027830850539 ) ) ;
#27847=CARTESIAN_POINT ( 'NONE',  ( -149.0929263765338249, 3.094860106618433360, 9.524999999999991473 ) ) ;
#27848=CARTESIAN_POINT ( 'NONE',  ( -177.7449999999999761, 4.716976649647094177, 6.492361379858945902 ) ) ;
#27857=CARTESIAN_POINT ( 'NONE',  ( -69.29292637653378506, 3.094860106618428031, -9.524999999999993250 ) ) ;
#27859=CYLINDRICAL_SURFACE ( 'NONE', #20390, 9.524999999999991473 ) ;
#27865=CARTESIAN_POINT ( 'NONE',  ( -173.0049999999999670, 6.826472737025115478, 4.959722759717899443 ) ) ;
#27874=( BOUNDED_CURVE ( )  B_SPLINE_CURVE ( 2, ( #4118, #42514, #52013, #63916, #25258, #5172, #30874, #15767, #14350, #35818, #46778 ),
 .UNSPECIFIED., .F., .F. ) 
 B_SPLINE_CURVE_WITH_KNOTS ( ( 3, 2, 2, 2, 2, 3 ),
 ( 0.4239130434782507617, 0.4260869565217289545, 0.4282608695652072028, 0.4304347826086854512, 0.4326086956521636440, 0.4347826086956418368 ),
 .UNSPECIFIED. ) 
 CURVE ( )  GEOMETRIC_REPRESENTATION_ITEM ( )  RATIONAL_B_SPLINE_CURVE ( ( 1.000000000000227374, 0.9510565162949260465, 1.000000000000000000, 0.9510565162951535312, 1.000000000000000000, 0.9510565162951535312, 1.000000000000000000, 0.9510565162951535312, 1.000000000000000000, 0.9510565162953860119, 0.9999999999997675193 ) ) 
 REPRESENTATION_ITEM ( '' )  );
#27877=CARTESIAN_POINT ( 'NONE',  ( -86.15499999999998693, 7.632228543268600340, 2.479861379858949277 ) ) ;
#27890=CARTESIAN_POINT ( 'NONE',  ( -59.69499999999997897, -8.437984349512085203, 5.166775262442717831E-16 ) ) ;
#27891=EDGE_LOOP ( 'NONE', ( #36731, #15338, #43477 ) ) ;
#27892=CARTESIAN_POINT ( 'NONE',  ( -195.0000000000000000, 0.000000000000000000, 0.000000000000000000 ) ) ;
#27900=CARTESIAN_POINT ( 'NONE',  ( -116.7549999999999812, 4.716976649647091513, -6.492361379858946790 ) ) ;
#27906=CARTESIAN_POINT ( 'NONE',  ( -146.6070736234661922, -8.102448949553172852, 5.886773742842742685 ) ) ;
#27908=CARTESIAN_POINT ( 'NONE',  ( -92.00707362346615525, -8.102448949553172852, -5.886773742842741797 ) ) ;
#27917=CARTESIAN_POINT ( 'NONE',  ( -133.7049999999999557, 2.607480562269073321, 8.024999999999991473 ) ) ;
#27919=CARTESIAN_POINT ( 'NONE',  ( -145.9429263765337907, 0.000000000000000000, 9.524999999999991473 ) ) ;
#27921=CARTESIAN_POINT ( 'NONE',  ( -142.1949999999999932, 8.437984349512085203, -1.550032578732815448E-15 ) ) ;
#27924=CARTESIAN_POINT ( 'NONE',  ( -125.2449999999999903, -4.716976649647093289, -6.492361379858945902 ) ) ;
#27931=CARTESIAN_POINT ( 'NONE',  ( -178.9429263765338192, 0.000000000000000000, 9.524999999999991473 ) ) ;
#27933=CARTESIAN_POINT ( 'NONE',  ( -59.09499999999997044, -2.607480562269071545, -8.024999999999991473 ) ) ;
#27940=CARTESIAN_POINT ( 'NONE',  ( -98.09292637653378222, 3.094860106618433360, 9.524999999999991473 ) ) ;
#27949=ORIENTED_EDGE ( 'NONE', *, *, #10323, .F. ) ;
#27954=ADVANCED_FACE ( 'NONE', ( #9189 ), #57463, .T. ) ;
#27963=CARTESIAN_POINT ( 'NONE',  ( -116.3070736234661666, -10.01517768586948698, 6.132527647946031529E-16 ) ) ;
#27967=VECTOR ( 'NONE', #22696, 999.9999999999998863 ) ;
#27970=CARTESIAN_POINT ( 'NONE',  ( -94.64499999999999602, 4.716976649647091513, -6.492361379858946790 ) ) ;
#27989=CARTESIAN_POINT ( 'NONE',  ( -178.5570736234661808, -1.166476076187852838E-15, -9.524999999999991473 ) ) ;
#27994=CARTESIAN_POINT ( 'NONE',  ( -68.24292637653380211, 5.598654528085804216, 7.705886871421366635 ) ) ;
#27996=EDGE_LOOP ( 'NONE', ( #63595, #16083, #26924, #26874 ) ) ;
#28001=CARTESIAN_POINT ( 'NONE',  ( -162.9549999999999841, -7.632228543268599452, 2.479861379858951054 ) ) ;
#28004=CARTESIAN_POINT ( 'NONE',  ( -178.3449999999999989, 7.632228543268599452, -2.479861379858951942 ) ) ;
#28005=CARTESIAN_POINT ( 'NONE',  ( -157.1949999999999932, 8.437984349512086979, -1.550032578732815448E-15 ) ) ;
#28012=CARTESIAN_POINT ( 'NONE',  ( -71.45499999999998408, 7.632228543268599452, -2.479861379858951942 ) ) ;
#28014=FACE_OUTER_BOUND ( 'NONE', #20942, .T. ) ;
#28017=CARTESIAN_POINT ( 'NONE',  ( -75.59499999999998465, 2.607480562269072433, 8.024999999999991473 ) ) ;
#28021=CARTESIAN_POINT ( 'NONE',  ( -176.6929263765337907, 10.01517768586948698, -1.839758294383808966E-15 ) ) ;
#28030=CARTESIAN_POINT ( 'NONE',  ( -119.3929263765337936, 8.102448949553176405, 5.886773742842740909 ) ) ;
#28038=CARTESIAN_POINT ( 'NONE',  ( -91.94292637653380496, 0.000000000000000000, 9.524999999999991473 ) ) ;
#28039=CARTESIAN_POINT ( 'NONE',  ( -69.05707362346618083, 0.000000000000000000, 9.524999999999991473 ) ) ;
#28041=CARTESIAN_POINT ( 'NONE',  ( -110.6049999999999756, 6.826472737025113702, -4.959722759717902107 ) ) ;
#28055=ORIENTED_EDGE ( 'NONE', *, *, #21403, .T. ) ;
#28057=DIRECTION ( 'NONE',  ( -1.000000000000000000, -0.000000000000000000, -0.000000000000000000 ) ) ;
#28066=CARTESIAN_POINT ( 'NONE',  ( -49.79292637653379217, -3.094860106618429807, 9.524999999999991473 ) ) ;
#28069=FACE_OUTER_BOUND ( 'NONE', #18230, .T. ) ;
#28070=CARTESIAN_POINT ( 'NONE',  ( -144.3549999999999898, -4.716976649647093289, -6.492361379858945902 ) ) ;
#28082=CARTESIAN_POINT ( 'NONE',  ( -56.75499999999997414, 4.716976649647091513, -6.492361379858946790 ) ) ;
#28093=CARTESIAN_POINT ( 'NONE',  ( -147.0570736234661808, 0.000000000000000000, 9.524999999999991473 ) ) ;
#28104=CARTESIAN_POINT ( 'NONE',  ( -108.4449999999999790, 0.000000000000000000, 8.024999999999991473 ) ) ;
#28106=CARTESIAN_POINT ( 'NONE',  ( -75.14499999999999602, -4.716976649647092401, 6.492361379858946790 ) ) ;
#28111=ORIENTED_EDGE ( 'NONE', *, *, #35925, .T. ) ;
#28112=CARTESIAN_POINT ( 'NONE',  ( -121.1929263765337907, -10.01517768586948698, 6.132527647946031529E-16 ) ) ;
#28114=CARTESIAN_POINT ( 'NONE',  ( -136.4949999999999477, 6.826472737025113702, -4.959722759717902107 ) ) ;
#28116=MANIFOLD_SOLID_BREP ( 'Cut-Sweep1', #28366 ) ;
#28117=DIRECTION ( 'NONE',  ( 0.000000000000000000, 0.000000000000000000, 1.000000000000000000 ) ) ;
#28125=CARTESIAN_POINT ( 'NONE',  ( -117.4429263765338050, -1.166476076187852838E-15, -9.524999999999991473 ) ) ;
#28128=CARTESIAN_POINT ( 'NONE',  ( -144.3549999999999898, -4.716976649647093289, -6.492361379858945902 ) ) ;
#28141=CARTESIAN_POINT ( 'NONE',  ( -50.15499999999997982, 7.632228543268600340, 2.479861379858949277 ) ) ;
#28148=EDGE_CURVE ( 'NONE', #6192, #3199, #13820, .T. ) ;
#28154=CARTESIAN_POINT ( 'NONE',  ( -173.1550000000000011, 7.632228543268600340, 2.479861379858949277 ) ) ;
#28163=( BOUNDED_CURVE ( )  B_SPLINE_CURVE ( 2, ( #59117, #49625, #58786, #38055, #32050, #10937, #5998, #54864, #43364, #27773, #48262 ),
 .UNSPECIFIED., .F., .F. ) 
 B_SPLINE_CURVE_WITH_KNOTS ( ( 3, 2, 2, 2, 2, 3 ),
 ( 0.8369565217391304879, 0.8391304347826087362, 0.8413043478260869845, 0.8434782608695652328, 0.8456521739130434812, 0.8478260869565217295 ),
 .UNSPECIFIED. ) 
 CURVE ( )  GEOMETRIC_REPRESENTATION_ITEM ( )  RATIONAL_B_SPLINE_CURVE ( ( 1.000000000000000000, 0.9510565162951535312, 1.000000000000000000, 0.9510565162951535312, 1.000000000000000000, 0.9510565162951535312, 1.000000000000000000, 0.9510565162951535312, 1.000000000000000000, 0.9510565162951535312, 1.000000000000000000 ) ) 
 REPRESENTATION_ITEM ( '' )  );
#28165=EDGE_CURVE ( 'NONE', #23235, #36781, #26011, .T. ) ;
#28166=ORIENTED_EDGE ( 'NONE', *, *, #64031, .F. ) ;
#28167=DIRECTION ( 'NONE',  ( -1.000000000000000000, -0.000000000000000000, -0.000000000000000000 ) ) ;
#28168=CARTESIAN_POINT ( 'NONE',  ( -90.20499999999999829, -2.607480562269071545, -8.024999999999991473 ) ) ;
#28177=EDGE_CURVE ( 'NONE', #16622, #41269, #25517, .T. ) ;
#28184=CARTESIAN_POINT ( 'NONE',  ( -103.6449999999999818, 4.716976649647091513, -6.492361379858946790 ) ) ;
#28189=CARTESIAN_POINT ( 'NONE',  ( -20.00017592768050179, 12.00007330319154697, -0.3280245013256660735 ) ) ;
#28190=CARTESIAN_POINT ( 'NONE',  ( -154.7929263765337851, -3.094860106618429807, 9.524999999999991473 ) ) ;
#28192=CARTESIAN_POINT ( 'NONE',  ( -176.9950000000000045, -6.826472737025115478, 4.959722759717900331 ) ) ;
#28200=CARTESIAN_POINT ( 'NONE',  ( -68.84292637653379643, 9.058813317711329915, -2.943386871421373119 ) ) ;
#28205=CARTESIAN_POINT ( 'NONE',  ( -174.0570736234661808, 0.000000000000000000, 9.524999999999991473 ) ) ;
#28211=CARTESIAN_POINT ( 'NONE',  ( -166.5550000000000068, 0.000000000000000000, 8.024999999999991473 ) ) ;
#28221=CARTESIAN_POINT ( 'NONE',  ( -79.55499999999999261, 0.000000000000000000, 8.024999999999991473 ) ) ;
#28225=CARTESIAN_POINT ( 'NONE',  ( -72.20707362346617231, 3.094860106618433360, 9.524999999999991473 ) ) ;
#28227=CARTESIAN_POINT ( 'NONE',  ( -113.9929263765338021, 8.102448949553172852, -5.886773742842744461 ) ) ;
#28232=CARTESIAN_POINT ( 'NONE',  ( -58.19500000000000028, 8.437984349512085203, -1.550032578732815448E-15 ) ) ;
#28239=CARTESIAN_POINT ( 'NONE',  ( -56.84499999999997755, -7.632228543268599452, 2.479861379858951054 ) ) ;
#28243=CARTESIAN_POINT ( 'NONE',  ( -118.1049999999999898, -6.826472737025115478, 4.959722759717900331 ) ) ;
#28250=CARTESIAN_POINT ( 'NONE',  ( -147.5070736234661695, 8.102448949553176405, 5.886773742842740909 ) ) ;
#28254=CARTESIAN_POINT ( 'NONE',  ( -81.35707362346616378, 5.598654528085804216, 7.705886871421366635 ) ) ;
#28265=CARTESIAN_POINT ( 'NONE',  ( -131.4549999999999841, 7.632228543268599452, -2.479861379858951942 ) ) ;
#28270=CARTESIAN_POINT ( 'NONE',  ( -143.8449999999999989, -7.632228543268599452, 2.479861379858951054 ) ) ;
#28271=CARTESIAN_POINT ( 'NONE',  ( -132.2949999999999875, -2.607480562269069768, 8.024999999999991473 ) ) ;
#28275=CARTESIAN_POINT ( 'NONE',  ( -146.6070736234661638, -8.102448949553174629, 5.886773742842742685 ) ) ;
#28279=CARTESIAN_POINT ( 'NONE',  ( -178.7929263765338135, -3.094860106618429807, 9.524999999999991473 ) ) ;
#28281=CARTESIAN_POINT ( 'NONE',  ( -63.14499999999998181, -4.716976649647092401, 6.492361379858946790 ) ) ;
#28286=AXIS2_PLACEMENT_3D ( 'NONE', #52803, #53482, #14442 ) ;
#28289=CARTESIAN_POINT ( 'NONE',  ( -90.89292637653380780, -8.102448949553172852, -5.886773742842741797 ) ) ;
#28291=( BOUNDED_CURVE ( )  B_SPLINE_CURVE ( 2, ( #8664, #4049, #3325, #9724, #20600, #24814, #14278, #52630, #14637, #35744, #36479 ),
 .UNSPECIFIED., .F., .F. ) 
 B_SPLINE_CURVE_WITH_KNOTS ( ( 3, 2, 2, 2, 2, 3 ),
 ( 0.8478260869565217295, 0.8499999999999999778, 0.8521739130434782261, 0.8543478260869564744, 0.8565217391304348338, 0.8586956521739130821 ),
 .UNSPECIFIED. ) 
 CURVE ( )  GEOMETRIC_REPRESENTATION_ITEM ( )  RATIONAL_B_SPLINE_CURVE ( ( 1.000000000000000000, 0.9510565162951535312, 1.000000000000000000, 0.9510565162951535312, 1.000000000000000000, 0.9510565162951535312, 1.000000000000000000, 0.9510565162951535312, 1.000000000000000000, 0.9510565162951535312, 1.000000000000000000 ) ) 
 REPRESENTATION_ITEM ( '' )  );
#28296=VERTEX_POINT ( 'NONE', #57981 ) ;
#28299=ORIENTED_EDGE ( 'NONE', *, *, #44181, .F. ) ;
#28317=CARTESIAN_POINT ( 'NONE',  ( -93.95707362346617231, 9.058813317711329915, -2.943386871421373119 ) ) ;
#28318=AXIS2_PLACEMENT_3D ( 'NONE', #46225, #23682, #13123 ) ;
#28320=CARTESIAN_POINT ( 'NONE',  ( -92.09499999999998465, -2.607480562269071545, -8.024999999999991473 ) ) ;
#28340=CARTESIAN_POINT ( 'NONE',  ( -179.6070736234661922, -8.102448949553172852, 5.886773742842742685 ) ) ;
#28343=CARTESIAN_POINT ( 'NONE',  ( -114.0570736234661808, 0.000000000000000000, 9.524999999999991473 ) ) ;
#28349=CARTESIAN_POINT ( 'NONE',  ( -149.9070736234666015, -3.094860106611606820, 9.525000000004951062 ) ) ;
#28351=CARTESIAN_POINT ( 'NONE',  ( -160.1049999999999613, -6.826472737025115478, 4.959722759717900331 ) ) ;
#28354=CARTESIAN_POINT ( 'NONE',  ( -175.3449999999999989, 7.632228543268599452, -2.479861379858951942 ) ) ;
#28356=CARTESIAN_POINT ( 'NONE',  ( -159.4449999999999932, 0.000000000000000000, 8.024999999999991473 ) ) ;
#28360=CARTESIAN_POINT ( 'NONE',  ( -76.85499999999998977, 4.716976649647094177, 6.492361379858945902 ) ) ;
#28361=B_SPLINE_CURVE_WITH_KNOTS ( 'NONE', 3,
 ( #52211, #36405, #68727, #67317, #9979, #46617, #52894, #62392, #20523, #14210, #13856, #25787, #14920, #47300, #35668, #30350, #14544, #57105, #67670, #42032, #20155, #19470, #36748, #36020, #56775, #57462, #31399, #19823, #8927, #40612, #3974, #8590, #25444, #57819, #41311, #9645 ),
 .UNSPECIFIED., .F., .F.,
 ( 4, 2, 2, 2, 2, 2, 2, 2, 2, 2, 2, 2, 2, 2, 2, 2, 2, 4 ),
 ( 0.02371714007185215731, 0.02470529243674880401, 0.02569344480164545072, 0.02668159716654209743, 0.02766974953143874066, 0.02865790189633538737, 0.02964605426123203408, 0.03063420662612868078, 0.03162235899102532749, 0.03261051135592197420, 0.03359866372081862090, 0.03458681608571526761, 0.03557496845061191432, 0.03656312081550856102, 0.03755127318040520773, 0.03804534936285353108, 0.03853942554530184750, 0.03952757791019850808 ),
 .UNSPECIFIED. ) ;
#28365=CARTESIAN_POINT ( 'NONE',  ( -66.59499999999998465, 2.607480562269072433, 8.024999999999991473 ) ) ;
#28366=CLOSED_SHELL ( 'NONE', ( #64427, #48541, #30465, #26728, #55830, #18130, #12772, #7725, #30554, #20131, #30904, #27578, #48535, #18619, #65841, #67186, #64664, #66256, #36708, #15671, #27232, #32019, #25544, #38822, #51009, #794, #6670, #62575, #21448, #64861, #54940, #64502, #27533, #51320, #29721, #17357, #37288, #20004, #15461, #55910, #37809, #68146, #47576, #33759, #50388, #50198, #13107, #47071, #44520, #41236, #45046, #64494, #55689, #31206, #2300, #29942, #19393, #20831, #34424, #33519, #5942, #18510, #23173, #68096, #60147, #41984, #13646, #16959, #36342, #18025, #29374, #13416, #24372, #41999, #46682, #30823, #860, #64335, #49900, #17505, #49927, #4244, #23349, #1361, #2979, #18736, #36833, #5913, #29292, #26811, #64847, #62418, #49406, #18146, #26588, #31123, #34285, #66208, #4098, #15915, #1193, #57934, #5543, #4514, #25713, #29051, #48820, #2068, #3743, #65300, #10747, #55078, #27954, #18668, #8169, #16171, #17748, #3134, #8018 ) ) ;
#28374=LINE ( 'NONE', #2288, #59613 ) ;
#28391=CARTESIAN_POINT ( 'NONE',  ( -111.5049999999999955, -6.826472737025113702, -4.959722759717900331 ) ) ;
#28392=ORIENTED_EDGE ( 'NONE', *, *, #18753, .T. ) ;
#28397=CARTESIAN_POINT ( 'NONE',  ( -68.45707362346617231, -9.058813317711329915, 2.943386871421371787 ) ) ;
#28404=ORIENTED_EDGE ( 'NONE', *, *, #50250, .F. ) ;
#28412=LINE ( 'NONE', #34067, #5167 ) ;
#28414=CARTESIAN_POINT ( 'NONE',  ( -103.9429263765338050, 0.000000000000000000, 9.524999999999991473 ) ) ;
#28419=FACE_OUTER_BOUND ( 'NONE', #69010, .T. ) ;
#28421=CARTESIAN_POINT ( 'NONE',  ( -136.1049999999999898, -6.826472737025115478, 4.959722759717900331 ) ) ;
#28428=CARTESIAN_POINT ( 'NONE',  ( -156.8929263765338078, -8.102448949553174629, -5.886773742842741797 ) ) ;
#28432=DIRECTION ( 'NONE',  ( -1.000000000000000000, -0.000000000000000000, -0.000000000000000000 ) ) ;
#28433=CARTESIAN_POINT ( 'NONE',  ( -108.4429263765338050, -1.166476076187852838E-15, -9.524999999999991473 ) ) ;
#28437=CARTESIAN_POINT ( 'NONE',  ( -49.55707362346617373, -1.166476076187852838E-15, -9.524999999999991473 ) ) ;
#28449=CARTESIAN_POINT ( 'NONE',  ( -195.0000000000000000, 0.000000000000000000, 0.000000000000000000 ) ) ;
#28451=CYLINDRICAL_SURFACE ( 'NONE', #34849, 9.524999999999991473 ) ;
#28453=CARTESIAN_POINT ( 'NONE',  ( -98.54499999999998749, -7.632228543268600340, -2.479861379858950166 ) ) ;
#28455=CARTESIAN_POINT ( 'NONE',  ( -81.74499999999999034, 4.716976649647094177, 6.492361379858945902 ) ) ;
#28469=CARTESIAN_POINT ( 'NONE',  ( -119.5429263765338135, 9.058813317711329915, 2.943386871421369566 ) ) ;
#28471=CARTESIAN_POINT ( 'NONE',  ( -141.7450000000000045, 4.716976649647094177, 6.492361379858945902 ) ) ;
#28475=CARTESIAN_POINT ( 'NONE',  ( -173.9929263765338021, 8.102448949553172852, -5.886773742842744461 ) ) ;
#28482=CARTESIAN_POINT ( 'NONE',  ( -131.7570736234661695, -5.598654528085801552, 7.705886871421367523 ) ) ;
#28486=CARTESIAN_POINT ( 'NONE',  ( -141.3550000000000182, -4.716976649647093289, -6.492361379858945902 ) ) ;
#28501=ORIENTED_EDGE ( 'NONE', *, *, #20500, .T. ) ;
#28506=CARTESIAN_POINT ( 'NONE',  ( -53.90499999999997272, 2.607480562269069324, -8.024999999999993250 ) ) ;
#28523=CARTESIAN_POINT ( 'NONE',  ( -195.0000000000000000, 0.000000000000000000, 9.524999999999991473 ) ) ;
#28524=CARTESIAN_POINT ( 'NONE',  ( -164.6049999999999898, 6.826472737025113702, -4.959722759717902107 ) ) ;
#28534=CARTESIAN_POINT ( 'NONE',  ( -88.10499999999998977, -6.826472737025115478, 4.959722759717900331 ) ) ;
#28547=CARTESIAN_POINT ( 'NONE',  ( -108.1449999999999960, -4.716976649647092401, 6.492361379858946790 ) ) ;
#28551=CARTESIAN_POINT ( 'NONE',  ( -154.4929263765338305, -8.102448949553172852, 5.886773742842742685 ) ) ;
#28553=CARTESIAN_POINT ( 'NONE',  ( -163.3449999999999989, 7.632228543268599452, -2.479861379858951942 ) ) ;
#28562=CARTESIAN_POINT ( 'NONE',  ( -66.74292637653380211, -5.598654528085803328, -7.705886871421366635 ) ) ;
#28572=CARTESIAN_POINT ( 'NONE',  ( -167.0049999999999670, 6.826472737025115478, 4.959722759717899443 ) ) ;
#28578=EDGE_CURVE ( 'NONE', #68565, #65809, #55092, .T. ) ;
#28582=ORIENTED_EDGE ( 'NONE', *, *, #61769, .T. ) ;
#28586=CARTESIAN_POINT ( 'NONE',  ( -85.70499999999998408, 2.607480562269072433, 8.024999999999991473 ) ) ;
#28589=( BOUNDED_CURVE ( )  B_SPLINE_CURVE ( 2, ( #28125, #22197, #32382, #16268, #44046, #37742, #59459, #64765, #11290, #16603, #54197 ),
 .UNSPECIFIED., .F., .F. ) 
 B_SPLINE_CURVE_WITH_KNOTS ( ( 3, 2, 2, 2, 2, 3 ),
 ( 0.4891304347825970456, 0.4913043478260752384, 0.4934782608695534312, 0.4956521739130317350, 0.4978260869565099278, 0.4999999999999881206 ),
 .UNSPECIFIED. ) 
 CURVE ( )  GEOMETRIC_REPRESENTATION_ITEM ( )  RATIONAL_B_SPLINE_CURVE ( ( 1.000000000000262457, 0.9510565162948910745, 1.000000000000000000, 0.9510565162951535312, 1.000000000000000000, 0.9510565162951535312, 1.000000000000000000, 0.9510565162951535312, 1.000000000000000000, 0.9510565162954209839, 0.9999999999997325473 ) ) 
 REPRESENTATION_ITEM ( '' )  );
#28593=CARTESIAN_POINT ( 'NONE',  ( -169.1929263765338476, -10.01517768586948698, 6.132527647946031529E-16 ) ) ;
#28599=CARTESIAN_POINT ( 'NONE',  ( -61.64499999999998892, 4.716976649647091513, -6.492361379858946790 ) ) ;
#28604=CARTESIAN_POINT ( 'NONE',  ( -48.59292637653380353, -3.094860106618431139, -9.524999999999991473 ) ) ;
#28605=CARTESIAN_POINT ( 'NONE',  ( -139.5570736234661808, -1.166476076187852838E-15, -9.524999999999991473 ) ) ;
#28609=CARTESIAN_POINT ( 'NONE',  ( -50.24499999999998323, -4.716976649647093289, -6.492361379858945902 ) ) ;
#28612=CARTESIAN_POINT ( 'NONE',  ( -114.8049999999999926, -8.437984349512085203, 5.166775262442717831E-16 ) ) ;
#28619=CARTESIAN_POINT ( 'NONE',  ( -154.4070736234661467, 3.094860106618428031, -9.524999999999993250 ) ) ;
#28621=( BOUNDED_CURVE ( )  B_SPLINE_CURVE ( 2, ( #4902, #606, #65019, #38351, #53455, #16876, #59754, #17233, #11564, #27716, #60099 ),
 .UNSPECIFIED., .F., .F. ) 
 B_SPLINE_CURVE_WITH_KNOTS ( ( 3, 2, 2, 2, 2, 3 ),
 ( 0.4673913043478151175, 0.4695652173912933103, 0.4717391304347715031, 0.4739130434782496959, 0.4760869565217279442, 0.4782608695652061370 ),
 .UNSPECIFIED. ) 
 CURVE ( )  GEOMETRIC_REPRESENTATION_ITEM ( )  RATIONAL_B_SPLINE_CURVE ( ( 1.000000000000247358, 0.9510565162949060625, 1.000000000000000000, 0.9510565162951535312, 1.000000000000000000, 0.9510565162951535312, 1.000000000000000000, 0.9510565162951535312, 1.000000000000000000, 0.9510565162954072171, 0.9999999999997463140 ) ) 
 REPRESENTATION_ITEM ( '' )  );
#28622=CARTESIAN_POINT ( 'NONE',  ( -59.60707362346616378, -8.102448949553174629, 5.886773742842742685 ) ) ;
#28624=CARTESIAN_POINT ( 'NONE',  ( -87.80707362346616662, 10.01517768586948698, -1.839758294383808571E-15 ) ) ;
#28634=CARTESIAN_POINT ( 'NONE',  ( -127.7049999999999699, 2.607480562269073321, 8.024999999999991473 ) ) ;
#28635=CARTESIAN_POINT ( 'NONE',  ( -164.5429263765338135, 9.058813317711329915, 2.943386871421369566 ) ) ;
#28637=CARTESIAN_POINT ( 'NONE',  ( -134.3949999999999250, -6.826472737025115478, -4.959722759717899443 ) ) ;
#28638=CARTESIAN_POINT ( 'NONE',  ( -124.7949999999999733, 2.607480562269069324, -8.024999999999993250 ) ) ;
#28645=CARTESIAN_POINT ( 'NONE',  ( -180.2929263765338419, 3.094860106618428031, -9.524999999999993250 ) ) ;
#28647=CARTESIAN_POINT ( 'NONE',  ( -47.09499999999999886, -2.607480562269071545, -8.024999999999991473 ) ) ;
#28652=CARTESIAN_POINT ( 'NONE',  ( -93.14292637653380780, 5.598654528085800663, -7.705886871421367523 ) ) ;
#28667=CARTESIAN_POINT ( 'NONE',  ( -195.0000000000000000, 0.000000000000000000, 0.000000000000000000 ) ) ;
#28681=CARTESIAN_POINT ( 'NONE',  ( -91.49499999999997613, 6.826472737025113702, -4.959722759717902107 ) ) ;
#28698=CARTESIAN_POINT ( 'NONE',  ( -178.4070736234662036, 3.094860106618428031, -9.524999999999993250 ) ) ;
#28701=CARTESIAN_POINT ( 'NONE',  ( -109.2570736234661837, 5.598654528085800663, -7.705886871421367523 ) ) ;
#28704=DIRECTION ( 'NONE',  ( -1.000000000000000000, -0.000000000000000000, -0.000000000000000000 ) ) ;
#28705=CARTESIAN_POINT ( 'NONE',  ( -85.55707362346618083, -1.166476076187852838E-15, -9.524999999999991473 ) ) ;
#28713=CARTESIAN_POINT ( 'NONE',  ( -159.2050000000000125, -2.607480562269071545, -8.024999999999991473 ) ) ;
#28715=CARTESIAN_POINT ( 'NONE',  ( -183.5367403587429180, -4.194181754694801256, -7.955897757997197672 ) ) ;
#28716=CARTESIAN_POINT ( 'NONE',  ( -161.3950000000000102, -6.826472737025115478, -4.959722759717899443 ) ) ;
#28719=CARTESIAN_POINT ( 'NONE',  ( -155.3950000000000102, -6.826472737025113702, -4.959722759717900331 ) ) ;
#28721=FACE_OUTER_BOUND ( 'NONE', #27996, .T. ) ;
#28723=CARTESIAN_POINT ( 'NONE',  ( -71.15499999999998693, 7.632228543268600340, 2.479861379858949277 ) ) ;
#28728=CARTESIAN_POINT ( 'NONE',  ( -74.84499999999998465, -7.632228543268599452, 2.479861379858951054 ) ) ;
#28744=ORIENTED_EDGE ( 'NONE', *, *, #17429, .F. ) ;
#28754=CARTESIAN_POINT ( 'NONE',  ( -102.6549999999999869, -7.632228543268600340, -2.479861379858950166 ) ) ;
#28767=ORIENTED_EDGE ( 'NONE', *, *, #39932, .F. ) ;
#28786=CARTESIAN_POINT ( 'NONE',  ( -134.4549999999999841, 7.632228543268599452, -2.479861379858951942 ) ) ;
#28794=ORIENTED_EDGE ( 'NONE', *, *, #30441, .T. ) ;
#28798=CARTESIAN_POINT ( 'NONE',  ( -51.65499999999997982, -7.632228543268600340, -2.479861379858950166 ) ) ;
#28800=CARTESIAN_POINT ( 'NONE',  ( -124.2570736234661837, 5.598654528085800663, -7.705886871421367523 ) ) ;
#28802=CARTESIAN_POINT ( 'NONE',  ( -195.0000000000000000, 0.000000000000000000, 0.000000000000000000 ) ) ;
#28808=CARTESIAN_POINT ( 'NONE',  ( -144.2070736234666697, 3.094860106626365237, 9.524999999994228972 ) ) ;
#28815=CARTESIAN_POINT ( 'NONE',  ( -102.2949999999999733, -2.607480562269069768, 8.024999999999991473 ) ) ;
#28819=CARTESIAN_POINT ( 'NONE',  ( -75.44499999999997897, 0.000000000000000000, 8.024999999999991473 ) ) ;
#28827=CARTESIAN_POINT ( 'NONE',  ( -116.2429263765338021, 5.598654528085804216, 7.705886871421366635 ) ) ;
#28828=CARTESIAN_POINT ( 'NONE',  ( -137.6949999999999932, -8.437984349512085203, 5.166775262442717831E-16 ) ) ;
#28841=ORIENTED_EDGE ( 'NONE', *, *, #4618, .T. ) ;
#28842=CARTESIAN_POINT ( 'NONE',  ( -132.5049999999999955, -6.826472737025113702, -4.959722759717900331 ) ) ;
#28855=CARTESIAN_POINT ( 'NONE',  ( -59.00499999999998124, 6.826472737025115478, 4.959722759717899443 ) ) ;
#28870=CARTESIAN_POINT ( 'NONE',  ( -165.9549999999999841, -7.632228543268599452, 2.479861379858951054 ) ) ;
#28874=ORIENTED_EDGE ( 'NONE', *, *, #30441, .F. ) ;
#28879=CARTESIAN_POINT ( 'NONE',  ( -72.95499999999999829, -7.632228543268599452, 2.479861379858951054 ) ) ;
#28893=CARTESIAN_POINT ( 'NONE',  ( -110.2449999999999903, -4.716976649647093289, -6.492361379858945902 ) ) ;
#28896=CARTESIAN_POINT ( 'NONE',  ( -17.22936139948035361, 11.13022047738569675, 4.487408569146854376 ) ) ;
#28897=CARTESIAN_POINT ( 'NONE',  ( -156.1429263765338078, 5.598654528085800663, -7.705886871421367523 ) ) ;
#28898=CARTESIAN_POINT ( 'NONE',  ( -168.5949999999999989, 2.607480562269073321, 8.024999999999991473 ) ) ;
#28907=CARTESIAN_POINT ( 'NONE',  ( -64.34292637653379643, -9.058813317711329915, 2.943386871421371787 ) ) ;
#28917=CARTESIAN_POINT ( 'NONE',  ( -168.3550000000000182, -4.716976649647093289, -6.492361379858945902 ) ) ;
#28919=CARTESIAN_POINT ( 'NONE',  ( -111.5929263765347059, -3.094860106633758434, -9.524999999988855492 ) ) ;
#28927=CARTESIAN_POINT ( 'NONE',  ( -85.55499999999999261, 0.000000000000000000, 8.024999999999991473 ) ) ;
#28934=EDGE_LOOP ( 'NONE', ( #44327, #31769, #46662, #3731 ) ) ;
#28935=CARTESIAN_POINT ( 'NONE',  ( -51.59499999999997755, 2.607480562269073321, 8.024999999999991473 ) ) ;
#28943=CARTESIAN_POINT ( 'NONE',  ( -56.99499999999999034, -6.826472737025113702, 4.959722759717902107 ) ) ;
#28949=CARTESIAN_POINT ( 'NONE',  ( -102.6549999999999869, -7.632228543268600340, -2.479861379858950166 ) ) ;
#28951=CYLINDRICAL_SURFACE ( 'NONE', #38481, 9.524999999999991473 ) ;
#28954=CARTESIAN_POINT ( 'NONE',  ( -152.3070736234661240, -10.01517768586948698, 6.132527647946031529E-16 ) ) ;
#28957=CARTESIAN_POINT ( 'NONE',  ( -85.25707362346616947, 5.598654528085800663, -7.705886871421367523 ) ) ;
#28963=EDGE_CURVE ( 'NONE', #32796, #31059, #11544, .T. ) ;
#28966=CARTESIAN_POINT ( 'NONE',  ( -134.6050000000000182, 6.826472737025113702, -4.959722759717902107 ) ) ;
#28967=EDGE_CURVE ( 'NONE', #64020, #31165, #23671, .T. ) ;
#28969=CARTESIAN_POINT ( 'NONE',  ( -146.3929263765337794, 8.102448949553176405, 5.886773742842740909 ) ) ;
#28971=CARTESIAN_POINT ( 'NONE',  ( -138.2949999999999591, -2.607480562269069768, 8.024999999999991473 ) ) ;
#28973=CARTESIAN_POINT ( 'NONE',  ( -127.4949999999999903, 6.826472737025113702, -4.959722759717902107 ) ) ;
#28978=CARTESIAN_POINT ( 'NONE',  ( -146.0070736234661410, -8.102448949553174629, -5.886773742842741797 ) ) ;
#28982=CARTESIAN_POINT ( 'NONE',  ( -177.8929263765338078, -8.102448949553172852, -5.886773742842741797 ) ) ;
#28984=CARTESIAN_POINT ( 'NONE',  ( -50.99499999999999034, -6.826472737025115478, 4.959722759717900331 ) ) ;
#28989=CARTESIAN_POINT ( 'NONE',  ( -96.74292637653380211, -5.598654528085803328, -7.705886871421366635 ) ) ;
#29002=VERTEX_POINT ( 'NONE', #52810 ) ;
#29015=CARTESIAN_POINT ( 'NONE',  ( -81.29499999999998749, -2.607480562269069768, 8.024999999999991473 ) ) ;
#29032=CARTESIAN_POINT ( 'NONE',  ( -180.3570736234661638, 5.598654528085804216, 7.705886871421366635 ) ) ;
#29035=EDGE_CURVE ( 'NONE', #54235, #57448, #66842, .T. ) ;
#29036=CARTESIAN_POINT ( 'NONE',  ( -114.2070736234661581, 3.094860106618433360, 9.524999999999991473 ) ) ;
#29047=CARTESIAN_POINT ( 'NONE',  ( -159.5049999999999955, -6.826472737025115478, -4.959722759717899443 ) ) ;
#29050=CARTESIAN_POINT ( 'NONE',  ( -167.3949999999999534, -6.826472737025115478, -4.959722759717899443 ) ) ;
#29051=ADVANCED_FACE ( 'NONE', ( #41936 ), #9202, .T. ) ;
#29052=CARTESIAN_POINT ( 'NONE',  ( -154.9449999999999932, -9.827790563157499189E-16, -8.024999999999991473 ) ) ;
#29058=CARTESIAN_POINT ( 'NONE',  ( -74.90499999999997272, 2.607480562269068880, -8.024999999999993250 ) ) ;
#29061=CARTESIAN_POINT ( 'NONE',  ( -70.19499999999997897, 8.437984349512086979, -1.550032578732815448E-15 ) ) ;
#29063=DIRECTION ( 'NONE',  ( -1.000000000000000000, -0.000000000000000000, -0.000000000000000000 ) ) ;
#29091=CARTESIAN_POINT ( 'NONE',  ( -111.4449999999999932, 0.000000000000000000, 8.024999999999991473 ) ) ;
#29096=CARTESIAN_POINT ( 'NONE',  ( -11.02951865299722556, -11.60758465034584930, 3.056320357840781377 ) ) ;
#29113=CARTESIAN_POINT ( 'NONE',  ( -131.7549999999999955, 4.716976649647091513, -6.492361379858946790 ) ) ;
#29121=DIRECTION ( 'NONE',  ( -1.000000000000000000, -0.000000000000000000, -0.000000000000000000 ) ) ;
#29130=ORIENTED_EDGE ( 'NONE', *, *, #65861, .T. ) ;
#29133=CYLINDRICAL_SURFACE ( 'NONE', #53735, 9.524999999999991473 ) ;
#29135=CARTESIAN_POINT ( 'NONE',  ( -51.80707362346617373, 10.01517768586948698, -1.839758294383808571E-15 ) ) ;
#29140=CARTESIAN_POINT ( 'NONE',  ( -177.2070736234662434, 3.094860106619617746, 9.524999999999131717 ) ) ;
#29143=CARTESIAN_POINT ( 'NONE',  ( -145.4070736234666015, 3.094860106610764827, -9.525000000005562129 ) ) ;
#29147=CARTESIAN_POINT ( 'NONE',  ( -98.75499999999999545, 4.716976649647091513, -6.492361379858946790 ) ) ;
#29151=CARTESIAN_POINT ( 'NONE',  ( -96.59499999999998465, 2.607480562269072433, 8.024999999999991473 ) ) ;
#29153=CARTESIAN_POINT ( 'NONE',  ( -73.34499999999999886, 7.632228543268599452, -2.479861379858951942 ) ) ;
#29156=CYLINDRICAL_SURFACE ( 'NONE', #47481, 9.524999999999991473 ) ;
#29161=CARTESIAN_POINT ( 'NONE',  ( -119.0929263765337964, 3.094860106618433360, 9.524999999999991473 ) ) ;
#29162=CARTESIAN_POINT ( 'NONE',  ( -139.4949999999999761, 6.826472737025113702, -4.959722759717902107 ) ) ;
#29169=ORIENTED_EDGE ( 'NONE', *, *, #218, .F. ) ;
#29180=CARTESIAN_POINT ( 'NONE',  ( -136.1049999999999898, -6.826472737025113702, 4.959722759717902107 ) ) ;
#29195=CARTESIAN_POINT ( 'NONE',  ( -48.80499999999997129, -8.437984349512086979, 5.166775262442717831E-16 ) ) ;
#29198=ORIENTED_EDGE ( 'NONE', *, *, #56873, .T. ) ;
#29213=CARTESIAN_POINT ( 'NONE',  ( -122.7570736234661695, -5.598654528085801552, 7.705886871421367523 ) ) ;
#29214=DIRECTION ( 'NONE',  ( 0.000000000000000000, 0.000000000000000000, 1.000000000000000000 ) ) ;
#29215=CARTESIAN_POINT ( 'NONE',  ( -163.8549999999999898, 4.716976649647094177, 6.492361379858945902 ) ) ;
#29231=CARTESIAN_POINT ( 'NONE',  ( -76.70499999999999829, 2.607480562269073321, 8.024999999999991473 ) ) ;
#29235=( BOUNDED_CURVE ( )  B_SPLINE_CURVE ( 2, ( #7293, #29420, #13948, #40031, #61089, #62122, #24148, #17845, #45656, #45983, #13234 ),
 .UNSPECIFIED., .F., .F. ) 
 B_SPLINE_CURVE_WITH_KNOTS ( ( 3, 2, 2, 2, 2, 3 ),
 ( 0.8478260869565217295, 0.8499999999999999778, 0.8521739130434782261, 0.8543478260869564744, 0.8565217391304348338, 0.8586956521739130821 ),
 .UNSPECIFIED. ) 
 CURVE ( )  GEOMETRIC_REPRESENTATION_ITEM ( )  RATIONAL_B_SPLINE_CURVE ( ( 1.000000000000000000, 0.9510565162951535312, 1.000000000000000000, 0.9510565162951535312, 1.000000000000000000, 0.9510565162951535312, 1.000000000000000000, 0.9510565162951535312, 1.000000000000000000, 0.9510565162951535312, 1.000000000000000000 ) ) 
 REPRESENTATION_ITEM ( '' )  );
#29236=CARTESIAN_POINT ( 'NONE',  ( -63.65707362346617515, 9.058813317711329915, 2.943386871421369566 ) ) ;
#29244=CARTESIAN_POINT ( 'NONE',  ( -105.2949999999999875, -2.607480562269069768, 8.024999999999991473 ) ) ;
#29251=CARTESIAN_POINT ( 'NONE',  ( -19.96716105561538512, 11.98620757464661146, 0.6605852583158889901 ) ) ;
#29253=CARTESIAN_POINT ( 'NONE',  ( -140.8429263765338249, 9.058813317711329915, -2.943386871421373119 ) ) ;
#29254=CARTESIAN_POINT ( 'NONE',  ( -170.0949999999999704, -2.607480562269071545, -8.024999999999991473 ) ) ;
#29271=CARTESIAN_POINT ( 'NONE',  ( -161.0049999999999955, 6.826472737025115478, 4.959722759717899443 ) ) ;
#29285=CARTESIAN_POINT ( 'NONE',  ( -87.80499999999999261, -8.437984349512086979, 5.166775262442717831E-16 ) ) ;
#29292=ADVANCED_FACE ( 'NONE', ( #12269 ), #55189, .T. ) ;
#29298=CARTESIAN_POINT ( 'NONE',  ( -57.74499999999999034, 4.716976649647094177, 6.492361379858945902 ) ) ;
#29302=CARTESIAN_POINT ( 'NONE',  ( -87.44292637653380496, -1.166476076187852838E-15, -9.524999999999991473 ) ) ;
#29306=CARTESIAN_POINT ( 'NONE',  ( -49.79499999999998039, 2.607480562269069324, -8.024999999999993250 ) ) ;
#29311=CARTESIAN_POINT ( 'NONE',  ( -107.9050000000000011, 2.607480562269068880, -8.024999999999993250 ) ) ;
#29312=ORIENTED_EDGE ( 'NONE', *, *, #36666, .T. ) ;
#29315=CARTESIAN_POINT ( 'NONE',  ( -144.3570736234661638, 5.598654528085804216, 7.705886871421366635 ) ) ;
#29319=CARTESIAN_POINT ( 'NONE',  ( -80.90707362346614673, -3.094860106618429807, 9.524999999999991473 ) ) ;
#29327=CARTESIAN_POINT ( 'NONE',  ( -121.5549999999999926, 0.000000000000000000, 8.024999999999991473 ) ) ;
#29331=CARTESIAN_POINT ( 'NONE',  ( -132.1449999999999818, -4.716976649647092401, 6.492361379858946790 ) ) ;
#29332=CARTESIAN_POINT ( 'NONE',  ( -118.7950000000000017, 2.607480562269069324, -8.024999999999993250 ) ) ;
#29335=EDGE_CURVE ( 'NONE', #51718, #34770, #38110, .T. ) ;
#29339=CARTESIAN_POINT ( 'NONE',  ( -121.9429263765338050, 0.000000000000000000, 9.524999999999991473 ) ) ;
#29340=CARTESIAN_POINT ( 'NONE',  ( -171.5929263765338249, -3.094860106618431139, -9.524999999999991473 ) ) ;
#29341=CARTESIAN_POINT ( 'NONE',  ( -51.14499999999999602, -4.716976649647092401, 6.492361379858946790 ) ) ;
#29347=CARTESIAN_POINT ( 'NONE',  ( -98.39292637653380780, 8.102448949553176405, 5.886773742842740909 ) ) ;
#29361=CARTESIAN_POINT ( 'NONE',  ( -63.44292637653379785, -1.166476076187852838E-15, -9.524999999999991473 ) ) ;
#29369=CARTESIAN_POINT ( 'NONE',  ( -93.74292637653380211, -5.598654528085803328, -7.705886871421366635 ) ) ;
#29370=EDGE_CURVE ( 'NONE', #57245, #2500, #28163, .T. ) ;
#29371=CARTESIAN_POINT ( 'NONE',  ( -104.9070736234671273, -3.094860106602564720, 9.525000000011518253 ) ) ;
#29374=ADVANCED_FACE ( 'NONE', ( #317 ), #5293, .T. ) ;
#29376=CARTESIAN_POINT ( 'NONE',  ( -78.44499999999999318, 0.000000000000000000, 8.024999999999991473 ) ) ;
#29385=CARTESIAN_POINT ( 'NONE',  ( -75.89292637653379359, -8.102448949553174629, -5.886773742842741797 ) ) ;
#29394=CARTESIAN_POINT ( 'NONE',  ( -195.0000000000000000, 0.000000000000000000, 9.524999999999991473 ) ) ;
#29397=CARTESIAN_POINT ( 'NONE',  ( -172.1070736234661069, 8.102448949553171076, -5.886773742842744461 ) ) ;
#29399=CARTESIAN_POINT ( 'NONE',  ( -177.4429263765338192, -1.166476076187852838E-15, -9.524999999999991473 ) ) ;
#29401=CARTESIAN_POINT ( 'NONE',  ( -110.1570736234661751, -9.058813317711329915, -2.943386871421370898 ) ) ;
#29405=CARTESIAN_POINT ( 'NONE',  ( -84.50707362346616947, 8.102448949553176405, 5.886773742842740909 ) ) ;
#29413=CARTESIAN_POINT ( 'NONE',  ( -146.1549999999999727, 7.632228543268600340, 2.479861379858949277 ) ) ;
#29414=CYLINDRICAL_SURFACE ( 'NONE', #69012, 9.524999999999991473 ) ;
#29417=CARTESIAN_POINT ( 'NONE',  ( -161.6950000000000216, -8.437984349512085203, 5.166775262442717831E-16 ) ) ;
#29418=CARTESIAN_POINT ( 'NONE',  ( -157.6449999999999818, 4.716976649647091513, -6.492361379858946790 ) ) ;
#29420=CARTESIAN_POINT ( 'NONE',  ( -67.79292637653381348, -3.094860106618429807, 9.524999999999991473 ) ) ;
#29422=CARTESIAN_POINT ( 'NONE',  ( -123.1429263765338078, 5.598654528085800663, -7.705886871421367523 ) ) ;
#29423=CARTESIAN_POINT ( 'NONE',  ( -75.80499999999997840, -8.437984349512085203, 5.166775262442717831E-16 ) ) ;
#29427=CARTESIAN_POINT ( 'NONE',  ( -68.39499999999996760, -6.826472737025113702, -4.959722759717900331 ) ) ;
#29445=CARTESIAN_POINT ( 'NONE',  ( -60.50707362346616236, 8.102448949553176405, 5.886773742842740909 ) ) ;
#29446=VECTOR ( 'NONE', #1658, 1000.000000000000000 ) ;
#29461=ORIENTED_EDGE ( 'NONE', *, *, #13741, .F. ) ;
#29466=CARTESIAN_POINT ( 'NONE',  ( -106.9449999999999790, -9.827790563157499189E-16, -8.024999999999991473 ) ) ;
#29471=CARTESIAN_POINT ( 'NONE',  ( -12.48379447375185336, -11.19212576109403656, -4.332794091909712542 ) ) ;
#29488=CARTESIAN_POINT ( 'NONE',  ( -136.7050000000000125, 2.607480562269073321, 8.024999999999991473 ) ) ;
#29502=CARTESIAN_POINT ( 'NONE',  ( -50.75499999999999545, 4.716976649647091513, -6.492361379858946790 ) ) ;
#29507=CARTESIAN_POINT ( 'NONE',  ( -56.75707362346615525, -5.598654528085801552, 7.705886871421367523 ) ) ;
#29510=CARTESIAN_POINT ( 'NONE',  ( -177.0570736234661808, 0.000000000000000000, 9.524999999999991473 ) ) ;
#29516=CARTESIAN_POINT ( 'NONE',  ( -102.2049999999999983, -2.607480562269071545, -8.024999999999991473 ) ) ;
#29520=CARTESIAN_POINT ( 'NONE',  ( -98.69499999999999318, -8.437984349512086979, 5.166775262442717831E-16 ) ) ;
#29522=CARTESIAN_POINT ( 'NONE',  ( -82.34499999999998465, 7.632228543268599452, -2.479861379858951942 ) ) ;
#29527=CARTESIAN_POINT ( 'NONE',  ( -112.7929263765337851, -3.094860106618429807, 9.524999999999991473 ) ) ;
#29528=CARTESIAN_POINT ( 'NONE',  ( -133.9449999999999932, -9.827790563157499189E-16, -8.024999999999991473 ) ) ;
#29534=VERTEX_POINT ( 'NONE', #47149 ) ;
#29547=CARTESIAN_POINT ( 'NONE',  ( -135.5049999999999670, -6.826472737025113702, -4.959722759717900331 ) ) ;
#29549=CARTESIAN_POINT ( 'NONE',  ( -125.7570736234661695, -5.598654528085801552, 7.705886871421367523 ) ) ;
#29551=CARTESIAN_POINT ( 'NONE',  ( -172.3429263765338249, -9.058813317711329915, 2.943386871421371787 ) ) ;
#29579=CARTESIAN_POINT ( 'NONE',  ( -163.5550000000000068, 0.000000000000000000, 8.024999999999991473 ) ) ;
#29588=CARTESIAN_POINT ( 'NONE',  ( -195.0000000000000000, 0.000000000000000000, 0.000000000000000000 ) ) ;
#29591=CARTESIAN_POINT ( 'NONE',  ( -77.15499999999998693, 7.632228543268600340, 2.479861379858949277 ) ) ;
#29593=CARTESIAN_POINT ( 'NONE',  ( -54.44292637653380496, -1.166476076187852838E-15, -9.524999999999991473 ) ) ;
#29603=CARTESIAN_POINT ( 'NONE',  ( -54.05707362346618083, 0.000000000000000000, 9.524999999999991473 ) ) ;
#29606=CARTESIAN_POINT ( 'NONE',  ( -102.8949999999999960, 6.826472737025116366, 4.959722759717898555 ) ) ;
#29614=CARTESIAN_POINT ( 'NONE',  ( -142.9429263765337907, 0.000000000000000000, 9.524999999999991473 ) ) ;
#29617=CARTESIAN_POINT ( 'NONE',  ( -165.2949999999999591, -2.607480562269069768, 8.024999999999991473 ) ) ;
#29620=AXIS2_PLACEMENT_3D ( 'NONE', #11193, #53753, #5549 ) ;
#29632=EDGE_CURVE ( 'NONE', #44394, #67626, #30859, .T. ) ;
#29635=CARTESIAN_POINT ( 'NONE',  ( -110.7570736234661837, -5.598654528085801552, 7.705886871421367523 ) ) ;
#29639=CARTESIAN_POINT ( 'NONE',  ( -156.8050000000000068, -8.437984349512086979, 5.166775262442717831E-16 ) ) ;
#29643=ORIENTED_EDGE ( 'NONE', *, *, #53915, .F. ) ;
#29647=DIRECTION ( 'NONE',  ( 0.000000000000000000, 0.000000000000000000, 1.000000000000000000 ) ) ;
#29653=CARTESIAN_POINT ( 'NONE',  ( -71.75499999999998124, 4.716976649647091513, -6.492361379858946790 ) ) ;
#29665=CARTESIAN_POINT ( 'NONE',  ( -57.59499999999998465, 2.607480562269073321, 8.024999999999991473 ) ) ;
#29667=( BOUNDED_CURVE ( )  B_SPLINE_CURVE ( 2, ( #42601, #32685, #17252, #38018, #47909, #32003, #57445, #59084, #53473, #16556, #27041 ),
 .UNSPECIFIED., .F., .F. ) 
 B_SPLINE_CURVE_WITH_KNOTS ( ( 3, 2, 2, 2, 2, 3 ),
 ( 0.04347826086956423780, 0.04565217391304245143, 0.04782608695652066505, 0.04999999999999887174, 0.05217391304347707842, 0.05434782608695529205 ),
 .UNSPECIFIED. ) 
 CURVE ( )  GEOMETRIC_REPRESENTATION_ITEM ( )  RATIONAL_B_SPLINE_CURVE ( ( 1.000000000000021982, 0.9510565162951315488, 1.000000000000000000, 0.9510565162951535312, 1.000000000000000000, 0.9510565162951535312, 1.000000000000000000, 0.9510565162951535312, 1.000000000000000000, 0.9510565162951811757, 0.9999999999999723554 ) ) 
 REPRESENTATION_ITEM ( '' )  );
#29671=CARTESIAN_POINT ( 'NONE',  ( -87.29292637653379927, 3.094860106618428031, -9.524999999999993250 ) ) ;
#29673=CARTESIAN_POINT ( 'NONE',  ( -49.34499999999997044, 7.632228543268599452, -2.479861379858951942 ) ) ;
#29676=CARTESIAN_POINT ( 'NONE',  ( -107.6049999999999756, 6.826472737025113702, -4.959722759717902107 ) ) ;
#29680=CARTESIAN_POINT ( 'NONE',  ( -139.8570736234661638, -5.598654528085803328, -7.705886871421366635 ) ) ;
#29682=CARTESIAN_POINT ( 'NONE',  ( -59.30707362346615952, -10.01517768586948698, 6.132527647946031529E-16 ) ) ;
#29684=CARTESIAN_POINT ( 'NONE',  ( -86.45707362346617231, -9.058813317711329915, 2.943386871421371787 ) ) ;
#29687=CARTESIAN_POINT ( 'NONE',  ( -96.14292637653380780, 5.598654528085800663, -7.705886871421367523 ) ) ;
#29692=CARTESIAN_POINT ( 'NONE',  ( -125.6050000000000040, 6.826472737025113702, -4.959722759717902107 ) ) ;
#29693=CARTESIAN_POINT ( 'NONE',  ( -158.2429263765338021, 5.598654528085804216, 7.705886871421366635 ) ) ;
#29695=CARTESIAN_POINT ( 'NONE',  ( -138.7450000000000045, 4.716976649647094177, 6.492361379858945902 ) ) ;
#29697=CARTESIAN_POINT ( 'NONE',  ( -116.0949999999999704, -2.607480562269071545, -8.024999999999991473 ) ) ;
#29703=CARTESIAN_POINT ( 'NONE',  ( -174.2929263765338419, 3.094860106618428031, -9.524999999999993250 ) ) ;
#29714=CARTESIAN_POINT ( 'NONE',  ( -85.34292637653381064, -9.058813317711329915, 2.943386871421371787 ) ) ;
#29721=ADVANCED_FACE ( 'NONE', ( #37289 ), #60075, .T. ) ;
#29736=CARTESIAN_POINT ( 'NONE',  ( -93.89292637653377938, -8.102448949553174629, -5.886773742842741797 ) ) ;
#29741=VECTOR ( 'NONE', #7159, 1000.000000000000000 ) ;
#29742=CARTESIAN_POINT ( 'NONE',  ( -71.00707362346615525, -8.102448949553174629, -5.886773742842741797 ) ) ;
#29744=CARTESIAN_POINT ( 'NONE',  ( -82.49499999999997613, 6.826472737025113702, -4.959722759717902107 ) ) ;
#29745=VERTEX_POINT ( 'NONE', #64675 ) ;
#29761=CARTESIAN_POINT ( 'NONE',  ( -172.5570736234661808, -1.166476076187852838E-15, -9.524999999999991473 ) ) ;
#29764=( BOUNDED_CURVE ( )  B_SPLINE_CURVE ( 2, ( #52097, #67555, #10207, #62954, #31644, #35894, #41904, #53124, #24984, #20039, #19353 ),
 .UNSPECIFIED., .F., .F. ) 
 B_SPLINE_CURVE_WITH_KNOTS ( ( 3, 2, 2, 2, 2, 3 ),
 ( 0.6195652173912895577, 0.6217391304347678060, 0.6239130434782459433, 0.6260869565217243027, 0.6282608695652024400, 0.6304347826086806883 ),
 .UNSPECIFIED. ) 
 CURVE ( )  GEOMETRIC_REPRESENTATION_ITEM ( )  RATIONAL_B_SPLINE_CURVE ( ( 1.000000000000332401, 0.9510565162948211304, 1.000000000000000000, 0.9510565162951535312, 1.000000000000000000, 0.9510565162951535312, 1.000000000000000000, 0.9510565162951535312, 1.000000000000000000, 0.9510565162954909280, 0.9999999999996626032 ) ) 
 REPRESENTATION_ITEM ( '' )  );
#29765=CARTESIAN_POINT ( 'NONE',  ( -112.1070736234661496, 8.102448949553171076, -5.886773742842744461 ) ) ;
#29766=CARTESIAN_POINT ( 'NONE',  ( -183.0000000000000000, 7.623482428031956637, -5.710353812986356026 ) ) ;
#29774=CARTESIAN_POINT ( 'NONE',  ( -146.7549999999999955, 4.716976649647091513, -6.492361379858946790 ) ) ;
#29778=CARTESIAN_POINT ( 'NONE',  ( -166.6449999999999818, 4.716976649647091513, -6.492361379858946790 ) ) ;
#29779=CARTESIAN_POINT ( 'NONE',  ( -146.0949999999999989, -2.607480562269071545, -8.024999999999991473 ) ) ;
#29782=CYLINDRICAL_SURFACE ( 'NONE', #68434, 9.524999999999991473 ) ;
#29786=CARTESIAN_POINT ( 'NONE',  ( -64.85499999999997556, 4.716976649647094177, 6.492361379858945902 ) ) ;
#29791=CARTESIAN_POINT ( 'NONE',  ( -62.39499999999998181, -6.826472737025113702, -4.959722759717900331 ) ) ;
#29812=CARTESIAN_POINT ( 'NONE',  ( -145.1929263765337907, -10.01517768586948698, 6.132527647946031529E-16 ) ) ;
#29816=CARTESIAN_POINT ( 'NONE',  ( -112.3449999999999847, 7.632228543268599452, -2.479861379858951942 ) ) ;
#29819=CARTESIAN_POINT ( 'NONE',  ( -53.69292637653380496, 10.01517768586948698, -1.839758294383808966E-15 ) ) ;
#29820=CARTESIAN_POINT ( 'NONE',  ( -10.75962301985815017, -11.70357532857513938, -2.654319096146382062 ) ) ;
#29834=CARTESIAN_POINT ( 'NONE',  ( -131.6049999999999898, 6.826472737025113702, -4.959722759717902107 ) ) ;
#29848=CARTESIAN_POINT ( 'NONE',  ( -179.0050000000000239, 6.826472737025116366, 4.959722759717898555 ) ) ;
#29853=CARTESIAN_POINT ( 'NONE',  ( -52.85707362346617089, -5.598654528085803328, -7.705886871421366635 ) ) ;
#29855=CARTESIAN_POINT ( 'NONE',  ( -173.2449999999999761, -4.716976649647093289, -6.492361379858945902 ) ) ;
#29859=EDGE_CURVE ( 'NONE', #3684, #62473, #9317, .T. ) ;
#29862=CARTESIAN_POINT ( 'NONE',  ( -95.75499999999999545, 4.716976649647091513, -6.492361379858946790 ) ) ;
#29867=CARTESIAN_POINT ( 'NONE',  ( -99.29499999999998749, -2.607480562269069768, 8.024999999999991473 ) ) ;
#29869=CARTESIAN_POINT ( 'NONE',  ( -68.54499999999998749, -7.632228543268600340, -2.479861379858950166 ) ) ;
#29880=CARTESIAN_POINT ( 'NONE',  ( -110.9929263765338163, 8.102448949553171076, -5.886773742842744461 ) ) ;
#29881=CARTESIAN_POINT ( 'NONE',  ( -130.0449999999999875, 7.632228543268600340, 2.479861379858949277 ) ) ;
#29887=AXIS2_PLACEMENT_3D ( 'NONE', #41627, #68005, #9945 ) ;
#29899=CARTESIAN_POINT ( 'NONE',  ( -132.3549999999999898, -4.716976649647093289, -6.492361379858945902 ) ) ;
#29903=CARTESIAN_POINT ( 'NONE',  ( -120.2070736234661865, 3.094860106618433360, 9.524999999999991473 ) ) ;
#29927=CARTESIAN_POINT ( 'NONE',  ( -159.9549999999999841, -7.632228543268599452, 2.479861379858951054 ) ) ;
#29938=CARTESIAN_POINT ( 'NONE',  ( -73.55499999999997840, 0.000000000000000000, 8.024999999999991473 ) ) ;
#29939=ORIENTED_EDGE ( 'NONE', *, *, #12094, .T. ) ;
#29942=ADVANCED_FACE ( 'NONE', ( #55833 ), #49538, .T. ) ;
#29953=CARTESIAN_POINT ( 'NONE',  ( -99.44499999999999318, 0.000000000000000000, 8.024999999999991473 ) ) ;
#29961=CARTESIAN_POINT ( 'NONE',  ( -140.0929263765337964, 3.094860106618433360, 9.524999999999991473 ) ) ;
#29964=CARTESIAN_POINT ( 'NONE',  ( -170.8449999999999989, -7.632228543268599452, 2.479861379858951054 ) ) ;
#29974=ORIENTED_EDGE ( 'NONE', *, *, #1609, .F. ) ;
#29975=CARTESIAN_POINT ( 'NONE',  ( -164.4549999999999841, 7.632228543268599452, -2.479861379858951942 ) ) ;
#29988=CARTESIAN_POINT ( 'NONE',  ( -75.50499999999998124, -6.826472737025113702, -4.959722759717900331 ) ) ;
#30000=CARTESIAN_POINT ( 'NONE',  ( -53.39499999999998892, -6.826472737025115478, -4.959722759717899443 ) ) ;
#30004=CARTESIAN_POINT ( 'NONE',  ( -86.69292637653380496, 10.01517768586948698, -1.839758294383808966E-15 ) ) ;
#30011=CARTESIAN_POINT ( 'NONE',  ( -103.2549999999999812, -4.716976649647092401, 6.492361379858946790 ) ) ;
#30016=CARTESIAN_POINT ( 'NONE',  ( -145.5570736234661808, -1.166476076187852838E-15, -9.524999999999991473 ) ) ;
#30019=CARTESIAN_POINT ( 'NONE',  ( -71.45707362346617231, -9.058813317711329915, 2.943386871421371787 ) ) ;
#30027=CARTESIAN_POINT ( 'NONE',  ( -123.6549999999999869, -7.632228543268600340, -2.479861379858950166 ) ) ;
#30031=CARTESIAN_POINT ( 'NONE',  ( -127.4950000000000045, 6.826472737025113702, -4.959722759717902107 ) ) ;
#30033=CARTESIAN_POINT ( 'NONE',  ( -117.7449999999999903, 4.716976649647094177, 6.492361379858945902 ) ) ;
#30039=CARTESIAN_POINT ( 'NONE',  ( -174.1429263765338078, 5.598654528085800663, -7.705886871421367523 ) ) ;
#30041=CARTESIAN_POINT ( 'NONE',  ( -50.54499999999998039, -7.632228543268600340, -2.479861379858950166 ) ) ;
#30047=CARTESIAN_POINT ( 'NONE',  ( -86.24292637653380211, 5.598654528085804216, 7.705886871421366635 ) ) ;
#30062=CARTESIAN_POINT ( 'NONE',  ( -105.2049999999999841, -2.607480562269071545, -8.024999999999991473 ) ) ;
#30070=CARTESIAN_POINT ( 'NONE',  ( -86.39499999999999602, -6.826472737025115478, -4.959722759717899443 ) ) ;
#30072=EDGE_CURVE ( 'NONE', #19085, #41992, #67788, .T. ) ;
#30086=DIRECTION ( 'NONE',  ( -1.000000000000000000, -0.000000000000000000, -0.000000000000000000 ) ) ;
#30088=CARTESIAN_POINT ( 'NONE',  ( -167.3070736234662093, -10.01517768586948698, 6.132527647946031529E-16 ) ) ;
#30090=CARTESIAN_POINT ( 'NONE',  ( -106.4070736234661609, 3.094860106618428031, -9.524999999999993250 ) ) ;
#30095=CARTESIAN_POINT ( 'NONE',  ( -107.5429263765337993, 9.058813317711329915, 2.943386871421369566 ) ) ;
#30096=CARTESIAN_POINT ( 'NONE',  ( -106.5570736234661666, -1.166476076187852838E-15, -9.524999999999991473 ) ) ;
#30100=CARTESIAN_POINT ( 'NONE',  ( -147.9550000000000125, -7.632228543268599452, 2.479861379858951054 ) ) ;
#30102=CARTESIAN_POINT ( 'NONE',  ( -147.8929263765338078, -8.102448949553174629, -5.886773742842741797 ) ) ;
#30103=CARTESIAN_POINT ( 'NONE',  ( -160.7949999999999591, 2.607480562269068880, -8.024999999999993250 ) ) ;
#30104=CARTESIAN_POINT ( 'NONE',  ( -145.4949999999999477, 6.826472737025113702, -4.959722759717902107 ) ) ;
#30108=CARTESIAN_POINT ( 'NONE',  ( -61.40499999999999403, -2.607480562269069768, 8.024999999999991473 ) ) ;
#30112=CARTESIAN_POINT ( 'NONE',  ( -58.49499999999998323, 6.826472737025113702, -4.959722759717902107 ) ) ;
#30141=CARTESIAN_POINT ( 'NONE',  ( -115.0449999999999875, 7.632228543268600340, 2.479861379858949277 ) ) ;
#30144=( BOUNDED_CURVE ( )  B_SPLINE_CURVE ( 2, ( #31095, #41350, #62753, #52252, #15322, #58193, #20914, #47336, #25822, #42070, #31435 ),
 .UNSPECIFIED., .F., .F. ) 
 B_SPLINE_CURVE_WITH_KNOTS ( ( 3, 2, 2, 2, 2, 3 ),
 ( 0.5326086956521612903, 0.5347826086956395386, 0.5369565217391176759, 0.5391304347825959242, 0.5413043478260740615, 0.5434782608695523098 ),
 .UNSPECIFIED. ) 
 CURVE ( )  GEOMETRIC_REPRESENTATION_ITEM ( )  RATIONAL_B_SPLINE_CURVE ( ( 1.000000000000284883, 0.9510565162948685369, 1.000000000000000000, 0.9510565162951535312, 1.000000000000000000, 0.9510565162951535312, 1.000000000000000000, 0.9510565162951535312, 1.000000000000000000, 0.9510565162954435214, 0.9999999999997100097 ) ) 
 REPRESENTATION_ITEM ( '' )  );
#30163=CARTESIAN_POINT ( 'NONE',  ( -125.0049999999999812, 6.826472737025116366, 4.959722759717898555 ) ) ;
#30167=CARTESIAN_POINT ( 'NONE',  ( -114.0570736234661808, 0.000000000000000000, 9.524999999999991473 ) ) ;
#30168=ORIENTED_EDGE ( 'NONE', *, *, #60350, .F. ) ;
#30172=EDGE_CURVE ( 'NONE', #17985, #44158, #54688, .T. ) ;
#30176=CARTESIAN_POINT ( 'NONE',  ( -179.9049999999999727, 2.607480562269068880, -8.024999999999993250 ) ) ;
#30179=CARTESIAN_POINT ( 'NONE',  ( -55.70707362346616520, -3.094860106618431139, -9.524999999999991473 ) ) ;
#30180=CARTESIAN_POINT ( 'NONE',  ( -177.5949999999999989, 2.607480562269072433, 8.024999999999991473 ) ) ;
#30185=CARTESIAN_POINT ( 'NONE',  ( -94.25499999999999545, -4.716976649647092401, 6.492361379858946790 ) ) ;
#30188=CARTESIAN_POINT ( 'NONE',  ( -89.84499999999999886, -7.632228543268599452, 2.479861379858951054 ) ) ;
#30190=CARTESIAN_POINT ( 'NONE',  ( -65.84499999999998465, -7.632228543268599452, 2.479861379858951054 ) ) ;
#30200=CARTESIAN_POINT ( 'NONE',  ( -116.9929263765337879, 8.102448949553171076, -5.886773742842744461 ) ) ;
#30201=CARTESIAN_POINT ( 'NONE',  ( -125.8449999999999847, -7.632228543268599452, 2.479861379858951054 ) ) ;
#30218=CARTESIAN_POINT ( 'NONE',  ( -134.3050000000000068, 8.437984349512086979, -1.550032578732815448E-15 ) ) ;
#30221=CARTESIAN_POINT ( 'NONE',  ( -122.7570736234661695, -5.598654528085801552, 7.705886871421367523 ) ) ;
#30244=CARTESIAN_POINT ( 'NONE',  ( -151.8549999999999898, 4.716976649647094177, 6.492361379858945902 ) ) ;
#30259=FACE_OUTER_BOUND ( 'NONE', #10397, .T. ) ;
#30262=CARTESIAN_POINT ( 'NONE',  ( -78.35499999999997556, -4.716976649647093289, -6.492361379858945902 ) ) ;
#30268=ORIENTED_EDGE ( 'NONE', *, *, #61855, .F. ) ;
#30273=CARTESIAN_POINT ( 'NONE',  ( -96.29500000000000171, -2.607480562269069768, 8.024999999999991473 ) ) ;
#30274=CYLINDRICAL_SURFACE ( 'NONE', #34129, 9.524999999999991473 ) ;
#30279=CARTESIAN_POINT ( 'NONE',  ( -141.1429263765338078, 5.598654528085800663, -7.705886871421367523 ) ) ;
#30280=CARTESIAN_POINT ( 'NONE',  ( -158.6949999999999648, -8.437984349512085203, 5.166775262442717831E-16 ) ) ;
#30291=LINE ( 'NONE', #35259, #39448 ) ;
#30296=CARTESIAN_POINT ( 'NONE',  ( -164.9049999999999727, 2.607480562269069324, -8.024999999999993250 ) ) ;
#30304=CARTESIAN_POINT ( 'NONE',  ( -57.05707362346618083, 0.000000000000000000, 9.524999999999991473 ) ) ;
#30310=CARTESIAN_POINT ( 'NONE',  ( -142.5570736234661808, -1.166476076187852838E-15, -9.524999999999991473 ) ) ;
#30311=CARTESIAN_POINT ( 'NONE',  ( -71.00499999999996703, 6.826472737025115478, 4.959722759717899443 ) ) ;
#30313=ORIENTED_EDGE ( 'NONE', *, *, #9635, .F. ) ;
#30318=FACE_OUTER_BOUND ( 'NONE', #40678, .T. ) ;
#30326=CARTESIAN_POINT ( 'NONE',  ( -179.1550000000000011, 7.632228543268600340, 2.479861379858949277 ) ) ;
#30333=VERTEX_POINT ( 'NONE', #40917 ) ;
#30337=CARTESIAN_POINT ( 'NONE',  ( -106.2549999999999955, -4.716976649647092401, 6.492361379858946790 ) ) ;
#30340=CARTESIAN_POINT ( 'NONE',  ( -137.9070736234661751, -3.094860106618429807, 9.524999999999991473 ) ) ;
#30344=CARTESIAN_POINT ( 'NONE',  ( -78.50707362346615525, 8.102448949553176405, 5.886773742842740909 ) ) ;
#30350=CARTESIAN_POINT ( 'NONE',  ( -19.96684271803530564, -11.98607768299615728, -0.6619469921969921566 ) ) ;
#30352=CARTESIAN_POINT ( 'NONE',  ( -118.2549999999999812, -4.716976649647092401, 6.492361379858946790 ) ) ;
#30354=CARTESIAN_POINT ( 'NONE',  ( -125.3949999999999818, -6.826472737025115478, -4.959722759717899443 ) ) ;
#30362=FACE_OUTER_BOUND ( 'NONE', #1000, .T. ) ;
#30363=CARTESIAN_POINT ( 'NONE',  ( -170.5429263765338135, 9.058813317711329915, 2.943386871421369566 ) ) ;
#30370=CARTESIAN_POINT ( 'NONE',  ( -82.79292637653379927, -3.094860106618429807, 9.524999999999991473 ) ) ;
#30378=CARTESIAN_POINT ( 'NONE',  ( -156.5070736234661410, 8.102448949553176405, 5.886773742842740909 ) ) ;
#30381=CARTESIAN_POINT ( 'NONE',  ( -150.0570736234661808, 0.000000000000000000, 9.524999999999991473 ) ) ;
#30393=CARTESIAN_POINT ( 'NONE',  ( -103.8549999999999898, 4.716976649647094177, 6.492361379858945902 ) ) ;
#30396=CARTESIAN_POINT ( 'NONE',  ( -103.7070736234671671, -3.094860106634834018, -9.524999999988075672 ) ) ;
#30402=CARTESIAN_POINT ( 'NONE',  ( -77.39499999999999602, -6.826472737025115478, -4.959722759717899443 ) ) ;
#30418=LINE ( 'NONE', #20232, #61084 ) ;
#30419=CARTESIAN_POINT ( 'NONE',  ( -171.0570736234661808, 0.000000000000000000, 9.524999999999991473 ) ) ;
#30423=CARTESIAN_POINT ( 'NONE',  ( -104.3070736234661666, -10.01517768586948698, 6.132527647946031529E-16 ) ) ;
#30430=( BOUNDED_CURVE ( )  B_SPLINE_CURVE ( 2, ( #56095, #56443, #6870, #2588, #51184, #45600, #39265, #67348, #67017, #18807, #40290 ),
 .UNSPECIFIED., .F., .F. ) 
 B_SPLINE_CURVE_WITH_KNOTS ( ( 3, 2, 2, 2, 2, 3 ),
 ( 0.7500000000000000000, 0.7521739130434782483, 0.7543478260869564966, 0.7565217391304347450, 0.7586956521739129933, 0.7608695652173913526 ),
 .UNSPECIFIED. ) 
 CURVE ( )  GEOMETRIC_REPRESENTATION_ITEM ( )  RATIONAL_B_SPLINE_CURVE ( ( 1.000000000000000000, 0.9510565162951535312, 1.000000000000000000, 0.9510565162951535312, 1.000000000000000000, 0.9510565162951535312, 1.000000000000000000, 0.9510565162951535312, 1.000000000000000000, 0.9510565162951535312, 1.000000000000000000 ) ) 
 REPRESENTATION_ITEM ( '' )  );
#30435=CARTESIAN_POINT ( 'NONE',  ( -147.3549999999999898, -4.716976649647093289, -6.492361379858945902 ) ) ;
#30438=CARTESIAN_POINT ( 'NONE',  ( -151.4949999999999761, 6.826472737025113702, -4.959722759717902107 ) ) ;
#30439=CARTESIAN_POINT ( 'NONE',  ( -152.3949999999999818, -6.826472737025113702, -4.959722759717900331 ) ) ;
#30441=EDGE_CURVE ( 'NONE', #20781, #40082, #28589, .T. ) ;
#30447=CARTESIAN_POINT ( 'NONE',  ( -68.00499999999998124, 6.826472737025116366, 4.959722759717898555 ) ) ;
#30449=VECTOR ( 'NONE', #50921, 1000.000000000000000 ) ;
#30450=CARTESIAN_POINT ( 'NONE',  ( -65.39499999999998181, -6.826472737025113702, -4.959722759717900331 ) ) ;
#30452=CARTESIAN_POINT ( 'NONE',  ( -142.8570736234661638, -5.598654528085803328, -7.705886871421366635 ) ) ;
#30456=( BOUNDED_CURVE ( )  B_SPLINE_CURVE ( 2, ( #27030, #48563, #260, #54128, #25665, #47183, #68604, #20399, #58057, #9863, #12245 ),
 .UNSPECIFIED., .F., .F. ) 
 B_SPLINE_CURVE_WITH_KNOTS ( ( 3, 2, 2, 2, 2, 3 ),
 ( 0.9782608695652174058, 0.9804347826086956541, 0.9826086956521739024, 0.9847826086956521507, 0.9869565217391303991, 0.9891304347826086474 ),
 .UNSPECIFIED. ) 
 CURVE ( )  GEOMETRIC_REPRESENTATION_ITEM ( )  RATIONAL_B_SPLINE_CURVE ( ( 1.000000000000000000, 0.9510565162951535312, 1.000000000000000000, 0.9510565162951535312, 1.000000000000000000, 0.9510565162951535312, 1.000000000000000000, 0.9510565162951535312, 1.000000000000000000, 0.9510565162951535312, 1.000000000000000000 ) ) 
 REPRESENTATION_ITEM ( '' )  );
#30460=EDGE_CURVE ( 'NONE', #25339, #11319, #35802, .T. ) ;
#30465=ADVANCED_FACE ( 'NONE', ( #6355 ), #39862, .T. ) ;
#30490=CARTESIAN_POINT ( 'NONE',  ( -110.9950000000000045, -6.826472737025115478, 4.959722759717900331 ) ) ;
#30493=CARTESIAN_POINT ( 'NONE',  ( -164.1570736234661751, -9.058813317711329915, -2.943386871421370898 ) ) ;
#30505=CARTESIAN_POINT ( 'NONE',  ( -140.3929263765338078, 8.102448949553176405, 5.886773742842740909 ) ) ;
#30507=CARTESIAN_POINT ( 'NONE',  ( -127.8549999999999898, 4.716976649647094177, 6.492361379858945902 ) ) ;
#30523=CARTESIAN_POINT ( 'NONE',  ( -179.6049999999999898, 6.826472737025113702, -4.959722759717902107 ) ) ;
#30525=CARTESIAN_POINT ( 'NONE',  ( -50.45707362346615810, -9.058813317711329915, 2.943386871421371787 ) ) ;
#30527=CARTESIAN_POINT ( 'NONE',  ( -178.1949999999999648, 8.437984349512086979, -1.550032578732815448E-15 ) ) ;
#30535=CARTESIAN_POINT ( 'NONE',  ( -87.95499999999999829, -7.632228543268599452, 2.479861379858951054 ) ) ;
#30537=CARTESIAN_POINT ( 'NONE',  ( -168.8070736234661808, 10.01517768586948698, -1.839758294383808966E-15 ) ) ;
#30540=CARTESIAN_POINT ( 'NONE',  ( -92.39499999999998181, -6.826472737025113702, -4.959722759717900331 ) ) ;
#30542=CARTESIAN_POINT ( 'NONE',  ( -65.69499999999999318, -8.437984349512085203, 5.166775262442717831E-16 ) ) ;
#30549=ORIENTED_EDGE ( 'NONE', *, *, #6120, .T. ) ;
#30551=CARTESIAN_POINT ( 'NONE',  ( -101.0929263765338106, 3.094860106618433360, 9.524999999999991473 ) ) ;
#30552=CARTESIAN_POINT ( 'NONE',  ( -125.2449999999999903, -4.716976649647093289, -6.492361379858945902 ) ) ;
#30554=ADVANCED_FACE ( 'NONE', ( #39796 ), #34817, .T. ) ;
#30557=DIRECTION ( 'NONE',  ( 0.000000000000000000, 0.000000000000000000, 1.000000000000000000 ) ) ;
#30559=ORIENTED_EDGE ( 'NONE', *, *, #59801, .F. ) ;
#30565=CARTESIAN_POINT ( 'NONE',  ( -98.00707362346616947, -8.102448949553174629, -5.886773742842741797 ) ) ;
#30571=CARTESIAN_POINT ( 'NONE',  ( -124.1049999999999756, -6.826472737025113702, 4.959722759717902107 ) ) ;
#30574=CARTESIAN_POINT ( 'NONE',  ( -118.4070736234661751, 3.094860106618428031, -9.524999999999993250 ) ) ;
#30575=VERTEX_POINT ( 'NONE', #55588 ) ;
#30582=CARTESIAN_POINT ( 'NONE',  ( -195.0000000000000000, 0.000000000000000000, 9.524999999999991473 ) ) ;
#30592=CARTESIAN_POINT ( 'NONE',  ( -139.9429263765337907, 0.000000000000000000, 9.524999999999991473 ) ) ;
#30599=CARTESIAN_POINT ( 'NONE',  ( -62.69292637653379785, 10.01517768586948698, -1.839758294383808571E-15 ) ) ;
#30601=CARTESIAN_POINT ( 'NONE',  ( -157.1049999999999898, -6.826472737025115478, 4.959722759717900331 ) ) ;
#30605=CARTESIAN_POINT ( 'NONE',  ( -184.0000000000000000, -8.446573402700972011, 1.153699593821606140 ) ) ;
#30612=EDGE_LOOP ( 'NONE', ( #60608, #43981 ) ) ;
#30616=CARTESIAN_POINT ( 'NONE',  ( -64.10499999999997556, -6.826472737025115478, 4.959722759717900331 ) ) ;
#30621=ORIENTED_EDGE ( 'NONE', *, *, #6583, .F. ) ;
#30629=CARTESIAN_POINT ( 'NONE',  ( -94.49499999999999034, 6.826472737025113702, -4.959722759717902107 ) ) ;
#30634=CARTESIAN_POINT ( 'NONE',  ( -71.69292637653379074, 10.01517768586948698, -1.839758294383808966E-15 ) ) ;
#30637=CARTESIAN_POINT ( 'NONE',  ( -143.2429263765338021, 5.598654528085804216, 7.705886871421366635 ) ) ;
#30639=CARTESIAN_POINT ( 'NONE',  ( -156.2949999999999591, -2.607480562269069768, 8.024999999999991473 ) ) ;
#30652=CARTESIAN_POINT ( 'NONE',  ( -142.9429263765337907, 0.000000000000000000, 9.524999999999991473 ) ) ;
#30657=EDGE_CURVE ( 'NONE', #62435, #52329, #31814, .T. ) ;
#30659=CARTESIAN_POINT ( 'NONE',  ( -158.9050000000000011, 2.607480562269069324, -8.024999999999993250 ) ) ;
#30662=CARTESIAN_POINT ( 'NONE',  ( -46.88569120782204891, 5.598654528085803328, -7.705886871421366635 ) ) ;
#30669=CARTESIAN_POINT ( 'NONE',  ( -58.49292637653379501, -8.102448949553174629, 5.886773742842742685 ) ) ;
#30671=CARTESIAN_POINT ( 'NONE',  ( -77.90499999999997272, 2.607480562269069324, -8.024999999999993250 ) ) ;
#30676=CARTESIAN_POINT ( 'NONE',  ( -183.3519149756361912, 1.436423777000723276E-13, -9.173085024363883733 ) ) ;
#30683=CARTESIAN_POINT ( 'NONE',  ( -179.0050000000000239, 6.826472737025116366, 4.959722759717898555 ) ) ;
#30687=ORIENTED_EDGE ( 'NONE', *, *, #12925, .T. ) ;
#30692=CARTESIAN_POINT ( 'NONE',  ( -92.60500000000000398, 6.826472737025113702, -4.959722759717902107 ) ) ;
#30695=CARTESIAN_POINT ( 'NONE',  ( -45.00000000000000000, 0.000000000000000000, 0.000000000000000000 ) ) ;
#30697=CARTESIAN_POINT ( 'NONE',  ( -140.4570736234661865, -9.058813317711329915, 2.943386871421371787 ) ) ;
#30699=CARTESIAN_POINT ( 'NONE',  ( -76.70707362346617231, -3.094860106618431139, -9.524999999999991473 ) ) ;
#30710=CARTESIAN_POINT ( 'NONE',  ( -120.6549999999999869, -7.632228543268600340, -2.479861379858950166 ) ) ;
#30712=CARTESIAN_POINT ( 'NONE',  ( -128.3949999999999534, -6.826472737025115478, -4.959722759717899443 ) ) ;
#30724=CARTESIAN_POINT ( 'NONE',  ( -173.5429263765338135, 9.058813317711329915, 2.943386871421369566 ) ) ;
#30725=CARTESIAN_POINT ( 'NONE',  ( -181.3449999999999989, 7.632228543268599452, -2.479861379858951942 ) ) ;
#30735=CARTESIAN_POINT ( 'NONE',  ( -81.89292637653382201, -8.102448949553172852, -5.886773742842741797 ) ) ;
#30755=CARTESIAN_POINT ( 'NONE',  ( -103.1049999999999756, -6.826472737025113702, 4.959722759717902107 ) ) ;
#30763=CARTESIAN_POINT ( 'NONE',  ( -104.7570736234661695, -5.598654528085801552, 7.705886871421367523 ) ) ;
#30769=CARTESIAN_POINT ( 'NONE',  ( -67.94499999999999318, -9.827790563157499189E-16, -8.024999999999991473 ) ) ;
#30785=TOROIDAL_SURFACE ( 'NONE', #3802, 9.525000000000000355, 1.000000000000000888 ) ;
#30787=CARTESIAN_POINT ( 'NONE',  ( -172.8570736234661922, -5.598654528085803328, -7.705886871421366635 ) ) ;
#30789=CARTESIAN_POINT ( 'NONE',  ( -107.6070736234661638, -8.102448949553172852, 5.886773742842742685 ) ) ;
#30793=DIRECTION ( 'NONE',  ( -1.000000000000000000, -0.000000000000000000, -0.000000000000000000 ) ) ;
#30795=DIRECTION ( 'NONE',  ( 0.000000000000000000, 0.000000000000000000, 1.000000000000000000 ) ) ;
#30798=CARTESIAN_POINT ( 'NONE',  ( -149.7549999999999955, 4.716976649647091513, -6.492361379858946790 ) ) ;
#30802=CARTESIAN_POINT ( 'NONE',  ( -159.5949999999999989, 2.607480562269073321, 8.024999999999991473 ) ) ;
#30804=CARTESIAN_POINT ( 'NONE',  ( -147.2949999999999875, -2.607480562269069768, 8.024999999999991473 ) ) ;
#30812=CARTESIAN_POINT ( 'NONE',  ( -61.85499999999998266, 4.716976649647094177, 6.492361379858945902 ) ) ;
#30816=CARTESIAN_POINT ( 'NONE',  ( -59.69499999999998607, -8.437984349512086979, 5.166775262442717831E-16 ) ) ;
#30823=ADVANCED_FACE ( 'NONE', ( #31254 ), #52754, .T. ) ;
#30824=CARTESIAN_POINT ( 'NONE',  ( -177.5929263765339101, -3.094860106619935269, -9.524999999998900790 ) ) ;
#30850=CARTESIAN_POINT ( 'NONE',  ( -99.29499999999997328, -2.607480562269069768, 8.024999999999991473 ) ) ;
#30854=CARTESIAN_POINT ( 'NONE',  ( -46.54801840586653583, 4.937396119256769467, -6.795742752749552196 ) ) ;
#30859=( BOUNDED_CURVE ( )  B_SPLINE_CURVE ( 2, ( #25628, #68569, #63628, #67519, #10170, #31609, #46098, #19319, #20365, #62237, #63285 ),
 .UNSPECIFIED., .F., .F. ) 
 B_SPLINE_CURVE_WITH_KNOTS ( ( 3, 2, 2, 2, 2, 3 ),
 ( 0.3804347826086865170, 0.3826086956521647098, 0.3847826086956429026, 0.3869565217391210954, 0.3891304347825992882, 0.3913043478260775365 ),
 .UNSPECIFIED. ) 
 CURVE ( )  GEOMETRIC_REPRESENTATION_ITEM ( )  RATIONAL_B_SPLINE_CURVE ( ( 1.000000000000206279, 0.9510565162949473628, 1.000000000000000000, 0.9510565162951535312, 1.000000000000000000, 0.9510565162951535312, 1.000000000000000000, 0.9510565162951535312, 1.000000000000000000, 0.9510565162953660279, 0.9999999999997875033 ) ) 
 REPRESENTATION_ITEM ( '' )  );
#30865=VERTEX_POINT ( 'NONE', #37988 ) ;
#30869=CARTESIAN_POINT ( 'NONE',  ( -127.4049999999999869, -2.607480562269069768, 8.024999999999991473 ) ) ;
#30870=CARTESIAN_POINT ( 'NONE',  ( -183.9999999999999147, -5.631006485181712762, 5.770458336139917321 ) ) ;
#30873=VECTOR ( 'NONE', #31414, 1000.000000000000000 ) ;
#30874=CARTESIAN_POINT ( 'NONE',  ( -125.5429263765337993, 9.058813317711329915, 2.943386871421369566 ) ) ;
#30878=VERTEX_POINT ( 'NONE', #28038 ) ;
#30882=CARTESIAN_POINT ( 'NONE',  ( -154.7929263765341830, -3.094860106612178363, 9.525000000004535394 ) ) ;
#30883=CARTESIAN_POINT ( 'NONE',  ( -174.5049999999999955, -6.826472737025115478, -4.959722759717899443 ) ) ;
#30886=CARTESIAN_POINT ( 'NONE',  ( -47.15707362346616094, -9.058813317711329915, -2.943386871421370898 ) ) ;
#30888=VECTOR ( 'NONE', #61451, 1000.000000000000000 ) ;
#30889=CARTESIAN_POINT ( 'NONE',  ( -174.4449999999999932, 0.000000000000000000, 8.024999999999991473 ) ) ;
#30894=CARTESIAN_POINT ( 'NONE',  ( -11.94499203678653032, 11.32543297781502289, -3.971327892791007841 ) ) ;
#30895=CARTESIAN_POINT ( 'NONE',  ( -92.60500000000000398, 6.826472737025113702, -4.959722759717902107 ) ) ;
#30899=CARTESIAN_POINT ( 'NONE',  ( -85.79499999999997328, 2.607480562269069324, -8.024999999999993250 ) ) ;
#30901=CARTESIAN_POINT ( 'NONE',  ( -72.89499999999999602, 6.826472737025116366, 4.959722759717898555 ) ) ;
#30904=ADVANCED_FACE ( 'NONE', ( #16177 ), #65710, .T. ) ;
#30911=CARTESIAN_POINT ( 'NONE',  ( -107.6929263765338050, 10.01517768586948698, -1.839758294383808571E-15 ) ) ;
#30913=CARTESIAN_POINT ( 'NONE',  ( -132.7450000000000045, 4.716976649647094177, 6.492361379858945902 ) ) ;
#30924=CARTESIAN_POINT ( 'NONE',  ( -97.55707362346618083, -1.166476076187852838E-15, -9.524999999999991473 ) ) ;
#30928=CARTESIAN_POINT ( 'NONE',  ( -118.4049999999999869, -2.607480562269069768, 8.024999999999991473 ) ) ;
#30930=CARTESIAN_POINT ( 'NONE',  ( -124.5570736234661808, -1.166476076187852838E-15, -9.524999999999991473 ) ) ;
#30932=LINE ( 'NONE', #36952, #66162 ) ;
#30955=CARTESIAN_POINT ( 'NONE',  ( -60.14292637653380069, 5.598654528085800663, -7.705886871421367523 ) ) ;
#30958=CARTESIAN_POINT ( 'NONE',  ( -149.0049999999999386, 6.826472737025116366, 4.959722759717898555 ) ) ;
#30965=CARTESIAN_POINT ( 'NONE',  ( -70.19292637653380496, -10.01517768586948698, 6.132527647946031529E-16 ) ) ;
#30972=CARTESIAN_POINT ( 'NONE',  ( -69.35499999999998977, -4.716976649647093289, -6.492361379858945902 ) ) ;
#30977=CARTESIAN_POINT ( 'NONE',  ( -90.20707362346733760, 3.094860106637524755, 9.524999999986121679 ) ) ;
#30983=DIRECTION ( 'NONE',  ( -1.000000000000000000, -0.000000000000000000, -0.000000000000000000 ) ) ;
#30987=AXIS2_PLACEMENT_3D ( 'NONE', #26064, #20452, #15894 ) ;
#30989=CARTESIAN_POINT ( 'NONE',  ( -100.4949999999999761, 6.826472737025113702, -4.959722759717902107 ) ) ;
#30993=( BOUNDED_CURVE ( )  B_SPLINE_CURVE ( 2, ( #1110, #12415, #49386, #33543, #44833, #28593, #54297, #33876, #17050, #27551, #38532 ),
 .UNSPECIFIED., .F., .F. ) 
 B_SPLINE_CURVE_WITH_KNOTS ( ( 3, 2, 2, 2, 2, 3 ),
 ( 0.1086956521739105563, 0.1108695652173887630, 0.1130434782608669697, 0.1152173913043451903, 0.1173913043478233970, 0.1195652173913016036 ),
 .UNSPECIFIED. ) 
 CURVE ( )  GEOMETRIC_REPRESENTATION_ITEM ( )  RATIONAL_B_SPLINE_CURVE ( ( 1.000000000000055955, 0.9510565162950975759, 1.000000000000000000, 0.9510565162951535312, 1.000000000000000000, 0.9510565162951535312, 1.000000000000000000, 0.9510565162951535312, 1.000000000000000000, 0.9510565162952153706, 0.9999999999999381606 ) ) 
 REPRESENTATION_ITEM ( '' )  );
#30996=CARTESIAN_POINT ( 'NONE',  ( -130.4929263765338021, -8.102448949553172852, 5.886773742842742685 ) ) ;
#30998=CARTESIAN_POINT ( 'NONE',  ( -153.2949999999999875, -2.607480562269069768, 8.024999999999991473 ) ) ;
#31009=CARTESIAN_POINT ( 'NONE',  ( -143.0929263765343364, 3.094860106627105090, 9.524999999993692512 ) ) ;
#31014=CARTESIAN_POINT ( 'NONE',  ( -149.6049999999999898, 6.826472737025113702, -4.959722759717902107 ) ) ;
#31026=CARTESIAN_POINT ( 'NONE',  ( -68.90499999999998693, 2.607480562269069324, -8.024999999999993250 ) ) ;
#31030=CARTESIAN_POINT ( 'NONE',  ( -195.0000000000000000, 0.000000000000000000, 0.000000000000000000 ) ) ;
#31040=CARTESIAN_POINT ( 'NONE',  ( -182.6049999999999613, 6.826472737025113702, -4.959722759717902107 ) ) ;
#31045=ORIENTED_EDGE ( 'NONE', *, *, #965, .F. ) ;
#31047=CARTESIAN_POINT ( 'NONE',  ( -184.0000000000000000, 0.000000000000000000, 0.000000000000000000 ) ) ;
#31052=CARTESIAN_POINT ( 'NONE',  ( -96.05499999999999261, -9.827790563157499189E-16, -8.024999999999991473 ) ) ;
#31056=CARTESIAN_POINT ( 'NONE',  ( -129.2070736234661581, 3.094860106618433360, 9.524999999999991473 ) ) ;
#31058=CARTESIAN_POINT ( 'NONE',  ( -72.80707362346615241, 10.01517768586948698, -1.839758294383808571E-15 ) ) ;
#31059=VERTEX_POINT ( 'NONE', #57756 ) ;
#31062=CARTESIAN_POINT ( 'NONE',  ( -195.0000000000000000, 1.166476076187852838E-15, -9.524999999999991473 ) ) ;
#31063=CARTESIAN_POINT ( 'NONE',  ( -99.89292637653379359, -8.102448949553174629, -5.886773742842741797 ) ) ;
#31065=CARTESIAN_POINT ( 'NONE',  ( -112.7049999999999699, 2.607480562269073321, 8.024999999999991473 ) ) ;
#31068=CARTESIAN_POINT ( 'NONE',  ( -129.2949999999999875, -2.607480562269069768, 8.024999999999991473 ) ) ;
#31074=CARTESIAN_POINT ( 'NONE',  ( -166.1929263765337907, -10.01517768586948698, 6.132527647946031529E-16 ) ) ;
#31083=CARTESIAN_POINT ( 'NONE',  ( -86.39292637653380780, 8.102448949553176405, 5.886773742842740909 ) ) ;
#31086=CARTESIAN_POINT ( 'NONE',  ( -165.7429263765338305, -5.598654528085803328, -7.705886871421366635 ) ) ;
#31090=CARTESIAN_POINT ( 'NONE',  ( -176.0049999999999670, 6.826472737025115478, 4.959722759717899443 ) ) ;
#31091=VERTEX_POINT ( 'NONE', #63012 ) ;
#31095=CARTESIAN_POINT ( 'NONE',  ( -111.4429263765338050, -1.166476076187852838E-15, -9.524999999999991473 ) ) ;
#31100=CARTESIAN_POINT ( 'NONE',  ( -100.7070736234671955, -3.094860106635371810, -9.524999999987684873 ) ) ;
#31101=CARTESIAN_POINT ( 'NONE',  ( -98.45499999999998408, 7.632228543268599452, -2.479861379858951942 ) ) ;
#31109=CARTESIAN_POINT ( 'NONE',  ( -71.99500000000000455, -6.826472737025115478, 4.959722759717900331 ) ) ;
#31114=ORIENTED_EDGE ( 'NONE', *, *, #10323, .T. ) ;
#31116=DIRECTION ( 'NONE',  ( -1.000000000000000000, -0.000000000000000000, -0.000000000000000000 ) ) ;
#31123=ADVANCED_FACE ( 'NONE', ( #19758 ), #35951, .T. ) ;
#31128=CARTESIAN_POINT ( 'NONE',  ( -158.6070736234661922, -8.102448949553172852, 5.886773742842742685 ) ) ;
#31131=CARTESIAN_POINT ( 'NONE',  ( -100.2570736234661695, 5.598654528085800663, -7.705886871421367523 ) ) ;
#31135=CARTESIAN_POINT ( 'NONE',  ( -108.4429263765338050, -1.166476076187852838E-15, -9.524999999999991473 ) ) ;
#31137=CARTESIAN_POINT ( 'NONE',  ( -114.5070736234661837, 8.102448949553176405, 5.886773742842740909 ) ) ;
#31140=CARTESIAN_POINT ( 'NONE',  ( -140.3049999999999500, 8.437984349512085203, -1.550032578732815448E-15 ) ) ;
#31143=CARTESIAN_POINT ( 'NONE',  ( -153.7450000000000045, 4.716976649647094177, 6.492361379858945902 ) ) ;
#31144=CARTESIAN_POINT ( 'NONE',  ( -148.7950000000000159, 2.607480562269069324, -8.024999999999993250 ) ) ;
#31151=CARTESIAN_POINT ( 'NONE',  ( -61.55499999999998550, 0.000000000000000000, 8.024999999999991473 ) ) ;
#31159=CARTESIAN_POINT ( 'NONE',  ( -82.25707362346616947, 5.598654528085800663, -7.705886871421367523 ) ) ;
#31165=VERTEX_POINT ( 'NONE', #17097 ) ;
#31166=VERTEX_POINT ( 'NONE', #33248 ) ;
#31178=CARTESIAN_POINT ( 'NONE',  ( -101.2429263765338021, 5.598654528085804216, 7.705886871421366635 ) ) ;
#31184=CARTESIAN_POINT ( 'NONE',  ( -104.6949999999999790, -8.437984349512085203, 5.166775262442717831E-16 ) ) ;
#31197=ORIENTED_EDGE ( 'NONE', *, *, #19924, .F. ) ;
#31206=ADVANCED_FACE ( 'NONE', ( #60316 ), #30274, .T. ) ;
#31215=CARTESIAN_POINT ( 'NONE',  ( -182.2429263765338021, 5.598654528085804216, 7.705886871421366635 ) ) ;
#31218=CARTESIAN_POINT ( 'NONE',  ( -181.4050000000000011, -2.607480562269069768, 8.024999999999991473 ) ) ;
#31221=CARTESIAN_POINT ( 'NONE',  ( -178.9449999999999932, -9.827790563157499189E-16, -8.024999999999991473 ) ) ;
#31223=CARTESIAN_POINT ( 'NONE',  ( -180.7449999999999761, 4.716976649647094177, 6.492361379858945902 ) ) ;
#31225=CARTESIAN_POINT ( 'NONE',  ( -195.0000000000000000, 1.166476076187852838E-15, -9.524999999999991473 ) ) ;
#31228=CARTESIAN_POINT ( 'NONE',  ( -94.85499999999998977, 4.716976649647094177, 6.492361379858945902 ) ) ;
#31232=CARTESIAN_POINT ( 'NONE',  ( -90.14499999999999602, -4.716976649647092401, 6.492361379858946790 ) ) ;
#31234=CARTESIAN_POINT ( 'NONE',  ( -61.04499999999998749, 7.632228543268600340, 2.479861379858949277 ) ) ;
#31240=CARTESIAN_POINT ( 'NONE',  ( -74.69292637653377653, 10.01517768586948698, -1.839758294383808966E-15 ) ) ;
#31249=CARTESIAN_POINT ( 'NONE',  ( -175.2570736234661695, 5.598654528085800663, -7.705886871421367523 ) ) ;
#31254=FACE_OUTER_BOUND ( 'NONE', #4170, .T. ) ;
#31258=CARTESIAN_POINT ( 'NONE',  ( -119.3049999999999926, 8.437984349512086979, -1.550032578732815448E-15 ) ) ;
#31265=ORIENTED_EDGE ( 'NONE', *, *, #31787, .T. ) ;
#31272=ORIENTED_EDGE ( 'NONE', *, *, #965, .T. ) ;
#31273=CARTESIAN_POINT ( 'NONE',  ( -55.55707362346618083, -1.166476076187852838E-15, -9.524999999999991473 ) ) ;
#31288=EDGE_CURVE ( 'NONE', #65490, #9180, #52488, .T. ) ;
#31290=CARTESIAN_POINT ( 'NONE',  ( -54.74292637653380211, -5.598654528085803328, -7.705886871421366635 ) ) ;
#31293=CARTESIAN_POINT ( 'NONE',  ( -156.6550000000000011, -7.632228543268600340, -2.479861379858950166 ) ) ;
#31300=CARTESIAN_POINT ( 'NONE',  ( -70.49292637653378790, -8.102448949553174629, 5.886773742842742685 ) ) ;
#31304=FACE_OUTER_BOUND ( 'NONE', #38682, .T. ) ;
#31307=CARTESIAN_POINT ( 'NONE',  ( -63.50499999999998124, -6.826472737025115478, -4.959722759717899443 ) ) ;
#31320=CARTESIAN_POINT ( 'NONE',  ( -114.8949999999999818, 6.826472737025115478, 4.959722759717899443 ) ) ;
#31323=CARTESIAN_POINT ( 'NONE',  ( -93.29499999999998749, -2.607480562269069768, 8.024999999999991473 ) ) ;
#31330=CARTESIAN_POINT ( 'NONE',  ( -136.7929263765338135, -3.094860106618429807, 9.524999999999991473 ) ) ;
#31332=CARTESIAN_POINT ( 'NONE',  ( -153.5949999999999989, 2.607480562269073321, 8.024999999999991473 ) ) ;
#31347=CARTESIAN_POINT ( 'NONE',  ( -152.1549999999999727, 7.632228543268600340, 2.479861379858949277 ) ) ;
#31363=CARTESIAN_POINT ( 'NONE',  ( -63.05499999999998550, -9.827790563157499189E-16, -8.024999999999991473 ) ) ;
#31374=CARTESIAN_POINT ( 'NONE',  ( -182.1549999999999727, 7.632228543268600340, 2.479861379858949277 ) ) ;
#31386=CARTESIAN_POINT ( 'NONE',  ( -93.95499999999998408, -7.632228543268599452, 2.479861379858951054 ) ) ;
#31390=CARTESIAN_POINT ( 'NONE',  ( -131.7570736234661695, -5.598654528085801552, 7.705886871421367523 ) ) ;
#31396=CARTESIAN_POINT ( 'NONE',  ( -75.50707362346616947, 8.102448949553176405, 5.886773742842740909 ) ) ;
#31399=CARTESIAN_POINT ( 'NONE',  ( -18.05120619030912721, -11.32434288914918596, 3.974503633080903597 ) ) ;
#31402=CARTESIAN_POINT ( 'NONE',  ( -114.0549999999999926, -9.827790563157499189E-16, -8.024999999999991473 ) ) ;
#31405=CARTESIAN_POINT ( 'NONE',  ( -127.0449999999999875, 7.632228543268600340, 2.479861379858949277 ) ) ;
#31412=CARTESIAN_POINT ( 'NONE',  ( -164.6929263765338476, 10.01517768586948698, -1.839758294383808571E-15 ) ) ;
#31414=DIRECTION ( 'NONE',  ( -1.000000000000000000, -0.000000000000000000, -0.000000000000000000 ) ) ;
#31419=CARTESIAN_POINT ( 'NONE',  ( -76.64292637653380780, -5.598654528085801552, 7.705886871421367523 ) ) ;
#31428=CARTESIAN_POINT ( 'NONE',  ( -175.2549999999999955, -4.716976649647092401, 6.492361379858946790 ) ) ;
#31433=CARTESIAN_POINT ( 'NONE',  ( -73.70707362346617231, -3.094860106618431139, -9.524999999999991473 ) ) ;
#31435=CARTESIAN_POINT ( 'NONE',  ( -109.9429263765338050, 0.000000000000000000, 9.524999999999991473 ) ) ;
#31443=CARTESIAN_POINT ( 'NONE',  ( -91.70499999999998408, 2.607480562269072433, 8.024999999999991473 ) ) ;
#31456=CARTESIAN_POINT ( 'NONE',  ( -71.69499999999999318, -8.437984349512085203, 5.166775262442717831E-16 ) ) ;
#31460=CARTESIAN_POINT ( 'NONE',  ( -124.5570736234661808, -1.166476076187852838E-15, -9.524999999999991473 ) ) ;
#31473=CARTESIAN_POINT ( 'NONE',  ( -149.5429263765338135, 9.058813317711329915, 2.943386871421369566 ) ) ;
#31476=CARTESIAN_POINT ( 'NONE',  ( -157.2570736234661979, 5.598654528085800663, -7.705886871421367523 ) ) ;
#31480=CARTESIAN_POINT ( 'NONE',  ( -99.50707362346614104, 8.102448949553176405, 5.886773742842740909 ) ) ;
#31487=CARTESIAN_POINT ( 'NONE',  ( -137.1550000000000011, 7.632228543268600340, 2.479861379858949277 ) ) ;
#31490=CARTESIAN_POINT ( 'NONE',  ( -158.2450000000000045, -4.716976649647093289, -6.492361379858945902 ) ) ;
#31491=CARTESIAN_POINT ( 'NONE',  ( -135.5949999999999989, 2.607480562269072433, 8.024999999999991473 ) ) ;
#31496=AXIS2_PLACEMENT_3D ( 'NONE', #7718, #50642, #23901 ) ;
#31498=CARTESIAN_POINT ( 'NONE',  ( -49.70499999999996987, 2.607480562269073321, 8.024999999999991473 ) ) ;
#31500=CARTESIAN_POINT ( 'NONE',  ( -52.19292637653380496, -10.01517768586948698, 6.132527647946031529E-16 ) ) ;
#31505=CARTESIAN_POINT ( 'NONE',  ( -154.8570736234661922, -5.598654528085803328, -7.705886871421366635 ) ) ;
#31511=CARTESIAN_POINT ( 'NONE',  ( -81.35707362346616378, 5.598654528085804216, 7.705886871421366635 ) ) ;
#31526=PRODUCT_DEFINITION_FORMATION_WITH_SPECIFIED_SOURCE ( 'ANY', '', #9133, .NOT_KNOWN. ) ;
#31542=CARTESIAN_POINT ( 'NONE',  ( -103.9449999999999932, -9.827790563157499189E-16, -8.024999999999991473 ) ) ;
#31543=ORIENTED_EDGE ( 'NONE', *, *, #69300, .T. ) ;
#31554=CARTESIAN_POINT ( 'NONE',  ( -63.05707362346617373, 0.000000000000000000, 9.524999999999991473 ) ) ;
#31568=ORIENTED_EDGE ( 'NONE', *, *, #1701, .T. ) ;
#31570=DIRECTION ( 'NONE',  ( -1.000000000000000000, -0.000000000000000000, -0.000000000000000000 ) ) ;
#31573=CARTESIAN_POINT ( 'NONE',  ( -173.0049999999999670, 6.826472737025116366, 4.959722759717898555 ) ) ;
#31577=CARTESIAN_POINT ( 'NONE',  ( -180.8949999999999534, 6.826472737025116366, 4.959722759717898555 ) ) ;
#31578=CARTESIAN_POINT ( 'NONE',  ( -163.1949999999999932, 8.437984349512086979, -1.550032578732815448E-15 ) ) ;
#31583=CARTESIAN_POINT ( 'NONE',  ( -9.999952640014225125, 12.00001973332723004, 0.3289108581718978574 ) ) ;
#31584=CARTESIAN_POINT ( 'NONE',  ( -81.95499999999998408, -7.632228543268599452, 2.479861379858951054 ) ) ;
#31586=( GEOMETRIC_REPRESENTATION_CONTEXT ( 3 ) GLOBAL_UNCERTAINTY_ASSIGNED_CONTEXT ( ( #13599 ) ) GLOBAL_UNIT_ASSIGNED_CONTEXT ( ( #10340, #63783, #37106 ) ) REPRESENTATION_CONTEXT ( 'NONE', 'WORKASPACE' ) );
#31590=CARTESIAN_POINT ( 'NONE',  ( -90.74499999999999034, 4.716976649647094177, 6.492361379858945902 ) ) ;
#31602=PRODUCT_DEFINITION_SHAPE ( 'NONE', 'NONE',  #45995 ) ;
#31605=AXIS2_PLACEMENT_3D ( 'NONE', #15616, #26480, #37090 ) ;
#31608=EDGE_CURVE ( 'NONE', #23846, #42940, #68214, .T. ) ;
#31609=CARTESIAN_POINT ( 'NONE',  ( -131.6929263765337907, 10.01517768586948698, -1.839758294383808966E-15 ) ) ;
#31615=CARTESIAN_POINT ( 'NONE',  ( -175.5570736234661808, -1.166476076187852838E-15, -9.524999999999991473 ) ) ;
#31619=CARTESIAN_POINT ( 'NONE',  ( -195.0000000000000000, 0.000000000000000000, 0.000000000000000000 ) ) ;
#31622=CARTESIAN_POINT ( 'NONE',  ( -122.0049999999999812, 6.826472737025115478, 4.959722759717899443 ) ) ;
#31625=CARTESIAN_POINT ( 'NONE',  ( -195.0000000000000000, 1.166476076187852838E-15, -9.524999999999991473 ) ) ;
#31635=LINE ( 'NONE', #30582, #17312 ) ;
#31637=CARTESIAN_POINT ( 'NONE',  ( -135.8070736234661808, 10.01517768586948698, -1.839758294383808966E-15 ) ) ;
#31644=CARTESIAN_POINT ( 'NONE',  ( -98.84292637653379643, 9.058813317711329915, -2.943386871421373119 ) ) ;
#31649=CARTESIAN_POINT ( 'NONE',  ( -53.99292637653379501, 8.102448949553171076, -5.886773742842744461 ) ) ;
#31653=CARTESIAN_POINT ( 'NONE',  ( -152.7549999999999955, 4.716976649647091513, -6.492361379858946790 ) ) ;
#31654=CARTESIAN_POINT ( 'NONE',  ( -72.05707362346616662, 0.000000000000000000, 9.524999999999991473 ) ) ;
#31667=CARTESIAN_POINT ( 'NONE',  ( -66.20499999999996987, -2.607480562269071545, -8.024999999999991473 ) ) ;
#31683=CARTESIAN_POINT ( 'NONE',  ( -117.8949999999999676, 6.826472737025115478, 4.959722759717899443 ) ) ;
#31685=CARTESIAN_POINT ( 'NONE',  ( -84.14499999999998181, -4.716976649647092401, 6.492361379858946790 ) ) ;
#31692=CARTESIAN_POINT ( 'NONE',  ( -131.0929263765337964, 3.094860106618433360, 9.524999999999991473 ) ) ;
#31694=CARTESIAN_POINT ( 'NONE',  ( -153.1450000000000102, -4.716976649647092401, 6.492361379858946790 ) ) ;
#31709=CARTESIAN_POINT ( 'NONE',  ( -151.5550000000000068, 0.000000000000000000, 8.024999999999991473 ) ) ;
#31713=ORIENTED_EDGE ( 'NONE', *, *, #32247, .F. ) ;
#31721=CARTESIAN_POINT ( 'NONE',  ( -64.25499999999998124, -4.716976649647092401, 6.492361379858946790 ) ) ;
#31732=CARTESIAN_POINT ( 'NONE',  ( -180.9550000000000125, -7.632228543268599452, 2.479861379858951054 ) ) ;
#31741=CARTESIAN_POINT ( 'NONE',  ( -91.25499999999999545, -4.716976649647092401, 6.492361379858946790 ) ) ;
#31745=CARTESIAN_POINT ( 'NONE',  ( -129.9570736234661865, 9.058813317711329915, -2.943386871421373119 ) ) ;
#31748=CARTESIAN_POINT ( 'NONE',  ( -61.25707362346617657, 5.598654528085800663, -7.705886871421367523 ) ) ;
#31757=CARTESIAN_POINT ( 'NONE',  ( -109.1050000000000040, -6.826472737025115478, 4.959722759717900331 ) ) ;
#31762=CARTESIAN_POINT ( 'NONE',  ( -116.2449999999999903, -4.716976649647093289, -6.492361379858945902 ) ) ;
#31767=CARTESIAN_POINT ( 'NONE',  ( -117.7429263765338021, -5.598654528085803328, -7.705886871421366635 ) ) ;
#31769=ORIENTED_EDGE ( 'NONE', *, *, #33550, .F. ) ;
#31770=CARTESIAN_POINT ( 'NONE',  ( -159.8929263765337794, -8.102448949553172852, -5.886773742842741797 ) ) ;
#31782=CARTESIAN_POINT ( 'NONE',  ( -74.84292637653381064, 9.058813317711329915, -2.943386871421373119 ) ) ;
#31785=CARTESIAN_POINT ( 'NONE',  ( -166.1929263765337907, -10.01517768586948698, 6.132527647946031529E-16 ) ) ;
#31787=EDGE_CURVE ( 'NONE', #33115, #42499, #42626, .T. ) ;
#31791=CARTESIAN_POINT ( 'NONE',  ( -179.1550000000000011, 7.632228543268600340, 2.479861379858949277 ) ) ;
#31796=CARTESIAN_POINT ( 'NONE',  ( -182.6070736234661638, -8.102448949553174629, 5.886773742842742685 ) ) ;
#31801=CARTESIAN_POINT ( 'NONE',  ( -97.25499999999999545, -4.716976649647092401, 6.492361379858946790 ) ) ;
#31810=CARTESIAN_POINT ( 'NONE',  ( -71.84499999999999886, -7.632228543268599452, 2.479861379858951054 ) ) ;
#31813=CARTESIAN_POINT ( 'NONE',  ( -121.2570736234661695, 5.598654528085800663, -7.705886871421367523 ) ) ;
#31814=CIRCLE ( 'NONE', #5958, 9.525000000000000355 ) ;
#31826=CARTESIAN_POINT ( 'NONE',  ( -156.0570736234661808, 0.000000000000000000, 9.524999999999991473 ) ) ;
#31828=CARTESIAN_POINT ( 'NONE',  ( -92.90707362346614673, -3.094860106618429807, 9.524999999999991473 ) ) ;
#31835=DIRECTION ( 'NONE',  ( 0.000000000000000000, 0.000000000000000000, 1.000000000000000000 ) ) ;
#31839=CARTESIAN_POINT ( 'NONE',  ( -139.5549999999999784, 0.000000000000000000, 8.024999999999991473 ) ) ;
#31842=CARTESIAN_POINT ( 'NONE',  ( -154.9449999999999932, -9.827790563157499189E-16, -8.024999999999991473 ) ) ;
#31845=CARTESIAN_POINT ( 'NONE',  ( -143.2449999999999761, -4.716976649647093289, -6.492361379858945902 ) ) ;
#31847=CARTESIAN_POINT ( 'NONE',  ( -180.9570736234661865, 9.058813317711329915, -2.943386871421373119 ) ) ;
#31852=CARTESIAN_POINT ( 'NONE',  ( -58.70499999999997698, 2.607480562269073321, 8.024999999999991473 ) ) ;
#31877=CARTESIAN_POINT ( 'NONE',  ( -46.64499999999998892, 4.716976649647091513, -6.492361379858946790 ) ) ;
#31888=CARTESIAN_POINT ( 'NONE',  ( -85.34292637653381064, -9.058813317711329915, 2.943386871421371787 ) ) ;
#31892=CARTESIAN_POINT ( 'NONE',  ( -100.0450000000000017, 7.632228543268600340, 2.479861379858949277 ) ) ;
#31909=( BOUNDED_SURFACE ( )  B_SPLINE_SURFACE ( 1, 2, ( 
 ( #38630, #49160, #60032, #34345, #11844, #18161, #22757, #44254, #33314, #60708, #55794, #17502, #12521, #55450, #61401, #65658, #55083, #50533, #29032, #38975, #17826, #66342, #857, #28340, #33988, #7272, #40008, #60372, #13216, #50188, #27989, #28698, #56128, #12172, #22400, #33644, #7953, #7602, #49843, #23108, #34673, #1913, #1582, #23427, #65999, #65313, #44938, #54735, #39646, #61065, #12880, #17158, #2254, #23781, #45286, #66704, #18520, #6541, #35396, #13564, #41042, #14631, #67389, #62456, #35738, #41737, #51223, #56847, #30787, #9361, #29761, #67745, #46691, #29397, #8658, #19544, #14275, #20235, #45962, #63162, #30419, #8320, #57172, #36474, #24458, #2632, #2969, #57896, #36093, #19180, #3319, #14998, #9007, #40686, #51922, #62100, #50873, #3678, #35034, #25175, #19884, #24805, #24129, #57535, #52286, #30088, #68108, #4044, #41384, #51560, #45637, #46325, #62790, #13928, #25511, #47024, #68439, #67056, #18839, #40328, #61738, #56485, #9717, #27219, #43142, #21625, #48759, #52626, #11062, #42110, #58928, #26867, #63505, #26205, #64877, #48405, #5422, #95, #64552, #53316, #15357, #16393, #69141, #16730, #59238, #37868, #38194, #10738, #32186, #25858, #32508, #36811, #37162, #58570, #5773, #63834, #53637, #461, #10402, #58228, #21991, #20594, #47368, #31128, #53972, #5100, #10050, #43494, #4378, #26548, #68803, #69472, #31476, #52961, #64186, #4750, #47747, #20947, #42444, #15679, #31826, #48068, #21261, #42797, #16043, #37521, #54670, #7193, #65576, #2173, #54999, #28619, #49418, #1845, #1498, #17426, #44177, #59596, #32887, #50118, #38892, #11414, #7527, #23355, #44857, #28954, #54323, #60980, #22323, #39227, #66261, #43819, #6471, #45204, #18088, #55369, #39574, #12799, #33567, #65228, #34265, #1140, #66625, #55721, #50444, #18443, #60627, #12441, #6147, #23704, #17076, #60299, #12100, #27577, #6827, #33903, #49095, #28250, #38555, #780, #59948, #11766, #33231, #27906, #49762, #22675, #23027, #44523, #65926, #17756, #30016, #18774, #61331, #24725, #40965, #3967, #50794, #62705, #29315, #39928, #2544, #25097, #24053, #8919, #40252, #34956, #45561, #51479, #46610, #8237, #3237, #46243, #52204, #61654, #45881, #41303, #19816, #13484, #8582, #57097, #13141, #19101, #67663, #19462, #30697, #56402, #25439, #62383, #29680, #14202, #46950, #51149, #34596, #2897, #68361, #68029, #24385, #13848, #56051, #35659, #67311, #30340, #40605, #7866, #51845, #66981, #3592, #14532, #35312, #62019, #36011, #57455, #56769, #9278, #42709, #42373, #21551, #20514, #63072, #68718, #43062, #64108, #42022, #26122, #48322, #58493, #63430, #63757, #15275, #17, #20870, #52549, #5021, #48000, #47658, #20144, #15963, #37443, #4670, #37081, #58841, #69400, #31390, #41654, #15609, #10656, #9973, #32112, #10320, #69064, #52887, #14912, #57812, #53564, #31745, #36395, #9638, #5350, #26792, #31056, #47289, #4294, #36742, #25776, #58158, #53233, #26474, #21190, #52075, #9157, #3830, #46836, #56980, #45767, #25314, #3104, #68585, #62933, #68241, #41883, #62590, #35875, #29549, #20023, #67185, #40834, #62253, #9512, #67534, #14404, #30930, #14079, #40481, #25646, #24271, #51020, #34821, #41520, #8794, #18975, #14779, #47166, #30221, #52428, #3465, #61900, #56276, #67899, #57321, #20382, #13721, #36258, #2781, #13362, #35179, #57682, #56640, #4173, #8466, #29903, #51361, #24962, #8104, #24598, #46472, #19691, #46114, #19335, #35542, #51713, #41189, #30574, #40691, #61067, #2972, #18523, #56488, #67392, #50191, #1917, #50876, #23785, #23432, #55797, #61404, #61742, #24133, #12885, #19184, #2258, #45640, #66345, #18841, #40011, #34348, #7604, #6915, #49847, #67059, #29036, #28343, #24461, #40332, #13569, #45966, #1586, #8323, #39308, #56132, #35037, #60712, #44941, #62104, #29765, #2635, #51226, #13931, #50536, #12526, #35400, #18165, #23111, #44606, #66003, #17829, #7957, #29401, #33991, #55453, #7276, #45289, #66706, #28701, #13219, #39650, #34678, #14634, #14277, #69144, #67749, #24810, #8661, #20596, #30789, #19548, #42112, #20949, #52289, #52964, #47027, #35741, #30090, #41740, #57899, #42446, #41046, #10055, #46329, #56850, #62460, #63508, #57176, #25861, #9009, #51925, #30423, #68442, #15359, #25178, #20238, #63165, #63837, #3680, #62793, #58231, #52628, #46694, #9364, #68110, #51564, #36096, #25513, #15002, #47749, #19888, #15683, #9720, #41386, #36476, #3323, #57538, #4047, #31131, #4383, #36814, #47370, #68805, #31480, #4752, #26207, #464, #5424, #22677, #5777, #42801, #32892, #27581, #11064, #1143, #22326, #43823, #6149, #54327, #32188, #59241, #11770, #32511, #54673, #33234, #69474, #38197, #17079, #16732, #26550, #37523, #65579, #37870, #10741, #43496, #53975, #37165, #65230, #44180, #782, #64554, #38558, #53639, #58574, #43145, #27223, #48761, #31828, #58930, #21994, #99, #49097, #26871, #27908, #59599, #10405, #64880, #53318, #6474, #48409, #59953, #21629, #16396, #11417, #5103, #49420, #48071, #21265, #64189, #16046, #13488, #40255, #17759, #60983, #18777, #2901, #50799, #65930, #18446, #66629, #8242, #28624, #23709, #33570, #44527, #1848, #44860, #56406, #38896, #23031, #29684, #66985, #39931, #49765, #66266, #51153, #23359, #34960, #28957, #61657, #24388, #60630, #12445, #61335, #34269, #33907, #55374, #45885, #17430, #50448, #13144, #2548, #55003, #60301, #2177, #45208, #12104, #55725, #7196, #39578, #39231, #50121, #6831, #24057, #28254, #1503, #18092, #29319, #12802, #7530, #34599, #56054, #7870, #45564, #51848, #9281, #14204, #19466, #67314, #19103, #56773, #41306, #68363, #30344, #35662, #62388, #40609, #40969, #4673, #52552, #57100, #62707, #9976, #25442, #8921, #30699, #3595, #52890, #36014, #3240, #63076, #57814, #14537, #31396, #4298, #25781, #46612, #52207, #47293, #14915, #25100, #26126, #57458, #36399, #68033, #9641, #3971, #19819, #46954, #62023, #13852, #31058, #20148, #35317, #15279, #68721, #20518, #36745, #8586, #42026, #30019, #41658, #63432, #51483, #58160, #24728, #46246, #67666, #21192, #53896, #43067, #6401, #32803, #54596, #11337, #5352, #27500, #64112, #47662, #53567, #48327, #21553, #42375, #69403, #37793, #10659, #43422, #48002, #38480, #48681, #69067, #64470, #11689, #65145, #58846, #38122, #42714, #26794, #27149, #33159, #19, #20873, #15966, #59516, #43743, #16990, #715, #37447, #16314, #49025, #63761, #54244, #26477, #383, #21910, #59874, #32114, #5698, #15612, #5024, #59167, #10994, #37086, #58497, #53236, #10322, #22245, #64808, #31748, #32433, #16652, #6063, #24912, #40432, #8752, #19647, #2363, #23883, #3064, #45732, #45392, #66815, #8055, #13674, #14032, #46069, #34776, #41143, #24227, #67486, #18625, #40789, #61847, #56230, #13316, #27831, #1056, #19283, #29507, #49334, #46429, #62207, #35492, #67852, #22599, #30179, #60229, #8418, #56939, #12032, #67145, #17352, #35136, #62546, #51666, #3419, #2734, #33489, #14363, #40103, #35832, #57278, #44102, #65500, #29853, #51319, #38814, #54918, #6745, #50972, #18934, #29135, #56589, #24555, #50626, #61493, #36209, #21367, #19975, #46793, #30525, #42533, #52715, #41474, #63931, #42893, #4483, #5189, #68899, #57637, #52027, #63600, #10144, #64286, #62889, #31931, #68197, #9110, #14735, #15780, #9459, #47841, #30886, #4134, #52384, #20699, #37263, #47117, #42210 ),
 ( #25601, #25951, #16138, #36908, #68540, #15445, #20339, #37616, #47476, #41842, #4852, #69238, #58321, #3783, #58663, #10493, #63258, #31577, #15106, #53059, #26632, #21034, #53409, #26299, #36579, #48155, #57998, #25270, #69564, #9811, #31221, #38647, #11862, #5515, #28004, #21727, #16822, #38294, #55103, #43578, #60048, #6930, #59694, #16494, #1599, #202, #26967, #10831, #22773, #32983, #43241, #44272, #23127, #54418, #28354, #49175, #37958, #32274, #43918, #33327, #44617, #64646, #12188, #48503, #59018, #59332, #65671, #11161, #49515, #32606, #54072, #5877, #875, #17517, #27321, #22415, #65329, #66014, #48853, #64969, #60383, #54748, #550, #11512, #22078, #53723, #6238, #27666, #17173, #49861, #6558, #17841, #1243, #38992, #33660, #46342, #34362, #12542, #12897, #67761, #24474, #55811, #13231, #51577, #67071, #7615, #2648, #29050, #24825, #7971, #44951, #35052, #29778, #34689, #3334, #45977, #67403, #18538, #24144, #19198, #56499, #45301, #39320, #56143, #8333, #50548, #51239, #50887, #66722, #23801, #60723, #34005, #2984, #40025, #55465, #56862, #40706, #62117, #8677, #7289, #13944, #1926, #18849, #35412, #61414, #29417, #45652, #28716, #61083, #40344, #2271, #30103, #39662, #50206, #61754, #23445, #13583, #66358, #18179, #30802, #10065, #62806, #68453, #68817, #53331, #20252, #26560, #14648, #31490, #15694, #37177, #42456, #19901, #63177, #20963, #5112, #52973, #68120, #20609, #42122, #10416, #52303, #25870, #35754, #46707, #4059, #47037, #58586, #41055, #25189, #31842, #69155, #63514, #51940, #41756, #48082, #25525, #19561, #31143, #63850, #62471, #36113, #57550, #15372, #36488, #9377, #15012, #14289, #57190, #52638, #36827, #4769, #9020, #30438, #4395, #47388, #3694, #57911, #9737, #58242, #41400, #26219, #47760, #33245, #42814, #33581, #17442, #11783, #48422, #12118, #37538, #22691, #64202, #59967, #53989, #11430, #16412, #21643, #69484, #21281, #58943, #43507, #797, #32525, #37885, #38569, #65241, #64565, #22004, #44192, #64893, #38907, #65590, #32202, #22339, #49433, #43158, #6846, #10755, #16742, #474, #59253, #6158, #38208, #28270, #54682, #16058, #6482, #27238, #1154, #11076, #53649, #59611, #5436, #5791, #27921, #60312, #55018, #26883, #112, #32907, #48772, #54340, #27590, #49111, #43834, #17093, #40618, #60997, #56068, #65942, #7208, #34279, #7542, #19112, #1516, #55387, #62034, #29695, #50810, #12457, #28971, #13862, #55737, #45895, #61343, #51164, #35328, #23371, #44870, #24069, #66643, #66278, #18102, #24401, #67323, #13153, #45573, #34970, #17771, #2909, #34608, #7883, #56782, #18458, #39592, #2189, #28637, #12815, #8597, #13496, #23042, #49777, #44538, #61666, #50130, #39241, #60640, #33920, #1859, #40264, #50461, #29331, #23719, #45218, #39941, #2561, #66993, #18786, #56419, #8253, #46625, #68733, #25792, #25109, #52219, #4684, #3980, #47674, #26137, #62398, #31068, #9986, #51859, #37097, #40980, #46965, #30712, #3606, #36411, #25451, #58507, #15290, #30031, #63443, #57467, #31405, #68043, #51492, #36025, #68372, #20163, #24739, #19829, #41669, #62722, #47307, #30354, #20880, #52564, #3251, #63087, #63774, #69078, #41319, #20530, #14551, #9293, #9653, #15622, #14927, #57825, #4309, #46255, #67678, #42038, #36754, #19476, #42384, #58170, #52899, #14215, #35678, #57110, #8934, #59525, #27508, #64123, #48689, #69413, #21923, #6410, #724, #43752, #53903, #42725, #22256, #29, #65508, #59883, #65153, #38825, #11345, #32814, #26486, #49035, #15975, #37802, #59177, #27842, #64482, #54254, #49344, #11004, #37458, #22608, #21202, #48011, #31762, #16998, #5709, #58861, #38490, #44111, #27158, #1064, #394, #10668, #53250, #64818, #6074, #17359, #32122, #33170, #53575, #10331, #5362, #11700, #26803, #54605, #48337, #21564, #43077, #43434, #5036, #16326, #16665, #38130, #32442, #12371, #66190, #61588, #55990, #49695, #12729, #1429, #60238, #39504, #28893, #45137, #51080, #7118, #24326, #61268, #39162, #50378, #67242, #55296, #33497, #33834, #19028, #45496, #28547, #34201, #2833, #18378, #50049, #23629, #1785, #45818, #2106, #65864, #7797, #50726, #55652, #12037, #66912, #18714, #60912, #66555, #40187, #29244, #18013, #54929, #7468, #2471, #23295, #23982, #34882, #39864, #13418, #56329, #28184, #8165, #13078, #34531, #6754, #29606, #44792, #22958, #17694, #44460, #60553, #4225, #13780, #4596, #58096, #52487, #19395, #52821, #8518, #63353, #35238, #30989, #25025, #52137, #57034, #62314, #40540, #61954, #29953, #14462, #41577, #3519, #8853, #9571, #36316, #35596, #62640, #15208, #35941, #9907, #36675, #3162, #62998, #20445, #14136, #47589, #51418, #57386, #41241, #30273, #46890, #9211, #68996, #25701, #56698, #47222, #67960, #41947, #51771, #24653, #46535, #30629, #3892, #46170, #19745, #25368, #68291, #57740, #40892, #31323, #14839, #67597, #20077, #26055, #68640, #32038, #11264, #64038, #69664, #302, #54520, #21478, #27761, #15882, #32719, #16919, #38402, #43672, #21129, #64392, #22177, #6331, #54174, #69335, #21836, #43348, #11616, #53499, #27074, #37014, #47934, #5282, #48249, #59805, #42309, #26403, #33083, #649, #64744, #53161, #42988, #49265, #26727, #20802, #32362, #65065, #63697, #37366, #58772, #16586, #37718, #10589, #16240, #15541, #38041, #59108, #10927, #58422, #53823, #10248, #31685, #4955, #59433, #42633, #5622, #48609, #5984, #27423, #48951, #44375, #7387, #66104, #29522, #55912, #8070, #34453, #28455, #50639, #17617, #974, #7028, #1703, #44714, #65432, #22875, #60824, #33755, #66464, #1345, #61506, #2019, #22524, #17933, #34793, #18638, #12284, #61188, #65780, #49966, #50300, #56245, #23221, #44022, #39082, #12997, #66830, #40118, #23897, #60476, #39423, #2378, #17281, #7714, #49611, #23544, #45054, #13334, #55205, #28819, #38745, #28106, #12644, #34108, #60152, #11962, #6666, #33418, #45410, #18288, #54847, #55566, #39773, #29153, #47128, #62560, #30901, #41853, #24570, #46083, #25285, #67869, #67502, #19302, #25615, #68554, #14377, #46807, #36224, #18947, #4146, #35848, #57292, #15119, #19662, #40807, #3429, #8436, #14048, #52399, #14749, #24243, #36596, #20351, #62905, #29869, #63274, #40450, #58014, #45745, #41489, #35508, #9124, #62222, #3079, #50986, #2751, #61866, #24932, #52044, #56953, #8769, #19988, #30190, #30542, #51683, #46444, #67161, #13692, #35151, #41158, #3799, #68213, #57651, #9478, #9825, #56606, #51335, #6857, #6168, #49787, #28281, #64579, #33256, #12126, #54002, #39251, #43171, #49119, #32918, #5804, #38579, #27599, #60651, #17452, #31234, #65602, #59622, #33592, #48781, #52729, #38221, #54350, #806, #25962, #27247, #22349, #64903, #27933, #32537, #23053, #54689, #4497, #43844, #65950, #1525, #43515, #22701, #482, #11440, #11791, #17779, #65252, #47491, #22013, #44199, #44550, #124, #55031, #16751, #17104, #21653, #16421, #38917, #11087, #6490, #49447, #37892, #59978, #1165, #59261, #60320, #66653, #39953, #51500, #33931, #18114, #3262, #62042, #13510, #44882, #61354, #46269, #18468, #8605, #24080, #13872, #24750, #55747, #7552, #56430, #29341, #28984, #50472, #56793, #30041, #45585, #8261, #67336, #50140, #35337, #67002, #18795, #67690, #50818, #2201, #34619, #39604, #45227, #19484, #45905, #55395, #40990, #12468, #24408, #61009, #7218, #1871, #28647, #23379, #2919, #12824 ) ),
 .UNSPECIFIED., .F., .F., .F. ) 
 B_SPLINE_SURFACE_WITH_KNOTS ( ( 2, 2 ),
 ( 3, 2, 2, 2, 2, 2, 2, 2, 2, 2, 2, 2, 2, 2, 2, 2, 2, 2, 2, 2, 2, 2, 2, 2, 2, 2, 2, 2, 2, 2, 2, 2, 2, 2, 2, 2, 2, 2, 2, 2, 2, 2, 2, 2, 2, 2, 2, 2, 2, 2, 2, 2, 2, 2, 2, 2, 2, 2, 2, 2, 2, 2, 2, 2, 2, 2, 2, 2, 2, 2, 2, 2, 2, 2, 2, 2, 2, 2, 2, 2, 2, 2, 2, 2, 2, 2, 2, 2, 2, 2, 2, 2, 2, 2, 2, 2, 2, 2, 2, 2, 2, 2, 2, 2, 2, 2, 2, 2, 2, 2, 2, 2, 2, 2, 2, 2, 2, 2, 2, 2, 2, 2, 2, 2, 2, 2, 2, 2, 2, 2, 2, 2, 2, 2, 2, 2, 2, 2, 2, 2, 2, 2, 2, 2, 2, 2, 2, 2, 2, 2, 2, 2, 2, 2, 2, 2, 2, 2, 2, 2, 2, 2, 2, 2, 2, 2, 2, 2, 2, 2, 2, 2, 2, 2, 2, 2, 2, 2, 2, 2, 2, 2, 2, 2, 2, 2, 2, 2, 2, 2, 2, 2, 2, 2, 2, 2, 2, 2, 2, 2, 2, 2, 2, 2, 2, 2, 2, 2, 2, 2, 2, 2, 2, 2, 2, 2, 2, 2, 2, 2, 2, 2, 2, 2, 2, 2, 2, 2, 2, 2, 2, 2, 2, 2, 2, 2, 2, 2, 2, 2, 2, 2, 2, 2, 2, 2, 2, 2, 2, 2, 2, 2, 2, 2, 2, 2, 2, 2, 2, 2, 2, 2, 2, 2, 2, 2, 2, 2, 2, 2, 2, 2, 2, 2, 2, 2, 2, 2, 2, 2, 2, 2, 2, 2, 2, 2, 2, 2, 2, 2, 2, 2, 2, 2, 2, 2, 2, 2, 2, 2, 2, 2, 2, 2, 2, 2, 2, 2, 2, 2, 2, 2, 2, 2, 2, 2, 2, 2, 2, 2, 2, 2, 2, 2, 2, 2, 2, 2, 2, 2, 2, 2, 2, 2, 2, 2, 2, 2, 2, 2, 2, 2, 2, 2, 2, 2, 2, 2, 2, 2, 2, 2, 2, 2, 2, 2, 2, 2, 2, 2, 2, 2, 2, 2, 2, 2, 2, 2, 2, 2, 2, 2, 2, 2, 2, 2, 2, 2, 2, 2, 2, 2, 2, 2, 2, 2, 2, 2, 2, 2, 2, 2, 2, 2, 2, 2, 2, 2, 2, 2, 2, 2, 2, 2, 2, 2, 2, 2, 2, 2, 2, 2, 2, 2, 2, 2, 2, 2, 2, 2, 2, 2, 2, 2, 2, 2, 2, 2, 2, 2, 2, 2, 2, 2, 2, 2, 2, 2, 2, 2, 2, 2, 2, 2, 2, 2, 2, 2, 2, 2, 2, 2, 2, 2, 2, 2, 3 ),
 ( 0.000000000000000000, 1.000000000000000000 ),
 ( 0.000000000000000000, 0.002173913043478260896, 0.004347826086956521792, 0.006521739130434782254, 0.008695652173913043584, 0.01086956521739130405, 0.01304347826086956451, 0.01521739130434782671, 0.01739130434782608717, 0.01956521739130434936, 0.02173913043478260809, 0.02391304347826087029, 0.02608695652173912902, 0.02826086956521739121, 0.03043478260869565341, 0.03260869565217391214, 0.03478260869565217434, 0.03695652173913043653, 0.03913043478260869873, 0.04130434782608695399, 0.04347826086956521618, 0.04565217391304347838, 0.04782608695652174058, 0.05000000000000000278, 0.05217391304347825803, 0.05434782608695652023, 0.05652173913043478243, 0.05869565217391304462, 0.06086956521739130682, 0.06304347826086956208, 0.06521739130434782428, 0.06739130434782608647, 0.06956521739130434867, 0.07173913043478261087, 0.07391304347826087306, 0.07608695652173913526, 0.07826086956521739746, 0.08043478260869564578, 0.08260869565217390798, 0.08478260869565217017, 0.08695652173913043237, 0.08913043478260869457, 0.09130434782608695676, 0.09347826086956521896, 0.09565217391304348116, 0.09782608695652174335, 0.1000000000000000056, 0.1021739130434782677, 0.1043478260869565161, 0.1065217391304347783, 0.1086956521739130405, 0.1108695652173913027, 0.1130434782608695649, 0.1152173913043478271, 0.1173913043478260892, 0.1195652173913043514, 0.1217391304347826136, 0.1239130434782608758, 0.1260869565217391242, 0.1282608695652174002, 0.1304347826086956486, 0.1326086956521739246, 0.1347826086956521729, 0.1369565217391304213, 0.1391304347826086973, 0.1413043478260869457, 0.1434782608695652217, 0.1456521739130434701, 0.1478260869565217461, 0.1499999999999999944, 0.1521739130434782705, 0.1543478260869565188, 0.1565217391304347949, 0.1586956521739130432, 0.1608695652173912916, 0.1630434782608695676, 0.1652173913043478160, 0.1673913043478260920, 0.1695652173913043403, 0.1717391304347826164, 0.1739130434782608647, 0.1760869565217391408, 0.1782608695652173891, 0.1804347826086956652, 0.1826086956521739135, 0.1847826086956521618, 0.1869565217391304379, 0.1891304347826086862, 0.1913043478260869623, 0.1934782608695652106, 0.1956521739130434867, 0.1978260869565217350, 0.2000000000000000111, 0.2021739130434782594, 0.2043478260869565355, 0.2065217391304347838, 0.2086956521739130321, 0.2108695652173913082, 0.2130434782608695565, 0.2152173913043478326, 0.2173913043478260809, 0.2195652173913043570, 0.2217391304347826053, 0.2239130434782608814, 0.2260869565217391297, 0.2282608695652173780, 0.2304347826086956541, 0.2326086956521739024, 0.2347826086956521785, 0.2369565217391304268, 0.2391304347826087029, 0.2413043478260869512, 0.2434782608695652273, 0.2456521739130434756, 0.2478260869565217517, 0.2500000000000000000, 0.2521739130434782483, 0.2543478260869564966, 0.2565217391304348005, 0.2586956521739130488, 0.2608695652173912971, 0.2630434782608695454, 0.2652173913043478493, 0.2673913043478260976, 0.2695652173913043459, 0.2717391304347825942, 0.2739130434782608425, 0.2760869565217391464, 0.2782608695652173947, 0.2804347826086956430, 0.2826086956521738913, 0.2847826086956521952, 0.2869565217391304435, 0.2891304347826086918, 0.2913043478260869401, 0.2934782608695652439, 0.2956521739130434923, 0.2978260869565217406, 0.2999999999999999889, 0.3021739130434782372, 0.3043478260869565410, 0.3065217391304347894, 0.3086956521739130377, 0.3108695652173912860, 0.3130434782608695898, 0.3152173913043478382, 0.3173913043478260865, 0.3195652173913043348, 0.3217391304347825831, 0.3239130434782608869, 0.3260869565217391353, 0.3282608695652173836, 0.3304347826086956319, 0.3326086956521739357, 0.3347826086956521840, 0.3369565217391304324, 0.3391304347826086807, 0.3413043478260869290, 0.3434782608695652328, 0.3456521739130434812, 0.3478260869565217295, 0.3499999999999999778, 0.3521739130434782816, 0.3543478260869565299, 0.3565217391304347783, 0.3586956521739130266, 0.3608695652173913304, 0.3630434782608695787, 0.3652173913043478271, 0.3673913043478260754, 0.3695652173913043237, 0.3717391304347826275, 0.3739130434782608758, 0.3760869565217391242, 0.3782608695652173725, 0.3804347826086956763, 0.3826086956521739246, 0.3847826086956521729, 0.3869565217391304213, 0.3891304347826086696, 0.3913043478260869734, 0.3934782608695652217, 0.3956521739130434701, 0.3978260869565217184, 0.4000000000000000222, 0.4021739130434782705, 0.4043478260869565188, 0.4065217391304347672, 0.4086956521739130710, 0.4108695652173913193, 0.4130434782608695676, 0.4152173913043478160, 0.4173913043478260643, 0.4195652173913043681, 0.4217391304347826164, 0.4239130434782608647, 0.4260869565217391131, 0.4282608695652174169, 0.4304347826086956652, 0.4326086956521739135, 0.4347826086956521618, 0.4369565217391304102, 0.4391304347826087140, 0.4413043478260869623, 0.4434782608695652106, 0.4456521739130434590, 0.4478260869565217628, 0.4500000000000000111, 0.4521739130434782594, 0.4543478260869565077, 0.4565217391304347561, 0.4586956521739130599, 0.4608695652173913082, 0.4630434782608695565, 0.4652173913043478048, 0.4673913043478261087, 0.4695652173913043570, 0.4717391304347826053, 0.4739130434782608536, 0.4760869565217391575, 0.4782608695652174058, 0.4804347826086956541, 0.4826086956521739024, 0.4847826086956521507, 0.4869565217391304546, 0.4891304347826087029, 0.4913043478260869512, 0.4934782608695651995, 0.4956521739130435034, 0.4978260869565217517, 0.5000000000000000000, 0.5021739130434782483, 0.5043478260869564966, 0.5065217391304347450, 0.5086956521739129933, 0.5108695652173913526, 0.5130434782608696009, 0.5152173913043478493, 0.5173913043478260976, 0.5195652173913043459, 0.5217391304347825942, 0.5239130434782608425, 0.5260869565217390909, 0.5282608695652173392, 0.5304347826086956985, 0.5326086956521739468, 0.5347826086956521952, 0.5369565217391304435, 0.5391304347826086918, 0.5413043478260869401, 0.5434782608695651884, 0.5456521739130434367, 0.5478260869565216851, 0.5500000000000000444, 0.5521739130434782927, 0.5543478260869565410, 0.5565217391304347894, 0.5586956521739130377, 0.5608695652173912860, 0.5630434782608695343, 0.5652173913043477826, 0.5673913043478261420, 0.5695652173913043903, 0.5717391304347826386, 0.5739130434782608869, 0.5760869565217391353, 0.5782608695652173836, 0.5804347826086956319, 0.5826086956521738802, 0.5847826086956521285, 0.5869565217391304879, 0.5891304347826087362, 0.5913043478260869845, 0.5934782608695652328, 0.5956521739130434812, 0.5978260869565217295, 0.5999999999999999778, 0.6021739130434782261, 0.6043478260869564744, 0.6065217391304348338, 0.6086956521739130821, 0.6108695652173913304, 0.6130434782608695787, 0.6152173913043478271, 0.6173913043478260754, 0.6195652173913043237, 0.6217391304347825720, 0.6239130434782608203, 0.6260869565217391797, 0.6282608695652174280, 0.6304347826086956763, 0.6326086956521739246, 0.6347826086956521729, 0.6369565217391304213, 0.6391304347826086696, 0.6413043478260869179, 0.6434782608695651662, 0.6456521739130435256, 0.6478260869565217739, 0.6500000000000000222, 0.6521739130434782705, 0.6543478260869565188, 0.6565217391304347672, 0.6586956521739130155, 0.6608695652173912638, 0.6630434782608695121, 0.6652173913043478715, 0.6673913043478261198, 0.6695652173913043681, 0.6717391304347826164, 0.6739130434782608647, 0.6760869565217391131, 0.6782608695652173614, 0.6804347826086956097, 0.6826086956521738580, 0.6847826086956522174, 0.6869565217391304657, 0.6891304347826087140, 0.6913043478260869623, 0.6934782608695652106, 0.6956521739130434590, 0.6978260869565217073, 0.6999999999999999556, 0.7021739130434783149, 0.7043478260869565633, 0.7065217391304348116, 0.7086956521739130599, 0.7108695652173913082, 0.7130434782608695565, 0.7152173913043478048, 0.7173913043478260532, 0.7195652173913043015, 0.7217391304347826608, 0.7239130434782609091, 0.7260869565217391575, 0.7282608695652174058, 0.7304347826086956541, 0.7326086956521739024, 0.7347826086956521507, 0.7369565217391303991, 0.7391304347826086474, 0.7413043478260870067, 0.7434782608695652550, 0.7456521739130435034, 0.7478260869565217517, 0.7500000000000000000, 0.7521739130434782483, 0.7543478260869564966, 0.7565217391304347450, 0.7586956521739129933, 0.7608695652173913526, 0.7630434782608696009, 0.7652173913043478493, 0.7673913043478260976, 0.7695652173913043459, 0.7717391304347825942, 0.7739130434782608425, 0.7760869565217390909, 0.7782608695652173392, 0.7804347826086956985, 0.7826086956521739468, 0.7847826086956521952, 0.7869565217391304435, 0.7891304347826086918, 0.7913043478260869401, 0.7934782608695651884, 0.7956521739130434367, 0.7978260869565216851, 0.8000000000000000444, 0.8021739130434782927, 0.8043478260869565410, 0.8065217391304347894, 0.8086956521739130377, 0.8108695652173912860, 0.8130434782608695343, 0.8152173913043477826, 0.8173913043478261420, 0.8195652173913043903, 0.8217391304347826386, 0.8239130434782608869, 0.8260869565217391353, 0.8282608695652173836, 0.8304347826086956319, 0.8326086956521738802, 0.8347826086956521285, 0.8369565217391304879, 0.8391304347826087362, 0.8413043478260869845, 0.8434782608695652328, 0.8456521739130434812, 0.8478260869565217295, 0.8499999999999999778, 0.8521739130434782261, 0.8543478260869564744, 0.8565217391304348338, 0.8586956521739130821, 0.8608695652173913304, 0.8630434782608695787, 0.8652173913043478271, 0.8673913043478260754, 0.8695652173913043237, 0.8717391304347825720, 0.8739130434782608203, 0.8760869565217391797, 0.8782608695652174280, 0.8804347826086956763, 0.8826086956521739246, 0.8847826086956521729, 0.8869565217391304213, 0.8891304347826086696, 0.8913043478260869179, 0.8934782608695651662, 0.8956521739130435256, 0.8978260869565217739, 0.9000000000000000222, 0.9021739130434782705, 0.9043478260869565188, 0.9065217391304347672, 0.9086956521739130155, 0.9108695652173912638, 0.9130434782608695121, 0.9152173913043478715, 0.9173913043478261198, 0.9195652173913043681, 0.9217391304347826164, 0.9239130434782608647, 0.9260869565217391131, 0.9282608695652173614, 0.9304347826086956097, 0.9326086956521738580, 0.9347826086956522174, 0.9369565217391304657, 0.9391304347826087140, 0.9413043478260869623, 0.9434782608695652106, 0.9456521739130434590, 0.9478260869565217073, 0.9499999999999999556, 0.9521739130434783149, 0.9543478260869565633, 0.9565217391304348116, 0.9586956521739130599, 0.9608695652173913082, 0.9630434782608695565, 0.9652173913043478048, 0.9673913043478260532, 0.9695652173913043015, 0.9717391304347826608, 0.9739130434782609091, 0.9760869565217391575, 0.9782608695652174058, 0.9804347826086956541, 0.9826086956521739024, 0.9847826086956521507, 0.9869565217391303991, 0.9891304347826086474, 0.9913043478260870067 ),
 .UNSPECIFIED. ) 
 GEOMETRIC_REPRESENTATION_ITEM ( )  RATIONAL_B_SPLINE_SURFACE ( (
 ( 1.000000000000000000, 0.9510565162951535312, 1.000000000000000000, 0.9510565162951535312, 1.000000000000000000, 0.9510565162951535312, 1.000000000000000000, 0.9510565162951535312, 1.000000000000000000, 0.9510565162951535312, 1.000000000000000000, 0.9510565162951535312, 1.000000000000000000, 0.9510565162951535312, 1.000000000000000000, 0.9510565162951535312, 1.000000000000000000, 0.9510565162951535312, 1.000000000000000000, 0.9510565162951535312, 1.000000000000000000, 0.9510565162951535312, 1.000000000000000000, 0.9510565162951535312, 1.000000000000000000, 0.9510565162951535312, 1.000000000000000000, 0.9510565162951535312, 1.000000000000000000, 0.9510565162951535312, 1.000000000000000000, 0.9510565162951535312, 1.000000000000000000, 0.9510565162951535312, 1.000000000000000000, 0.9510565162951535312, 1.000000000000000000, 0.9510565162951535312, 1.000000000000000000, 0.9510565162951535312, 1.000000000000000000, 0.9510565162951535312, 1.000000000000000000, 0.9510565162951535312, 1.000000000000000000, 0.9510565162951535312, 1.000000000000000000, 0.9510565162951535312, 1.000000000000000000, 0.9510565162951535312, 1.000000000000000000, 0.9510565162951535312, 1.000000000000000000, 0.9510565162951535312, 1.000000000000000000, 0.9510565162951535312, 1.000000000000000000, 0.9510565162951535312, 1.000000000000000000, 0.9510565162951535312, 1.000000000000000000, 0.9510565162951535312, 1.000000000000000000, 0.9510565162951535312, 1.000000000000000000, 0.9510565162951535312, 1.000000000000000000, 0.9510565162951535312, 1.000000000000000000, 0.9510565162951535312, 1.000000000000000000, 0.9510565162951535312, 1.000000000000000000, 0.9510565162951535312, 1.000000000000000000, 0.9510565162951535312, 1.000000000000000000, 0.9510565162951535312, 1.000000000000000000, 0.9510565162951535312, 1.000000000000000000, 0.9510565162951535312, 1.000000000000000000, 0.9510565162951535312, 1.000000000000000000, 0.9510565162951535312, 1.000000000000000000, 0.9510565162951535312, 1.000000000000000000, 0.9510565162951535312, 1.000000000000000000, 0.9510565162951535312, 1.000000000000000000, 0.9510565162951535312, 1.000000000000000000, 0.9510565162951535312, 1.000000000000000000, 0.9510565162951535312, 1.000000000000000000, 0.9510565162951535312, 1.000000000000000000, 0.9510565162951535312, 1.000000000000000000, 0.9510565162951535312, 1.000000000000000000, 0.9510565162951535312, 1.000000000000000000, 0.9510565162951535312, 1.000000000000000000, 0.9510565162951535312, 1.000000000000000000, 0.9510565162951535312, 1.000000000000000000, 0.9510565162951535312, 1.000000000000000000, 0.9510565162951535312, 1.000000000000000000, 0.9510565162951535312, 1.000000000000000000, 0.9510565162951535312, 1.000000000000000000, 0.9510565162951535312, 1.000000000000000000, 0.9510565162951535312, 1.000000000000000000, 0.9510565162951535312, 1.000000000000000000, 0.9510565162951535312, 1.000000000000000000, 0.9510565162951535312, 1.000000000000000000, 0.9510565162951535312, 1.000000000000000000, 0.9510565162951535312, 1.000000000000000000, 0.9510565162951535312, 1.000000000000000000, 0.9510565162951535312, 1.000000000000000000, 0.9510565162951535312, 1.000000000000000000, 0.9510565162951535312, 1.000000000000000000, 0.9510565162951535312, 1.000000000000000000, 0.9510565162951535312, 1.000000000000000000, 0.9510565162951535312, 1.000000000000000000, 0.9510565162951535312, 1.000000000000000000, 0.9510565162951535312, 1.000000000000000000, 0.9510565162951535312, 1.000000000000000000, 0.9510565162951535312, 1.000000000000000000, 0.9510565162951535312, 1.000000000000000000, 0.9510565162951535312, 1.000000000000000000, 0.9510565162951535312, 1.000000000000000000, 0.9510565162951535312, 1.000000000000000000, 0.9510565162951535312, 1.000000000000000000, 0.9510565162951535312, 1.000000000000000000, 0.9510565162951535312, 1.000000000000000000, 0.9510565162951535312, 1.000000000000000000, 0.9510565162951535312, 1.000000000000000000, 0.9510565162951535312, 1.000000000000000000, 0.9510565162951535312, 1.000000000000000000, 0.9510565162951535312, 1.000000000000000000, 0.9510565162951535312, 1.000000000000000000, 0.9510565162951535312, 1.000000000000000000, 0.9510565162951535312, 1.000000000000000000, 0.9510565162951535312, 1.000000000000000000, 0.9510565162951535312, 1.000000000000000000, 0.9510565162951535312, 1.000000000000000000, 0.9510565162951535312, 1.000000000000000000, 0.9510565162951535312, 1.000000000000000000, 0.9510565162951535312, 1.000000000000000000, 0.9510565162951535312, 1.000000000000000000, 0.9510565162951535312, 1.000000000000000000, 0.9510565162951535312, 1.000000000000000000, 0.9510565162951535312, 1.000000000000000000, 0.9510565162951535312, 1.000000000000000000, 0.9510565162951535312, 1.000000000000000000, 0.9510565162951535312, 1.000000000000000000, 0.9510565162951535312, 1.000000000000000000, 0.9510565162951535312, 1.000000000000000000, 0.9510565162951535312, 1.000000000000000000, 0.9510565162951535312, 1.000000000000000000, 0.9510565162951535312, 1.000000000000000000, 0.9510565162951535312, 1.000000000000000000, 0.9510565162951535312, 1.000000000000000000, 0.9510565162951535312, 1.000000000000000000, 0.9510565162951535312, 1.000000000000000000, 0.9510565162951535312, 1.000000000000000000, 0.9510565162951535312, 1.000000000000000000, 0.9510565162951535312, 1.000000000000000000, 0.9510565162951535312, 1.000000000000000000, 0.9510565162951535312, 1.000000000000000000, 0.9510565162951535312, 1.000000000000000000, 0.9510565162951535312, 1.000000000000000000, 0.9510565162951535312, 1.000000000000000000, 0.9510565162951535312, 1.000000000000000000, 0.9510565162951535312, 1.000000000000000000, 0.9510565162951535312, 1.000000000000000000, 0.9510565162951535312, 1.000000000000000000, 0.9510565162951535312, 1.000000000000000000, 0.9510565162951535312, 1.000000000000000000, 0.9510565162951535312, 1.000000000000000000, 0.9510565162951535312, 1.000000000000000000, 0.9510565162951535312, 1.000000000000000000, 0.9510565162951535312, 1.000000000000000000, 0.9510565162951535312, 1.000000000000000000, 0.9510565162951535312, 1.000000000000000000, 0.9510565162951535312, 1.000000000000000000, 0.9510565162951535312, 1.000000000000000000, 0.9510565162951535312, 1.000000000000000000, 0.9510565162951535312, 1.000000000000000000, 0.9510565162951535312, 1.000000000000000000, 0.9510565162951535312, 1.000000000000000000, 0.9510565162951535312, 1.000000000000000000, 0.9510565162951535312, 1.000000000000000000, 0.9510565162951535312, 1.000000000000000000, 0.9510565162951535312, 1.000000000000000000, 0.9510565162951535312, 1.000000000000000000, 0.9510565162951535312, 1.000000000000000000, 0.9510565162951535312, 1.000000000000000000, 0.9510565162951535312, 1.000000000000000000, 0.9510565162951535312, 1.000000000000000000, 0.9510565162951535312, 1.000000000000000000, 0.9510565162951535312, 1.000000000000000000, 0.9510565162951535312, 1.000000000000000000, 0.9510565162951535312, 1.000000000000000000, 0.9510565162951535312, 1.000000000000000000, 0.9510565162951535312, 1.000000000000000000, 0.9510565162951535312, 1.000000000000000000, 0.9510565162951535312, 1.000000000000000000, 0.9510565162951535312, 1.000000000000000000, 0.9510565162951535312, 1.000000000000000000, 0.9510565162951535312, 1.000000000000000000, 0.9510565162951535312, 1.000000000000000000, 0.9510565162951535312, 1.000000000000000000, 0.9510565162951535312, 1.000000000000000000, 0.9510565162951535312, 1.000000000000000000, 0.9510565162951535312, 1.000000000000000000, 0.9510565162951535312, 1.000000000000000000, 0.9510565162951535312, 1.000000000000000000, 0.9510565162951535312, 1.000000000000000000, 0.9510565162951535312, 1.000000000000000000, 0.9510565162951535312, 1.000000000000000000, 0.9510565162951535312, 1.000000000000000000, 0.9510565162951535312, 1.000000000000000000, 0.9510565162951535312, 1.000000000000000000, 0.9510565162951535312, 1.000000000000000000, 0.9510565162951535312, 1.000000000000000000, 0.9510565162951535312, 1.000000000000000000, 0.9510565162951535312, 1.000000000000000000, 0.9510565162951535312, 1.000000000000000000, 0.9510565162951535312, 1.000000000000000000, 0.9510565162951535312, 1.000000000000000000, 0.9510565162951535312, 1.000000000000000000, 0.9510565162951535312, 1.000000000000000000, 0.9510565162951535312, 1.000000000000000000, 0.9510565162951535312, 1.000000000000000000, 0.9510565162951535312, 1.000000000000000000, 0.9510565162951535312, 1.000000000000000000, 0.9510565162951535312, 1.000000000000000000, 0.9510565162951535312, 1.000000000000000000, 0.9510565162951535312, 1.000000000000000000, 0.9510565162951535312, 1.000000000000000000, 0.9510565162951535312, 1.000000000000000000, 0.9510565162951535312, 1.000000000000000000, 0.9510565162951535312, 1.000000000000000000, 0.9510565162951535312, 1.000000000000000000, 0.9510565162951535312, 1.000000000000000000, 0.9510565162951535312, 1.000000000000000000, 0.9510565162951535312, 1.000000000000000000, 0.9510565162951535312, 1.000000000000000000, 0.9510565162951535312, 1.000000000000000000, 0.9510565162951535312, 1.000000000000000000, 0.9510565162951535312, 1.000000000000000000, 0.9510565162951535312, 1.000000000000000000, 0.9510565162951535312, 1.000000000000000000, 0.9510565162951535312, 1.000000000000000000, 0.9510565162951535312, 1.000000000000000000, 0.9510565162951535312, 1.000000000000000000, 0.9510565162951535312, 1.000000000000000000, 0.9510565162951535312, 1.000000000000000000, 0.9510565162951535312, 1.000000000000000000, 0.9510565162951535312, 1.000000000000000000, 0.9510565162951535312, 1.000000000000000000, 0.9510565162951535312, 1.000000000000000000, 0.9510565162951535312, 1.000000000000000000, 0.9510565162951535312, 1.000000000000000000, 0.9510565162951535312, 1.000000000000000000, 0.9510565162951535312, 1.000000000000000000, 0.9510565162951535312, 1.000000000000000000, 0.9510565162951535312, 1.000000000000000000, 0.9510565162951535312, 1.000000000000000000, 0.9510565162951535312, 1.000000000000000000, 0.9510565162951535312, 1.000000000000000000, 0.9510565162951535312, 1.000000000000000000, 0.9510565162951535312, 1.000000000000000000, 0.9510565162951535312, 1.000000000000000000, 0.9510565162951535312, 1.000000000000000000, 0.9510565162951535312, 1.000000000000000000, 0.9510565162951535312, 1.000000000000000000, 0.9510565162951535312, 1.000000000000000000, 0.9510565162951535312, 1.000000000000000000, 0.9510565162951535312, 1.000000000000000000, 0.9510565162951535312, 1.000000000000000000, 0.9510565162951535312, 1.000000000000000000, 0.9510565162951535312, 1.000000000000000000, 0.9510565162951535312, 1.000000000000000000, 0.9510565162951535312, 1.000000000000000000, 0.9510565162951535312, 1.000000000000000000, 0.9510565162951535312, 1.000000000000000000, 0.9510565162951535312, 1.000000000000000000, 0.9510565162951535312, 1.000000000000000000, 0.9510565162951535312, 1.000000000000000000, 0.9510565162951535312, 1.000000000000000000, 0.9510565162951535312, 1.000000000000000000, 0.9510565162951535312, 1.000000000000000000, 0.9510565162951535312, 1.000000000000000000, 0.9510565162951535312, 1.000000000000000000, 0.9510565162951535312, 1.000000000000000000, 0.9510565162951535312, 1.000000000000000000, 0.9510565162951535312, 1.000000000000000000, 0.9510565162951535312, 1.000000000000000000, 0.9510565162951535312, 1.000000000000000000, 0.9510565162951535312, 1.000000000000000000, 0.9510565162951535312, 1.000000000000000000, 0.9510565162951535312, 1.000000000000000000, 0.9510565162951535312, 1.000000000000000000, 0.9510565162951535312, 1.000000000000000000, 0.9510565162951535312, 1.000000000000000000, 0.9510565162951535312, 1.000000000000000000, 0.9510565162951535312, 1.000000000000000000, 0.9510565162951535312, 1.000000000000000000, 0.9510565162951535312, 1.000000000000000000, 0.9510565162951535312, 1.000000000000000000, 0.9510565162951535312, 1.000000000000000000, 0.9510565162951535312, 1.000000000000000000, 0.9510565162951535312, 1.000000000000000000, 0.9510565162951535312, 1.000000000000000000, 0.9510565162951535312, 1.000000000000000000, 0.9510565162951535312, 1.000000000000000000, 0.9510565162951535312, 1.000000000000000000, 0.9510565162951535312, 1.000000000000000000, 0.9510565162951535312, 1.000000000000000000, 0.9510565162951535312, 1.000000000000000000, 0.9510565162951535312, 1.000000000000000000, 0.9510565162951535312, 1.000000000000000000, 0.9510565162951535312, 1.000000000000000000, 0.9510565162951535312, 1.000000000000000000, 0.9510565162951535312, 1.000000000000000000, 0.9510565162951535312, 1.000000000000000000, 0.9510565162951535312, 1.000000000000000000, 0.9510565162951535312, 1.000000000000000000, 0.9510565162951535312, 1.000000000000000000, 0.9510565162951535312, 1.000000000000000000, 0.9510565162951535312, 1.000000000000000000, 0.9510565162951535312, 1.000000000000000000, 0.9510565162951535312, 1.000000000000000000, 0.9510565162951535312, 1.000000000000000000, 0.9510565162951535312, 1.000000000000000000, 0.9510565162951535312, 1.000000000000000000, 0.9510565162951535312, 1.000000000000000000, 0.9510565162951535312, 1.000000000000000000, 0.9510565162951535312, 1.000000000000000000, 0.9510565162951535312, 1.000000000000000000, 0.9510565162951535312, 1.000000000000000000, 0.9510565162951535312, 1.000000000000000000, 0.9510565162951535312, 1.000000000000000000, 0.9510565162951535312, 1.000000000000000000, 0.9510565162951535312, 1.000000000000000000, 0.9510565162951535312, 1.000000000000000000, 0.9510565162951535312, 1.000000000000000000, 0.9510565162951535312, 1.000000000000000000, 0.9510565162951535312, 1.000000000000000000, 0.9510565162951535312, 1.000000000000000000, 0.9510565162951535312, 1.000000000000000000, 0.9510565162951535312, 1.000000000000000000, 0.9510565162951535312, 1.000000000000000000, 0.9510565162951535312, 1.000000000000000000, 0.9510565162951535312, 1.000000000000000000, 0.9510565162951535312, 1.000000000000000000, 0.9510565162951535312, 1.000000000000000000, 0.9510565162951535312, 1.000000000000000000, 0.9510565162951535312, 1.000000000000000000, 0.9510565162951535312, 1.000000000000000000, 0.9510565162951535312, 1.000000000000000000, 0.9510565162951535312, 1.000000000000000000, 0.9510565162951535312, 1.000000000000000000, 0.9510565162951535312, 1.000000000000000000, 0.9510565162951535312, 1.000000000000000000, 0.9510565162951535312, 1.000000000000000000, 0.9510565162951535312, 1.000000000000000000, 0.9510565162951535312, 1.000000000000000000, 0.9510565162951535312, 1.000000000000000000, 0.9510565162951535312, 1.000000000000000000, 0.9510565162951535312, 1.000000000000000000, 0.9510565162951535312, 1.000000000000000000, 0.9510565162951535312, 1.000000000000000000, 0.9510565162951535312, 1.000000000000000000, 0.9510565162951535312, 1.000000000000000000, 0.9510565162951535312, 1.000000000000000000, 0.9510565162951535312, 1.000000000000000000, 0.9510565162951535312, 1.000000000000000000, 0.9510565162951535312, 1.000000000000000000, 0.9510565162951535312, 1.000000000000000000, 0.9510565162951535312, 1.000000000000000000, 0.9510565162951535312, 1.000000000000000000, 0.9510565162951535312, 1.000000000000000000, 0.9510565162951535312, 1.000000000000000000, 0.9510565162951535312, 1.000000000000000000, 0.9510565162951535312, 1.000000000000000000, 0.9510565162951535312, 1.000000000000000000, 0.9510565162951535312, 1.000000000000000000, 0.9510565162951535312, 1.000000000000000000, 0.9510565162951535312, 1.000000000000000000, 0.9510565162951535312, 1.000000000000000000, 0.9510565162951535312, 1.000000000000000000, 0.9510565162951535312, 1.000000000000000000, 0.9510565162951535312, 1.000000000000000000, 0.9510565162951535312, 1.000000000000000000, 0.9510565162951535312, 1.000000000000000000, 0.9510565162951535312, 1.000000000000000000, 0.9510565162951535312, 1.000000000000000000, 0.9510565162951535312, 1.000000000000000000, 0.9510565162951535312, 1.000000000000000000, 0.9510565162951535312, 1.000000000000000000, 0.9510565162951535312, 1.000000000000000000, 0.9510565162951535312, 1.000000000000000000, 0.9510565162951535312, 1.000000000000000000, 0.9510565162951535312, 1.000000000000000000, 0.9510565162951535312, 1.000000000000000000, 0.9510565162951535312, 1.000000000000000000, 0.9510565162951535312, 1.000000000000000000, 0.9510565162951535312, 1.000000000000000000, 0.9510565162951535312, 1.000000000000000000, 0.9510565162951535312, 1.000000000000000000, 0.9510565162951535312, 1.000000000000000000, 0.9510565162951535312, 1.000000000000000000, 0.9510565162951535312, 1.000000000000000000, 0.9510565162951535312, 1.000000000000000000, 0.9510565162951535312, 1.000000000000000000, 0.9510565162951535312, 1.000000000000000000, 0.9510565162951535312, 1.000000000000000000, 0.9510565162951535312, 1.000000000000000000, 0.9510565162951535312, 1.000000000000000000, 0.9510565162951535312, 1.000000000000000000, 0.9510565162951535312, 1.000000000000000000, 0.9510565162951535312, 1.000000000000000000, 0.9510565162951535312, 1.000000000000000000, 0.9510565162951535312, 1.000000000000000000, 0.9510565162951535312, 1.000000000000000000, 0.9510565162951535312, 1.000000000000000000, 0.9510565162951535312, 1.000000000000000000, 0.9510565162951535312, 1.000000000000000000, 0.9510565162951535312, 1.000000000000000000, 0.9510565162951535312, 1.000000000000000000, 0.9510565162951535312, 1.000000000000000000, 0.9510565162951535312, 1.000000000000000000, 0.9510565162951535312, 1.000000000000000000, 0.9510565162951535312, 1.000000000000000000, 0.9510565162951535312, 1.000000000000000000, 0.9510565162951535312, 1.000000000000000000, 0.9510565162951535312, 1.000000000000000000, 0.9510565162951535312, 1.000000000000000000, 0.9510565162951535312, 1.000000000000000000, 0.9510565162951535312, 1.000000000000000000, 0.9510565162951535312, 1.000000000000000000, 0.9510565162951535312, 1.000000000000000000, 0.9510565162951535312, 1.000000000000000000, 0.9510565162951535312, 1.000000000000000000, 0.9510565162951535312, 1.000000000000000000, 0.9510565162951535312, 1.000000000000000000, 0.9510565162951535312, 1.000000000000000000, 0.9510565162951535312, 1.000000000000000000, 0.9510565162951535312, 1.000000000000000000, 0.9510565162951535312, 1.000000000000000000, 0.9510565162951535312, 1.000000000000000000, 0.9510565162951535312, 1.000000000000000000, 0.9510565162951535312, 1.000000000000000000, 0.9510565162951535312, 1.000000000000000000, 0.9510565162951535312, 1.000000000000000000, 0.9510565162951535312, 1.000000000000000000, 0.9510565162951535312, 1.000000000000000000, 0.9510565162951535312, 1.000000000000000000, 0.9510565162951535312, 1.000000000000000000, 0.9510565162951535312, 1.000000000000000000, 0.9510565162951535312, 1.000000000000000000, 0.9510565162951535312, 1.000000000000000000, 0.9510565162951535312, 1.000000000000000000, 0.9510565162951535312, 1.000000000000000000, 0.9510565162951535312, 1.000000000000000000, 0.9510565162951535312, 1.000000000000000000, 0.9510565162951535312, 1.000000000000000000, 0.9510565162951535312, 1.000000000000000000, 0.9510565162951535312, 1.000000000000000000, 0.9510565162951535312, 1.000000000000000000, 0.9510565162951535312, 1.000000000000000000, 0.9510565162951535312, 1.000000000000000000, 0.9510565162951535312, 1.000000000000000000, 0.9510565162951535312, 1.000000000000000000, 0.9510565162951535312, 1.000000000000000000, 0.9510565162951535312, 1.000000000000000000, 0.9510565162951535312, 1.000000000000000000, 0.9510565162951535312, 1.000000000000000000, 0.9510565162951535312, 1.000000000000000000, 0.9510565162951535312, 1.000000000000000000, 0.9510565162951535312, 1.000000000000000000, 0.9510565162951535312, 1.000000000000000000, 0.9510565162951535312, 1.000000000000000000, 0.9510565162951535312, 1.000000000000000000, 0.9510565162951535312, 1.000000000000000000, 0.9510565162951535312, 1.000000000000000000, 0.9510565162951535312, 1.000000000000000000, 0.9510565162951535312, 1.000000000000000000, 0.9510565162951535312, 1.000000000000000000, 0.9510565162951535312, 1.000000000000000000, 0.9510565162951535312, 1.000000000000000000, 0.9510565162951535312, 1.000000000000000000, 0.9510565162951535312, 1.000000000000000000, 0.9510565162951535312, 1.000000000000000000, 0.9510565162951535312, 1.000000000000000000, 0.9510565162951535312, 1.000000000000000000, 0.9510565162951535312, 1.000000000000000000, 0.9510565162951535312, 1.000000000000000000, 0.9510565162951535312, 1.000000000000000000, 0.9510565162951535312, 1.000000000000000000, 0.9510565162951535312, 1.000000000000000000, 0.9510565162951535312, 1.000000000000000000, 0.9510565162951535312, 1.000000000000000000),
 ( 1.000000000000000000, 0.9510565162951535312, 1.000000000000000000, 0.9510565162951535312, 1.000000000000000000, 0.9510565162951535312, 1.000000000000000000, 0.9510565162951535312, 1.000000000000000000, 0.9510565162951535312, 1.000000000000000000, 0.9510565162951535312, 1.000000000000000000, 0.9510565162951535312, 1.000000000000000000, 0.9510565162951535312, 1.000000000000000000, 0.9510565162951535312, 1.000000000000000000, 0.9510565162951535312, 1.000000000000000000, 0.9510565162951535312, 1.000000000000000000, 0.9510565162951535312, 1.000000000000000000, 0.9510565162951535312, 1.000000000000000000, 0.9510565162951535312, 1.000000000000000000, 0.9510565162951535312, 1.000000000000000000, 0.9510565162951535312, 1.000000000000000000, 0.9510565162951535312, 1.000000000000000000, 0.9510565162951535312, 1.000000000000000000, 0.9510565162951535312, 1.000000000000000000, 0.9510565162951535312, 1.000000000000000000, 0.9510565162951535312, 1.000000000000000000, 0.9510565162951535312, 1.000000000000000000, 0.9510565162951535312, 1.000000000000000000, 0.9510565162951535312, 1.000000000000000000, 0.9510565162951535312, 1.000000000000000000, 0.9510565162951535312, 1.000000000000000000, 0.9510565162951535312, 1.000000000000000000, 0.9510565162951535312, 1.000000000000000000, 0.9510565162951535312, 1.000000000000000000, 0.9510565162951535312, 1.000000000000000000, 0.9510565162951535312, 1.000000000000000000, 0.9510565162951535312, 1.000000000000000000, 0.9510565162951535312, 1.000000000000000000, 0.9510565162951535312, 1.000000000000000000, 0.9510565162951535312, 1.000000000000000000, 0.9510565162951535312, 1.000000000000000000, 0.9510565162951535312, 1.000000000000000000, 0.9510565162951535312, 1.000000000000000000, 0.9510565162951535312, 1.000000000000000000, 0.9510565162951535312, 1.000000000000000000, 0.9510565162951535312, 1.000000000000000000, 0.9510565162951535312, 1.000000000000000000, 0.9510565162951535312, 1.000000000000000000, 0.9510565162951535312, 1.000000000000000000, 0.9510565162951535312, 1.000000000000000000, 0.9510565162951535312, 1.000000000000000000, 0.9510565162951535312, 1.000000000000000000, 0.9510565162951535312, 1.000000000000000000, 0.9510565162951535312, 1.000000000000000000, 0.9510565162951535312, 1.000000000000000000, 0.9510565162951535312, 1.000000000000000000, 0.9510565162951535312, 1.000000000000000000, 0.9510565162951535312, 1.000000000000000000, 0.9510565162951535312, 1.000000000000000000, 0.9510565162951535312, 1.000000000000000000, 0.9510565162951535312, 1.000000000000000000, 0.9510565162951535312, 1.000000000000000000, 0.9510565162951535312, 1.000000000000000000, 0.9510565162951535312, 1.000000000000000000, 0.9510565162951535312, 1.000000000000000000, 0.9510565162951535312, 1.000000000000000000, 0.9510565162951535312, 1.000000000000000000, 0.9510565162951535312, 1.000000000000000000, 0.9510565162951535312, 1.000000000000000000, 0.9510565162951535312, 1.000000000000000000, 0.9510565162951535312, 1.000000000000000000, 0.9510565162951535312, 1.000000000000000000, 0.9510565162951535312, 1.000000000000000000, 0.9510565162951535312, 1.000000000000000000, 0.9510565162951535312, 1.000000000000000000, 0.9510565162951535312, 1.000000000000000000, 0.9510565162951535312, 1.000000000000000000, 0.9510565162951535312, 1.000000000000000000, 0.9510565162951535312, 1.000000000000000000, 0.9510565162951535312, 1.000000000000000000, 0.9510565162951535312, 1.000000000000000000, 0.9510565162951535312, 1.000000000000000000, 0.9510565162951535312, 1.000000000000000000, 0.9510565162951535312, 1.000000000000000000, 0.9510565162951535312, 1.000000000000000000, 0.9510565162951535312, 1.000000000000000000, 0.9510565162951535312, 1.000000000000000000, 0.9510565162951535312, 1.000000000000000000, 0.9510565162951535312, 1.000000000000000000, 0.9510565162951535312, 1.000000000000000000, 0.9510565162951535312, 1.000000000000000000, 0.9510565162951535312, 1.000000000000000000, 0.9510565162951535312, 1.000000000000000000, 0.9510565162951535312, 1.000000000000000000, 0.9510565162951535312, 1.000000000000000000, 0.9510565162951535312, 1.000000000000000000, 0.9510565162951535312, 1.000000000000000000, 0.9510565162951535312, 1.000000000000000000, 0.9510565162951535312, 1.000000000000000000, 0.9510565162951535312, 1.000000000000000000, 0.9510565162951535312, 1.000000000000000000, 0.9510565162951535312, 1.000000000000000000, 0.9510565162951535312, 1.000000000000000000, 0.9510565162951535312, 1.000000000000000000, 0.9510565162951535312, 1.000000000000000000, 0.9510565162951535312, 1.000000000000000000, 0.9510565162951535312, 1.000000000000000000, 0.9510565162951535312, 1.000000000000000000, 0.9510565162951535312, 1.000000000000000000, 0.9510565162951535312, 1.000000000000000000, 0.9510565162951535312, 1.000000000000000000, 0.9510565162951535312, 1.000000000000000000, 0.9510565162951535312, 1.000000000000000000, 0.9510565162951535312, 1.000000000000000000, 0.9510565162951535312, 1.000000000000000000, 0.9510565162951535312, 1.000000000000000000, 0.9510565162951535312, 1.000000000000000000, 0.9510565162951535312, 1.000000000000000000, 0.9510565162951535312, 1.000000000000000000, 0.9510565162951535312, 1.000000000000000000, 0.9510565162951535312, 1.000000000000000000, 0.9510565162951535312, 1.000000000000000000, 0.9510565162951535312, 1.000000000000000000, 0.9510565162951535312, 1.000000000000000000, 0.9510565162951535312, 1.000000000000000000, 0.9510565162951535312, 1.000000000000000000, 0.9510565162951535312, 1.000000000000000000, 0.9510565162951535312, 1.000000000000000000, 0.9510565162951535312, 1.000000000000000000, 0.9510565162951535312, 1.000000000000000000, 0.9510565162951535312, 1.000000000000000000, 0.9510565162951535312, 1.000000000000000000, 0.9510565162951535312, 1.000000000000000000, 0.9510565162951535312, 1.000000000000000000, 0.9510565162951535312, 1.000000000000000000, 0.9510565162951535312, 1.000000000000000000, 0.9510565162951535312, 1.000000000000000000, 0.9510565162951535312, 1.000000000000000000, 0.9510565162951535312, 1.000000000000000000, 0.9510565162951535312, 1.000000000000000000, 0.9510565162951535312, 1.000000000000000000, 0.9510565162951535312, 1.000000000000000000, 0.9510565162951535312, 1.000000000000000000, 0.9510565162951535312, 1.000000000000000000, 0.9510565162951535312, 1.000000000000000000, 0.9510565162951535312, 1.000000000000000000, 0.9510565162951535312, 1.000000000000000000, 0.9510565162951535312, 1.000000000000000000, 0.9510565162951535312, 1.000000000000000000, 0.9510565162951535312, 1.000000000000000000, 0.9510565162951535312, 1.000000000000000000, 0.9510565162951535312, 1.000000000000000000, 0.9510565162951535312, 1.000000000000000000, 0.9510565162951535312, 1.000000000000000000, 0.9510565162951535312, 1.000000000000000000, 0.9510565162951535312, 1.000000000000000000, 0.9510565162951535312, 1.000000000000000000, 0.9510565162951535312, 1.000000000000000000, 0.9510565162951535312, 1.000000000000000000, 0.9510565162951535312, 1.000000000000000000, 0.9510565162951535312, 1.000000000000000000, 0.9510565162951535312, 1.000000000000000000, 0.9510565162951535312, 1.000000000000000000, 0.9510565162951535312, 1.000000000000000000, 0.9510565162951535312, 1.000000000000000000, 0.9510565162951535312, 1.000000000000000000, 0.9510565162951535312, 1.000000000000000000, 0.9510565162951535312, 1.000000000000000000, 0.9510565162951535312, 1.000000000000000000, 0.9510565162951535312, 1.000000000000000000, 0.9510565162951535312, 1.000000000000000000, 0.9510565162951535312, 1.000000000000000000, 0.9510565162951535312, 1.000000000000000000, 0.9510565162951535312, 1.000000000000000000, 0.9510565162951535312, 1.000000000000000000, 0.9510565162951535312, 1.000000000000000000, 0.9510565162951535312, 1.000000000000000000, 0.9510565162951535312, 1.000000000000000000, 0.9510565162951535312, 1.000000000000000000, 0.9510565162951535312, 1.000000000000000000, 0.9510565162951535312, 1.000000000000000000, 0.9510565162951535312, 1.000000000000000000, 0.9510565162951535312, 1.000000000000000000, 0.9510565162951535312, 1.000000000000000000, 0.9510565162951535312, 1.000000000000000000, 0.9510565162951535312, 1.000000000000000000, 0.9510565162951535312, 1.000000000000000000, 0.9510565162951535312, 1.000000000000000000, 0.9510565162951535312, 1.000000000000000000, 0.9510565162951535312, 1.000000000000000000, 0.9510565162951535312, 1.000000000000000000, 0.9510565162951535312, 1.000000000000000000, 0.9510565162951535312, 1.000000000000000000, 0.9510565162951535312, 1.000000000000000000, 0.9510565162951535312, 1.000000000000000000, 0.9510565162951535312, 1.000000000000000000, 0.9510565162951535312, 1.000000000000000000, 0.9510565162951535312, 1.000000000000000000, 0.9510565162951535312, 1.000000000000000000, 0.9510565162951535312, 1.000000000000000000, 0.9510565162951535312, 1.000000000000000000, 0.9510565162951535312, 1.000000000000000000, 0.9510565162951535312, 1.000000000000000000, 0.9510565162951535312, 1.000000000000000000, 0.9510565162951535312, 1.000000000000000000, 0.9510565162951535312, 1.000000000000000000, 0.9510565162951535312, 1.000000000000000000, 0.9510565162951535312, 1.000000000000000000, 0.9510565162951535312, 1.000000000000000000, 0.9510565162951535312, 1.000000000000000000, 0.9510565162951535312, 1.000000000000000000, 0.9510565162951535312, 1.000000000000000000, 0.9510565162951535312, 1.000000000000000000, 0.9510565162951535312, 1.000000000000000000, 0.9510565162951535312, 1.000000000000000000, 0.9510565162951535312, 1.000000000000000000, 0.9510565162951535312, 1.000000000000000000, 0.9510565162951535312, 1.000000000000000000, 0.9510565162951535312, 1.000000000000000000, 0.9510565162951535312, 1.000000000000000000, 0.9510565162951535312, 1.000000000000000000, 0.9510565162951535312, 1.000000000000000000, 0.9510565162951535312, 1.000000000000000000, 0.9510565162951535312, 1.000000000000000000, 0.9510565162951535312, 1.000000000000000000, 0.9510565162951535312, 1.000000000000000000, 0.9510565162951535312, 1.000000000000000000, 0.9510565162951535312, 1.000000000000000000, 0.9510565162951535312, 1.000000000000000000, 0.9510565162951535312, 1.000000000000000000, 0.9510565162951535312, 1.000000000000000000, 0.9510565162951535312, 1.000000000000000000, 0.9510565162951535312, 1.000000000000000000, 0.9510565162951535312, 1.000000000000000000, 0.9510565162951535312, 1.000000000000000000, 0.9510565162951535312, 1.000000000000000000, 0.9510565162951535312, 1.000000000000000000, 0.9510565162951535312, 1.000000000000000000, 0.9510565162951535312, 1.000000000000000000, 0.9510565162951535312, 1.000000000000000000, 0.9510565162951535312, 1.000000000000000000, 0.9510565162951535312, 1.000000000000000000, 0.9510565162951535312, 1.000000000000000000, 0.9510565162951535312, 1.000000000000000000, 0.9510565162951535312, 1.000000000000000000, 0.9510565162951535312, 1.000000000000000000, 0.9510565162951535312, 1.000000000000000000, 0.9510565162951535312, 1.000000000000000000, 0.9510565162951535312, 1.000000000000000000, 0.9510565162951535312, 1.000000000000000000, 0.9510565162951535312, 1.000000000000000000, 0.9510565162951535312, 1.000000000000000000, 0.9510565162951535312, 1.000000000000000000, 0.9510565162951535312, 1.000000000000000000, 0.9510565162951535312, 1.000000000000000000, 0.9510565162951535312, 1.000000000000000000, 0.9510565162951535312, 1.000000000000000000, 0.9510565162951535312, 1.000000000000000000, 0.9510565162951535312, 1.000000000000000000, 0.9510565162951535312, 1.000000000000000000, 0.9510565162951535312, 1.000000000000000000, 0.9510565162951535312, 1.000000000000000000, 0.9510565162951535312, 1.000000000000000000, 0.9510565162951535312, 1.000000000000000000, 0.9510565162951535312, 1.000000000000000000, 0.9510565162951535312, 1.000000000000000000, 0.9510565162951535312, 1.000000000000000000, 0.9510565162951535312, 1.000000000000000000, 0.9510565162951535312, 1.000000000000000000, 0.9510565162951535312, 1.000000000000000000, 0.9510565162951535312, 1.000000000000000000, 0.9510565162951535312, 1.000000000000000000, 0.9510565162951535312, 1.000000000000000000, 0.9510565162951535312, 1.000000000000000000, 0.9510565162951535312, 1.000000000000000000, 0.9510565162951535312, 1.000000000000000000, 0.9510565162951535312, 1.000000000000000000, 0.9510565162951535312, 1.000000000000000000, 0.9510565162951535312, 1.000000000000000000, 0.9510565162951535312, 1.000000000000000000, 0.9510565162951535312, 1.000000000000000000, 0.9510565162951535312, 1.000000000000000000, 0.9510565162951535312, 1.000000000000000000, 0.9510565162951535312, 1.000000000000000000, 0.9510565162951535312, 1.000000000000000000, 0.9510565162951535312, 1.000000000000000000, 0.9510565162951535312, 1.000000000000000000, 0.9510565162951535312, 1.000000000000000000, 0.9510565162951535312, 1.000000000000000000, 0.9510565162951535312, 1.000000000000000000, 0.9510565162951535312, 1.000000000000000000, 0.9510565162951535312, 1.000000000000000000, 0.9510565162951535312, 1.000000000000000000, 0.9510565162951535312, 1.000000000000000000, 0.9510565162951535312, 1.000000000000000000, 0.9510565162951535312, 1.000000000000000000, 0.9510565162951535312, 1.000000000000000000, 0.9510565162951535312, 1.000000000000000000, 0.9510565162951535312, 1.000000000000000000, 0.9510565162951535312, 1.000000000000000000, 0.9510565162951535312, 1.000000000000000000, 0.9510565162951535312, 1.000000000000000000, 0.9510565162951535312, 1.000000000000000000, 0.9510565162951535312, 1.000000000000000000, 0.9510565162951535312, 1.000000000000000000, 0.9510565162951535312, 1.000000000000000000, 0.9510565162951535312, 1.000000000000000000, 0.9510565162951535312, 1.000000000000000000, 0.9510565162951535312, 1.000000000000000000, 0.9510565162951535312, 1.000000000000000000, 0.9510565162951535312, 1.000000000000000000, 0.9510565162951535312, 1.000000000000000000, 0.9510565162951535312, 1.000000000000000000, 0.9510565162951535312, 1.000000000000000000, 0.9510565162951535312, 1.000000000000000000, 0.9510565162951535312, 1.000000000000000000, 0.9510565162951535312, 1.000000000000000000, 0.9510565162951535312, 1.000000000000000000, 0.9510565162951535312, 1.000000000000000000, 0.9510565162951535312, 1.000000000000000000, 0.9510565162951535312, 1.000000000000000000, 0.9510565162951535312, 1.000000000000000000, 0.9510565162951535312, 1.000000000000000000, 0.9510565162951535312, 1.000000000000000000, 0.9510565162951535312, 1.000000000000000000, 0.9510565162951535312, 1.000000000000000000, 0.9510565162951535312, 1.000000000000000000, 0.9510565162951535312, 1.000000000000000000, 0.9510565162951535312, 1.000000000000000000, 0.9510565162951535312, 1.000000000000000000, 0.9510565162951535312, 1.000000000000000000, 0.9510565162951535312, 1.000000000000000000, 0.9510565162951535312, 1.000000000000000000, 0.9510565162951535312, 1.000000000000000000, 0.9510565162951535312, 1.000000000000000000, 0.9510565162951535312, 1.000000000000000000, 0.9510565162951535312, 1.000000000000000000, 0.9510565162951535312, 1.000000000000000000, 0.9510565162951535312, 1.000000000000000000, 0.9510565162951535312, 1.000000000000000000, 0.9510565162951535312, 1.000000000000000000, 0.9510565162951535312, 1.000000000000000000, 0.9510565162951535312, 1.000000000000000000, 0.9510565162951535312, 1.000000000000000000, 0.9510565162951535312, 1.000000000000000000, 0.9510565162951535312, 1.000000000000000000, 0.9510565162951535312, 1.000000000000000000, 0.9510565162951535312, 1.000000000000000000, 0.9510565162951535312, 1.000000000000000000, 0.9510565162951535312, 1.000000000000000000, 0.9510565162951535312, 1.000000000000000000, 0.9510565162951535312, 1.000000000000000000, 0.9510565162951535312, 1.000000000000000000, 0.9510565162951535312, 1.000000000000000000, 0.9510565162951535312, 1.000000000000000000, 0.9510565162951535312, 1.000000000000000000, 0.9510565162951535312, 1.000000000000000000, 0.9510565162951535312, 1.000000000000000000, 0.9510565162951535312, 1.000000000000000000, 0.9510565162951535312, 1.000000000000000000, 0.9510565162951535312, 1.000000000000000000, 0.9510565162951535312, 1.000000000000000000, 0.9510565162951535312, 1.000000000000000000, 0.9510565162951535312, 1.000000000000000000, 0.9510565162951535312, 1.000000000000000000, 0.9510565162951535312, 1.000000000000000000, 0.9510565162951535312, 1.000000000000000000, 0.9510565162951535312, 1.000000000000000000, 0.9510565162951535312, 1.000000000000000000, 0.9510565162951535312, 1.000000000000000000, 0.9510565162951535312, 1.000000000000000000, 0.9510565162951535312, 1.000000000000000000, 0.9510565162951535312, 1.000000000000000000, 0.9510565162951535312, 1.000000000000000000, 0.9510565162951535312, 1.000000000000000000, 0.9510565162951535312, 1.000000000000000000, 0.9510565162951535312, 1.000000000000000000, 0.9510565162951535312, 1.000000000000000000, 0.9510565162951535312, 1.000000000000000000, 0.9510565162951535312, 1.000000000000000000, 0.9510565162951535312, 1.000000000000000000, 0.9510565162951535312, 1.000000000000000000, 0.9510565162951535312, 1.000000000000000000, 0.9510565162951535312, 1.000000000000000000, 0.9510565162951535312, 1.000000000000000000, 0.9510565162951535312, 1.000000000000000000, 0.9510565162951535312, 1.000000000000000000, 0.9510565162951535312, 1.000000000000000000, 0.9510565162951535312, 1.000000000000000000, 0.9510565162951535312, 1.000000000000000000, 0.9510565162951535312, 1.000000000000000000, 0.9510565162951535312, 1.000000000000000000, 0.9510565162951535312, 1.000000000000000000, 0.9510565162951535312, 1.000000000000000000, 0.9510565162951535312, 1.000000000000000000, 0.9510565162951535312, 1.000000000000000000, 0.9510565162951535312, 1.000000000000000000, 0.9510565162951535312, 1.000000000000000000, 0.9510565162951535312, 1.000000000000000000, 0.9510565162951535312, 1.000000000000000000, 0.9510565162951535312, 1.000000000000000000, 0.9510565162951535312, 1.000000000000000000, 0.9510565162951535312, 1.000000000000000000, 0.9510565162951535312, 1.000000000000000000, 0.9510565162951535312, 1.000000000000000000, 0.9510565162951535312, 1.000000000000000000, 0.9510565162951535312, 1.000000000000000000, 0.9510565162951535312, 1.000000000000000000, 0.9510565162951535312, 1.000000000000000000, 0.9510565162951535312, 1.000000000000000000, 0.9510565162951535312, 1.000000000000000000, 0.9510565162951535312, 1.000000000000000000, 0.9510565162951535312, 1.000000000000000000, 0.9510565162951535312, 1.000000000000000000, 0.9510565162951535312, 1.000000000000000000, 0.9510565162951535312, 1.000000000000000000, 0.9510565162951535312, 1.000000000000000000, 0.9510565162951535312, 1.000000000000000000, 0.9510565162951535312, 1.000000000000000000, 0.9510565162951535312, 1.000000000000000000, 0.9510565162951535312, 1.000000000000000000, 0.9510565162951535312, 1.000000000000000000, 0.9510565162951535312, 1.000000000000000000, 0.9510565162951535312, 1.000000000000000000, 0.9510565162951535312, 1.000000000000000000, 0.9510565162951535312, 1.000000000000000000, 0.9510565162951535312, 1.000000000000000000, 0.9510565162951535312, 1.000000000000000000, 0.9510565162951535312, 1.000000000000000000, 0.9510565162951535312, 1.000000000000000000, 0.9510565162951535312, 1.000000000000000000, 0.9510565162951535312, 1.000000000000000000, 0.9510565162951535312, 1.000000000000000000, 0.9510565162951535312, 1.000000000000000000, 0.9510565162951535312, 1.000000000000000000, 0.9510565162951535312, 1.000000000000000000, 0.9510565162951535312, 1.000000000000000000, 0.9510565162951535312, 1.000000000000000000, 0.9510565162951535312, 1.000000000000000000, 0.9510565162951535312, 1.000000000000000000, 0.9510565162951535312, 1.000000000000000000, 0.9510565162951535312, 1.000000000000000000, 0.9510565162951535312, 1.000000000000000000, 0.9510565162951535312, 1.000000000000000000, 0.9510565162951535312, 1.000000000000000000, 0.9510565162951535312, 1.000000000000000000, 0.9510565162951535312, 1.000000000000000000, 0.9510565162951535312, 1.000000000000000000, 0.9510565162951535312, 1.000000000000000000, 0.9510565162951535312, 1.000000000000000000, 0.9510565162951535312, 1.000000000000000000, 0.9510565162951535312, 1.000000000000000000, 0.9510565162951535312, 1.000000000000000000, 0.9510565162951535312, 1.000000000000000000, 0.9510565162951535312, 1.000000000000000000, 0.9510565162951535312, 1.000000000000000000, 0.9510565162951535312, 1.000000000000000000, 0.9510565162951535312, 1.000000000000000000, 0.9510565162951535312, 1.000000000000000000, 0.9510565162951535312, 1.000000000000000000, 0.9510565162951535312, 1.000000000000000000) ) ) 
 REPRESENTATION_ITEM ( '' )  SURFACE ( )  );
#31914=AXIS2_PLACEMENT_3D ( 'NONE', #57399, #20816, #9223 ) ;
#31928=CARTESIAN_POINT ( 'NONE',  ( -168.9549999999999841, -7.632228543268599452, 2.479861379858951054 ) ) ;
#31931=CARTESIAN_POINT ( 'NONE',  ( -48.20707362346614389, 3.094860106618433360, 9.524999999999991473 ) ) ;
#31933=CARTESIAN_POINT ( 'NONE',  ( -164.9949999999999761, -6.826472737025113702, 4.959722759717902107 ) ) ;
#31938=CARTESIAN_POINT ( 'NONE',  ( -81.20499999999999829, -2.607480562269071545, -8.024999999999991473 ) ) ;
#31944=CARTESIAN_POINT ( 'NONE',  ( -79.04499999999998749, 7.632228543268600340, 2.479861379858949277 ) ) ;
#31946=CARTESIAN_POINT ( 'NONE',  ( -135.0570736234661808, 0.000000000000000000, 9.524999999999991473 ) ) ;
#31947=AXIS2_PLACEMENT_3D ( 'NONE', #8968, #51889, #63473 ) ;
#31962=VECTOR ( 'NONE', #64420, 1000.000000000000000 ) ;
#31970=CARTESIAN_POINT ( 'NONE',  ( -123.5049999999999955, -6.826472737025113702, -4.959722759717900331 ) ) ;
#31994=ORIENTED_EDGE ( 'NONE', *, *, #16573, .F. ) ;
#32002=CARTESIAN_POINT ( 'NONE',  ( -147.8050000000000068, -8.437984349512085203, 5.166775262442717831E-16 ) ) ;
#32003=CARTESIAN_POINT ( 'NONE',  ( -176.3070736234661808, -10.01517768586948698, 6.132527647946031529E-16 ) ) ;
#32015=CARTESIAN_POINT ( 'NONE',  ( -64.85499999999997556, 4.716976649647094177, 6.492361379858945902 ) ) ;
#32019=ADVANCED_FACE ( 'NONE', ( #55115 ), #49875, .T. ) ;
#32027=CARTESIAN_POINT ( 'NONE',  ( -97.64292637653380780, -5.598654528085801552, 7.705886871421367523 ) ) ;
#32033=AXIS2_PLACEMENT_3D ( 'NONE', #24158, #29063, #8348 ) ;
#32036=CARTESIAN_POINT ( 'NONE',  ( -108.5949999999999847, 2.607480562269072433, 8.024999999999991473 ) ) ;
#32038=CARTESIAN_POINT ( 'NONE',  ( -92.39499999999998181, -6.826472737025115478, -4.959722759717899443 ) ) ;
#32045=CARTESIAN_POINT ( 'NONE',  ( -138.1429263765338078, 5.598654528085800663, -7.705886871421367523 ) ) ;
#32047=CARTESIAN_POINT ( 'NONE',  ( -147.7449999999999761, 4.716976649647094177, 6.492361379858945902 ) ) ;
#32050=CARTESIAN_POINT ( 'NONE',  ( -66.95707362346617231, 9.058813317711329915, -2.943386871421373119 ) ) ;
#32064=CARTESIAN_POINT ( 'NONE',  ( -150.9550000000000125, -7.632228543268599452, 2.479861379858951054 ) ) ;
#32078=CARTESIAN_POINT ( 'NONE',  ( -66.65499999999998693, -7.632228543268600340, -2.479861379858950166 ) ) ;
#32080=CARTESIAN_POINT ( 'NONE',  ( -116.5450000000000017, -7.632228543268600340, -2.479861379858950166 ) ) ;
#32093=CARTESIAN_POINT ( 'NONE',  ( -171.9549999999999841, -7.632228543268599452, 2.479861379858951054 ) ) ;
#32095=CARTESIAN_POINT ( 'NONE',  ( -87.50707362346615525, 8.102448949553176405, 5.886773742842740909 ) ) ;
#32099=DIRECTION ( 'NONE',  ( 0.000000000000000000, -1.000000000000000000, 0.000000000000000000 ) ) ;
#32106=CARTESIAN_POINT ( 'NONE',  ( -93.80499999999999261, -8.437984349512085203, 5.166775262442717831E-16 ) ) ;
#32112=CARTESIAN_POINT ( 'NONE',  ( -131.0070736234661410, -8.102448949553172852, -5.886773742842741797 ) ) ;
#32114=CARTESIAN_POINT ( 'NONE',  ( -63.05707362346617373, 0.000000000000000000, 9.524999999999991473 ) ) ;
#32115=EDGE_CURVE ( 'NONE', #1748, #2564, #69495, .T. ) ;
#32116=CARTESIAN_POINT ( 'NONE',  ( -80.99292637653380211, 8.102448949553172852, -5.886773742842744461 ) ) ;
#32120=CARTESIAN_POINT ( 'NONE',  ( -112.1049999999999756, -6.826472737025115478, 4.959722759717900331 ) ) ;
#32122=CARTESIAN_POINT ( 'NONE',  ( -114.1449999999999960, -4.716976649647092401, 6.492361379858946790 ) ) ;
#32127=CARTESIAN_POINT ( 'NONE',  ( -153.2070736234665844, 3.094860106624618190, 9.524999999995499067 ) ) ;
#32129=CARTESIAN_POINT ( 'NONE',  ( -163.0429263765338135, -9.058813317711329915, -2.943386871421370898 ) ) ;
#32130=CARTESIAN_POINT ( 'NONE',  ( -173.3950000000000102, -6.826472737025115478, -4.959722759717899443 ) ) ;
#32136=CARTESIAN_POINT ( 'NONE',  ( -75.89292637653379359, -8.102448949553172852, -5.886773742842741797 ) ) ;
#32138=CARTESIAN_POINT ( 'NONE',  ( -166.4929263765338021, -8.102448949553174629, 5.886773742842742685 ) ) ;
#32145=CARTESIAN_POINT ( 'NONE',  ( -183.8050000000000068, -8.437984349512086979, 5.166775262442717831E-16 ) ) ;
#32146=EDGE_LOOP ( 'NONE', ( #37569, #44750, #38880, #5835 ) ) ;
#32155=CARTESIAN_POINT ( 'NONE',  ( -97.10499999999998977, -6.826472737025113702, 4.959722759717902107 ) ) ;
#32170=CARTESIAN_POINT ( 'NONE',  ( -72.44499999999997897, 0.000000000000000000, 8.024999999999991473 ) ) ;
#32179=CARTESIAN_POINT ( 'NONE',  ( -119.1550000000000011, 7.632228543268600340, 2.479861379858949277 ) ) ;
#32184=CARTESIAN_POINT ( 'NONE',  ( -160.0429263765338135, -9.058813317711329915, -2.943386871421370898 ) ) ;
#32186=CARTESIAN_POINT ( 'NONE',  ( -160.8570736234661922, -5.598654528085803328, -7.705886871421366635 ) ) ;
#32188=CARTESIAN_POINT ( 'NONE',  ( -97.10707362346617799, 8.102448949553171076, -5.886773742842744461 ) ) ;
#32198=CARTESIAN_POINT ( 'NONE',  ( -137.9049999999999727, 2.607480562269068880, -8.024999999999993250 ) ) ;
#32202=CARTESIAN_POINT ( 'NONE',  ( -145.4949999999999477, 6.826472737025113702, -4.959722759717902107 ) ) ;
#32204=CARTESIAN_POINT ( 'NONE',  ( -140.6949999999999648, -8.437984349512086979, 5.166775262442717831E-16 ) ) ;
#32209=CARTESIAN_POINT ( 'NONE',  ( -54.05499999999999261, -9.827790563157499189E-16, -8.024999999999991473 ) ) ;
#32212=CARTESIAN_POINT ( 'NONE',  ( -138.5929263765343649, -3.094860106628043894, -9.524999999993006838 ) ) ;
#32215=CARTESIAN_POINT ( 'NONE',  ( -108.8929263765338078, -8.102448949553172852, -5.886773742842741797 ) ) ;
#32217=CARTESIAN_POINT ( 'NONE',  ( -153.2929263765341830, 3.094860106611874162, -9.525000000004759215 ) ) ;
#32232=EDGE_LOOP ( 'NONE', ( #56558, #863, #64315, #39363 ) ) ;
#32235=DIRECTION ( 'NONE',  ( 0.000000000000000000, 0.000000000000000000, 1.000000000000000000 ) ) ;
#32241=CARTESIAN_POINT ( 'NONE',  ( -184.0000000000000000, -7.358988424933670558, 3.200923985616050071 ) ) ;
#32244=CARTESIAN_POINT ( 'NONE',  ( -98.54499999999998749, -7.632228543268600340, -2.479861379858950166 ) ) ;
#32247=EDGE_CURVE ( 'NONE', #9325, #16622, #26896, .T. ) ;
#32255=CARTESIAN_POINT ( 'NONE',  ( -62.30707362346616662, -10.01517768586948698, 6.132527647946031529E-16 ) ) ;
#32257=CARTESIAN_POINT ( 'NONE',  ( -166.2570736234661695, 5.598654528085800663, -7.705886871421367523 ) ) ;
#32268=CYLINDRICAL_SURFACE ( 'NONE', #65972, 9.524999999999991473 ) ;
#32270=CARTESIAN_POINT ( 'NONE',  ( -167.3049999999999784, 8.437984349512085203, -1.550032578732815448E-15 ) ) ;
#32274=CARTESIAN_POINT ( 'NONE',  ( -174.8950000000000102, 6.826472737025116366, 4.959722759717898555 ) ) ;
#32275=CARTESIAN_POINT ( 'NONE',  ( -166.3449999999999989, 7.632228543268599452, -2.479861379858951942 ) ) ;
#32278=CARTESIAN_POINT ( 'NONE',  ( -89.54292637653379927, 9.058813317711329915, 2.943386871421369566 ) ) ;
#32279=CARTESIAN_POINT ( 'NONE',  ( -15.00000000000000000, 10.90871211463571200, -5.000000000000000000 ) ) ;
#32280=CARTESIAN_POINT ( 'NONE',  ( -80.00500000000000966, 6.826472737025116366, 4.959722759717898555 ) ) ;
#32281=FACE_OUTER_BOUND ( 'NONE', #17469, .T. ) ;
#32282=CARTESIAN_POINT ( 'NONE',  ( -168.3570736234661922, 5.598654528085804216, 7.705886871421366635 ) ) ;
#32286=CARTESIAN_POINT ( 'NONE',  ( -82.94499999999999318, -9.827790563157499189E-16, -8.024999999999991473 ) ) ;
#32289=CARTESIAN_POINT ( 'NONE',  ( -134.0070736234661695, -8.102448949553174629, -5.886773742842741797 ) ) ;
#32308=CARTESIAN_POINT ( 'NONE',  ( -45.00000000000000000, 1.166476076187854022E-15, -9.525000000000000355 ) ) ;
#32310=CARTESIAN_POINT ( 'NONE',  ( -111.3549999999999898, -4.716976649647093289, -6.492361379858945902 ) ) ;
#32313=EDGE_CURVE ( 'NONE', #3787, #29002, #34983, .T. ) ;
#32319=( BOUNDED_CURVE ( )  B_SPLINE_CURVE ( 2, ( #40039, #66738, #18556, #41072, #14662, #26572, #16072, #53661, #31505, #21657, #36840 ),
 .UNSPECIFIED., .F., .F. ) 
 B_SPLINE_CURVE_WITH_KNOTS ( ( 3, 2, 2, 2, 2, 3 ),
 ( 0.1956521739130388515, 0.1978260869565170443, 0.1999999999999952649, 0.2021739130434734855, 0.2043478260869517060, 0.2065217391304298988 ),
 .UNSPECIFIED. ) 
 CURVE ( )  GEOMETRIC_REPRESENTATION_ITEM ( )  RATIONAL_B_SPLINE_CURVE ( ( 1.000000000000104361, 0.9510565162950492812, 1.000000000000000000, 0.9510565162951535312, 1.000000000000000000, 0.9510565162951535312, 1.000000000000000000, 0.9510565162951535312, 1.000000000000000000, 0.9510565162952635543, 0.9999999999998899769 ) ) 
 REPRESENTATION_ITEM ( '' )  );
#32326=CARTESIAN_POINT ( 'NONE',  ( -130.9429263765338192, 0.000000000000000000, 9.524999999999991473 ) ) ;
#32337=CARTESIAN_POINT ( 'NONE',  ( -50.54292637653379217, 9.058813317711329915, 2.943386871421369566 ) ) ;
#32340=CARTESIAN_POINT ( 'NONE',  ( -140.3049999999999500, 8.437984349512085203, -1.550032578732815448E-15 ) ) ;
#32343=SURFACE_STYLE_USAGE ( .BOTH. , #37690 ) ;
#32348=CARTESIAN_POINT ( 'NONE',  ( -60.95499999999998408, -7.632228543268599452, 2.479861379858951054 ) ) ;
#32360=CARTESIAN_POINT ( 'NONE',  ( -107.6949999999999790, -8.437984349512086979, 5.166775262442717831E-16 ) ) ;
#32362=CARTESIAN_POINT ( 'NONE',  ( -86.54499999999998749, -7.632228543268600340, -2.479861379858950166 ) ) ;
#32364=VECTOR ( 'NONE', #69020, 1000.000000000000000 ) ;
#32369=CARTESIAN_POINT ( 'NONE',  ( -132.2929263765338135, 3.094860106618428031, -9.524999999999993250 ) ) ;
#32370=CARTESIAN_POINT ( 'NONE',  ( -148.1950000000000216, 8.437984349512085203, -1.550032578732815448E-15 ) ) ;
#32378=CARTESIAN_POINT ( 'NONE',  ( -132.6570736234661751, 9.058813317711329915, 2.943386871421369566 ) ) ;
#32382=CARTESIAN_POINT ( 'NONE',  ( -117.1429263765337936, 5.598654528085800663, -7.705886871421367523 ) ) ;
#32385=CARTESIAN_POINT ( 'NONE',  ( -151.4049999999999443, -2.607480562269069768, 8.024999999999991473 ) ) ;
#32400=CARTESIAN_POINT ( 'NONE',  ( -62.15499999999998693, 7.632228543268600340, 2.479861379858949277 ) ) ;
#32402=CARTESIAN_POINT ( 'NONE',  ( -123.5949999999999704, 2.607480562269073321, 8.024999999999991473 ) ) ;
#32413=FACE_OUTER_BOUND ( 'NONE', #45210, .T. ) ;
#32417=CARTESIAN_POINT ( 'NONE',  ( -176.4550000000000125, 7.632228543268599452, -2.479861379858951942 ) ) ;
#32421=( BOUNDED_CURVE ( )  B_SPLINE_CURVE ( 2, ( #4088, #15059, #10450, #48115, #5146, #62846, #14686, #26592, #4434, #36158, #25554 ),
 .UNSPECIFIED., .F., .F. ) 
 B_SPLINE_CURVE_WITH_KNOTS ( ( 3, 2, 2, 2, 2, 3 ),
 ( 0.5326086956521615123, 0.5347826086956397607, 0.5369565217391178980, 0.5391304347825961463, 0.5413043478260742836, 0.5434782608695525319 ),
 .UNSPECIFIED. ) 
 CURVE ( )  GEOMETRIC_REPRESENTATION_ITEM ( )  RATIONAL_B_SPLINE_CURVE ( ( 1.000000000000279998, 0.9510565162948735329, 1.000000000000000000, 0.9510565162951535312, 1.000000000000000000, 0.9510565162951535312, 1.000000000000000000, 0.9510565162951535312, 1.000000000000000000, 0.9510565162954385254, 0.9999999999997150057 ) ) 
 REPRESENTATION_ITEM ( '' )  );
#32428=CARTESIAN_POINT ( 'NONE',  ( -85.85499999999998977, 4.716976649647094177, 6.492361379858945902 ) ) ;
#32433=CARTESIAN_POINT ( 'NONE',  ( -61.10707362346615668, 8.102448949553171076, -5.886773742842744461 ) ) ;
#32440=CARTESIAN_POINT ( 'NONE',  ( -108.5049999999999812, -6.826472737025115478, -4.959722759717899443 ) ) ;
#32442=CARTESIAN_POINT ( 'NONE',  ( -111.7449999999999903, 4.716976649647094177, 6.492361379858945902 ) ) ;
#32446=CARTESIAN_POINT ( 'NONE',  ( -165.2929263765338135, 3.094860106618428031, -9.524999999999993250 ) ) ;
#32447=CARTESIAN_POINT ( 'NONE',  ( -177.4449999999999932, 0.000000000000000000, 8.024999999999991473 ) ) ;
#32453=CARTESIAN_POINT ( 'NONE',  ( -61.49292637653379501, -8.102448949553174629, 5.886773742842742685 ) ) ;
#32456=CARTESIAN_POINT ( 'NONE',  ( -74.24292637653380211, 5.598654528085804216, 7.705886871421366635 ) ) ;
#32461=EDGE_CURVE ( 'NONE', #63556, #60379, #1168, .T. ) ;
#32463=CARTESIAN_POINT ( 'NONE',  ( -148.5570736234661808, -1.166476076187852838E-15, -9.524999999999991473 ) ) ;
#32466=CARTESIAN_POINT ( 'NONE',  ( -182.6049999999999613, 6.826472737025113702, -4.959722759717902107 ) ) ;
#32480=CARTESIAN_POINT ( 'NONE',  ( -95.30499999999997840, 8.437984349512086979, -1.550032578732815448E-15 ) ) ;
#32485=CARTESIAN_POINT ( 'NONE',  ( -127.7929263765345240, -3.094860106606396322, 9.525000000008734702 ) ) ;
#32491=CARTESIAN_POINT ( 'NONE',  ( -63.29499999999998749, -2.607480562269069768, 8.024999999999991473 ) ) ;
#32493=CARTESIAN_POINT ( 'NONE',  ( -49.64292637653380780, -5.598654528085801552, 7.705886871421367523 ) ) ;
#32501=CARTESIAN_POINT ( 'NONE',  ( -115.5549999999999926, 0.000000000000000000, 8.024999999999991473 ) ) ;
#32503=CARTESIAN_POINT ( 'NONE',  ( -73.64292637653380780, -5.598654528085801552, 7.705886871421367523 ) ) ;
#32508=CARTESIAN_POINT ( 'NONE',  ( -160.5570736234661808, -1.166476076187852838E-15, -9.524999999999991473 ) ) ;
#32511=CARTESIAN_POINT ( 'NONE',  ( -96.65707362346617515, 9.058813317711329915, 2.943386871421369566 ) ) ;
#32521=CARTESIAN_POINT ( 'NONE',  ( -144.5049999999999670, -6.826472737025115478, -4.959722759717899443 ) ) ;
#32525=CARTESIAN_POINT ( 'NONE',  ( -146.9950000000000045, -6.826472737025115478, 4.959722759717900331 ) ) ;
#32527=CARTESIAN_POINT ( 'NONE',  ( -136.3449999999999989, 7.632228543268599452, -2.479861379858951942 ) ) ;
#32532=LINE ( 'NONE', #22697, #26023 ) ;
#32534=CARTESIAN_POINT ( 'NONE',  ( -53.30499999999998550, 8.437984349512085203, -1.550032578732815448E-15 ) ) ;
#32537=CARTESIAN_POINT ( 'NONE',  ( -58.94499999999998607, -9.827790563157499189E-16, -8.024999999999991473 ) ) ;
#32539=CARTESIAN_POINT ( 'NONE',  ( -103.4070736234671699, 3.094860106602026040, -9.525000000011910828 ) ) ;
#32544=CARTESIAN_POINT ( 'NONE',  ( -106.1929263765338050, -10.01517768586948698, 6.132527647946031529E-16 ) ) ;
#32547=CARTESIAN_POINT ( 'NONE',  ( -184.0000000000000000, 0.000000000000000000, -8.524999999999977263 ) ) ;
#32566=DIRECTION ( 'NONE',  ( 0.000000000000000000, 0.000000000000000000, 1.000000000000000000 ) ) ;
#32567=CARTESIAN_POINT ( 'NONE',  ( -81.44292637653380496, -1.166476076187852838E-15, -9.524999999999991473 ) ) ;
#32568=VERTEX_POINT ( 'NONE', #26812 ) ;
#32574=CARTESIAN_POINT ( 'NONE',  ( -90.29499999999997328, -2.607480562269069768, 8.024999999999991473 ) ) ;
#32580=CARTESIAN_POINT ( 'NONE',  ( -175.1929263765337623, -10.01517768586948698, 6.132527647946031529E-16 ) ) ;
#32584=VERTEX_POINT ( 'NONE', #10680 ) ;
#32591=DIRECTION ( 'NONE',  ( -1.000000000000000000, -0.000000000000000000, -0.000000000000000000 ) ) ;
#32594=CARTESIAN_POINT ( 'NONE',  ( -69.29292637653378506, 3.094860106618428031, -9.524999999999993250 ) ) ;
#32602=CARTESIAN_POINT ( 'NONE',  ( -170.6050000000000182, 6.826472737025113702, -4.959722759717902107 ) ) ;
#32606=CARTESIAN_POINT ( 'NONE',  ( -173.0949999999999989, -2.607480562269071545, -8.024999999999991473 ) ) ;
#32608=CARTESIAN_POINT ( 'NONE',  ( -164.2450000000000045, -4.716976649647093289, -6.492361379858945902 ) ) ;
#32617=CARTESIAN_POINT ( 'NONE',  ( -84.05499999999999261, -9.827790563157499189E-16, -8.024999999999991473 ) ) ;
#32622=CARTESIAN_POINT ( 'NONE',  ( -82.79499999999998749, 2.607480562269069324, -8.024999999999993250 ) ) ;
#32632=CARTESIAN_POINT ( 'NONE',  ( -90.44292637653379074, -1.166476076187852838E-15, -9.524999999999991473 ) ) ;
#32636=CARTESIAN_POINT ( 'NONE',  ( -51.29292637653378506, 3.094860106618428031, -9.524999999999993250 ) ) ;
#32640=EDGE_CURVE ( 'NONE', #9643, #13980, #17541, .T. ) ;
#32651=CARTESIAN_POINT ( 'NONE',  ( -112.1049999999999756, -6.826472737025113702, 4.959722759717902107 ) ) ;
#32668=CARTESIAN_POINT ( 'NONE',  ( -14.33443387982028483, -10.92428437323945367, 4.966394326244869539 ) ) ;
#32680=CARTESIAN_POINT ( 'NONE',  ( -52.19292637653380496, -10.01517768586948698, 6.132527647946031529E-16 ) ) ;
#32684=CARTESIAN_POINT ( 'NONE',  ( -143.7549999999999955, 4.716976649647091513, -6.492361379858946790 ) ) ;
#32685=CARTESIAN_POINT ( 'NONE',  ( -176.9070736234662604, -3.094860106617245421, 9.525000000000854783 ) ) ;
#32688=CARTESIAN_POINT ( 'NONE',  ( -115.7949999999999875, 2.607480562269068880, -8.024999999999993250 ) ) ;
#32696=CARTESIAN_POINT ( 'NONE',  ( -54.20499999999997698, -2.607480562269071545, -8.024999999999991473 ) ) ;
#32708=AXIS2_PLACEMENT_3D ( 'NONE', #15022, #3702, #25198 ) ;
#32717=CARTESIAN_POINT ( 'NONE',  ( -108.2949999999999733, -2.607480562269069768, 8.024999999999991473 ) ) ;
#32719=CARTESIAN_POINT ( 'NONE',  ( -91.04499999999998749, 7.632228543268600340, 2.479861379858949277 ) ) ;
#32722=DIRECTION ( 'NONE',  ( 0.000000000000000000, 0.000000000000000000, -1.000000000000000000 ) ) ;
#32728=CARTESIAN_POINT ( 'NONE',  ( -120.8929263765338078, -8.102448949553172852, -5.886773742842741797 ) ) ;
#32730=CARTESIAN_POINT ( 'NONE',  ( -148.0449999999999875, 7.632228543268600340, 2.479861379858949277 ) ) ;
#32734=CARTESIAN_POINT ( 'NONE',  ( -46.79499999999996618, 2.607480562269069324, -8.024999999999993250 ) ) ;
#32738=( BOUNDED_CURVE ( )  B_SPLINE_CURVE ( 2, ( #26092, #68330, #25743, #30669, #35978, #14174, #8883, #3562, #57782, #15244, #14879 ),
 .UNSPECIFIED., .F., .F. ) 
 B_SPLINE_CURVE_WITH_KNOTS ( ( 3, 2, 2, 2, 2, 3 ),
 ( 0.9130434782608695121, 0.9152173913043478715, 0.9173913043478261198, 0.9195652173913043681, 0.9217391304347826164, 0.9239130434782608647 ),
 .UNSPECIFIED. ) 
 CURVE ( )  GEOMETRIC_REPRESENTATION_ITEM ( )  RATIONAL_B_SPLINE_CURVE ( ( 1.000000000000000000, 0.9510565162951535312, 1.000000000000000000, 0.9510565162951535312, 1.000000000000000000, 0.9510565162951535312, 1.000000000000000000, 0.9510565162951535312, 1.000000000000000000, 0.9510565162951535312, 1.000000000000000000 ) ) 
 REPRESENTATION_ITEM ( '' )  );
#32745=CARTESIAN_POINT ( 'NONE',  ( -50.90707362346616804, -3.094860106618429807, 9.524999999999991473 ) ) ;
#32748=CARTESIAN_POINT ( 'NONE',  ( -137.3049999999999784, 8.437984349512086979, -1.550032578732815448E-15 ) ) ;
#32765=CARTESIAN_POINT ( 'NONE',  ( -52.85499999999998266, 4.716976649647094177, 6.492361379858945902 ) ) ;
#32766=CARTESIAN_POINT ( 'NONE',  ( -118.1949999999999790, 8.437984349512085203, -1.550032578732815448E-15 ) ) ;
#32782=CARTESIAN_POINT ( 'NONE',  ( -175.7049999999999557, 2.607480562269073321, 8.024999999999991473 ) ) ;
#32789=CARTESIAN_POINT ( 'NONE',  ( -184.0000000000000000, -8.446573402700972011, 1.153699593821606140 ) ) ;
#32795=CARTESIAN_POINT ( 'NONE',  ( -85.25499999999998124, -4.716976649647092401, 6.492361379858946790 ) ) ;
#32796=VERTEX_POINT ( 'NONE', #17370 ) ;
#32803=CARTESIAN_POINT ( 'NONE',  ( -69.65707362346616094, 9.058813317711329915, 2.943386871421369566 ) ) ;
#32806=EDGE_LOOP ( 'NONE', ( #11912, #39031, #16657, #31265 ) ) ;
#32811=CARTESIAN_POINT ( 'NONE',  ( -105.8050000000000068, -8.437984349512085203, 5.166775262442717831E-16 ) ) ;
#32814=CARTESIAN_POINT ( 'NONE',  ( -118.4949999999999903, 6.826472737025113702, -4.959722759717902107 ) ) ;
#32821=CARTESIAN_POINT ( 'NONE',  ( -151.9429263765338192, 0.000000000000000000, 9.524999999999991473 ) ) ;
#32822=CARTESIAN_POINT ( 'NONE',  ( -172.7950000000000159, 2.607480562269068880, -8.024999999999993250 ) ) ;
#32830=CARTESIAN_POINT ( 'NONE',  ( -77.69292637653380496, 10.01517768586948698, -1.839758294383808571E-15 ) ) ;
#32839=CARTESIAN_POINT ( 'NONE',  ( -165.6550000000000011, -7.632228543268600340, -2.479861379858950166 ) ) ;
#32843=CYLINDRICAL_SURFACE ( 'NONE', #67948, 9.524999999999991473 ) ;
#32846=CARTESIAN_POINT ( 'NONE',  ( -182.1570736234661751, -9.058813317711329915, -2.943386871421370898 ) ) ;
#32848=( BOUNDED_CURVE ( )  B_SPLINE_CURVE ( 2, ( #8711, #34725, #56537, #19238, #24512, #29812, #18579, #40745, #46028, #2315, #67441 ),
 .UNSPECIFIED., .F., .F. ) 
 B_SPLINE_CURVE_WITH_KNOTS ( ( 3, 2, 2, 2, 2, 3 ),
 ( 0.2826086956521672300, 0.2847826086956454783, 0.2869565217391236711, 0.2891304347826018084, 0.2913043478260800012, 0.2934782608695582495 ),
 .UNSPECIFIED. ) 
 CURVE ( )  GEOMETRIC_REPRESENTATION_ITEM ( )  RATIONAL_B_SPLINE_CURVE ( ( 1.000000000000149880, 0.9510565162950035401, 1.000000000000000000, 0.9510565162951535312, 1.000000000000000000, 0.9510565162951535312, 1.000000000000000000, 0.9510565162951535312, 1.000000000000000000, 0.9510565162953109608, 0.9999999999998425704 ) ) 
 REPRESENTATION_ITEM ( '' )  );
#32852=CARTESIAN_POINT ( 'NONE',  ( -96.35499999999997556, -4.716976649647093289, -6.492361379858945902 ) ) ;
#32865=CARTESIAN_POINT ( 'NONE',  ( -64.79500000000000171, 2.607480562269068880, -8.024999999999993250 ) ) ;
#32866=VERTEX_POINT ( 'NONE', #55661 ) ;
#32878=CARTESIAN_POINT ( 'NONE',  ( -114.3549999999999898, -4.716976649647093289, -6.492361379858945902 ) ) ;
#32880=VERTEX_POINT ( 'NONE', #1439 ) ;
#32883=CARTESIAN_POINT ( 'NONE',  ( -73.79292637653378506, -3.094860106618429807, 9.524999999999991473 ) ) ;
#32885=CARTESIAN_POINT ( 'NONE',  ( -160.9429263765338192, 0.000000000000000000, 9.524999999999991473 ) ) ;
#32887=CARTESIAN_POINT ( 'NONE',  ( -153.3570736234661922, 5.598654528085804216, 7.705886871421366635 ) ) ;
#32891=EDGE_CURVE ( 'NONE', #52874, #57448, #22969, .T. ) ;
#32892=CARTESIAN_POINT ( 'NONE',  ( -98.30707362346616662, -10.01517768586948698, 6.132527647946031529E-16 ) ) ;
#32895=ORIENTED_EDGE ( 'NONE', *, *, #44732, .T. ) ;
#32901=CARTESIAN_POINT ( 'NONE',  ( -129.6550000000000011, -7.632228543268600340, -2.479861379858950166 ) ) ;
#32907=CARTESIAN_POINT ( 'NONE',  ( -141.4449999999999932, 0.000000000000000000, 8.024999999999991473 ) ) ;
#32909=CARTESIAN_POINT ( 'NONE',  ( -126.5949999999999847, 2.607480562269072433, 8.024999999999991473 ) ) ;
#32915=CARTESIAN_POINT ( 'NONE',  ( -53.90499999999997272, 2.607480562269068880, -8.024999999999993250 ) ) ;
#32918=CARTESIAN_POINT ( 'NONE',  ( -61.94499999999998607, -9.827790563157499189E-16, -8.024999999999991473 ) ) ;
#32923=CARTESIAN_POINT ( 'NONE',  ( -101.8429263765338106, 9.058813317711329915, -2.943386871421373119 ) ) ;
#32925=CARTESIAN_POINT ( 'NONE',  ( -163.5570736234661524, -1.166476076187852838E-15, -9.524999999999991473 ) ) ;
#32947=CARTESIAN_POINT ( 'NONE',  ( -118.8570736234661780, -5.598654528085803328, -7.705886871421366635 ) ) ;
#32949=CARTESIAN_POINT ( 'NONE',  ( -88.04499999999998749, 7.632228543268600340, 2.479861379858949277 ) ) ;
#32972=CARTESIAN_POINT ( 'NONE',  ( -68.84292637653379643, 9.058813317711329915, -2.943386871421373119 ) ) ;
#32980=CARTESIAN_POINT ( 'NONE',  ( -162.3549999999999898, -4.716976649647093289, -6.492361379858945902 ) ) ;
#32982=CARTESIAN_POINT ( 'NONE',  ( -148.1070736234661354, 8.102448949553172852, -5.886773742842744461 ) ) ;
#32983=CARTESIAN_POINT ( 'NONE',  ( -176.0949999999999704, -2.607480562269071545, -8.024999999999991473 ) ) ;
#32985=CARTESIAN_POINT ( 'NONE',  ( -169.1949999999999932, 8.437984349512086979, -1.550032578732815448E-15 ) ) ;
#32991=B_SPLINE_CURVE_WITH_KNOTS ( 'NONE', 1,
 ( #48320, #378 ),
 .UNSPECIFIED., .F., .F.,
 ( 2, 2 ),
 ( 0.000000000000000000, 1.000000000000000000 ),
 .UNSPECIFIED. ) ;
#32992=CARTESIAN_POINT ( 'NONE',  ( -87.65499999999998693, -7.632228543268600340, -2.479861379858950166 ) ) ;
#32994=CARTESIAN_POINT ( 'NONE',  ( -80.54499999999998749, -7.632228543268600340, -2.479861379858950166 ) ) ;
#32999=VECTOR ( 'NONE', #9107, 1000.000000000000000 ) ;
#33003=CARTESIAN_POINT ( 'NONE',  ( -50.54292637653379217, 9.058813317711329915, 2.943386871421369566 ) ) ;
#33017=CARTESIAN_POINT ( 'NONE',  ( -69.95707362346617231, 9.058813317711329915, -2.943386871421373119 ) ) ;
#33019=CARTESIAN_POINT ( 'NONE',  ( -110.9049999999999727, 2.607480562269069324, -8.024999999999993250 ) ) ;
#33031=ORIENTED_EDGE ( 'NONE', *, *, #10582, .T. ) ;
#33037=CARTESIAN_POINT ( 'NONE',  ( -129.4429263765338192, -1.166476076187852838E-15, -9.524999999999991473 ) ) ;
#33044=CARTESIAN_POINT ( 'NONE',  ( -105.4429263765338050, -1.166476076187852838E-15, -9.524999999999991473 ) ) ;
#33050=CARTESIAN_POINT ( 'NONE',  ( -48.14292637653380780, 5.598654528085800663, -7.705886871421367523 ) ) ;
#33053=CARTESIAN_POINT ( 'NONE',  ( -138.8050000000000068, -8.437984349512085203, 5.166775262442717831E-16 ) ) ;
#33059=CARTESIAN_POINT ( 'NONE',  ( -105.8929263765337936, -8.102448949553174629, -5.886773742842741797 ) ) ;
#33060=FILL_AREA_STYLE_COLOUR ( '', #66440 ) ;
#33064=EDGE_CURVE ( 'NONE', #35517, #33393, #2028, .T. ) ;
#33066=CARTESIAN_POINT ( 'NONE',  ( -54.65499999999997982, -7.632228543268600340, -2.479861379858950166 ) ) ;
#33074=CARTESIAN_POINT ( 'NONE',  ( -128.9929263765338021, 8.102448949553172852, -5.886773742842744461 ) ) ;
#33081=CARTESIAN_POINT ( 'NONE',  ( -107.0949999999999847, -2.607480562269071545, -8.024999999999991473 ) ) ;
#33083=CARTESIAN_POINT ( 'NONE',  ( -87.74499999999999034, 4.716976649647094177, 6.492361379858945902 ) ) ;
#33091=CARTESIAN_POINT ( 'NONE',  ( -126.5929263765337964, -3.094860106618431139, -9.524999999999991473 ) ) ;
#33093=CARTESIAN_POINT ( 'NONE',  ( -151.3449999999999989, 7.632228543268599452, -2.479861379858951942 ) ) ;
#33094=DIRECTION ( 'NONE',  ( 0.000000000000000000, 0.000000000000000000, 1.000000000000000000 ) ) ;
#33109=CARTESIAN_POINT ( 'NONE',  ( -142.7049999999999557, 2.607480562269072433, 8.024999999999991473 ) ) ;
#33115=VERTEX_POINT ( 'NONE', #22443 ) ;
#33117=AXIS2_PLACEMENT_3D ( 'NONE', #64238, #16096, #32235 ) ;
#33126=CARTESIAN_POINT ( 'NONE',  ( -50.90499999999997982, 2.607480562269069324, -8.024999999999993250 ) ) ;
#33127=CARTESIAN_POINT ( 'NONE',  ( -119.6950000000000074, -8.437984349512085203, 5.166775262442717831E-16 ) ) ;
#33142=CARTESIAN_POINT ( 'NONE',  ( -168.0550000000000068, -9.827790563157499189E-16, -8.024999999999991473 ) ) ;
#33153=EDGE_CURVE ( 'NONE', #56538, #55506, #61778, .T. ) ;
#33156=CARTESIAN_POINT ( 'NONE',  ( -90.05499999999997840, -9.827790563157499189E-16, -8.024999999999991473 ) ) ;
#33157=ORIENTED_EDGE ( 'NONE', *, *, #16044, .F. ) ;
#33159=CARTESIAN_POINT ( 'NONE',  ( -65.60707362346616378, -8.102448949553172852, 5.886773742842742685 ) ) ;
#33167=CARTESIAN_POINT ( 'NONE',  ( -102.3549999999999898, -4.716976649647093289, -6.492361379858945902 ) ) ;
#33170=CARTESIAN_POINT ( 'NONE',  ( -113.9949999999999903, -6.826472737025115478, 4.959722759717900331 ) ) ;
#33175=CARTESIAN_POINT ( 'NONE',  ( -153.7429263765338021, -5.598654528085803328, -7.705886871421366635 ) ) ;
#33177=CARTESIAN_POINT ( 'NONE',  ( -174.4449999999999932, 0.000000000000000000, 8.024999999999991473 ) ) ;
#33183=ORIENTED_EDGE ( 'NONE', *, *, #63536, .F. ) ;
#33184=CARTESIAN_POINT ( 'NONE',  ( -65.39292637653379359, 8.102448949553176405, 5.886773742842740909 ) ) ;
#33189=CARTESIAN_POINT ( 'NONE',  ( -142.3429263765338249, -9.058813317711329915, 2.943386871421371787 ) ) ;
#33193=CARTESIAN_POINT ( 'NONE',  ( -173.1550000000000011, 7.632228543268600340, 2.479861379858949277 ) ) ;
#33198=CYLINDRICAL_SURFACE ( 'NONE', #62169, 9.524999999999991473 ) ;
#33204=CARTESIAN_POINT ( 'NONE',  ( -79.70499999999996987, 2.607480562269072433, 8.024999999999991473 ) ) ;
#33214=CARTESIAN_POINT ( 'NONE',  ( -63.59499999999997755, 2.607480562269073321, 8.024999999999991473 ) ) ;
#33215=ORIENTED_EDGE ( 'NONE', *, *, #42934, .T. ) ;
#33216=CYLINDRICAL_SURFACE ( 'NONE', #64275, 9.524999999999991473 ) ;
#33220=DIRECTION ( 'NONE',  ( -1.000000000000000000, -0.000000000000000000, -0.000000000000000000 ) ) ;
#33223=CARTESIAN_POINT ( 'NONE',  ( -184.0000000000000000, 6.735557395310425260E-16, -5.499999999999985789 ) ) ;
#33225=CARTESIAN_POINT ( 'NONE',  ( -115.4049999999999727, -2.607480562269069768, 8.024999999999991473 ) ) ;
#33231=CARTESIAN_POINT ( 'NONE',  ( -146.7570736234661695, -5.598654528085801552, 7.705886871421367523 ) ) ;
#33234=CARTESIAN_POINT ( 'NONE',  ( -96.35707362346616378, 5.598654528085804216, 7.705886871421366635 ) ) ;
#33242=CARTESIAN_POINT ( 'NONE',  ( -132.8050000000000068, -8.437984349512085203, 5.166775262442717831E-16 ) ) ;
#33245=CARTESIAN_POINT ( 'NONE',  ( -149.9949999999999193, -6.826472737025115478, 4.959722759717900331 ) ) ;
#33246=CARTESIAN_POINT ( 'NONE',  ( -131.2450000000000045, -4.716976649647093289, -6.492361379858945902 ) ) ;
#33248=CARTESIAN_POINT ( 'NONE',  ( -87.44292637653380496, -1.166476076187852838E-15, -9.524999999999991473 ) ) ;
#33254=CARTESIAN_POINT ( 'NONE',  ( -182.2429263765338021, 5.598654528085804216, 7.705886871421366635 ) ) ;
#33256=CARTESIAN_POINT ( 'NONE',  ( -62.84499999999998465, -7.632228543268599452, 2.479861379858951054 ) ) ;
#33263=CARTESIAN_POINT ( 'NONE',  ( -75.35707362346617799, 5.598654528085804216, 7.705886871421366635 ) ) ;
#33264=CARTESIAN_POINT ( 'NONE',  ( -99.44292637653380496, -1.166476076187852838E-15, -9.524999999999991473 ) ) ;
#33266=( BOUNDED_CURVE ( )  B_SPLINE_CURVE ( 2, ( #60495, #12307, #66495, #55930, #19327, #9149, #35534, #30565, #68579, #2774, #30924 ),
 .UNSPECIFIED., .F., .F. ) 
 B_SPLINE_CURVE_WITH_KNOTS ( ( 3, 2, 2, 2, 2, 3 ),
 ( 0.6086956521738987602, 0.6108695652173770085, 0.6130434782608551458, 0.6152173913043333942, 0.6173913043478115314, 0.6195652173912897798 ),
 .UNSPECIFIED. ) 
 CURVE ( )  GEOMETRIC_REPRESENTATION_ITEM ( )  RATIONAL_B_SPLINE_CURVE ( ( 1.000000000000322409, 0.9510565162948311224, 1.000000000000000000, 0.9510565162951535312, 1.000000000000000000, 0.9510565162951535312, 1.000000000000000000, 0.9510565162951535312, 1.000000000000000000, 0.9510565162954809360, 0.9999999999996725952 ) ) 
 REPRESENTATION_ITEM ( '' )  );
#33267=CARTESIAN_POINT ( 'NONE',  ( -162.6570736234661751, 9.058813317711329915, 2.943386871421369566 ) ) ;
#33275=AXIS2_PLACEMENT_3D ( 'NONE', #25429, #19807, #14522 ) ;
#33288=EDGE_LOOP ( 'NONE', ( #52784, #9507, #42279, #48491 ) ) ;
#33290=CARTESIAN_POINT ( 'NONE',  ( -119.6070736234661638, -8.102448949553174629, 5.886773742842742685 ) ) ;
#33294=CARTESIAN_POINT ( 'NONE',  ( -93.74499999999999034, 4.716976649647094177, 6.492361379858945902 ) ) ;
#33295=ORIENTED_EDGE ( 'NONE', *, *, #6321, .F. ) ;
#33307=CARTESIAN_POINT ( 'NONE',  ( -184.0000000000000000, 0.000000000000000000, 0.000000000000000000 ) ) ;
#33314=CARTESIAN_POINT ( 'NONE',  ( -181.8570736234661638, -5.598654528085803328, -7.705886871421366635 ) ) ;
#33320=CARTESIAN_POINT ( 'NONE',  ( -149.7570736234661979, -5.598654528085801552, 7.705886871421367523 ) ) ;
#33324=CARTESIAN_POINT ( 'NONE',  ( -156.3549999999999898, -4.716976649647093289, -6.492361379858945902 ) ) ;
#33327=CARTESIAN_POINT ( 'NONE',  ( -174.5949999999999989, 2.607480562269073321, 8.024999999999991473 ) ) ;
#33328=CARTESIAN_POINT ( 'NONE',  ( -161.5449999999999875, -7.632228543268600340, -2.479861379858950166 ) ) ;
#33332=DIRECTION ( 'NONE',  ( -1.000000000000000000, -0.000000000000000000, -0.000000000000000000 ) ) ;
#33333=CARTESIAN_POINT ( 'NONE',  ( -69.65499999999998693, -7.632228543268600340, -2.479861379858950166 ) ) ;
#33335=DIRECTION ( 'NONE',  ( -1.000000000000000000, -0.000000000000000000, -0.000000000000000000 ) ) ;
#33337=CARTESIAN_POINT ( 'NONE',  ( -79.19499999999997897, 8.437984349512086979, -1.550032578732815448E-15 ) ) ;
#33342=DIRECTION ( 'NONE',  ( -1.000000000000000000, -0.000000000000000000, -0.000000000000000000 ) ) ;
#33358=CARTESIAN_POINT ( 'NONE',  ( -70.25707362346616947, 5.598654528085800663, -7.705886871421367523 ) ) ;
#33360=CARTESIAN_POINT ( 'NONE',  ( -115.7049999999999841, 2.607480562269072433, 8.024999999999991473 ) ) ;
#33366=CARTESIAN_POINT ( 'NONE',  ( -57.29292637653379217, 3.094860106618428031, -9.524999999999993250 ) ) ;
#33367=CARTESIAN_POINT ( 'NONE',  ( -67.55707362346618083, -1.166476076187852838E-15, -9.524999999999991473 ) ) ;
#33369=EDGE_CURVE ( 'NONE', #246, #2194, #49785, .T. ) ;
#33377=CARTESIAN_POINT ( 'NONE',  ( -152.6070736234661354, -8.102448949553174629, 5.886773742842742685 ) ) ;
#33383=CARTESIAN_POINT ( 'NONE',  ( -104.9929263765337879, 8.102448949553172852, -5.886773742842744461 ) ) ;
#33389=CARTESIAN_POINT ( 'NONE',  ( -143.0050000000000239, 6.826472737025116366, 4.959722759717898555 ) ) ;
#33393=VERTEX_POINT ( 'NONE', #20272 ) ;
#33401=CARTESIAN_POINT ( 'NONE',  ( -51.95499999999996987, -7.632228543268599452, 2.479861379858951054 ) ) ;
#33408=CARTESIAN_POINT ( 'NONE',  ( -128.3929263765338078, 8.102448949553176405, 5.886773742842740909 ) ) ;
#33416=CARTESIAN_POINT ( 'NONE',  ( -113.3949999999999818, -6.826472737025113702, -4.959722759717900331 ) ) ;
#33418=CARTESIAN_POINT ( 'NONE',  ( -74.24499999999999034, -4.716976649647093289, -6.492361379858945902 ) ) ;
#33427=CARTESIAN_POINT ( 'NONE',  ( -128.6929263765337907, 10.01517768586948698, -1.839758294383808571E-15 ) ) ;
#33428=CARTESIAN_POINT ( 'NONE',  ( -139.0450000000000159, 7.632228543268600340, 2.479861379858949277 ) ) ;
#33436=EDGE_CURVE ( 'NONE', #65805, #59038, #56964, .T. ) ;
#33445=CARTESIAN_POINT ( 'NONE',  ( -142.1049999999999613, -6.826472737025113702, 4.959722759717902107 ) ) ;
#33457=( BOUNDED_CURVE ( )  B_SPLINE_CURVE ( 2, ( #9120, #42220, #15453, #36918, #8430, #30537, #53069, #22425, #32282, #4862, #58329 ),
 .UNSPECIFIED., .F., .F. ) 
 B_SPLINE_CURVE_WITH_KNOTS ( ( 3, 2, 2, 2, 2, 3 ),
 ( 0.09782608695651952291, 0.09999999999999774347, 0.1021739130434759502, 0.1043478260869541568, 0.1065217391304323635, 0.1086956521739105841 ),
 .UNSPECIFIED. ) 
 CURVE ( )  GEOMETRIC_REPRESENTATION_ITEM ( )  RATIONAL_B_SPLINE_CURVE ( ( 1.000000000000049960, 0.9510565162951035711, 1.000000000000000000, 0.9510565162951535312, 1.000000000000000000, 0.9510565162951535312, 1.000000000000000000, 0.9510565162951535312, 1.000000000000000000, 0.9510565162952088203, 0.9999999999999447109 ) ) 
 REPRESENTATION_ITEM ( '' )  );
#33461=CARTESIAN_POINT ( 'NONE',  ( -53.60499999999998266, 6.826472737025113702, -4.959722759717902107 ) ) ;
#33472=ORIENTED_EDGE ( 'NONE', *, *, #14902, .T. ) ;
#33476=CARTESIAN_POINT ( 'NONE',  ( -171.2049999999999841, -2.607480562269071545, -8.024999999999991473 ) ) ;
#33484=CARTESIAN_POINT ( 'NONE',  ( -86.90499999999998693, 2.607480562269068880, -8.024999999999993250 ) ) ;
#33489=CARTESIAN_POINT ( 'NONE',  ( -53.90707362346615383, -3.094860106618429807, 9.524999999999991473 ) ) ;
#33493=AXIS2_PLACEMENT_3D ( 'NONE', #21179, #32099, #63745 ) ;
#33497=CARTESIAN_POINT ( 'NONE',  ( -108.7449999999999903, 4.716976649647094177, 6.492361379858945902 ) ) ;
#33501=CARTESIAN_POINT ( 'NONE',  ( -17.50807934363836083, 11.19244030607554663, -4.328528619389988563 ) ) ;
#33503=CARTESIAN_POINT ( 'NONE',  ( -148.7929263765337566, -3.094860106618429807, 9.524999999999991473 ) ) ;
#33506=CARTESIAN_POINT ( 'NONE',  ( -179.3950000000000102, -6.826472737025115478, -4.959722759717899443 ) ) ;
#33516=CARTESIAN_POINT ( 'NONE',  ( -65.99292637653377369, 8.102448949553171076, -5.886773742842744461 ) ) ;
#33519=ADVANCED_FACE ( 'NONE', ( #50486 ), #39965, .T. ) ;
#33524=EDGE_CURVE ( 'NONE', #69107, #29745, #30430, .T. ) ;
#33528=CARTESIAN_POINT ( 'NONE',  ( -169.2549999999999955, -4.716976649647092401, 6.492361379858946790 ) ) ;
#33536=CARTESIAN_POINT ( 'NONE',  ( -83.30499999999999261, 8.437984349512086979, -1.550032578732815448E-15 ) ) ;
#33543=CARTESIAN_POINT ( 'NONE',  ( -169.4929263765338305, -8.102448949553174629, 5.886773742842742685 ) ) ;
#33544=CARTESIAN_POINT ( 'NONE',  ( -114.1429263765338078, 5.598654528085800663, -7.705886871421367523 ) ) ;
#33550=EDGE_CURVE ( 'NONE', #68105, #12632, #44880, .T. ) ;
#33551=CARTESIAN_POINT ( 'NONE',  ( -61.19499999999997897, 8.437984349512085203, -1.550032578732815448E-15 ) ) ;
#33555=CARTESIAN_POINT ( 'NONE',  ( -49.04292637653379217, -9.058813317711329915, -2.943386871421370898 ) ) ;
#33561=CARTESIAN_POINT ( 'NONE',  ( -111.3549999999999898, -4.716976649647093289, -6.492361379858945902 ) ) ;
#33565=DIRECTION ( 'NONE',  ( 0.000000000000000000, 0.000000000000000000, 1.000000000000000000 ) ) ;
#33567=CARTESIAN_POINT ( 'NONE',  ( -150.3570736234661638, 5.598654528085804216, 7.705886871421366635 ) ) ;
#33570=CARTESIAN_POINT ( 'NONE',  ( -87.50707362346614104, 8.102448949553176405, 5.886773742842740909 ) ) ;
#33577=CARTESIAN_POINT ( 'NONE',  ( -131.1550000000000011, 7.632228543268600340, 2.479861379858949277 ) ) ;
#33581=CARTESIAN_POINT ( 'NONE',  ( -149.6949999999999648, -8.437984349512085203, 5.166775262442717831E-16 ) ) ;
#33583=CARTESIAN_POINT ( 'NONE',  ( -126.1450000000000102, -4.716976649647092401, 6.492361379858946790 ) ) ;
#33589=DIRECTION ( 'NONE',  ( -1.000000000000000000, -0.000000000000000000, -0.000000000000000000 ) ) ;
#33590=CARTESIAN_POINT ( 'NONE',  ( -181.3429263765338249, -9.058813317711329915, 2.943386871421371787 ) ) ;
#33592=CARTESIAN_POINT ( 'NONE',  ( -60.59499999999997755, 2.607480562269073321, 8.024999999999991473 ) ) ;
#33598=CARTESIAN_POINT ( 'NONE',  ( -99.74292637653380211, -5.598654528085803328, -7.705886871421366635 ) ) ;
#33601=DIRECTION ( 'NONE',  ( -1.000000000000000000, -0.000000000000000000, -0.000000000000000000 ) ) ;
#33621=CARTESIAN_POINT ( 'NONE',  ( -93.50707362346618368, 8.102448949553176405, 5.886773742842740909 ) ) ;
#33626=CARTESIAN_POINT ( 'NONE',  ( -91.19499999999999318, 8.437984349512085203, -1.550032578732815448E-15 ) ) ;
#33638=ORIENTED_EDGE ( 'NONE', *, *, #54702, .F. ) ;
#33639=ORIENTED_EDGE ( 'NONE', *, *, #6321, .T. ) ;
#33641=CARTESIAN_POINT ( 'NONE',  ( -195.0000000000000000, 0.000000000000000000, 0.000000000000000000 ) ) ;
#33644=CARTESIAN_POINT ( 'NONE',  ( -177.8070736234661808, 10.01517768586948698, -1.839758294383808571E-15 ) ) ;
#33656=CARTESIAN_POINT ( 'NONE',  ( -163.2549999999999955, -4.716976649647092401, 6.492361379858946790 ) ) ;
#33657=DIRECTION ( 'NONE',  ( -1.000000000000000000, -0.000000000000000000, -0.000000000000000000 ) ) ;
#33658=CARTESIAN_POINT ( 'NONE',  ( -183.8592518627806953, -8.440169527594953536, -1.989286698146640164 ) ) ;
#33660=CARTESIAN_POINT ( 'NONE',  ( -169.3449999999999989, 7.632228543268599452, -2.479861379858951942 ) ) ;
#33661=CARTESIAN_POINT ( 'NONE',  ( -155.0949999999999704, -2.607480562269071545, -8.024999999999991473 ) ) ;
#33663=ORIENTED_EDGE ( 'NONE', *, *, #63536, .T. ) ;
#33667=CARTESIAN_POINT ( 'NONE',  ( -70.10499999999998977, -6.826472737025115478, 4.959722759717900331 ) ) ;
#33671=CARTESIAN_POINT ( 'NONE',  ( -66.74499999999999034, 4.716976649647094177, 6.492361379858945902 ) ) ;
#33693=DIRECTION ( 'NONE',  ( -0.000000000000000000, 1.000000000000000000, 1.224646799147353207E-16 ) ) ;
#33695=CARTESIAN_POINT ( 'NONE',  ( -112.4049999999999869, -2.607480562269069768, 8.024999999999991473 ) ) ;
#33704=ORIENTED_EDGE ( 'NONE', *, *, #29035, .T. ) ;
#33719=CARTESIAN_POINT ( 'NONE',  ( -131.4549999999999841, 7.632228543268599452, -2.479861379858951942 ) ) ;
#33730=CARTESIAN_POINT ( 'NONE',  ( -109.3429263765338106, -9.058813317711329915, 2.943386871421371787 ) ) ;
#33735=AXIS2_PLACEMENT_3D ( 'NONE', #24255, #20006, #14063 ) ;
#33753=CARTESIAN_POINT ( 'NONE',  ( -95.84499999999998465, -7.632228543268599452, 2.479861379858951054 ) ) ;
#33755=CARTESIAN_POINT ( 'NONE',  ( -80.24499999999997613, -4.716976649647093289, -6.492361379858945902 ) ) ;
#33759=ADVANCED_FACE ( 'NONE', ( #37481 ), #11723, .T. ) ;
#33766=CARTESIAN_POINT ( 'NONE',  ( -119.9929263765338021, 8.102448949553171076, -5.886773742842744461 ) ) ;
#33768=CARTESIAN_POINT ( 'NONE',  ( -133.3449999999999989, 7.632228543268599452, -2.479861379858951942 ) ) ;
#33781=CARTESIAN_POINT ( 'NONE',  ( -139.4049999999999727, -2.607480562269069768, 8.024999999999991473 ) ) ;
#33794=CARTESIAN_POINT ( 'NONE',  ( -62.30499999999997840, 8.437984349512086979, -1.550032578732815448E-15 ) ) ;
#33796=DIRECTION ( 'NONE',  ( -1.000000000000000000, -0.000000000000000000, -0.000000000000000000 ) ) ;
#33798=CARTESIAN_POINT ( 'NONE',  ( -56.30499999999999972, 8.437984349512086979, -1.550032578732815448E-15 ) ) ;
#33811=CARTESIAN_POINT ( 'NONE',  ( -160.5550000000000068, 0.000000000000000000, 8.024999999999991473 ) ) ;
#33812=VERTEX_POINT ( 'NONE', #32463 ) ;
#33816=CARTESIAN_POINT ( 'NONE',  ( -183.9999999999999716, -8.313263101079598982, 1.518308302792259701 ) ) ;
#33821=CARTESIAN_POINT ( 'NONE',  ( -80.90499999999995850, 2.607480562269068880, -8.024999999999993250 ) ) ;
#33834=CARTESIAN_POINT ( 'NONE',  ( -108.5949999999999847, 2.607480562269073321, 8.024999999999991473 ) ) ;
#33838=CARTESIAN_POINT ( 'NONE',  ( -17.51489521397122573, 11.19178930173965725, 4.333724509350330933 ) ) ;
#33840=CARTESIAN_POINT ( 'NONE',  ( -155.3929263765337794, 8.102448949553176405, 5.886773742842740909 ) ) ;
#33841=CARTESIAN_POINT ( 'NONE',  ( -170.6949999999999932, -8.437984349512085203, 5.166775262442717831E-16 ) ) ;
#33848=CARTESIAN_POINT ( 'NONE',  ( -69.74292637653380211, -5.598654528085803328, -7.705886871421366635 ) ) ;
#33850=( BOUNDED_CURVE ( )  B_SPLINE_CURVE ( 2, ( #64892, #49776, #65240, #39240, #12456, #33918, #38568, #55386, #16741, #49109, #59966 ),
 .UNSPECIFIED., .F., .F. ) 
 B_SPLINE_CURVE_WITH_KNOTS ( ( 3, 2, 2, 2, 2, 3 ),
 ( 0.9347826086956522174, 0.9369565217391304657, 0.9391304347826087140, 0.9413043478260869623, 0.9434782608695652106, 0.9456521739130434590 ),
 .UNSPECIFIED. ) 
 CURVE ( )  GEOMETRIC_REPRESENTATION_ITEM ( )  RATIONAL_B_SPLINE_CURVE ( ( 1.000000000000000000, 0.9510565162951535312, 1.000000000000000000, 0.9510565162951535312, 1.000000000000000000, 0.9510565162951535312, 1.000000000000000000, 0.9510565162951535312, 1.000000000000000000, 0.9510565162951535312, 1.000000000000000000 ) ) 
 REPRESENTATION_ITEM ( '' )  );
#33858=CARTESIAN_POINT ( 'NONE',  ( -166.1049999999999898, -6.826472737025113702, 4.959722759717902107 ) ) ;
#33859=EDGE_LOOP ( 'NONE', ( #41272, #61124, #6387, #30549 ) ) ;
#33869=CARTESIAN_POINT ( 'NONE',  ( -78.95499999999998408, -7.632228543268599452, 2.479861379858951054 ) ) ;
#33876=CARTESIAN_POINT ( 'NONE',  ( -168.8929263765337794, -8.102448949553174629, -5.886773742842741797 ) ) ;
#33877=CARTESIAN_POINT ( 'NONE',  ( -113.3929263765337936, 8.102448949553176405, 5.886773742842740909 ) ) ;
#33882=CARTESIAN_POINT ( 'NONE',  ( -58.49499999999998323, 6.826472737025113702, -4.959722759717902107 ) ) ;
#33890=CARTESIAN_POINT ( 'NONE',  ( -57.89499999999996760, 6.826472737025115478, 4.959722759717899443 ) ) ;
#33896=CARTESIAN_POINT ( 'NONE',  ( -114.0549999999999926, -9.827790563157499189E-16, -8.024999999999991473 ) ) ;
#33903=CARTESIAN_POINT ( 'NONE',  ( -147.8070736234661524, 10.01517768586948698, -1.839758294383808571E-15 ) ) ;
#33907=CARTESIAN_POINT ( 'NONE',  ( -84.20707362346614389, 3.094860106618433360, 9.524999999999991473 ) ) ;
#33916=CARTESIAN_POINT ( 'NONE',  ( -135.0549999999999784, -9.827790563157499189E-16, -8.024999999999991473 ) ) ;
#33918=CARTESIAN_POINT ( 'NONE',  ( -55.19292637653379785, -10.01517768586948698, 6.132527647946031529E-16 ) ) ;
#33920=CARTESIAN_POINT ( 'NONE',  ( -132.7450000000000045, 4.716976649647094177, 6.492361379858945902 ) ) ;
#33922=CARTESIAN_POINT ( 'NONE',  ( -128.6949999999999932, -8.437984349512086979, 5.166775262442717831E-16 ) ) ;
#33929=CARTESIAN_POINT ( 'NONE',  ( -181.0429263765338135, -9.058813317711329915, -2.943386871421370898 ) ) ;
#33931=CARTESIAN_POINT ( 'NONE',  ( -53.54499999999998039, -7.632228543268600340, -2.479861379858950166 ) ) ;
#33934=CARTESIAN_POINT ( 'NONE',  ( -103.2570736234661695, 5.598654528085800663, -7.705886871421367523 ) ) ;
#33938=CARTESIAN_POINT ( 'NONE',  ( -96.59292637653379643, -3.094860106618431139, -9.524999999999991473 ) ) ;
#33945=CARTESIAN_POINT ( 'NONE',  ( -163.1929263765338192, -10.01517768586948698, 6.132527647946031529E-16 ) ) ;
#33969=CARTESIAN_POINT ( 'NONE',  ( -87.59499999999999886, 2.607480562269073321, 8.024999999999991473 ) ) ;
#33973=EDGE_CURVE ( 'NONE', #41992, #32584, #52054, .T. ) ;
#33987=DIRECTION ( 'NONE',  ( -1.000000000000000000, -0.000000000000000000, -0.000000000000000000 ) ) ;
#33988=CARTESIAN_POINT ( 'NONE',  ( -179.4570736234661865, -9.058813317711329915, 2.943386871421371787 ) ) ;
#33991=CARTESIAN_POINT ( 'NONE',  ( -110.0070736234661837, -8.102448949553172852, -5.886773742842741797 ) ) ;
#34002=CARTESIAN_POINT ( 'NONE',  ( -155.9049999999999443, 2.607480562269068880, -8.024999999999993250 ) ) ;
#34004=CARTESIAN_POINT ( 'NONE',  ( -183.4562580486119430, -2.476980957186634136, -8.746383672357369576 ) ) ;
#34005=CARTESIAN_POINT ( 'NONE',  ( -163.7950000000000159, 2.607480562269068880, -8.024999999999993250 ) ) ;
#34007=CARTESIAN_POINT ( 'NONE',  ( -153.1450000000000102, -4.716976649647092401, 6.492361379858946790 ) ) ;
#34009=DIRECTION ( 'NONE',  ( 0.000000000000000000, 0.000000000000000000, 1.000000000000000000 ) ) ;
#34013=CARTESIAN_POINT ( 'NONE',  ( -74.00499999999996703, 6.826472737025116366, 4.959722759717898555 ) ) ;
#34017=CARTESIAN_POINT ( 'NONE',  ( -70.34499999999998465, 7.632228543268599452, -2.479861379858951942 ) ) ;
#34023=CARTESIAN_POINT ( 'NONE',  ( -175.9429263765337907, 0.000000000000000000, 9.524999999999991473 ) ) ;
#34045=CARTESIAN_POINT ( 'NONE',  ( -102.8049999999999784, -8.437984349512086979, 5.166775262442717831E-16 ) ) ;
#34049=CARTESIAN_POINT ( 'NONE',  ( -56.99292637653380211, 8.102448949553172852, -5.886773742842744461 ) ) ;
#34052=EDGE_CURVE ( 'NONE', #52470, #34254, #59194, .T. ) ;
#34056=EDGE_LOOP ( 'NONE', ( #67257, #62072, #1985, #38048 ) ) ;
#34067=CARTESIAN_POINT ( 'NONE',  ( -195.0000000000000000, 0.000000000000000000, 5.499999999999985789 ) ) ;
#34077=CARTESIAN_POINT ( 'NONE',  ( -128.7549999999999955, 4.716976649647091513, -6.492361379858946790 ) ) ;
#34096=CARTESIAN_POINT ( 'NONE',  ( -177.3570736234661638, 5.598654528085804216, 7.705886871421366635 ) ) ;
#34106=CARTESIAN_POINT ( 'NONE',  ( -99.89499999999998181, 6.826472737025115478, 4.959722759717899443 ) ) ;
#34108=CARTESIAN_POINT ( 'NONE',  ( -74.84499999999998465, -7.632228543268599452, 2.479861379858951054 ) ) ;
#34118=CARTESIAN_POINT ( 'NONE',  ( -127.7929263765337993, -3.094860106618429807, 9.524999999999991473 ) ) ;
#34119=CARTESIAN_POINT ( 'NONE',  ( -136.1949999999999363, 8.437984349512085203, -1.550032578732815448E-15 ) ) ;
#34122=CARTESIAN_POINT ( 'NONE',  ( -127.5570736234661950, -1.166476076187852838E-15, -9.524999999999991473 ) ) ;
#34129=AXIS2_PLACEMENT_3D ( 'NONE', #12121, #51081, #7798 ) ;
#34131=CARTESIAN_POINT ( 'NONE',  ( -131.1570736234661751, -9.058813317711329915, -2.943386871421370898 ) ) ;
#34135=CARTESIAN_POINT ( 'NONE',  ( -138.9549999999999841, -7.632228543268599452, 2.479861379858951054 ) ) ;
#34153=CARTESIAN_POINT ( 'NONE',  ( -57.80499999999998550, -8.437984349512086979, 5.166775262442717831E-16 ) ) ;
#34160=CARTESIAN_POINT ( 'NONE',  ( -87.74292637653380211, -5.598654528085803328, -7.705886871421366635 ) ) ;
#34163=EDGE_CURVE ( 'NONE', #67977, #56670, #4465, .T. ) ;
#34166=EDGE_CURVE ( 'NONE', #61370, #41269, #38064, .T. ) ;
#34172=CARTESIAN_POINT ( 'NONE',  ( -121.7070736234669397, -3.094860106631069918, -9.524999999990811261 ) ) ;
#34174=CARTESIAN_POINT ( 'NONE',  ( -166.7049999999999557, 2.607480562269073321, 8.024999999999991473 ) ) ;
#34179=EDGE_CURVE ( 'NONE', #56168, #23696, #18478, .T. ) ;
#34187=CARTESIAN_POINT ( 'NONE',  ( -75.95499999999998408, -7.632228543268599452, 2.479861379858951054 ) ) ;
#34201=CARTESIAN_POINT ( 'NONE',  ( -107.9949999999999761, -6.826472737025115478, 4.959722759717900331 ) ) ;
#34205=CARTESIAN_POINT ( 'NONE',  ( -195.0000000000000000, 1.166476076187852838E-15, -9.524999999999991473 ) ) ;
#34207=CARTESIAN_POINT ( 'NONE',  ( -150.5929263765337964, -3.094860106618431139, -9.524999999999991473 ) ) ;
#34208=CARTESIAN_POINT ( 'NONE',  ( -164.5449999999999875, -7.632228543268600340, -2.479861379858950166 ) ) ;
#34215=EDGE_LOOP ( 'NONE', ( #31197, #33183, #46387, #12842 ) ) ;
#34216=CARTESIAN_POINT ( 'NONE',  ( -64.49292637653380211, -8.102448949553172852, 5.886773742842742685 ) ) ;
#34222=CARTESIAN_POINT ( 'NONE',  ( -170.9049999999999727, 2.607480562269069324, -8.024999999999993250 ) ) ;
#34235=CARTESIAN_POINT ( 'NONE',  ( -88.40499999999997272, -2.607480562269069768, 8.024999999999991473 ) ) ;
#34241=CARTESIAN_POINT ( 'NONE',  ( -126.7429263765338163, -5.598654528085803328, -7.705886871421366635 ) ) ;
#34248=CARTESIAN_POINT ( 'NONE',  ( -50.69499999999998607, -8.437984349512085203, 5.166775262442717831E-16 ) ) ;
#34254=VERTEX_POINT ( 'NONE', #22542 ) ;
#34255=CARTESIAN_POINT ( 'NONE',  ( -53.84499999999997755, -7.632228543268599452, 2.479861379858951054 ) ) ;
#34256=ORIENTED_EDGE ( 'NONE', *, *, #2997, .F. ) ;
#34259=CARTESIAN_POINT ( 'NONE',  ( -104.3049999999999784, 8.437984349512085203, -1.550032578732815448E-15 ) ) ;
#34265=CARTESIAN_POINT ( 'NONE',  ( -150.0570736234661808, 0.000000000000000000, 9.524999999999991473 ) ) ;
#34269=CARTESIAN_POINT ( 'NONE',  ( -84.35707362346617799, 5.598654528085804216, 7.705886871421366635 ) ) ;
#34277=CARTESIAN_POINT ( 'NONE',  ( -132.0549999999999784, -9.827790563157499189E-16, -8.024999999999991473 ) ) ;
#34279=CARTESIAN_POINT ( 'NONE',  ( -139.6449999999999818, 4.716976649647091513, -6.492361379858946790 ) ) ;
#34280=CARTESIAN_POINT ( 'NONE',  ( -127.3449999999999847, 7.632228543268599452, -2.479861379858951942 ) ) ;
#34284=( BOUNDED_CURVE ( )  B_SPLINE_CURVE ( 2, ( #22016, #32539, #33934, #38918, #43519, #16754, #54004, #38223, #1873, #55034, #55397 ),
 .UNSPECIFIED., .F., .F. ) 
 B_SPLINE_CURVE_WITH_KNOTS ( ( 3, 2, 2, 2, 2, 3 ),
 ( 0.5760869565217255905, 0.5782608695652037278, 0.5804347826086819762, 0.5826086956521601135, 0.5847826086956383618, 0.5869565217391166101 ),
 .UNSPECIFIED. ) 
 CURVE ( )  GEOMETRIC_REPRESENTATION_ITEM ( )  RATIONAL_B_SPLINE_CURVE ( ( 1.000000000000304867, 0.9510565162948485529, 1.000000000000000000, 0.9510565162951535312, 1.000000000000000000, 0.9510565162951535312, 1.000000000000000000, 0.9510565162951535312, 1.000000000000000000, 0.9510565162954659479, 0.9999999999996875832 ) ) 
 REPRESENTATION_ITEM ( '' )  );
#34285=ADVANCED_FACE ( 'NONE', ( #50662 ), #6354, .T. ) ;
#34290=CARTESIAN_POINT ( 'NONE',  ( -180.8929263765338362, -8.102448949553172852, -5.886773742842741797 ) ) ;
#34297=CARTESIAN_POINT ( 'NONE',  ( -95.84292637653379643, 9.058813317711329915, -2.943386871421373119 ) ) ;
#34309=EDGE_CURVE ( 'NONE', #1545, #56168, #26059, .T. ) ;
#34314=CARTESIAN_POINT ( 'NONE',  ( -64.19292637653380496, -10.01517768586948698, 6.132527647946031529E-16 ) ) ;
#34322=CARTESIAN_POINT ( 'NONE',  ( -93.59292637653493330, -3.094860106637388864, -9.524999999986219379 ) ) ;
#34329=CARTESIAN_POINT ( 'NONE',  ( -79.19499999999997897, 8.437984349512085203, -1.550032578732815448E-15 ) ) ;
#34331=VECTOR ( 'NONE', #3835, 1000.000000000000000 ) ;
#34336=EDGE_LOOP ( 'NONE', ( #6782, #49995, #51552, #16232 ) ) ;
#34339=ORIENTED_EDGE ( 'NONE', *, *, #60350, .T. ) ;
#34341=ORIENTED_EDGE ( 'NONE', *, *, #18194, .T. ) ;
#34345=CARTESIAN_POINT ( 'NONE',  ( -182.6070736234661638, -8.102448949553172852, 5.886773742842742685 ) ) ;
#34348=CARTESIAN_POINT ( 'NONE',  ( -114.9570736234661723, 9.058813317711329915, -2.943386871421373119 ) ) ;
#34351=CARTESIAN_POINT ( 'NONE',  ( -85.25707362346616947, 5.598654528085800663, -7.705886871421367523 ) ) ;
#34356=VECTOR ( 'NONE', #15547, 1000.000000000000000 ) ;
#34359=CARTESIAN_POINT ( 'NONE',  ( -155.0050000000000239, 6.826472737025116366, 4.959722759717898555 ) ) ;
#34361=CARTESIAN_POINT ( 'NONE',  ( -183.6416822935978530, -6.162375212911135769, -6.406072214693263156 ) ) ;
#34362=CARTESIAN_POINT ( 'NONE',  ( -169.0449999999999875, 7.632228543268600340, 2.479861379858949277 ) ) ;
#34364=CARTESIAN_POINT ( 'NONE',  ( -159.5949999999999989, 2.607480562269072433, 8.024999999999991473 ) ) ;
#34366=EDGE_CURVE ( 'NONE', #59038, #55900, #33266, .T. ) ;
#34369=CARTESIAN_POINT ( 'NONE',  ( -77.15499999999998693, 7.632228543268600340, 2.479861379858949277 ) ) ;
#34373=CARTESIAN_POINT ( 'NONE',  ( -71.24499999999999034, -4.716976649647093289, -6.492361379858945902 ) ) ;
#34389=CARTESIAN_POINT ( 'NONE',  ( -133.5570736234661808, -1.166476076187852838E-15, -9.524999999999991473 ) ) ;
#34394=EDGE_CURVE ( 'NONE', #66538, #29534, #12319, .T. ) ;
#34404=CARTESIAN_POINT ( 'NONE',  ( -122.0949999999999847, -2.607480562269071545, -8.024999999999991473 ) ) ;
#34409=CARTESIAN_POINT ( 'NONE',  ( -10.67256264059687787, -11.73548369089732724, 2.509972884434803930 ) ) ;
#34412=FACE_OUTER_BOUND ( 'NONE', #63419, .T. ) ;
#34422=CARTESIAN_POINT ( 'NONE',  ( -132.0549999999999784, -9.827790563157499189E-16, -8.024999999999991473 ) ) ;
#34424=ADVANCED_FACE ( 'NONE', ( #13356 ), #4165, .T. ) ;
#34427=CARTESIAN_POINT ( 'NONE',  ( -195.0000000000000000, 0.000000000000000000, 0.000000000000000000 ) ) ;
#34434=CARTESIAN_POINT ( 'NONE',  ( -51.05707362346617373, 0.000000000000000000, 9.524999999999991473 ) ) ;
#34439=CARTESIAN_POINT ( 'NONE',  ( -91.64292637653380780, -5.598654528085801552, 7.705886871421367523 ) ) ;
#34446=CARTESIAN_POINT ( 'NONE',  ( -100.1049999999999898, -6.826472737025115478, 4.959722759717900331 ) ) ;
#34450=CARTESIAN_POINT ( 'NONE',  ( -99.59499999999998465, 2.607480562269072433, 8.024999999999991473 ) ) ;
#34453=CARTESIAN_POINT ( 'NONE',  ( -81.89499999999999602, 6.826472737025116366, 4.959722759717898555 ) ) ;
#34462=CARTESIAN_POINT ( 'NONE',  ( -116.0929263765337822, 3.094860106618433360, 9.524999999999991473 ) ) ;
#34463=CARTESIAN_POINT ( 'NONE',  ( -142.3449999999999989, 7.632228543268599452, -2.479861379858951942 ) ) ;
#34469=CARTESIAN_POINT ( 'NONE',  ( -173.6929263765337907, 10.01517768586948698, -1.839758294383808966E-15 ) ) ;
#34476=CARTESIAN_POINT ( 'NONE',  ( -130.7070736234668402, -3.094860106629389040, -9.524999999992031618 ) ) ;
#34481=CARTESIAN_POINT ( 'NONE',  ( -130.4050000000000011, -2.607480562269069768, 8.024999999999991473 ) ) ;
#34484=CARTESIAN_POINT ( 'NONE',  ( -73.94292637653379074, 0.000000000000000000, 9.524999999999991473 ) ) ;
#34500=CARTESIAN_POINT ( 'NONE',  ( -87.89292637653377938, -8.102448949553174629, -5.886773742842741797 ) ) ;
#34509=DIRECTION ( 'NONE',  ( -1.000000000000000000, -0.000000000000000000, -0.000000000000000000 ) ) ;
#34510=CARTESIAN_POINT ( 'NONE',  ( -163.2549999999999955, -4.716976649647092401, 6.492361379858946790 ) ) ;
#34516=ORIENTED_EDGE ( 'NONE', *, *, #18289, .T. ) ;
#34519=DIRECTION ( 'NONE',  ( -1.000000000000000000, -0.000000000000000000, -0.000000000000000000 ) ) ;
#34520=CARTESIAN_POINT ( 'NONE',  ( -78.80500000000000682, -8.437984349512085203, 5.166775262442717831E-16 ) ) ;
#34523=CARTESIAN_POINT ( 'NONE',  ( -64.40707362346617515, 3.094860106618428031, -9.524999999999993250 ) ) ;
#34524=CARTESIAN_POINT ( 'NONE',  ( -150.8070736234661808, 10.01517768586948698, -1.839758294383808966E-15 ) ) ;
#34526=VERTEX_POINT ( 'NONE', #59365 ) ;
#34528=CARTESIAN_POINT ( 'NONE',  ( -52.70707362346615099, -3.094860106618431139, -9.524999999999991473 ) ) ;
#34531=CARTESIAN_POINT ( 'NONE',  ( -103.1950000000000074, 8.437984349512085203, -1.550032578732815448E-15 ) ) ;
#34535=CARTESIAN_POINT ( 'NONE',  ( -19.82863456809962344, 11.92953265915295624, 1.308243074720540022 ) ) ;
#34536=CARTESIAN_POINT ( 'NONE',  ( -144.5929263765337964, -3.094860106618431139, -9.524999999999991473 ) ) ;
#34538=CARTESIAN_POINT ( 'NONE',  ( -165.7450000000000045, 4.716976649647094177, 6.492361379858945902 ) ) ;
#34543=DIRECTION ( 'NONE',  ( -1.000000000000000000, -0.000000000000000000, -0.000000000000000000 ) ) ;
#34558=CARTESIAN_POINT ( 'NONE',  ( -162.9549999999999841, -7.632228543268599452, 2.479861379858951054 ) ) ;
#34567=CARTESIAN_POINT ( 'NONE',  ( -82.40499999999998693, -2.607480562269069768, 8.024999999999991473 ) ) ;
#34568=CARTESIAN_POINT ( 'NONE',  ( -195.0000000000000000, 1.166476076187852838E-15, -9.524999999999991473 ) ) ;
#34576=CARTESIAN_POINT ( 'NONE',  ( -54.29499999999998749, -2.607480562269069768, 8.024999999999991473 ) ) ;
#34578=( BOUNDED_CURVE ( )  B_SPLINE_CURVE ( 2, ( #56504, #45308, #29422, #66728, #18545, #40032, #8340, #13237, #2655, #61761, #13590 ),
 .UNSPECIFIED., .F., .F. ) 
 B_SPLINE_CURVE_WITH_KNOTS ( ( 3, 2, 2, 2, 2, 3 ),
 ( 0.4456521739130328563, 0.4478260869565111046, 0.4499999999999892975, 0.4521739130434675458, 0.4543478260869457386, 0.4565217391304239314 ),
 .UNSPECIFIED. ) 
 CURVE ( )  GEOMETRIC_REPRESENTATION_ITEM ( )  RATIONAL_B_SPLINE_CURVE ( ( 1.000000000000238698, 0.9510565162949148332, 1.000000000000000000, 0.9510565162951535312, 1.000000000000000000, 0.9510565162951535312, 1.000000000000000000, 0.9510565162951535312, 1.000000000000000000, 0.9510565162953972251, 0.9999999999997563060 ) ) 
 REPRESENTATION_ITEM ( '' )  );
#34585=CARTESIAN_POINT ( 'NONE',  ( -50.54499999999998039, -7.632228543268600340, -2.479861379858950166 ) ) ;
#34590=CARTESIAN_POINT ( 'NONE',  ( -104.6050000000000040, 6.826472737025113702, -4.959722759717902107 ) ) ;
#34596=CARTESIAN_POINT ( 'NONE',  ( -139.2570736234661695, 5.598654528085800663, -7.705886871421367523 ) ) ;
#34599=CARTESIAN_POINT ( 'NONE',  ( -80.45707362346617231, -9.058813317711329915, 2.943386871421371787 ) ) ;
#34600=CARTESIAN_POINT ( 'NONE',  ( -95.54292637653379927, 9.058813317711329915, 2.943386871421369566 ) ) ;
#34604=CARTESIAN_POINT ( 'NONE',  ( -123.3549999999999898, -4.716976649647093289, -6.492361379858945902 ) ) ;
#34605=FACE_OUTER_BOUND ( 'NONE', #4274, .T. ) ;
#34608=CARTESIAN_POINT ( 'NONE',  ( -135.2950000000000159, -2.607480562269069768, 8.024999999999991473 ) ) ;
#34610=CARTESIAN_POINT ( 'NONE',  ( -122.6949999999999790, -8.437984349512086979, 5.166775262442717831E-16 ) ) ;
#34615=EDGE_CURVE ( 'NONE', #42104, #63360, #1956, .T. ) ;
#34616=CARTESIAN_POINT ( 'NONE',  ( -121.0429263765337993, -9.058813317711329915, -2.943386871421370898 ) ) ;
#34617=CARTESIAN_POINT ( 'NONE',  ( -177.7429263765338021, -5.598654528085803328, -7.705886871421366635 ) ) ;
#34619=CARTESIAN_POINT ( 'NONE',  ( -48.89499999999999602, 6.826472737025116366, 4.959722759717898555 ) ) ;
#34629=CARTESIAN_POINT ( 'NONE',  ( -97.79292637653381348, -3.094860106618429807, 9.524999999999991473 ) ) ;
#34653=CARTESIAN_POINT ( 'NONE',  ( -80.24499999999997613, -4.716976649647093289, -6.492361379858945902 ) ) ;
#34661=CARTESIAN_POINT ( 'NONE',  ( -76.34292637653379643, -9.058813317711329915, 2.943386871421371787 ) ) ;
#34669=CARTESIAN_POINT ( 'NONE',  ( -136.9429263765338192, 0.000000000000000000, 9.524999999999991473 ) ) ;
#34673=CARTESIAN_POINT ( 'NONE',  ( -177.0570736234661808, 0.000000000000000000, 9.524999999999991473 ) ) ;
#34678=CARTESIAN_POINT ( 'NONE',  ( -108.8070736234661666, 10.01517768586948698, -1.839758294383808571E-15 ) ) ;
#34682=CARTESIAN_POINT ( 'NONE',  ( 0.000000000000000000, 1.408343819019453020E-15, -10.99999999999995381 ) ) ;
#34685=CARTESIAN_POINT ( 'NONE',  ( -148.8549999999999898, 4.716976649647094177, 6.492361379858945902 ) ) ;
#34689=CARTESIAN_POINT ( 'NONE',  ( -166.4950000000000045, 6.826472737025113702, -4.959722759717902107 ) ) ;
#34691=CARTESIAN_POINT ( 'NONE',  ( -159.8950000000000102, 6.826472737025115478, 4.959722759717899443 ) ) ;
#34696=CARTESIAN_POINT ( 'NONE',  ( -70.25499999999998124, -4.716976649647092401, 6.492361379858946790 ) ) ;
#34699=CARTESIAN_POINT ( 'NONE',  ( -167.5429263765338135, 9.058813317711329915, 2.943386871421369566 ) ) ;
#34700=CARTESIAN_POINT ( 'NONE',  ( -72.59499999999998465, 2.607480562269072433, 8.024999999999991473 ) ) ;
#34719=DIRECTION ( 'NONE',  ( 0.000000000000000000, -1.224646799147353454E-16, 1.000000000000000000 ) ) ;
#34725=CARTESIAN_POINT ( 'NONE',  ( -145.7929263765342967, -3.094860106610362926, 9.525000000005851675 ) ) ;
#34729=FACE_OUTER_BOUND ( 'NONE', #21454, .T. ) ;
#34730=CARTESIAN_POINT ( 'NONE',  ( -107.8449999999999989, -7.632228543268599452, 2.479861379858951054 ) ) ;
#34737=CARTESIAN_POINT ( 'NONE',  ( -10.25964068305781041, -11.89358858517478446, -1.623775006699102130 ) ) ;
#34752=CARTESIAN_POINT ( 'NONE',  ( -134.6050000000000182, 6.826472737025113702, -4.959722759717902107 ) ) ;
#34761=CARTESIAN_POINT ( 'NONE',  ( -157.1929263765337907, -10.01517768586948698, 6.132527647946031529E-16 ) ) ;
#34768=EDGE_CURVE ( 'NONE', #35517, #40833, #10445, .T. ) ;
#34770=VERTEX_POINT ( 'NONE', #31877 ) ;
#34771=CARTESIAN_POINT ( 'NONE',  ( -123.2070736234669255, 3.094860106630802576, 9.524999999991006661 ) ) ;
#34773=EDGE_CURVE ( 'NONE', #12077, #63927, #26585, .T. ) ;
#34776=CARTESIAN_POINT ( 'NONE',  ( -58.55707362346616662, -1.166476076187852838E-15, -9.524999999999991473 ) ) ;
#34787=CARTESIAN_POINT ( 'NONE',  ( -97.55499999999999261, 0.000000000000000000, 8.024999999999991473 ) ) ;
#34791=CARTESIAN_POINT ( 'NONE',  ( -97.64499999999999602, 4.716976649647091513, -6.492361379858946790 ) ) ;
#34793=CARTESIAN_POINT ( 'NONE',  ( -79.19499999999997897, 8.437984349512085203, -1.550032578732815448E-15 ) ) ;
#34799=ORIENTED_EDGE ( 'NONE', *, *, #49489, .F. ) ;
#34800=CARTESIAN_POINT ( 'NONE',  ( -118.3429263765338106, -9.058813317711329915, 2.943386871421371787 ) ) ;
#34802=CARTESIAN_POINT ( 'NONE',  ( -135.7450000000000045, 4.716976649647094177, 6.492361379858945902 ) ) ;
#34817=CYLINDRICAL_SURFACE ( 'NONE', #18483, 9.524999999999991473 ) ;
#34819=CARTESIAN_POINT ( 'NONE',  ( -132.2049999999999841, -2.607480562269071545, -8.024999999999991473 ) ) ;
#34821=CARTESIAN_POINT ( 'NONE',  ( -123.6570736234661751, 9.058813317711329915, 2.943386871421369566 ) ) ;
#34822=ORIENTED_EDGE ( 'NONE', *, *, #49489, .T. ) ;
#34835=CARTESIAN_POINT ( 'NONE',  ( -47.75499999999999545, 4.716976649647091513, -6.492361379858946790 ) ) ;
#34849=AXIS2_PLACEMENT_3D ( 'NONE', #27419, #17612, #49962 ) ;
#34850=CARTESIAN_POINT ( 'NONE',  ( -122.6070736234661780, -8.102448949553174629, 5.886773742842742685 ) ) ;
#34852=CARTESIAN_POINT ( 'NONE',  ( -166.4049999999999727, -2.607480562269069768, 8.024999999999991473 ) ) ;
#34868=CARTESIAN_POINT ( 'NONE',  ( -77.75499999999999545, 4.716976649647091513, -6.492361379858946790 ) ) ;
#34873=CARTESIAN_POINT ( 'NONE',  ( -63.20707362346617231, 3.094860106618433360, 9.524999999999991473 ) ) ;
#34874=CARTESIAN_POINT ( 'NONE',  ( -150.9570736234661581, 9.058813317711329915, -2.943386871421373119 ) ) ;
#34882=CARTESIAN_POINT ( 'NONE',  ( -104.2449999999999903, -4.716976649647093289, -6.492361379858945902 ) ) ;
#34889=CARTESIAN_POINT ( 'NONE',  ( -96.80707362346618083, 10.01517768586948698, -1.839758294383808966E-15 ) ) ;
#34890=CARTESIAN_POINT ( 'NONE',  ( -19.67620707751459008, 11.86859602145972836, 1.777522113161904782 ) ) ;
#34892=CARTESIAN_POINT ( 'NONE',  ( -141.7429263765338021, -5.598654528085803328, -7.705886871421366635 ) ) ;
#34894=CARTESIAN_POINT ( 'NONE',  ( -162.1449999999999818, -4.716976649647092401, 6.492361379858946790 ) ) ;
#34910=CARTESIAN_POINT ( 'NONE',  ( -158.3049999999999500, 8.437984349512086979, -1.550032578732815448E-15 ) ) ;
#34924=CARTESIAN_POINT ( 'NONE',  ( -72.50499999999998124, -6.826472737025113702, -4.959722759717900331 ) ) ;
#34935=ORIENTED_EDGE ( 'NONE', *, *, #61507, .T. ) ;
#34937=CARTESIAN_POINT ( 'NONE',  ( -49.64499999999999602, 4.716976649647091513, -6.492361379858946790 ) ) ;
#34947=CARTESIAN_POINT ( 'NONE',  ( -55.34499999999997755, 7.632228543268599452, -2.479861379858951942 ) ) ;
#34950=ORIENTED_EDGE ( 'NONE', *, *, #12701, .F. ) ;
#34953=CARTESIAN_POINT ( 'NONE',  ( -108.0549999999999784, -9.827790563157499189E-16, -8.024999999999991473 ) ) ;
#34956=CARTESIAN_POINT ( 'NONE',  ( -143.3070736234661240, -10.01517768586948698, 6.132527647946031529E-16 ) ) ;
#34960=CARTESIAN_POINT ( 'NONE',  ( -85.40707362346616094, 3.094860106618428031, -9.524999999999993250 ) ) ;
#34961=CARTESIAN_POINT ( 'NONE',  ( -95.24292637653381632, 5.598654528085804216, 7.705886871421366635 ) ) ;
#34964=AXIS2_PLACEMENT_3D ( 'NONE', #8500, #52798, #56673 ) ;
#34967=CARTESIAN_POINT ( 'NONE',  ( -121.7049999999999841, 2.607480562269073321, 8.024999999999991473 ) ) ;
#34970=CARTESIAN_POINT ( 'NONE',  ( -135.7450000000000045, 4.716976649647094177, 6.492361379858945902 ) ) ;
#34971=CARTESIAN_POINT ( 'NONE',  ( -115.7949999999999875, 2.607480562269069324, -8.024999999999993250 ) ) ;
#34972=VECTOR ( 'NONE', #22896, 1000.000000000000000 ) ;
#34978=CARTESIAN_POINT ( 'NONE',  ( -175.0429263765338135, -9.058813317711329915, -2.943386871421370898 ) ) ;
#34983=LINE ( 'NONE', #45587, #68051 ) ;
#34989=CARTESIAN_POINT ( 'NONE',  ( -85.04292637653381348, -9.058813317711329915, -2.943386871421370898 ) ) ;
#34993=CARTESIAN_POINT ( 'NONE',  ( -163.7929263765340693, -3.094860106613926298, 9.525000000003263523 ) ) ;
#35002=CARTESIAN_POINT ( 'NONE',  ( -63.59292637653378222, -3.094860106618431139, -9.524999999999991473 ) ) ;
#35003=( BOUNDED_CURVE ( )  B_SPLINE_CURVE ( 2, ( #44994, #67104, #51622, #46027, #19237, #45685, #18223, #13987, #66762, #62508, #35455 ),
 .UNSPECIFIED., .F., .F. ) 
 B_SPLINE_CURVE_WITH_KNOTS ( ( 3, 2, 2, 2, 2, 3 ),
 ( 0.8586956521739130821, 0.8608695652173913304, 0.8630434782608695787, 0.8652173913043478271, 0.8673913043478260754, 0.8695652173913043237 ),
 .UNSPECIFIED. ) 
 CURVE ( )  GEOMETRIC_REPRESENTATION_ITEM ( )  RATIONAL_B_SPLINE_CURVE ( ( 1.000000000000000000, 0.9510565162951535312, 1.000000000000000000, 0.9510565162951535312, 1.000000000000000000, 0.9510565162951535312, 1.000000000000000000, 0.9510565162951535312, 1.000000000000000000, 0.9510565162951535312, 1.000000000000000000 ) ) 
 REPRESENTATION_ITEM ( '' )  );
#35014=CARTESIAN_POINT ( 'NONE',  ( -71.90707362346616094, -3.094860106618429807, 9.524999999999991473 ) ) ;
#35015=CARTESIAN_POINT ( 'NONE',  ( -82.79499999999998749, 2.607480562269068880, -8.024999999999993250 ) ) ;
#35022=CARTESIAN_POINT ( 'NONE',  ( -75.74292637653380211, -5.598654528085803328, -7.705886871421366635 ) ) ;
#35024=AXIS2_PLACEMENT_3D ( 'NONE', #23844, #45349, #19242 ) ;
#35034=CARTESIAN_POINT ( 'NONE',  ( -168.3570736234661922, 5.598654528085804216, 7.705886871421366635 ) ) ;
#35037=CARTESIAN_POINT ( 'NONE',  ( -112.7070736234661581, -3.094860106618431139, -9.524999999999991473 ) ) ;
#35041=CARTESIAN_POINT ( 'NONE',  ( -133.5570736234661808, -1.166476076187852838E-15, -9.524999999999991473 ) ) ;
#35048=CARTESIAN_POINT ( 'NONE',  ( -147.5049999999999955, -6.826472737025115478, -4.959722759717899443 ) ) ;
#35050=CARTESIAN_POINT ( 'NONE',  ( -147.5929263765342796, -3.094860106626229346, -9.524999999994326672 ) ) ;
#35052=CARTESIAN_POINT ( 'NONE',  ( -166.7950000000000159, 2.607480562269068880, -8.024999999999993250 ) ) ;
#35053=CARTESIAN_POINT ( 'NONE',  ( -147.5949999999999704, 2.607480562269072433, 8.024999999999991473 ) ) ;
#35054=ORIENTED_EDGE ( 'NONE', *, *, #22393, .T. ) ;
#35058=CARTESIAN_POINT ( 'NONE',  ( -62.30499999999997840, 8.437984349512085203, -1.550032578732815448E-15 ) ) ;
#35061=CARTESIAN_POINT ( 'NONE',  ( -58.94499999999998607, -9.827790563157499189E-16, -8.024999999999991473 ) ) ;
#35091=CARTESIAN_POINT ( 'NONE',  ( -82.55707362346618083, -1.166476076187852838E-15, -9.524999999999991473 ) ) ;
#35092=CYLINDRICAL_SURFACE ( 'NONE', #35024, 9.524999999999991473 ) ;
#35093=CARTESIAN_POINT ( 'NONE',  ( -110.5449999999999875, -7.632228543268600340, -2.479861379858950166 ) ) ;
#35096=( BOUNDED_CURVE ( )  B_SPLINE_CURVE ( 2, ( #22295, #43794, #50775, #12775, #13121, #66601, #66954, #50093, #60600, #2148, #1823 ),
 .UNSPECIFIED., .F., .F. ) 
 B_SPLINE_CURVE_WITH_KNOTS ( ( 3, 2, 2, 2, 2, 3 ),
 ( 0.4999999999999882316, 0.5021739130434664800, 0.5043478260869446173, 0.5065217391304228656, 0.5086956521739010029, 0.5108695652173793622 ),
 .UNSPECIFIED. ) 
 CURVE ( )  GEOMETRIC_REPRESENTATION_ITEM ( )  RATIONAL_B_SPLINE_CURVE ( ( 1.000000000000264899, 0.9510565162948886320, 1.000000000000000000, 0.9510565162951535312, 1.000000000000000000, 0.9510565162951535312, 1.000000000000000000, 0.9510565162951535312, 1.000000000000000000, 0.9510565162954235374, 0.9999999999997299938 ) ) 
 REPRESENTATION_ITEM ( '' )  );
#35099=CARTESIAN_POINT ( 'NONE',  ( -53.84292637653378932, 9.058813317711329915, -2.943386871421373119 ) ) ;
#35100=CARTESIAN_POINT ( 'NONE',  ( -11.23735010877653728, -11.53731097901733804, -3.308824629120899363 ) ) ;
#35111=ORIENTED_EDGE ( 'NONE', *, *, #37222, .F. ) ;
#35117=CARTESIAN_POINT ( 'NONE',  ( -137.4549999999999841, 7.632228543268599452, -2.479861379858951942 ) ) ;
#35125=ORIENTED_EDGE ( 'NONE', *, *, #12701, .T. ) ;
#35132=CARTESIAN_POINT ( 'NONE',  ( -182.3049999999999500, 8.437984349512085203, -1.550032578732815448E-15 ) ) ;
#35136=CARTESIAN_POINT ( 'NONE',  ( -54.65707362346616804, 9.058813317711329915, 2.943386871421369566 ) ) ;
#35137=CARTESIAN_POINT ( 'NONE',  ( -175.3449999999999989, 7.632228543268599452, -2.479861379858951942 ) ) ;
#35141=CARTESIAN_POINT ( 'NONE',  ( -160.8570736234661922, -5.598654528085803328, -7.705886871421366635 ) ) ;
#35144=CARTESIAN_POINT ( 'NONE',  ( -89.90499999999998693, 2.607480562269068880, -8.024999999999993250 ) ) ;
#35149=CARTESIAN_POINT ( 'NONE',  ( -102.4449999999999932, 0.000000000000000000, 8.024999999999991473 ) ) ;
#35151=CARTESIAN_POINT ( 'NONE',  ( -64.94499999999999318, -9.827790563157499189E-16, -8.024999999999991473 ) ) ;
#35154=CARTESIAN_POINT ( 'NONE',  ( -56.90707362346616804, -3.094860106618429807, 9.524999999999991473 ) ) ;
#35160=CARTESIAN_POINT ( 'NONE',  ( -111.1429263765338078, 5.598654528085800663, -7.705886871421367523 ) ) ;
#35161=CARTESIAN_POINT ( 'NONE',  ( -129.8949999999999818, 6.826472737025116366, 4.959722759717898555 ) ) ;
#35173=CARTESIAN_POINT ( 'NONE',  ( -127.5570736234661950, -1.166476076187852838E-15, -9.524999999999991473 ) ) ;
#35175=CARTESIAN_POINT ( 'NONE',  ( -128.0049999999999670, 6.826472737025115478, 4.959722759717899443 ) ) ;
#35179=CARTESIAN_POINT ( 'NONE',  ( -120.9570736234661865, 9.058813317711329915, -2.943386871421373119 ) ) ;
#35192=EDGE_CURVE ( 'NONE', #27775, #65805, #42759, .T. ) ;
#35206=ORIENTED_EDGE ( 'NONE', *, *, #30172, .T. ) ;
#35208=CARTESIAN_POINT ( 'NONE',  ( -122.3070736234661808, -10.01517768586948698, 6.132527647946031529E-16 ) ) ;
#35210=CARTESIAN_POINT ( 'NONE',  ( -165.8050000000000068, -8.437984349512085203, 5.166775262442717831E-16 ) ) ;
#35211=ORIENTED_EDGE ( 'NONE', *, *, #47839, .F. ) ;
#35225=CARTESIAN_POINT ( 'NONE',  ( -72.05499999999997840, -9.827790563157499189E-16, -8.024999999999991473 ) ) ;
#35226=ORIENTED_EDGE ( 'NONE', *, *, #61863, .F. ) ;
#35238=CARTESIAN_POINT ( 'NONE',  ( -100.6449999999999818, 4.716976649647091513, -6.492361379858946790 ) ) ;
#35243=CARTESIAN_POINT ( 'NONE',  ( -183.2510368117331154, 0.000000000000000000, 8.774999999999991473 ) ) ;
#35244=CARTESIAN_POINT ( 'NONE',  ( -146.9929263765338021, 8.102448949553171076, -5.886773742842744461 ) ) ;
#35247=CARTESIAN_POINT ( 'NONE',  ( -164.6949999999999648, -8.437984349512085203, 5.166775262442717831E-16 ) ) ;
#35256=CONICAL_SURFACE ( 'NONE', #64485, 8.524999999999977263, 0.7853981633974552734 ) ;
#35259=CARTESIAN_POINT ( 'NONE',  ( -184.0000000000000000, 0.000000000000000000, 8.024999999999991473 ) ) ;
#35261=CARTESIAN_POINT ( 'NONE',  ( -173.6070736234661638, -8.102448949553174629, 5.886773742842742685 ) ) ;
#35264=CARTESIAN_POINT ( 'NONE',  ( -157.7049999999999557, 2.607480562269072433, 8.024999999999991473 ) ) ;
#35268=VERTEX_POINT ( 'NONE', #48729 ) ;
#35276=ORIENTED_EDGE ( 'NONE', *, *, #31608, .T. ) ;
#35279=EDGE_CURVE ( 'NONE', #58710, #42429, #49729, .T. ) ;
#35280=CARTESIAN_POINT ( 'NONE',  ( -72.65499999999998693, -7.632228543268600340, -2.479861379858950166 ) ) ;
#35295=CARTESIAN_POINT ( 'NONE',  ( -50.54499999999998039, -7.632228543268600340, -2.479861379858950166 ) ) ;
#35303=CARTESIAN_POINT ( 'NONE',  ( -58.04499999999998749, 7.632228543268600340, 2.479861379858949277 ) ) ;
#35307=CARTESIAN_POINT ( 'NONE',  ( -102.0549999999999926, -9.827790563157499189E-16, -8.024999999999991473 ) ) ;
#35312=CARTESIAN_POINT ( 'NONE',  ( -136.8570736234661638, -5.598654528085803328, -7.705886871421366635 ) ) ;
#35317=CARTESIAN_POINT ( 'NONE',  ( -72.50707362346616947, 8.102448949553176405, 5.886773742842740909 ) ) ;
#35320=CARTESIAN_POINT ( 'NONE',  ( -72.44292637653379074, -1.166476076187852838E-15, -9.524999999999991473 ) ) ;
#35325=CARTESIAN_POINT ( 'NONE',  ( -123.9549999999999841, -7.632228543268599452, 2.479861379858951054 ) ) ;
#35328=CARTESIAN_POINT ( 'NONE',  ( -137.3950000000000102, -6.826472737025115478, -4.959722759717899443 ) ) ;
#35330=CARTESIAN_POINT ( 'NONE',  ( -118.0450000000000017, 7.632228543268600340, 2.479861379858949277 ) ) ;
#35333=CARTESIAN_POINT ( 'NONE',  ( -146.7570736234661695, -5.598654528085801552, 7.705886871421367523 ) ) ;
#35335=CARTESIAN_POINT ( 'NONE',  ( -121.1929263765337907, -10.01517768586948698, 6.132527647946031529E-16 ) ) ;
#35336=CARTESIAN_POINT ( 'NONE',  ( -168.1429263765338078, 5.598654528085800663, -7.705886871421367523 ) ) ;
#35337=CARTESIAN_POINT ( 'NONE',  ( -49.79499999999998039, 2.607480562269068880, -8.024999999999993250 ) ) ;
#35344=ORIENTED_EDGE ( 'NONE', *, *, #13979, .F. ) ;
#35345=CARTESIAN_POINT ( 'NONE',  ( -87.29292637653381348, 3.094860106618428031, -9.524999999999993250 ) ) ;
#35352=CARTESIAN_POINT ( 'NONE',  ( -179.8429263765338249, 9.058813317711329915, -2.943386871421373119 ) ) ;
#35368=CARTESIAN_POINT ( 'NONE',  ( -107.6049999999999756, 6.826472737025113702, -4.959722759717902107 ) ) ;
#35379=CARTESIAN_POINT ( 'NONE',  ( -78.59499999999999886, 2.607480562269073321, 8.024999999999991473 ) ) ;
#35385=CARTESIAN_POINT ( 'NONE',  ( -75.44292637653379074, -1.166476076187852838E-15, -9.524999999999991473 ) ) ;
#35393=DIRECTION ( 'NONE',  ( 1.000000000000000000, 0.000000000000000000, 0.000000000000000000 ) ) ;
#35396=CARTESIAN_POINT ( 'NONE',  ( -174.3570736234661638, 5.598654528085804216, 7.705886871421366635 ) ) ;
#35400=CARTESIAN_POINT ( 'NONE',  ( -111.2070736234661865, 3.094860106618433360, 9.524999999999991473 ) ) ;
#35409=CARTESIAN_POINT ( 'NONE',  ( -152.7549999999999955, 4.716976649647091513, -6.492361379858946790 ) ) ;
#35412=CARTESIAN_POINT ( 'NONE',  ( -161.9950000000000045, -6.826472737025115478, 4.959722759717900331 ) ) ;
#35413=CARTESIAN_POINT ( 'NONE',  ( -146.3950000000000102, -6.826472737025113702, -4.959722759717900331 ) ) ;
#35420=CARTESIAN_POINT ( 'NONE',  ( -63.95499999999998408, -7.632228543268599452, 2.479861379858951054 ) ) ;
#35424=CARTESIAN_POINT ( 'NONE',  ( -61.79499999999998039, 2.607480562269069324, -8.024999999999993250 ) ) ;
#35426=CARTESIAN_POINT ( 'NONE',  ( -143.6070736234661354, -8.102448949553174629, 5.886773742842742685 ) ) ;
#35455=CARTESIAN_POINT ( 'NONE',  ( -64.94292637653380496, 0.000000000000000000, 9.524999999999991473 ) ) ;
#35460=CARTESIAN_POINT ( 'NONE',  ( -112.0449999999999875, 7.632228543268600340, 2.479861379858949277 ) ) ;
#35462=DIRECTION ( 'NONE',  ( 0.000000000000000000, -0.8090169943749472292, -0.5877852522924733591 ) ) ;
#35475=CARTESIAN_POINT ( 'NONE',  ( -125.9049999999999869, 2.607480562269068880, -8.024999999999993250 ) ) ;
#35479=DIRECTION ( 'NONE',  ( 0.000000000000000000, 0.000000000000000000, 1.000000000000000000 ) ) ;
#35489=CARTESIAN_POINT ( 'NONE',  ( -176.9050000000000011, 2.607480562269068880, -8.024999999999993250 ) ) ;
#35492=CARTESIAN_POINT ( 'NONE',  ( -56.15707362346616804, -9.058813317711329915, -2.943386871421370898 ) ) ;
#35494=CARTESIAN_POINT ( 'NONE',  ( -175.4949999999999761, 6.826472737025113702, -4.959722759717902107 ) ) ;
#35498=DIRECTION ( 'NONE',  ( -1.000000000000000000, -0.000000000000000000, -0.000000000000000000 ) ) ;
#35502=CARTESIAN_POINT ( 'NONE',  ( -89.30499999999999261, 8.437984349512085203, -1.550032578732815448E-15 ) ) ;
#35506=CARTESIAN_POINT ( 'NONE',  ( -93.89499999999996760, 6.826472737025115478, 4.959722759717899443 ) ) ;
#35508=CARTESIAN_POINT ( 'NONE',  ( -67.64499999999998181, 4.716976649647091513, -6.492361379858946790 ) ) ;
#35517=VERTEX_POINT ( 'NONE', #66058 ) ;
#35518=CARTESIAN_POINT ( 'NONE',  ( -110.8429263765337964, 9.058813317711329915, -2.943386871421373119 ) ) ;
#35519=CARTESIAN_POINT ( 'NONE',  ( -126.4450000000000074, 0.000000000000000000, 8.024999999999991473 ) ) ;
#35521=EDGE_CURVE ( 'NONE', #149, #51718, #17891, .T. ) ;
#35532=( BOUNDED_CURVE ( )  B_SPLINE_CURVE ( 2, ( #1506, #61336, #29687, #13490, #7199, #13145, #34600, #56056, #34961, #50122, #7872 ),
 .UNSPECIFIED., .F., .F. ) 
 B_SPLINE_CURVE_WITH_KNOTS ( ( 3, 2, 2, 2, 2, 3 ),
 ( 0.6413043478260718189, 0.6434782608695499562, 0.6456521739130283155, 0.6478260869565064528, 0.6499999999999847011, 0.6521739130434628384 ),
 .UNSPECIFIED. ) 
 CURVE ( )  GEOMETRIC_REPRESENTATION_ITEM ( )  RATIONAL_B_SPLINE_CURVE ( ( 1.000000000000339950, 0.9510565162948135809, 1.000000000000000000, 0.9510565162951535312, 1.000000000000000000, 0.9510565162951535312, 1.000000000000000000, 0.9510565162951535312, 1.000000000000000000, 0.9510565162955009200, 0.9999999999996526112 ) ) 
 REPRESENTATION_ITEM ( '' )  );
#35534=CARTESIAN_POINT ( 'NONE',  ( -98.15707362346617515, -9.058813317711329915, -2.943386871421370898 ) ) ;
#35536=CARTESIAN_POINT ( 'NONE',  ( -126.5070736234661979, 8.102448949553176405, 5.886773742842740909 ) ) ;
#35538=CARTESIAN_POINT ( 'NONE',  ( -132.6550000000000011, -7.632228543268600340, -2.479861379858950166 ) ) ;
#35542=CARTESIAN_POINT ( 'NONE',  ( -118.8570736234661780, -5.598654528085803328, -7.705886871421366635 ) ) ;
#35554=CARTESIAN_POINT ( 'NONE',  ( -48.65499999999997272, -7.632228543268600340, -2.479861379858950166 ) ) ;
#35556=EDGE_LOOP ( 'NONE', ( #37594, #40335, #56524, #14325 ) ) ;
#35565=DIRECTION ( 'NONE',  ( -1.000000000000000000, 0.000000000000000000, -0.000000000000000000 ) ) ;
#35566=DIRECTION ( 'NONE',  ( -1.000000000000000000, -0.000000000000000000, -0.000000000000000000 ) ) ;
#35567=CARTESIAN_POINT ( 'NONE',  ( -153.0550000000000068, -9.827790563157499189E-16, -8.024999999999991473 ) ) ;
#35581=CARTESIAN_POINT ( 'NONE',  ( -77.00499999999999545, 6.826472737025116366, 4.959722759717898555 ) ) ;
#35583=CARTESIAN_POINT ( 'NONE',  ( -61.55707362346617373, -1.166476076187852838E-15, -9.524999999999991473 ) ) ;
#35590=CARTESIAN_POINT ( 'NONE',  ( -184.0000000000000000, 0.000000000000000000, 0.000000000000000000 ) ) ;
#35592=EDGE_CURVE ( 'NONE', #25953, #51005, #47279, .T. ) ;
#35594=EDGE_CURVE ( 'NONE', #64619, #43539, #11691, .T. ) ;
#35596=CARTESIAN_POINT ( 'NONE',  ( -98.39499999999999602, -6.826472737025115478, -4.959722759717899443 ) ) ;
#35601=PLANE ( 'NONE',  #10069 ) ;
#35603=CARTESIAN_POINT ( 'NONE',  ( -145.0429263765338135, -9.058813317711329915, -2.943386871421370898 ) ) ;
#35605=CARTESIAN_POINT ( 'NONE',  ( -153.7450000000000045, 4.716976649647094177, 6.492361379858945902 ) ) ;
#35617=CARTESIAN_POINT ( 'NONE',  ( -172.8570736234661922, -5.598654528085803328, -7.705886871421366635 ) ) ;
#35621=CARTESIAN_POINT ( 'NONE',  ( -159.3549999999999898, -4.716976649647093289, -6.492361379858945902 ) ) ;
#35634=CARTESIAN_POINT ( 'NONE',  ( -75.80499999999997840, -8.437984349512086979, 5.166775262442717831E-16 ) ) ;
#35645=CARTESIAN_POINT ( 'NONE',  ( -55.79499999999998039, 2.607480562269068880, -8.024999999999993250 ) ) ;
#35655=CARTESIAN_POINT ( 'NONE',  ( -105.5049999999999812, -6.826472737025115478, -4.959722759717899443 ) ) ;
#35657=DIRECTION ( 'NONE',  ( -1.000000000000000000, -0.000000000000000000, -0.000000000000000000 ) ) ;
#35659=CARTESIAN_POINT ( 'NONE',  ( -138.2070736234661865, 3.094860106618433360, 9.524999999999991473 ) ) ;
#35662=CARTESIAN_POINT ( 'NONE',  ( -78.35707362346616378, 5.598654528085804216, 7.705886871421366635 ) ) ;
#35668=CARTESIAN_POINT ( 'NONE',  ( -19.83771012782007048, -11.93314589359951761, -1.305473525340978380 ) ) ;
#35674=CARTESIAN_POINT ( 'NONE',  ( -123.2049999999999699, -2.607480562269071545, -8.024999999999991473 ) ) ;
#35675=EDGE_CURVE ( 'NONE', #58449, #57125, #2155, .T. ) ;
#35678=CARTESIAN_POINT ( 'NONE',  ( -121.6449999999999960, 4.716976649647091513, -6.492361379858946790 ) ) ;
#35679=CARTESIAN_POINT ( 'NONE',  ( -119.0949999999999847, -2.607480562269071545, -8.024999999999991473 ) ) ;
#35685=CARTESIAN_POINT ( 'NONE',  ( -169.0429263765338135, -9.058813317711329915, -2.943386871421370898 ) ) ;
#35687=CARTESIAN_POINT ( 'NONE',  ( -182.3950000000000102, -6.826472737025115478, -4.959722759717899443 ) ) ;
#35694=CARTESIAN_POINT ( 'NONE',  ( -84.29292637653381348, 3.094860106618428031, -9.524999999999993250 ) ) ;
#35702=CARTESIAN_POINT ( 'NONE',  ( -135.5929263765344217, -3.094860106628851248, -9.524999999992420641 ) ) ;
#35713=CARTESIAN_POINT ( 'NONE',  ( -104.9049999999999869, 2.607480562269069324, -8.024999999999993250 ) ) ;
#35721=CARTESIAN_POINT ( 'NONE',  ( -85.04499999999998749, 7.632228543268600340, 2.479861379858949277 ) ) ;
#35723=( BOUNDED_CURVE ( )  B_SPLINE_CURVE ( 2, ( #55555, #66450, #8423, #8058, #23885, #50628, #55899, #40435, #34096, #29140, #29510 ),
 .UNSPECIFIED., .F., .F. ) 
 B_SPLINE_CURVE_WITH_KNOTS ( ( 3, 2, 2, 2, 2, 3 ),
 ( 0.03260869565217317662, 0.03478260869565139024, 0.03695652173912960387, 0.03913043478260781749, 0.04130434782608602418, 0.04347826086956423780 ),
 .UNSPECIFIED. ) 
 CURVE ( )  GEOMETRIC_REPRESENTATION_ITEM ( )  RATIONAL_B_SPLINE_CURVE ( ( 1.000000000000016653, 0.9510565162951370999, 1.000000000000000000, 0.9510565162951535312, 1.000000000000000000, 0.9510565162951535312, 1.000000000000000000, 0.9510565162951535312, 1.000000000000000000, 0.9510565162951755136, 0.9999999999999780176 ) ) 
 REPRESENTATION_ITEM ( '' )  );
#35738=CARTESIAN_POINT ( 'NONE',  ( -173.4570736234661865, -9.058813317711329915, 2.943386871421371787 ) ) ;
#35741=CARTESIAN_POINT ( 'NONE',  ( -106.5570736234661666, -1.166476076187852838E-15, -9.524999999999991473 ) ) ;
#35743=CARTESIAN_POINT ( 'NONE',  ( -183.3519149756361912, 1.436423777000723276E-13, -9.173085024363883733 ) ) ;
#35744=CARTESIAN_POINT ( 'NONE',  ( -64.70707362346617231, -3.094860106618431139, -9.524999999999991473 ) ) ;
#35746=CARTESIAN_POINT ( 'NONE',  ( -107.2429263765338021, 5.598654528085804216, 7.705886871421366635 ) ) ;
#35747=CARTESIAN_POINT ( 'NONE',  ( -81.44292637653380496, -1.166476076187852838E-15, -9.524999999999991473 ) ) ;
#35752=CARTESIAN_POINT ( 'NONE',  ( -153.9550000000000125, -7.632228543268599452, 2.479861379858951054 ) ) ;
#35754=CARTESIAN_POINT ( 'NONE',  ( -155.9949999999999761, -6.826472737025115478, 4.959722759717900331 ) ) ;
#35755=CARTESIAN_POINT ( 'NONE',  ( -143.6949999999999932, -8.437984349512086979, 5.166775262442717831E-16 ) ) ;
#35757=CARTESIAN_POINT ( 'NONE',  ( -181.5570736234661808, -1.166476076187852838E-15, -9.524999999999991473 ) ) ;
#35759=CARTESIAN_POINT ( 'NONE',  ( -68.30499999999997840, 8.437984349512085203, -1.550032578732815448E-15 ) ) ;
#35763=EDGE_CURVE ( 'NONE', #17310, #16969, #1332, .T. ) ;
#35764=CARTESIAN_POINT ( 'NONE',  ( -62.84499999999998465, -7.632228543268599452, 2.479861379858951054 ) ) ;
#35778=CARTESIAN_POINT ( 'NONE',  ( -61.40707362346617515, 3.094860106618428031, -9.524999999999993250 ) ) ;
#35795=CARTESIAN_POINT ( 'NONE',  ( -109.1949999999999648, 8.437984349512085203, -1.550032578732815448E-15 ) ) ;
#35802=( BOUNDED_CURVE ( )  B_SPLINE_CURVE ( 2, ( #21862, #32745, #38066, #54543, #39105, #997, #22544, #44401, #49632, #6011, #65455 ),
 .UNSPECIFIED., .F., .F. ) 
 B_SPLINE_CURVE_WITH_KNOTS ( ( 3, 2, 2, 2, 2, 3 ),
 ( 0.9565217391304348116, 0.9586956521739130599, 0.9608695652173913082, 0.9630434782608695565, 0.9652173913043478048, 0.9673913043478260532 ),
 .UNSPECIFIED. ) 
 CURVE ( )  GEOMETRIC_REPRESENTATION_ITEM ( )  RATIONAL_B_SPLINE_CURVE ( ( 1.000000000000000000, 0.9510565162951535312, 1.000000000000000000, 0.9510565162951535312, 1.000000000000000000, 0.9510565162951535312, 1.000000000000000000, 0.9510565162951535312, 1.000000000000000000, 0.9510565162951535312, 1.000000000000000000 ) ) 
 REPRESENTATION_ITEM ( '' )  );
#35812=CARTESIAN_POINT ( 'NONE',  ( -141.2929263765343535, 3.094860106609420125, -9.525000000006537348 ) ) ;
#35815=CARTESIAN_POINT ( 'NONE',  ( -127.5550000000000068, 0.000000000000000000, 8.024999999999991473 ) ) ;
#35817=CARTESIAN_POINT ( 'NONE',  ( -45.00000000000000000, 0.000000000000000000, 0.000000000000000000 ) ) ;
#35818=CARTESIAN_POINT ( 'NONE',  ( -125.0929263765345780, 3.094860106630937135, 9.524999999990908961 ) ) ;
#35829=CARTESIAN_POINT ( 'NONE',  ( -175.5549999999999784, 0.000000000000000000, 8.024999999999991473 ) ) ;
#35832=CARTESIAN_POINT ( 'NONE',  ( -53.45707362346615810, -9.058813317711329915, 2.943386871421371787 ) ) ;
#35834=CARTESIAN_POINT ( 'NONE',  ( -181.3449999999999989, 7.632228543268599452, -2.479861379858951942 ) ) ;
#35842=CARTESIAN_POINT ( 'NONE',  ( -90.35499999999998977, -4.716976649647093289, -6.492361379858945902 ) ) ;
#35846=CARTESIAN_POINT ( 'NONE',  ( -90.59499999999999886, 2.607480562269072433, 8.024999999999991473 ) ) ;
#35848=CARTESIAN_POINT ( 'NONE',  ( -70.64499999999998181, 4.716976649647091513, -6.492361379858946790 ) ) ;
#35851=CARTESIAN_POINT ( 'NONE',  ( -55.70707362346616520, -3.094860106618431139, -9.524999999999991473 ) ) ;
#35856=CARTESIAN_POINT ( 'NONE',  ( -118.9429263765338050, 0.000000000000000000, 9.524999999999991473 ) ) ;
#35857=CARTESIAN_POINT ( 'NONE',  ( -128.6950000000000216, -8.437984349512085203, 5.166775262442717831E-16 ) ) ;
#35872=CARTESIAN_POINT ( 'NONE',  ( -136.2549999999999955, -4.716976649647092401, 6.492361379858946790 ) ) ;
#35875=CARTESIAN_POINT ( 'NONE',  ( -125.9070736234661751, -3.094860106618429807, 9.524999999999991473 ) ) ;
#35879=EDGE_LOOP ( 'NONE', ( #54529, #40733, #69147, #55607 ) ) ;
#35894=CARTESIAN_POINT ( 'NONE',  ( -98.69292637653380496, 10.01517768586948698, -1.839758294383808966E-15 ) ) ;
#35901=CARTESIAN_POINT ( 'NONE',  ( -60.89292637653380780, -8.102448949553172852, -5.886773742842741797 ) ) ;
#35905=CARTESIAN_POINT ( 'NONE',  ( -148.4050000000000296, -2.607480562269069768, 8.024999999999991473 ) ) ;
#35912=EDGE_CURVE ( 'NONE', #51279, #49320, #6747, .T. ) ;
#35923=CARTESIAN_POINT ( 'NONE',  ( -67.40499999999997272, -2.607480562269069768, 8.024999999999991473 ) ) ;
#35925=EDGE_CURVE ( 'NONE', #33393, #25339, #54900, .T. ) ;
#35941=CARTESIAN_POINT ( 'NONE',  ( -97.94499999999999318, -9.827790563157499189E-16, -8.024999999999991473 ) ) ;
#35944=CARTESIAN_POINT ( 'NONE',  ( -72.44292637653379074, -1.166476076187852838E-15, -9.524999999999991473 ) ) ;
#35947=CARTESIAN_POINT ( 'NONE',  ( -139.0429263765338135, -9.058813317711329915, -2.943386871421370898 ) ) ;
#35949=CARTESIAN_POINT ( 'NONE',  ( -158.9950000000000045, -6.826472737025115478, 4.959722759717900331 ) ) ;
#35951=CYLINDRICAL_SURFACE ( 'NONE', #31914, 9.524999999999991473 ) ;
#35961=CARTESIAN_POINT ( 'NONE',  ( -144.1429263765338078, 5.598654528085800663, -7.705886871421367523 ) ) ;
#35965=ORIENTED_EDGE ( 'NONE', *, *, #16037, .T. ) ;
#35966=CARTESIAN_POINT ( 'NONE',  ( -163.2549999999999955, -4.716976649647092401, 6.492361379858946790 ) ) ;
#35970=EDGE_LOOP ( 'NONE', ( #31994, #63131, #25575, #4432 ) ) ;
#35978=CARTESIAN_POINT ( 'NONE',  ( -58.34292637653379643, -9.058813317711329915, 2.943386871421371787 ) ) ;
#35980=CARTESIAN_POINT ( 'NONE',  ( -72.05499999999997840, -9.827790563157499189E-16, -8.024999999999991473 ) ) ;
#35986=EDGE_CURVE ( 'NONE', #68105, #64619, #67931, .T. ) ;
#35992=CARTESIAN_POINT ( 'NONE',  ( -180.6550000000000011, -7.632228543268600340, -2.479861379858950166 ) ) ;
#35993=ORIENTED_EDGE ( 'NONE', *, *, #51973, .T. ) ;
#35997=CARTESIAN_POINT ( 'NONE',  ( -86.54292637653379927, 9.058813317711329915, 2.943386871421369566 ) ) ;
#36002=ORIENTED_EDGE ( 'NONE', *, *, #48971, .T. ) ;
#36004=CARTESIAN_POINT ( 'NONE',  ( -93.35499999999998977, -4.716976649647093289, -6.492361379858945902 ) ) ;
#36011=CARTESIAN_POINT ( 'NONE',  ( -136.5570736234661808, -1.166476076187852838E-15, -9.524999999999991473 ) ) ;
#36014=CARTESIAN_POINT ( 'NONE',  ( -76.25707362346616947, 5.598654528085800663, -7.705886871421367523 ) ) ;
#36020=CARTESIAN_POINT ( 'NONE',  ( -18.96673260019409213, -11.60629586887077203, 3.061218697616527429 ) ) ;
#36023=CARTESIAN_POINT ( 'NONE',  ( -124.8549999999999898, 4.716976649647094177, 6.492361379858945902 ) ) ;
#36025=CARTESIAN_POINT ( 'NONE',  ( -126.5949999999999847, 2.607480562269073321, 8.024999999999991473 ) ) ;
#36034=CARTESIAN_POINT ( 'NONE',  ( -167.3070736234662093, -10.01517768586948698, 6.132527647946031529E-16 ) ) ;
#36035=CARTESIAN_POINT ( 'NONE',  ( -167.5429263765338135, 9.058813317711329915, 2.943386871421369566 ) ) ;
#36043=CARTESIAN_POINT ( 'NONE',  ( -82.19292637653380496, -10.01517768586948698, 6.132527647946031529E-16 ) ) ;
#36046=EDGE_CURVE ( 'NONE', #24116, #13211, #49809, .T. ) ;
#36057=CARTESIAN_POINT ( 'NONE',  ( -103.9429263765338050, 0.000000000000000000, 9.524999999999991473 ) ) ;
#36064=CARTESIAN_POINT ( 'NONE',  ( -106.5549999999999784, 0.000000000000000000, 8.024999999999991473 ) ) ;
#36074=CARTESIAN_POINT ( 'NONE',  ( -68.54499999999998749, -7.632228543268600340, -2.479861379858950166 ) ) ;
#36081=ORIENTED_EDGE ( 'NONE', *, *, #50914, .T. ) ;
#36088=ORIENTED_EDGE ( 'NONE', *, *, #16931, .F. ) ;
#36093=CARTESIAN_POINT ( 'NONE',  ( -169.8570736234661922, -5.598654528085803328, -7.705886871421366635 ) ) ;
#36096=CARTESIAN_POINT ( 'NONE',  ( -102.0570736234661808, 0.000000000000000000, 9.524999999999991473 ) ) ;
#36104=CARTESIAN_POINT ( 'NONE',  ( -105.8070736234661666, 10.01517768586948698, -1.839758294383808966E-15 ) ) ;
#36109=CARTESIAN_POINT ( 'NONE',  ( -152.4550000000000125, 7.632228543268599452, -2.479861379858951942 ) ) ;
#36111=CARTESIAN_POINT ( 'NONE',  ( -60.05707362346616662, 0.000000000000000000, 9.524999999999991473 ) ) ;
#36113=CARTESIAN_POINT ( 'NONE',  ( -153.2949999999999875, -2.607480562269069768, 8.024999999999991473 ) ) ;
#36114=CARTESIAN_POINT ( 'NONE',  ( -145.7950000000000443, 2.607480562269069324, -8.024999999999993250 ) ) ;
#36123=CARTESIAN_POINT ( 'NONE',  ( -59.75499999999998835, 4.716976649647091513, -6.492361379858946790 ) ) ;
#36126=CARTESIAN_POINT ( 'NONE',  ( -66.29499999999998749, -2.607480562269069768, 8.024999999999991473 ) ) ;
#36138=CARTESIAN_POINT ( 'NONE',  ( -178.4929263765338021, -8.102448949553174629, 5.886773742842742685 ) ) ;
#36141=CARTESIAN_POINT ( 'NONE',  ( -195.0000000000000000, 1.166476076187852838E-15, -9.524999999999991473 ) ) ;
#36147=( BOUNDED_CURVE ( )  B_SPLINE_CURVE ( 2, ( #61753, #40705, #8676, #20251, #14647, #56860, #14287, #30102, #25188, #35050, #56498 ),
 .UNSPECIFIED., .F., .F. ) 
 B_SPLINE_CURVE_WITH_KNOTS ( ( 3, 2, 2, 2, 2, 3 ),
 ( 0.2608695652173851354, 0.2630434782608633282, 0.2652173913043415765, 0.2673913043478197693, 0.2695652173912979621, 0.2717391304347761549 ),
 .UNSPECIFIED. ) 
 CURVE ( )  GEOMETRIC_REPRESENTATION_ITEM ( )  RATIONAL_B_SPLINE_CURVE ( ( 1.000000000000138778, 0.9510565162950147533, 1.000000000000000000, 0.9510565162951535312, 1.000000000000000000, 0.9510565162951535312, 1.000000000000000000, 0.9510565162951535312, 1.000000000000000000, 0.9510565162952985263, 0.9999999999998550049 ) ) 
 REPRESENTATION_ITEM ( '' )  );
#36149=EDGE_CURVE ( 'NONE', #17985, #31091, #61923, .T. ) ;
#36153=CARTESIAN_POINT ( 'NONE',  ( -77.00707362346618368, -8.102448949553174629, -5.886773742842741797 ) ) ;
#36158=CARTESIAN_POINT ( 'NONE',  ( -108.2070736234670818, 3.094860106633760211, 9.524999999988855492 ) ) ;
#36169=CARTESIAN_POINT ( 'NONE',  ( -112.7949999999999733, 2.607480562269068880, -8.024999999999993250 ) ) ;
#36172=CARTESIAN_POINT ( 'NONE',  ( -156.4429263765338192, -1.166476076187852838E-15, -9.524999999999991473 ) ) ;
#36175=CARTESIAN_POINT ( 'NONE',  ( -179.0070736234661695, -8.102448949553174629, -5.886773742842741797 ) ) ;
#36178=DIRECTION ( 'NONE',  ( -1.000000000000000000, -0.000000000000000000, -0.000000000000000000 ) ) ;
#36189=CARTESIAN_POINT ( 'NONE',  ( -61.94292637653379785, 0.000000000000000000, 9.524999999999991473 ) ) ;
#36190=FACE_OUTER_BOUND ( 'NONE', #2976, .T. ) ;
#36191=CARTESIAN_POINT ( 'NONE',  ( -124.7049999999999841, 2.607480562269073321, 8.024999999999991473 ) ) ;
#36206=CARTESIAN_POINT ( 'NONE',  ( -182.9050000000000011, 2.607480562269068880, -8.024999999999993250 ) ) ;
#36209=CARTESIAN_POINT ( 'NONE',  ( -51.05707362346617373, 0.000000000000000000, 9.524999999999991473 ) ) ;
#36211=CARTESIAN_POINT ( 'NONE',  ( -174.8949999999999818, 6.826472737025115478, 4.959722759717899443 ) ) ;
#36219=CARTESIAN_POINT ( 'NONE',  ( -88.70499999999998408, 2.607480562269073321, 8.024999999999991473 ) ) ;
#36222=CARTESIAN_POINT ( 'NONE',  ( -86.39499999999998181, -6.826472737025113702, -4.959722759717900331 ) ) ;
#36224=CARTESIAN_POINT ( 'NONE',  ( -71.09499999999999886, -2.607480562269071545, -8.024999999999991473 ) ) ;
#36234=CARTESIAN_POINT ( 'NONE',  ( -104.5429263765337993, 9.058813317711329915, 2.943386871421369566 ) ) ;
#36235=CARTESIAN_POINT ( 'NONE',  ( -129.7450000000000045, 4.716976649647094177, 6.492361379858945902 ) ) ;
#36247=TOROIDAL_SURFACE ( 'NONE', #64269, 9.525000000000000355, 1.000000000000000888 ) ;
#36255=CARTESIAN_POINT ( 'NONE',  ( -122.4549999999999983, 7.632228543268599452, -2.479861379858951942 ) ) ;
#36257=PLANE ( 'NONE',  #6146 ) ;
#36258=CARTESIAN_POINT ( 'NONE',  ( -121.4070736234661751, 3.094860106618428031, -9.524999999999993250 ) ) ;
#36285=CARTESIAN_POINT ( 'NONE',  ( -57.44292637653381206, -1.166476076187852838E-15, -9.524999999999991473 ) ) ;
#36288=CARTESIAN_POINT ( 'NONE',  ( -155.3050000000000068, 8.437984349512085203, -1.550032578732815448E-15 ) ) ;
#36296=CARTESIAN_POINT ( 'NONE',  ( -70.34292637653381064, -9.058813317711329915, 2.943386871421371787 ) ) ;
#36303=CARTESIAN_POINT ( 'NONE',  ( -61.55499999999998550, 0.000000000000000000, 8.024999999999991473 ) ) ;
#36307=CARTESIAN_POINT ( 'NONE',  ( -90.80707362346615241, 10.01517768586948698, -1.839758294383808966E-15 ) ) ;
#36316=CARTESIAN_POINT ( 'NONE',  ( -98.54499999999998749, -7.632228543268600340, -2.479861379858950166 ) ) ;
#36323=CARTESIAN_POINT ( 'NONE',  ( -135.4429263765338192, -1.166476076187852838E-15, -9.524999999999991473 ) ) ;
#36326=CARTESIAN_POINT ( 'NONE',  ( -156.4449999999999932, 0.000000000000000000, 8.024999999999991473 ) ) ;
#36342=ADVANCED_FACE ( 'NONE', ( #28419 ), #27392, .T. ) ;
#36346=CARTESIAN_POINT ( 'NONE',  ( -151.2549999999999955, -4.716976649647092401, 6.492361379858946790 ) ) ;
#36360=ORIENTED_EDGE ( 'NONE', *, *, #50771, .T. ) ;
#36364=CARTESIAN_POINT ( 'NONE',  ( -74.30499999999997840, 8.437984349512086979, -1.550032578732815448E-15 ) ) ;
#36365=CARTESIAN_POINT ( 'NONE',  ( -80.45707362346617231, -9.058813317711329915, 2.943386871421371787 ) ) ;
#36378=CARTESIAN_POINT ( 'NONE',  ( -47.39499999999998181, -6.826472737025115478, -4.959722759717899443 ) ) ;
#36390=CARTESIAN_POINT ( 'NONE',  ( -97.70499999999998408, 2.607480562269073321, 8.024999999999991473 ) ) ;
#36395=CARTESIAN_POINT ( 'NONE',  ( -129.8070736234661240, 10.01517768586948698, -1.839758294383808571E-15 ) ) ;
#36399=CARTESIAN_POINT ( 'NONE',  ( -74.00707362346615525, -8.102448949553172852, -5.886773742842741797 ) ) ;
#36401=CARTESIAN_POINT ( 'NONE',  ( -92.39292637653379359, 8.102448949553176405, 5.886773742842740909 ) ) ;
#36405=CARTESIAN_POINT ( 'NONE',  ( -15.32976068146453485, -10.90871211463571555, -4.999999999999998224 ) ) ;
#36409=CARTESIAN_POINT ( 'NONE',  ( -107.4549999999999983, 7.632228543268599452, -2.479861379858951942 ) ) ;
#36411=CARTESIAN_POINT ( 'NONE',  ( -128.0949999999999704, -2.607480562269071545, -8.024999999999991473 ) ) ;
#36412=CARTESIAN_POINT ( 'NONE',  ( -112.5570736234661808, -1.166476076187852838E-15, -9.524999999999991473 ) ) ;
#36419=CARTESIAN_POINT ( 'NONE',  ( -160.3429263765337964, -9.058813317711329915, 2.943386871421371787 ) ) ;
#36429=CARTESIAN_POINT ( 'NONE',  ( -85.79292637653378506, -3.094860106618429807, 9.524999999999991473 ) ) ;
#36431=CARTESIAN_POINT ( 'NONE',  ( -166.0429263765338135, -9.058813317711329915, -2.943386871421370898 ) ) ;
#36436=CARTESIAN_POINT ( 'NONE',  ( -99.44292637653380496, -1.166476076187852838E-15, -9.524999999999991473 ) ) ;
#36448=CARTESIAN_POINT ( 'NONE',  ( -102.0570736234661808, 0.000000000000000000, 9.524999999999991473 ) ) ;
#36450=CARTESIAN_POINT ( 'NONE',  ( -99.20499999999998408, -2.607480562269071545, -8.024999999999991473 ) ) ;
#36458=CARTESIAN_POINT ( 'NONE',  ( -74.99499999999999034, -6.826472737025115478, 4.959722759717900331 ) ) ;
#36469=VERTEX_POINT ( 'NONE', #48573 ) ;
#36470=DIRECTION ( 'NONE',  ( -1.000000000000000000, -0.000000000000000000, -0.000000000000000000 ) ) ;
#36474=CARTESIAN_POINT ( 'NONE',  ( -170.6070736234661638, -8.102448949553172852, 5.886773742842742685 ) ) ;
#36476=CARTESIAN_POINT ( 'NONE',  ( -100.8570736234661780, -5.598654528085803328, -7.705886871421366635 ) ) ;
#36479=CARTESIAN_POINT ( 'NONE',  ( -64.55707362346618083, -1.166476076187852838E-15, -9.524999999999991473 ) ) ;
#36483=CARTESIAN_POINT ( 'NONE',  ( -114.8070736234661808, 10.01517768586948698, -1.839758294383808966E-15 ) ) ;
#36485=CARTESIAN_POINT ( 'NONE',  ( -140.1550000000000011, 7.632228543268600340, 2.479861379858949277 ) ) ;
#36488=CARTESIAN_POINT ( 'NONE',  ( -152.8449999999999989, -7.632228543268599452, 2.479861379858951054 ) ) ;
#36489=CARTESIAN_POINT ( 'NONE',  ( -148.0449999999999875, 7.632228543268600340, 2.479861379858949277 ) ) ;
#36493=CARTESIAN_POINT ( 'NONE',  ( -180.8070736234661524, 10.01517768586948698, -1.839758294383808966E-15 ) ) ;
#36497=CARTESIAN_POINT ( 'NONE',  ( -63.20499999999998408, -2.607480562269071545, -8.024999999999991473 ) ) ;
#36501=CARTESIAN_POINT ( 'NONE',  ( -65.09499999999998465, -2.607480562269071545, -8.024999999999991473 ) ) ;
#36504=DIRECTION ( 'NONE',  ( 0.000000000000000000, 0.000000000000000000, 1.000000000000000000 ) ) ;
#36507=CARTESIAN_POINT ( 'NONE',  ( -151.9429263765338192, 0.000000000000000000, 9.524999999999991473 ) ) ;
#36523=CARTESIAN_POINT ( 'NONE',  ( -195.0000000000000000, 1.166476076187852838E-15, -9.524999999999991473 ) ) ;
#36527=CARTESIAN_POINT ( 'NONE',  ( -77.45707362346617231, -9.058813317711329915, 2.943386871421371787 ) ) ;
#36529=ORIENTED_EDGE ( 'NONE', *, *, #61769, .F. ) ;
#36541=CARTESIAN_POINT ( 'NONE',  ( -100.9449999999999932, -9.827790563157499189E-16, -8.024999999999991473 ) ) ;
#36550=CYLINDRICAL_SURFACE ( 'NONE', #64342, 9.524999999999991473 ) ;
#36557=CARTESIAN_POINT ( 'NONE',  ( -141.4429263765337907, -1.166476076187852838E-15, -9.524999999999991473 ) ) ;
#36576=CARTESIAN_POINT ( 'NONE',  ( -178.1049999999999329, -6.826472737025115478, 4.959722759717900331 ) ) ;
#36579=CARTESIAN_POINT ( 'NONE',  ( -179.8449999999999989, -7.632228543268599452, 2.479861379858951054 ) ) ;
#36581=CARTESIAN_POINT ( 'NONE',  ( -178.0450000000000159, 7.632228543268600340, 2.479861379858949277 ) ) ;
#36587=CARTESIAN_POINT ( 'NONE',  ( -97.25499999999999545, -4.716976649647092401, 6.492361379858946790 ) ) ;
#36593=CARTESIAN_POINT ( 'NONE',  ( -88.94499999999997897, -9.827790563157499189E-16, -8.024999999999991473 ) ) ;
#36596=CARTESIAN_POINT ( 'NONE',  ( -68.99499999999999034, -6.826472737025115478, 4.959722759717900331 ) ) ;
#36600=DIRECTION ( 'NONE',  ( -1.000000000000000000, -0.000000000000000000, -0.000000000000000000 ) ) ;
#36602=( BOUNDED_CURVE ( )  B_SPLINE_CURVE ( 2, ( #26234, #49122, #59624, #17107, #27248, #6169, #38581, #10762, #63865, #32212, #58952 ),
 .UNSPECIFIED., .F., .F. ) 
 B_SPLINE_CURVE_WITH_KNOTS ( ( 3, 2, 2, 2, 2, 3 ),
 ( 0.3260869565217314192, 0.3282608695652096120, 0.3304347826086878048, 0.3326086956521661087, 0.3347826086956443015, 0.3369565217391224943 ),
 .UNSPECIFIED. ) 
 CURVE ( )  GEOMETRIC_REPRESENTATION_ITEM ( )  RATIONAL_B_SPLINE_CURVE ( ( 1.000000000000173639, 0.9510565162949797813, 1.000000000000000000, 0.9510565162951535312, 1.000000000000000000, 0.9510565162951535312, 1.000000000000000000, 0.9510565162951535312, 1.000000000000000000, 0.9510565162953322771, 0.9999999999998212541 ) ) 
 REPRESENTATION_ITEM ( '' )  );
#36607=CARTESIAN_POINT ( 'NONE',  ( -132.4449999999999932, 0.000000000000000000, 8.024999999999991473 ) ) ;
#36620=CARTESIAN_POINT ( 'NONE',  ( -118.2549999999999812, -4.716976649647092401, 6.492361379858946790 ) ) ;
#36623=DIRECTION ( 'NONE',  ( -1.000000000000000000, -0.000000000000000000, -0.000000000000000000 ) ) ;
#36632=VERTEX_POINT ( 'NONE', #36189 ) ;
#36638=VECTOR ( 'NONE', #27792, 1000.000000000000000 ) ;
#36643=CARTESIAN_POINT ( 'NONE',  ( -59.84292637653379643, 9.058813317711329915, -2.943386871421373119 ) ) ;
#36647=CARTESIAN_POINT ( 'NONE',  ( -149.7549999999999955, 4.716976649647091513, -6.492361379858946790 ) ) ;
#36656=DIRECTION ( 'NONE',  ( 0.000000000000000000, 0.000000000000000000, 1.000000000000000000 ) ) ;
#36658=CARTESIAN_POINT ( 'NONE',  ( -66.50499999999996703, -6.826472737025115478, -4.959722759717899443 ) ) ;
#36662=DIRECTION ( 'NONE',  ( -1.000000000000000000, -0.000000000000000000, -0.000000000000000000 ) ) ;
#36666=EDGE_CURVE ( 'NONE', #45861, #50251, #11270, .T. ) ;
#36675=CARTESIAN_POINT ( 'NONE',  ( -97.64499999999999602, 4.716976649647091513, -6.492361379858946790 ) ) ;
#36682=CARTESIAN_POINT ( 'NONE',  ( -129.8929263765338362, -8.102448949553172852, -5.886773742842741797 ) ) ;
#36685=CARTESIAN_POINT ( 'NONE',  ( -158.2450000000000045, -4.716976649647093289, -6.492361379858945902 ) ) ;
#36702=CARTESIAN_POINT ( 'NONE',  ( -152.7549999999999955, 4.716976649647091513, -6.492361379858946790 ) ) ;
#36703=ORIENTED_EDGE ( 'NONE', *, *, #18026, .T. ) ;
#36708=ADVANCED_FACE ( 'NONE', ( #26944 ), #17500, .T. ) ;
#36714=CARTESIAN_POINT ( 'NONE',  ( -60.20499999999998408, -2.607480562269071545, -8.024999999999991473 ) ) ;
#36720=AXIS2_PLACEMENT_3D ( 'NONE', #68878, #63581, #62867 ) ;
#36722=VERTEX_POINT ( 'NONE', #64951 ) ;
#36726=CARTESIAN_POINT ( 'NONE',  ( -179.4550000000000125, 7.632228543268599452, -2.479861379858951942 ) ) ;
#36731=ORIENTED_EDGE ( 'NONE', *, *, #41473, .F. ) ;
#36738=CARTESIAN_POINT ( 'NONE',  ( -99.05499999999999261, -9.827790563157499189E-16, -8.024999999999991473 ) ) ;
#36742=CARTESIAN_POINT ( 'NONE',  ( -128.7570736234661695, -5.598654528085801552, 7.705886871421367523 ) ) ;
#36745=CARTESIAN_POINT ( 'NONE',  ( -71.90707362346614673, -3.094860106618429807, 9.524999999999991473 ) ) ;
#36748=CARTESIAN_POINT ( 'NONE',  ( -19.33026007562384052, -11.73551398946232460, 2.520887762979119540 ) ) ;
#36750=CARTESIAN_POINT ( 'NONE',  ( -116.3049999999999784, 8.437984349512085203, -1.550032578732815448E-15 ) ) ;
#36754=CARTESIAN_POINT ( 'NONE',  ( -122.5449999999999875, -7.632228543268600340, -2.479861379858950166 ) ) ;
#36756=CARTESIAN_POINT ( 'NONE',  ( -111.5070736234661837, 8.102448949553176405, 5.886773742842740909 ) ) ;
#36760=CARTESIAN_POINT ( 'NONE',  ( -160.0429263765338135, -9.058813317711329915, -2.943386871421370898 ) ) ;
#36770=CARTESIAN_POINT ( 'NONE',  ( -76.04292637653379927, -9.058813317711329915, -2.943386871421370898 ) ) ;
#36777=CARTESIAN_POINT ( 'NONE',  ( -180.8050000000000068, -8.437984349512086979, 5.166775262442717831E-16 ) ) ;
#36781=VERTEX_POINT ( 'NONE', #21705 ) ;
#36782=CARTESIAN_POINT ( 'NONE',  ( -102.8929263765337936, -8.102448949553174629, -5.886773742842741797 ) ) ;
#36788=CARTESIAN_POINT ( 'NONE',  ( -93.80499999999999261, -8.437984349512086979, 5.166775262442717831E-16 ) ) ;
#36796=CARTESIAN_POINT ( 'NONE',  ( -70.64499999999998181, 4.716976649647091513, -6.492361379858946790 ) ) ;
#36811=CARTESIAN_POINT ( 'NONE',  ( -160.4070736234661751, 3.094860106618428031, -9.524999999999993250 ) ) ;
#36814=CARTESIAN_POINT ( 'NONE',  ( -99.95707362346617231, 9.058813317711329915, -2.943386871421373119 ) ) ;
#36817=CARTESIAN_POINT ( 'NONE',  ( -107.6929263765338050, 10.01517768586948698, -1.839758294383808966E-15 ) ) ;
#36823=CARTESIAN_POINT ( 'NONE',  ( -143.4550000000000125, 7.632228543268599452, -2.479861379858951942 ) ) ;
#36827=CARTESIAN_POINT ( 'NONE',  ( -151.9449999999999932, -9.827790563157499189E-16, -8.024999999999991473 ) ) ;
#36829=CARTESIAN_POINT ( 'NONE',  ( -141.1449999999999818, -4.716976649647092401, 6.492361379858946790 ) ) ;
#36833=ADVANCED_FACE ( 'NONE', ( #67054 ), #8316, .T. ) ;
#36836=CARTESIAN_POINT ( 'NONE',  ( -50.90499999999997982, 2.607480562269068880, -8.024999999999993250 ) ) ;
#36839=CARTESIAN_POINT ( 'NONE',  ( -142.5570736234661808, -1.166476076187852838E-15, -9.524999999999991473 ) ) ;
#36840=CARTESIAN_POINT ( 'NONE',  ( -154.5570736234661808, -1.166476076187852838E-15, -9.524999999999991473 ) ) ;
#36849=CARTESIAN_POINT ( 'NONE',  ( -78.59292637653379643, -3.094860106618431139, -9.524999999999991473 ) ) ;
#36860=ORIENTED_EDGE ( 'NONE', *, *, #32313, .T. ) ;
#36867=CARTESIAN_POINT ( 'NONE',  ( -85.94292637653380496, 0.000000000000000000, 9.524999999999991473 ) ) ;
#36870=CARTESIAN_POINT ( 'NONE',  ( -98.24499999999999034, -4.716976649647093289, -6.492361379858945902 ) ) ;
#36871=ORIENTED_EDGE ( 'NONE', *, *, #5075, .F. ) ;
#36884=CARTESIAN_POINT ( 'NONE',  ( -140.9929263765338305, 8.102448949553172852, -5.886773742842744461 ) ) ;
#36887=( BOUNDED_CURVE ( )  B_SPLINE_CURVE ( 2, ( #14955, #67351, #19147, #68067, #41003, #40650, #62059, #68398, #20192, #35702, #41347 ),
 .UNSPECIFIED., .F., .F. ) 
 B_SPLINE_CURVE_WITH_KNOTS ( ( 3, 2, 2, 2, 2, 3 ),
 ( 0.3478260869565133473, 0.3499999999999915401, 0.3521739130434697884, 0.3543478260869480367, 0.3565217391304262295, 0.3586956521739044224 ),
 .UNSPECIFIED. ) 
 CURVE ( )  GEOMETRIC_REPRESENTATION_ITEM ( )  RATIONAL_B_SPLINE_CURVE ( ( 1.000000000000188738, 0.9510565162949647933, 1.000000000000000000, 0.9510565162951535312, 1.000000000000000000, 0.9510565162951535312, 1.000000000000000000, 0.9510565162951535312, 1.000000000000000000, 0.9510565162953472651, 0.9999999999998062661 ) ) 
 REPRESENTATION_ITEM ( '' )  );
#36905=CARTESIAN_POINT ( 'NONE',  ( -165.8050000000000068, -8.437984349512085203, 5.166775262442717831E-16 ) ) ;
#36908=CARTESIAN_POINT ( 'NONE',  ( -182.9949999999999761, -6.826472737025115478, 4.959722759717900331 ) ) ;
#36909=EDGE_CURVE ( 'NONE', #32880, #39571, #50186, .T. ) ;
#36911=CARTESIAN_POINT ( 'NONE',  ( -167.3949999999999534, -6.826472737025113702, -4.959722759717900331 ) ) ;
#36913=LINE ( 'NONE', #31225, #62736 ) ;
#36916=CARTESIAN_POINT ( 'NONE',  ( -86.90499999999998693, 2.607480562269068880, -8.024999999999993250 ) ) ;
#36918=CARTESIAN_POINT ( 'NONE',  ( -169.1070736234661922, 8.102448949553172852, -5.886773742842744461 ) ) ;
#36920=CARTESIAN_POINT ( 'NONE',  ( -91.64499999999999602, 4.716976649647091513, -6.492361379858946790 ) ) ;
#36923=CARTESIAN_POINT ( 'NONE',  ( -171.4429263765337907, -1.166476076187852838E-15, -9.524999999999991473 ) ) ;
#36926=CARTESIAN_POINT ( 'NONE',  ( -74.39292637653380780, 8.102448949553176405, 5.886773742842740909 ) ) ;
#36931=LINE ( 'NONE', #58345, #66323 ) ;
#36948=CARTESIAN_POINT ( 'NONE',  ( -126.6549999999999869, -7.632228543268600340, -2.479861379858950166 ) ) ;
#36949=ORIENTED_EDGE ( 'NONE', *, *, #35675, .T. ) ;
#36952=CARTESIAN_POINT ( 'NONE',  ( -195.0000000000000000, 1.166476076187852838E-15, -9.524999999999991473 ) ) ;
#36961=CARTESIAN_POINT ( 'NONE',  ( -54.65707362346616804, 9.058813317711329915, 2.943386871421369566 ) ) ;
#36965=ORIENTED_EDGE ( 'NONE', *, *, #24005, .T. ) ;
#36978=CARTESIAN_POINT ( 'NONE',  ( -57.29292637653379217, 3.094860106618428031, -9.524999999999993250 ) ) ;
#36979=CARTESIAN_POINT ( 'NONE',  ( -151.5550000000000068, 0.000000000000000000, 8.024999999999991473 ) ) ;
#36987=VERTEX_POINT ( 'NONE', #8657 ) ;
#36989=EDGE_CURVE ( 'NONE', #12632, #43539, #30418, .T. ) ;
#36992=CARTESIAN_POINT ( 'NONE',  ( -84.44292637653380496, -1.166476076187852838E-15, -9.524999999999991473 ) ) ;
#36993=CARTESIAN_POINT ( 'NONE',  ( -68.15499999999997272, 7.632228543268600340, 2.479861379858949277 ) ) ;
#36998=EDGE_CURVE ( 'NONE', #6742, #65490, #13399, .T. ) ;
#37012=CARTESIAN_POINT ( 'NONE',  ( -121.9449999999999932, -9.827790563157499189E-16, -8.024999999999991473 ) ) ;
#37014=CARTESIAN_POINT ( 'NONE',  ( -88.79499999999998749, 2.607480562269068880, -8.024999999999993250 ) ) ;
#37021=ORIENTED_EDGE ( 'NONE', *, *, #16044, .T. ) ;
#37022=CARTESIAN_POINT ( 'NONE',  ( -132.8929263765337794, -8.102448949553172852, -5.886773742842741797 ) ) ;
#37025=CARTESIAN_POINT ( 'NONE',  ( -159.2949999999999875, -2.607480562269069768, 8.024999999999991473 ) ) ;
#37033=CARTESIAN_POINT ( 'NONE',  ( -144.4429263765337907, -1.166476076187852838E-15, -9.524999999999991473 ) ) ;
#37038=CARTESIAN_POINT ( 'NONE',  ( -151.7050000000000125, 2.607480562269072433, 8.024999999999991473 ) ) ;
#37050=CARTESIAN_POINT ( 'NONE',  ( -66.95499999999998408, -7.632228543268599452, 2.479861379858951054 ) ) ;
#37065=CARTESIAN_POINT ( 'NONE',  ( -47.69499999999999318, -8.437984349512085203, 5.166775262442717831E-16 ) ) ;
#37066=VERTEX_POINT ( 'NONE', #4042 ) ;
#37068=VECTOR ( 'NONE', #7472, 1000.000000000000000 ) ;
#37073=LINE ( 'NONE', #63063, #57999 ) ;
#37078=CARTESIAN_POINT ( 'NONE',  ( -91.55499999999997840, 0.000000000000000000, 8.024999999999991473 ) ) ;
#37081=CARTESIAN_POINT ( 'NONE',  ( -132.2070736234661297, 3.094860106618433360, 9.524999999999991473 ) ) ;
#37086=CARTESIAN_POINT ( 'NONE',  ( -62.15707362346617515, -9.058813317711329915, -2.943386871421370898 ) ) ;
#37088=CARTESIAN_POINT ( 'NONE',  ( -80.54292637653379927, 9.058813317711329915, 2.943386871421369566 ) ) ;
#37090=DIRECTION ( 'NONE',  ( 0.000000000000000000, 0.000000000000000000, 1.000000000000000000 ) ) ;
#37094=CARTESIAN_POINT ( 'NONE',  ( -109.4049999999999727, -2.607480562269069768, 8.024999999999991473 ) ) ;
#37097=CARTESIAN_POINT ( 'NONE',  ( -128.8449999999999989, -7.632228543268599452, 2.479861379858951054 ) ) ;
#37105=CARTESIAN_POINT ( 'NONE',  ( -161.2429263765338021, 5.598654528085804216, 7.705886871421366635 ) ) ;
#37106=( NAMED_UNIT ( * ) SI_UNIT ( $, .STERADIAN. ) SOLID_ANGLE_UNIT ( ) );
#37109=CARTESIAN_POINT ( 'NONE',  ( -190.0000000000000000, 0.000000000000000000, 0.000000000000000000 ) ) ;
#37115=CARTESIAN_POINT ( 'NONE',  ( -75.44292637653379074, -1.166476076187852838E-15, -9.524999999999991473 ) ) ;
#37123=CARTESIAN_POINT ( 'NONE',  ( -181.5550000000000068, 0.000000000000000000, 8.024999999999991473 ) ) ;
#37133=CARTESIAN_POINT ( 'NONE',  ( -90.80499999999996419, -8.437984349512086979, 5.166775262442717831E-16 ) ) ;
#37140=CARTESIAN_POINT ( 'NONE',  ( -83.60707362346617799, -8.102448949553174629, 5.886773742842742685 ) ) ;
#37144=CARTESIAN_POINT ( 'NONE',  ( -72.74499999999999034, 4.716976649647094177, 6.492361379858945902 ) ) ;
#37145=VERTEX_POINT ( 'NONE', #64876 ) ;
#37162=CARTESIAN_POINT ( 'NONE',  ( -160.2570736234661979, 5.598654528085800663, -7.705886871421367523 ) ) ;
#37165=CARTESIAN_POINT ( 'NONE',  ( -94.55707362346616662, -1.166476076187852838E-15, -9.524999999999991473 ) ) ;
#37171=FACE_OUTER_BOUND ( 'NONE', #32232, .T. ) ;
#37174=CARTESIAN_POINT ( 'NONE',  ( -143.6049999999999613, 6.826472737025113702, -4.959722759717902107 ) ) ;
#37177=CARTESIAN_POINT ( 'NONE',  ( -157.9449999999999932, -9.827790563157499189E-16, -8.024999999999991473 ) ) ;
#37178=CARTESIAN_POINT ( 'NONE',  ( -142.6449999999999818, 4.716976649647091513, -6.492361379858946790 ) ) ;
#37185=CARTESIAN_POINT ( 'NONE',  ( -49.40499999999996561, -2.607480562269069768, 8.024999999999991473 ) ) ;
#37188=CARTESIAN_POINT ( 'NONE',  ( -52.49292637653380922, -8.102448949553174629, 5.886773742842742685 ) ) ;
#37189=DIRECTION ( 'NONE',  ( -1.000000000000000000, -0.000000000000000000, -0.000000000000000000 ) ) ;
#37190=AXIS2_PLACEMENT_3D ( 'NONE', #62660, #41602, #3544 ) ;
#37213=CARTESIAN_POINT ( 'NONE',  ( -172.9429263765337907, 0.000000000000000000, 9.524999999999991473 ) ) ;
#37216=CARTESIAN_POINT ( 'NONE',  ( -101.3929263765337794, 8.102448949553176405, 5.886773742842740909 ) ) ;
#37219=CARTESIAN_POINT ( 'NONE',  ( -85.04292637653381348, -9.058813317711329915, -2.943386871421370898 ) ) ;
#37222=EDGE_CURVE ( 'NONE', #56906, #69443, #60624, .T. ) ;
#37224=CARTESIAN_POINT ( 'NONE',  ( -101.0949999999999989, -2.607480562269071545, -8.024999999999991473 ) ) ;
#37227=CARTESIAN_POINT ( 'NONE',  ( -140.7570736234661695, -5.598654528085801552, 7.705886871421367523 ) ) ;
#37240=VERTEX_POINT ( 'NONE', #44521 ) ;
#37241=DIRECTION ( 'NONE',  ( 0.000000000000000000, 0.000000000000000000, 1.000000000000000000 ) ) ;
#37258=CARTESIAN_POINT ( 'NONE',  ( -153.5929263765342228, -3.094860106624985452, -9.524999999995230837 ) ) ;
#37259=CARTESIAN_POINT ( 'NONE',  ( -172.1050000000000182, -6.826472737025115478, 4.959722759717900331 ) ) ;
#37263=CARTESIAN_POINT ( 'NONE',  ( -46.55707362346617373, -1.166476076187852838E-15, -9.524999999999991473 ) ) ;
#37264=CARTESIAN_POINT ( 'NONE',  ( -171.1449999999999818, -4.716976649647092401, 6.492361379858946790 ) ) ;
#37269=CARTESIAN_POINT ( 'NONE',  ( -15.00000000000000000, 10.90871211463577239, 5.000000000000000888 ) ) ;
#37270=CARTESIAN_POINT ( 'NONE',  ( -78.65499999999998693, -7.632228543268600340, -2.479861379858950166 ) ) ;
#37276=CARTESIAN_POINT ( 'NONE',  ( -80.69499999999999318, -8.437984349512086979, 5.166775262442717831E-16 ) ) ;
#37278=CARTESIAN_POINT ( 'NONE',  ( -134.7570736234661695, -5.598654528085801552, 7.705886871421367523 ) ) ;
#37288=ADVANCED_FACE ( 'NONE', ( #1844 ), #17753, .T. ) ;
#37289=FACE_OUTER_BOUND ( 'NONE', #51015, .T. ) ;
#37303=CARTESIAN_POINT ( 'NONE',  ( -120.8049999999999784, -8.437984349512086979, 5.166775262442717831E-16 ) ) ;
#37332=CARTESIAN_POINT ( 'NONE',  ( -58.34292637653379643, -9.058813317711329915, 2.943386871421371787 ) ) ;
#37335=CARTESIAN_POINT ( 'NONE',  ( -144.8049999999999216, -8.437984349512085203, 5.166775262442717831E-16 ) ) ;
#37348=CARTESIAN_POINT ( 'NONE',  ( -63.65499999999998693, -7.632228543268600340, -2.479861379858950166 ) ) ;
#37363=AXIS2_PLACEMENT_3D ( 'NONE', #18613, #29121, #49239 ) ;
#37364=CARTESIAN_POINT ( 'NONE',  ( -113.6949999999999790, -8.437984349512086979, 5.166775262442717831E-16 ) ) ;
#37366=CARTESIAN_POINT ( 'NONE',  ( -86.09499999999997044, -2.607480562269071545, -8.024999999999991473 ) ) ;
#37373=CARTESIAN_POINT ( 'NONE',  ( -136.9429263765338192, 0.000000000000000000, 9.524999999999991473 ) ) ;
#37376=CARTESIAN_POINT ( 'NONE',  ( -146.0949999999999989, -2.607480562269071545, -8.024999999999991473 ) ) ;
#37381=CARTESIAN_POINT ( 'NONE',  ( -46.94499999999998607, -9.827790563157499189E-16, -8.024999999999991473 ) ) ;
#37393=EDGE_LOOP ( 'NONE', ( #25596, #17432, #20292, #51546 ) ) ;
#37394=CARTESIAN_POINT ( 'NONE',  ( -149.0049999999999386, 6.826472737025115478, 4.959722759717899443 ) ) ;
#37403=CARTESIAN_POINT ( 'NONE',  ( -58.94292637653381206, 0.000000000000000000, 9.524999999999991473 ) ) ;
#37410=CARTESIAN_POINT ( 'NONE',  ( -65.15499999999998693, 7.632228543268600340, 2.479861379858949277 ) ) ;
#37411=CARTESIAN_POINT ( 'NONE',  ( -116.8449999999999847, -7.632228543268599452, 2.479861379858951054 ) ) ;
#37415=ORIENTED_EDGE ( 'NONE', *, *, #11363, .T. ) ;
#37426=CARTESIAN_POINT ( 'NONE',  ( -180.3549999999999898, -4.716976649647093289, -6.492361379858945902 ) ) ;
#37427=ORIENTED_EDGE ( 'NONE', *, *, #1701, .F. ) ;
#37429=( BOUNDED_CURVE ( )  B_SPLINE_CURVE ( 2, ( #46917, #52514, #14170, #46207, #67629, #51115, #4259, #14873, #2859, #3195, #30304 ),
 .UNSPECIFIED., .F., .F. ) 
 B_SPLINE_CURVE_WITH_KNOTS ( ( 3, 2, 2, 2, 2, 3 ),
 ( 0.9021739130434782705, 0.9043478260869565188, 0.9065217391304347672, 0.9086956521739130155, 0.9108695652173912638, 0.9130434782608695121 ),
 .UNSPECIFIED. ) 
 CURVE ( )  GEOMETRIC_REPRESENTATION_ITEM ( )  RATIONAL_B_SPLINE_CURVE ( ( 1.000000000000000000, 0.9510565162951535312, 1.000000000000000000, 0.9510565162951535312, 1.000000000000000000, 0.9510565162951535312, 1.000000000000000000, 0.9510565162951535312, 1.000000000000000000, 0.9510565162951535312, 1.000000000000000000 ) ) 
 REPRESENTATION_ITEM ( '' )  );
#37439=CARTESIAN_POINT ( 'NONE',  ( -93.20499999999998408, -2.607480562269071545, -8.024999999999991473 ) ) ;
#37443=CARTESIAN_POINT ( 'NONE',  ( -132.5070736234661410, 8.102448949553176405, 5.886773742842740909 ) ) ;
#37447=CARTESIAN_POINT ( 'NONE',  ( -64.40707362346617515, 3.094860106618428031, -9.524999999999993250 ) ) ;
#37455=CARTESIAN_POINT ( 'NONE',  ( -111.3549999999999898, -4.716976649647093289, -6.492361379858945902 ) ) ;
#37458=CARTESIAN_POINT ( 'NONE',  ( -116.8449999999999847, -7.632228543268599452, 2.479861379858951054 ) ) ;
#37466=CARTESIAN_POINT ( 'NONE',  ( -158.3929263765338078, 8.102448949553176405, 5.886773742842740909 ) ) ;
#37467=CARTESIAN_POINT ( 'NONE',  ( -174.5949999999999989, 2.607480562269073321, 8.024999999999991473 ) ) ;
#37477=CARTESIAN_POINT ( 'NONE',  ( -80.09292637653379643, 3.094860106618433360, 9.524999999999991473 ) ) ;
#37478=CARTESIAN_POINT ( 'NONE',  ( -195.0000000000000000, 0.000000000000000000, 0.000000000000000000 ) ) ;
#37480=EDGE_CURVE ( 'NONE', #246, #23187, #38429, .T. ) ;
#37481=FACE_OUTER_BOUND ( 'NONE', #25138, .T. ) ;
#37482=EDGE_CURVE ( 'NONE', #32568, #6742, #9443, .T. ) ;
#37483=CARTESIAN_POINT ( 'NONE',  ( -182.7549999999999955, 4.716976649647091513, -6.492361379858946790 ) ) ;
#37493=CARTESIAN_POINT ( 'NONE',  ( -89.60499999999997556, 6.826472737025113702, -4.959722759717902107 ) ) ;
#37503=CARTESIAN_POINT ( 'NONE',  ( -69.29499999999995907, -2.607480562269069768, 8.024999999999991473 ) ) ;
#37510=ORIENTED_EDGE ( 'NONE', *, *, #59551, .F. ) ;
#37515=CARTESIAN_POINT ( 'NONE',  ( -125.7550000000000097, 4.716976649647091513, -6.492361379858946790 ) ) ;
#37516=ORIENTED_EDGE ( 'NONE', *, *, #11768, .T. ) ;
#37521=CARTESIAN_POINT ( 'NONE',  ( -155.3070736234662093, -10.01517768586948698, 6.132527647946031529E-16 ) ) ;
#37523=CARTESIAN_POINT ( 'NONE',  ( -95.45707362346617231, -9.058813317711329915, 2.943386871421371787 ) ) ;
#37533=CARTESIAN_POINT ( 'NONE',  ( -136.4050000000000296, -2.607480562269069768, 8.024999999999991473 ) ) ;
#37538=CARTESIAN_POINT ( 'NONE',  ( -148.9449999999999932, -9.827790563157499189E-16, -8.024999999999991473 ) ) ;
#37541=CARTESIAN_POINT ( 'NONE',  ( -135.8949999999999818, 6.826472737025115478, 4.959722759717899443 ) ) ;
#37549=CARTESIAN_POINT ( 'NONE',  ( -54.80499999999999261, -8.437984349512085203, 5.166775262442717831E-16 ) ) ;
#37557=CARTESIAN_POINT ( 'NONE',  ( -105.1429263765338078, 5.598654528085800663, -7.705886871421367523 ) ) ;
#37560=CARTESIAN_POINT ( 'NONE',  ( -152.5429263765338135, 9.058813317711329915, 2.943386871421369566 ) ) ;
#37569=ORIENTED_EDGE ( 'NONE', *, *, #6039, .F. ) ;
#37586=CARTESIAN_POINT ( 'NONE',  ( -99.14499999999998181, -4.716976649647092401, 6.492361379858946790 ) ) ;
#37593=CARTESIAN_POINT ( 'NONE',  ( -62.60707362346615668, -8.102448949553174629, 5.886773742842742685 ) ) ;
#37594=ORIENTED_EDGE ( 'NONE', *, *, #41087, .F. ) ;
#37607=CARTESIAN_POINT ( 'NONE',  ( -169.5570736234661808, -1.166476076187852838E-15, -9.524999999999991473 ) ) ;
#37612=CARTESIAN_POINT ( 'NONE',  ( -166.4049999999999727, -2.607480562269069768, 8.024999999999991473 ) ) ;
#37616=CARTESIAN_POINT ( 'NONE',  ( -182.3950000000000102, -6.826472737025115478, -4.959722759717899443 ) ) ;
#37617=CARTESIAN_POINT ( 'NONE',  ( -168.2949999999999875, -2.607480562269069768, 8.024999999999991473 ) ) ;
#37623=CARTESIAN_POINT ( 'NONE',  ( -86.00499999999999545, 6.826472737025116366, 4.959722759717898555 ) ) ;
#37627=CARTESIAN_POINT ( 'NONE',  ( -83.54499999999998749, -7.632228543268600340, -2.479861379858950166 ) ) ;
#37656=CARTESIAN_POINT ( 'NONE',  ( -125.6049999999999898, 6.826472737025113702, -4.959722759717902107 ) ) ;
#37662=CARTESIAN_POINT ( 'NONE',  ( -83.09292637653379643, 3.094860106618433360, 9.524999999999991473 ) ) ;
#37676=CARTESIAN_POINT ( 'NONE',  ( -104.5429263765337993, 9.058813317711329915, 2.943386871421369566 ) ) ;
#37685=CARTESIAN_POINT ( 'NONE',  ( -141.0549999999999784, -9.827790563157499189E-16, -8.024999999999991473 ) ) ;
#37690=SURFACE_SIDE_STYLE ('',( #10905 ) ) ;
#37697=CARTESIAN_POINT ( 'NONE',  ( -58.55499999999999261, 0.000000000000000000, 8.024999999999991473 ) ) ;
#37708=ORIENTED_EDGE ( 'NONE', *, *, #8895, .F. ) ;
#37716=CARTESIAN_POINT ( 'NONE',  ( -105.5949999999999989, 2.607480562269072433, 8.024999999999991473 ) ) ;
#37718=CARTESIAN_POINT ( 'NONE',  ( -85.64499999999998181, 4.716976649647091513, -6.492361379858946790 ) ) ;
#37728=CARTESIAN_POINT ( 'NONE',  ( -134.0929263765338249, 3.094860106618433360, 9.524999999999991473 ) ) ;
#37730=CARTESIAN_POINT ( 'NONE',  ( -144.4449999999999932, 0.000000000000000000, 8.024999999999991473 ) ) ;
#37736=ORIENTED_EDGE ( 'NONE', *, *, #40060, .T. ) ;
#37739=CARTESIAN_POINT ( 'NONE',  ( -155.3929263765337794, 8.102448949553176405, 5.886773742842740909 ) ) ;
#37741=CARTESIAN_POINT ( 'NONE',  ( -59.09292637653378932, 3.094860106618433360, 9.524999999999991473 ) ) ;
#37742=CARTESIAN_POINT ( 'NONE',  ( -116.6929263765337907, 10.01517768586948698, -1.839758294383808966E-15 ) ) ;
#37743=CARTESIAN_POINT ( 'NONE',  ( -151.7929263765341830, -3.094860106611539319, 9.525000000005000800 ) ) ;
#37745=CARTESIAN_POINT ( 'NONE',  ( -146.7549999999999955, 4.716976649647091513, -6.492361379858946790 ) ) ;
#37761=CARTESIAN_POINT ( 'NONE',  ( -69.20499999999998408, -2.607480562269071545, -8.024999999999991473 ) ) ;
#37762=CARTESIAN_POINT ( 'NONE',  ( -124.9450000000000074, -9.827790563157499189E-16, -8.024999999999991473 ) ) ;
#37772=CARTESIAN_POINT ( 'NONE',  ( -169.2549999999999955, -4.716976649647092401, 6.492361379858946790 ) ) ;
#37783=EDGE_CURVE ( 'NONE', #54061, #29745, #20897, .T. ) ;
#37786=CARTESIAN_POINT ( 'NONE',  ( -87.05499999999999261, -9.827790563157499189E-16, -8.024999999999991473 ) ) ;
#37787=ORIENTED_EDGE ( 'NONE', *, *, #27614, .T. ) ;
#37793=CARTESIAN_POINT ( 'NONE',  ( -67.85707362346617799, -5.598654528085803328, -7.705886871421366635 ) ) ;
#37800=CARTESIAN_POINT ( 'NONE',  ( -115.2549999999999955, -4.716976649647092401, 6.492361379858946790 ) ) ;
#37802=CARTESIAN_POINT ( 'NONE',  ( -117.8949999999999676, 6.826472737025116366, 4.959722759717898555 ) ) ;
#37809=ADVANCED_FACE ( 'NONE', ( #25811 ), #47324, .T. ) ;
#37810=CARTESIAN_POINT ( 'NONE',  ( -164.0929263765337680, 3.094860106618433360, 9.524999999999991473 ) ) ;
#37811=CARTESIAN_POINT ( 'NONE',  ( -179.0949999999999704, -2.607480562269071545, -8.024999999999991473 ) ) ;
#37814=CARTESIAN_POINT ( 'NONE',  ( -61.64292637653380780, -5.598654528085801552, 7.705886871421367523 ) ) ;
#37817=CARTESIAN_POINT ( 'NONE',  ( -78.74292637653380211, -5.598654528085803328, -7.705886871421366635 ) ) ;
#37825=CARTESIAN_POINT ( 'NONE',  ( -178.8549999999999898, 4.716976649647094177, 6.492361379858945902 ) ) ;
#37830=CARTESIAN_POINT ( 'NONE',  ( -73.55707362346616662, -1.166476076187852838E-15, -9.524999999999991473 ) ) ;
#37833=( BOUNDED_CURVE ( )  B_SPLINE_CURVE ( 2, ( #41494, #35154, #56247, #13694, #19665, #41856, #25617, #40810, #14380, #35851, #41160 ),
 .UNSPECIFIED., .F., .F. ) 
 B_SPLINE_CURVE_WITH_KNOTS ( ( 3, 2, 2, 2, 2, 3 ),
 ( 0.9130434782608695121, 0.9152173913043478715, 0.9173913043478261198, 0.9195652173913043681, 0.9217391304347826164, 0.9239130434782608647 ),
 .UNSPECIFIED. ) 
 CURVE ( )  GEOMETRIC_REPRESENTATION_ITEM ( )  RATIONAL_B_SPLINE_CURVE ( ( 1.000000000000000000, 0.9510565162951535312, 1.000000000000000000, 0.9510565162951535312, 1.000000000000000000, 0.9510565162951535312, 1.000000000000000000, 0.9510565162951535312, 1.000000000000000000, 0.9510565162951535312, 1.000000000000000000 ) ) 
 REPRESENTATION_ITEM ( '' )  );
#37836=CARTESIAN_POINT ( 'NONE',  ( -101.1570736234661609, -9.058813317711329915, -2.943386871421370898 ) ) ;
#37837=CARTESIAN_POINT ( 'NONE',  ( -90.65499999999998693, -7.632228543268600340, -2.479861379858950166 ) ) ;
#37847=CARTESIAN_POINT ( 'NONE',  ( -66.74499999999999034, 4.716976649647094177, 6.492361379858945902 ) ) ;
#37857=ORIENTED_EDGE ( 'NONE', *, *, #5570, .T. ) ;
#37861=CARTESIAN_POINT ( 'NONE',  ( -124.4049999999999869, -2.607480562269069768, 8.024999999999991473 ) ) ;
#37868=CARTESIAN_POINT ( 'NONE',  ( -161.3070736234661808, -10.01517768586948698, 6.132527647946031529E-16 ) ) ;
#37870=CARTESIAN_POINT ( 'NONE',  ( -95.15707362346617515, -9.058813317711329915, -2.943386871421370898 ) ) ;
#37871=EDGE_CURVE ( 'NONE', #59688, #54235, #22623, .T. ) ;
#37881=CARTESIAN_POINT ( 'NONE',  ( -142.7049999999999557, 2.607480562269073321, 8.024999999999991473 ) ) ;
#37885=CARTESIAN_POINT ( 'NONE',  ( -146.8449999999999989, -7.632228543268599452, 2.479861379858951054 ) ) ;
#37887=CARTESIAN_POINT ( 'NONE',  ( -143.0949999999999704, -2.607480562269071545, -8.024999999999991473 ) ) ;
#37888=EDGE_LOOP ( 'NONE', ( #67551, #56028, #68584, #18229 ) ) ;
#37891=CARTESIAN_POINT ( 'NONE',  ( -53.60499999999998977, 6.826472737025113702, -4.959722759717902107 ) ) ;
#37892=CARTESIAN_POINT ( 'NONE',  ( -54.74499999999999034, 4.716976649647094177, 6.492361379858945902 ) ) ;
#37899=CARTESIAN_POINT ( 'NONE',  ( -106.3429263765338106, -9.058813317711329915, 2.943386871421371787 ) ) ;
#37915=CARTESIAN_POINT ( 'NONE',  ( -116.0070736234661553, -8.102448949553174629, -5.886773742842741797 ) ) ;
#37917=ORIENTED_EDGE ( 'NONE', *, *, #29370, .T. ) ;
#37923=CARTESIAN_POINT ( 'NONE',  ( -101.5449999999999875, -7.632228543268600340, -2.479861379858950166 ) ) ;
#37935=DIRECTION ( 'NONE',  ( 0.000000000000000000, 0.000000000000000000, 1.000000000000000000 ) ) ;
#37937=CARTESIAN_POINT ( 'NONE',  ( -79.94292637653380496, 0.000000000000000000, 9.524999999999991473 ) ) ;
#37955=CARTESIAN_POINT ( 'NONE',  ( -173.4549999999999841, 7.632228543268599452, -2.479861379858951942 ) ) ;
#37958=CARTESIAN_POINT ( 'NONE',  ( -175.0450000000000159, 7.632228543268600340, 2.479861379858949277 ) ) ;
#37959=CARTESIAN_POINT ( 'NONE',  ( -162.5949999999999704, 2.607480562269072433, 8.024999999999991473 ) ) ;
#37961=FACE_OUTER_BOUND ( 'NONE', #24074, .T. ) ;
#37964=CARTESIAN_POINT ( 'NONE',  ( -82.70499999999999829, 2.607480562269073321, 8.024999999999991473 ) ) ;
#37965=FACE_OUTER_BOUND ( 'NONE', #7646, .T. ) ;
#37969=CARTESIAN_POINT ( 'NONE',  ( -80.39499999999998181, -6.826472737025113702, -4.959722759717900331 ) ) ;
#37988=CARTESIAN_POINT ( 'NONE',  ( -127.9429263765338192, 0.000000000000000000, 9.524999999999991473 ) ) ;
#37990=CARTESIAN_POINT ( 'NONE',  ( -110.0050000000000097, 6.826472737025115478, 4.959722759717899443 ) ) ;
#37998=ORIENTED_EDGE ( 'NONE', *, *, #49174, .T. ) ;
#37999=CARTESIAN_POINT ( 'NONE',  ( -14.66964813207146889, -10.90871211463571200, 5.000000000000000888 ) ) ;
#38016=CARTESIAN_POINT ( 'NONE',  ( -139.7049999999999841, 2.607480562269073321, 8.024999999999991473 ) ) ;
#38018=CARTESIAN_POINT ( 'NONE',  ( -176.6070736234661354, -8.102448949553174629, 5.886773742842742685 ) ) ;
#38028=CARTESIAN_POINT ( 'NONE',  ( -53.45499999999997698, 7.632228543268599452, -2.479861379858951942 ) ) ;
#38031=DIRECTION ( 'NONE',  ( -1.000000000000000000, -0.000000000000000000, -0.000000000000000000 ) ) ;
#38035=CARTESIAN_POINT ( 'NONE',  ( -1.000000000000028644, 1.469576158976823553E-15, -11.99999999999999645 ) ) ;
#38039=CARTESIAN_POINT ( 'NONE',  ( -113.9949999999999903, -6.826472737025113702, 4.959722759717902107 ) ) ;
#38041=CARTESIAN_POINT ( 'NONE',  ( -85.04499999999998749, 7.632228543268600340, 2.479861379858949277 ) ) ;
#38046=CARTESIAN_POINT ( 'NONE',  ( -167.7570736234661695, -5.598654528085801552, 7.705886871421367523 ) ) ;
#38048=ORIENTED_EDGE ( 'NONE', *, *, #13979, .T. ) ;
#38049=CARTESIAN_POINT ( 'NONE',  ( -122.6929263765337907, 10.01517768586948698, -1.839758294383808571E-15 ) ) ;
#38051=CARTESIAN_POINT ( 'NONE',  ( -147.4449999999999932, 0.000000000000000000, 8.024999999999991473 ) ) ;
#38052=CYLINDRICAL_SURFACE ( 'NONE', #63958, 9.524999999999991473 ) ;
#38055=CARTESIAN_POINT ( 'NONE',  ( -67.10707362346616378, 8.102448949553172852, -5.886773742842744461 ) ) ;
#38062=CARTESIAN_POINT ( 'NONE',  ( -132.8070736234661524, 10.01517768586948698, -1.839758294383808966E-15 ) ) ;
#38064=LINE ( 'NONE', #69015, #66263 ) ;
#38066=CARTESIAN_POINT ( 'NONE',  ( -50.75707362346618368, -5.598654528085801552, 7.705886871421367523 ) ) ;
#38069=CARTESIAN_POINT ( 'NONE',  ( -137.6049999999999613, 6.826472737025113702, -4.959722759717902107 ) ) ;
#38082=CARTESIAN_POINT ( 'NONE',  ( -95.75707362346618368, -5.598654528085801552, 7.705886871421367523 ) ) ;
#38084=CARTESIAN_POINT ( 'NONE',  ( -62.90499999999997272, 2.607480562269069324, -8.024999999999993250 ) ) ;
#38086=CARTESIAN_POINT ( 'NONE',  ( -118.4949999999999903, 6.826472737025113702, -4.959722759717902107 ) ) ;
#38100=CARTESIAN_POINT ( 'NONE',  ( -169.7050000000000125, 2.607480562269073321, 8.024999999999991473 ) ) ;
#38104=AXIS2_PLACEMENT_3D ( 'NONE', #13924, #35393, #47365 ) ;
#38110=( BOUNDED_CURVE ( )  B_SPLINE_CURVE ( 2, ( #39072, #60463, #18626, #44703, #66094, #50286, #60807, #40104, #12630, #2009, #23530, #45042, #19651, #14365, #35834, #13677, #67855, #9813, #31223, #9461, #15107, #52716, #46071, #4135, #41145, #57280, #67487, #62547, #20701, #46795, #25952, #68901, #19285, #40792, #9111, #30527, #36581, #52029, #25602, #30180, #62209, #47478, #68198, #3785, #3066, #14035, #25274, #19977, #4485, #8422, #41475, #61848, #62892, #35494, #35137, #24914, #14736, #36211, #57638, #41844, #30889, #56591, #52387, #47118, #58000, #68542, #20340, #63260, #29855, #51321, #24556, #56940, #8755, #51668, #3420, #46431, #38296, #58665, #49176, #47844, #54419, #43579, #37264, #877, #69240, #42894, #42213, #53061, #5881, #53412, #64287, #16140, #59695, #15446, #11514, #32985, #48854, #63601, #21369, #27323, #4854, #37617, #54073, #26300, #42535, #22079, #59334, #36911, #6240, #64971, #5191, #553, #21035, #63933, #32275, #58322, #10495, #11162, #15781, #59021, #16823, #26633, #27667, #31933, #48156, #53725, #21729, #69565, #32608, #43242, #10833, #10146, #5516, #16495, #26969, #31578, #48505, #203, #64649, #37959, #1928, #11865, #45303, #43919, #61085, #23130, #33328, #7616, #65330, #13232, #2272, #54749, #23802, #50890, #44952, #66724, #22776, #34691, #6560, #34364, #28356, #22416, #18539, #66359, #6931, #17176, #56145, #18180, #38649, #40029, #60050, #7972, #29418, #61415, #12898, #28005, #55104, #49517, #7290, #1600, #1244, #60384, #49863, #12189, #44619, #50207, #44274, #28719, #65672, #33661, #29052, #17521, #39665, #38993, #66015, #55812, #17843, #39321, #23447, #60724, #12543, #55467, #34007, #50549, #13585, #2650, #4060, #30439, #9380, #63178, #45654, #25191, #40708, #51941, #46708, #52305, #41402, #25526, #67404, #9740, #8335, #15016, #68122, #19902, #20253, #47039, #62120, #62807, #41056, #19199, #57913, #31144, #24826, #67072, #13945, #14290, #36489, #51579, #14649, #35053, #24145, #30804, #67764, #18850, #56501, #56864, #68455, #35413, #40346, #29779, #61755, #36114, #8678, #30104, #3335, #3696, #51242, #57551, #41757, #2985, #24475, #46343, #45979, #19563, #62472, #35755, #57192, #9021, #31845, #37887, #63515, #15696, #37178, #5113, #68818, #47761, #113, #15375, #69487, #59254, #53333, #64567, #36829, #58244, #42815, #32204, #20964, #21644, #53650, #58587, #4397, #10417, #26886, #69156, #16745, #38210, #11078, #21283, #10067, #5438, #42124, #11432, #10756, #43161, #27239, #16413, #42458, #26562, #48083, #64203, #25871, #16059, #476, #22005, #32527, #5793, #64895, #37541, #47389, #31491, #43508, #52974, #58944, #52640, #48424, #59612, #20612, #4770, #26223, #53991, #48774, #63853, #6848, #44872, #1155, #11784, #38571, #22342, #50132, #43836, #65593, #28271, #60642, #50464, #49112, #12458, #23720, #44540, #33246, #45219, #17445, #60314, #23045, #1519, #12817, #38908, #66279, #7210, #54342, #65242, #60999, #49778, #65944, #798, #2191, #33922, #12119, #17094, #61344, #39943, #44193, #1862, #59970, #28973, #34280, #18103, #54684, #6160, #17772, #32909, #55388, #23372, #33583, #6483, #39593, #27591, #66644, #55738, #27924, #7544, #49435, #28638, #18461, #22692, #55020, #39244, #26053, #19116, #8598, #66994, #40620, #67325, #42631, #4953, #8937, #34610, #10246, #13154, #26401, #47932, #37012, #52819, #58420, #45896, #69333, #67680, #62035, #24072, #40265, #56784, #40983, #13863, #62399, #53159, #19477, #56072, #2911, #20800, #21127, #35679, #7886, #29332, #4594, #24402, #50811, #14216, #35330, #31683, #30033, #51493, #3254, #2562, #47587, #42307, #24741, #45576, #18787, #46257, #61670, #29697, #13499, #34971, #56420, #68994, #8254, #57112, #51166, #31320, #63695, #15539, #38400, #5620, #16584, #38039, #11959, #37364, #60150, #33416, #972, #64036, #43346, #49263, #5280, #27072, #48607, #59431, #10587, #59106, #11614, #26725, #11262, #17279, #300, #6328, #48247, #69662, #54172, #43670, #21834, #58770, #53497, #54845, #15880, #38743, #16917, #64741, #22873, #6664, #59803, #32036, #28104, #32717, #49609, #5982, #27759, #32360, #42986, #21476, #64390, #33081, #16238, #27421, #53821, #48949, #647, #22175, #65063, #1343, #54518, #37716, #22522, #44020, #65430, #10925, #12995, #24241, #50298, #8068, #18636, #65778, #55203, #2749, #7712, #40447, #17931, #7026, #44373, #45742, #2376, #50984, #35149, #28815, #61864, #60822, #51332, #49964, #56604, #13331, #39421, #7385, #12642, #23895, #8434, #66828, #40116, #13690, #67159, #34106, #61504, #34450, #55564, #29867, #18945, #17614, #23542, #29520, #28453, #2017, #45052, #66462, #60474, #18286, #34791, #1700, #61186, #3077, #39771, #39080, #55909, #29151, #50637, #45408, #56243, #12282, #33753, #23218, #44712, #66102, #68552, #41156, #58332, #10157, #9822, #41487, #8767, #4143, #14046, #35506, #47489, #46081, #63272, #58012, #62557, #52041, #46805, #68210, #67499, #30540, #42223, #63613, #41851, #68912, #36920, #15457, #52397, #3797, #40805, #53072, #31590, #35846, #15117, #24568, #31232, #62903, #30188, #25613, #56949, #51681, #20710, #19300, #36593, #25283, #3427, #52727, #62220, #24929, #4495, #46442, #25960, #67867, #47126, #19660, #14375, #57290, #9122, #19986, #14747, #36222, #57649, #20349, #9475, #30899, #65339, #564, #26309, #887, #4866, #17187, #38661, #27674, #43591, #53421, #10506, #63945, #22089, #15792, #37627, #42904, #59031, #64297, #32286, #32622, #43929, #59345, #47854, #16149, #11522, #60059, #27335, #69249, #11874, #10842, #38306, #48865, #21048, #37276, #32994, #37969, #22428, #48168, #58674, #42545, #6249, #54084, #54429, #33337, #31944, #64979, #53737, #5892, #16835, #5200, #59709, #69576, #5530, #26981, #49185, #26644, #21381, #48514, #211, #21742, #43253, #64659, #16503, #11175, #40355, #13594, #7300, #28017, #49873, #65683, #17852, #39330, #28728, #1255, #1611, #2282, #17531, #1939, #61424, #55478, #50898, #66369, #44628, #18190, #2661, #23138, #55113, #34700, #23811, #24156, #7983, #60733, #66735, #39001, #60394, #44962, #34373, #66025, #45313, #55821, #12551, #6572, #34017, #29061, #50217, #18862, #61765, #40035, #23456, #6940, #49526, #39676, #54759, #12908, #18550, #29427, #13244, #61098, #7627, #50559, #56156, #22786, #45661, #67077, #44286, #12197, #33671, #28365, #51590, #36126, #24838, #62481, #45989, #46354, #57925, #30450, #63187, #36501, #67413, #19209, #67774, #19574, #4068, #41067, #57561, #8685, #40719, #62129, #2992, #14300, #24482, #13956, #35764, #3707, #68465, #29791, #25202, #41766, #57200, #35424, #15027, #3345, #9032, #51950, #46719, #52315, #68132, #9391, #19911, #41414, #25532, #62817, #14657, #30816, #51251, #56508, #47046, #20261, #35061, #8346, #56874, #30112, #24377, #44847, #35303, #33890, #40597, #66971, #23344, #56762, #55358, #28943, #28239, #39214, #61647, #39565, #50435, #2162, #45871, #1487, #67304, #19091, #34947, #49749, #7519, #13475, #60614, #60968, #12787, #12429, #18766, #66251, #34255, #18078, #56040, #62010, #50784, #2535, #13839, #8227, #55711, #24045, #66617, #23694, #23016, #44512, #45194, #65916, #18432, #7181, #39918, #61322, #13133, #17744, #34585, #45549, #28609, #7854, #56392, #29306, #50106, #40243, #29673, #51141, #1835, #2885, #49278, #26741, #48622, #22895, #1362, #5634, #11629, #10603, #60164, #65446, #6345, #16258, #37381, #32734, #64049 ),
 .UNSPECIFIED., .F., .F. ) 
 B_SPLINE_CURVE_WITH_KNOTS ( ( 3, 2, 2, 2, 2, 2, 2, 2, 2, 2, 2, 2, 2, 2, 2, 2, 2, 2, 2, 2, 2, 2, 2, 2, 2, 2, 2, 2, 2, 2, 2, 2, 2, 2, 2, 2, 2, 2, 2, 2, 2, 2, 2, 2, 2, 2, 2, 2, 2, 2, 2, 2, 2, 2, 2, 2, 2, 2, 2, 2, 2, 2, 2, 2, 2, 2, 2, 2, 2, 2, 2, 2, 2, 2, 2, 2, 2, 2, 2, 2, 2, 2, 2, 2, 2, 2, 2, 2, 2, 2, 2, 2, 2, 2, 2, 2, 2, 2, 2, 2, 2, 2, 2, 2, 2, 2, 2, 2, 2, 2, 2, 2, 2, 2, 2, 2, 2, 2, 2, 2, 2, 2, 2, 2, 2, 2, 2, 2, 2, 2, 2, 2, 2, 2, 2, 2, 2, 2, 2, 2, 2, 2, 2, 2, 2, 2, 2, 2, 2, 2, 2, 2, 2, 2, 2, 2, 2, 2, 2, 2, 2, 2, 2, 2, 2, 2, 2, 2, 2, 2, 2, 2, 2, 2, 2, 2, 2, 2, 2, 2, 2, 2, 2, 2, 2, 2, 2, 2, 2, 2, 2, 2, 2, 2, 2, 2, 2, 2, 2, 2, 2, 2, 2, 2, 2, 2, 2, 2, 2, 2, 2, 2, 2, 2, 2, 2, 2, 2, 2, 2, 2, 2, 2, 2, 2, 2, 2, 2, 2, 2, 2, 2, 2, 2, 2, 2, 2, 2, 2, 2, 2, 2, 2, 2, 2, 2, 2, 2, 2, 2, 2, 2, 2, 2, 2, 2, 2, 2, 2, 2, 2, 2, 2, 2, 2, 2, 2, 2, 2, 2, 2, 2, 2, 2, 2, 2, 2, 2, 2, 2, 2, 2, 2, 2, 2, 2, 2, 2, 2, 2, 2, 2, 2, 2, 2, 2, 2, 2, 2, 2, 2, 2, 2, 2, 2, 2, 2, 2, 2, 2, 2, 2, 2, 2, 2, 2, 2, 2, 2, 2, 2, 2, 2, 2, 2, 2, 2, 2, 2, 2, 2, 2, 2, 2, 2, 2, 2, 2, 2, 2, 2, 2, 2, 2, 2, 2, 2, 2, 2, 2, 2, 2, 2, 2, 2, 2, 2, 2, 2, 2, 2, 2, 2, 2, 2, 2, 2, 2, 2, 2, 2, 2, 2, 2, 2, 2, 2, 2, 2, 2, 2, 2, 2, 2, 2, 2, 2, 2, 2, 2, 2, 2, 2, 2, 2, 2, 2, 2, 2, 2, 2, 2, 2, 2, 2, 2, 2, 2, 2, 2, 2, 2, 2, 2, 2, 2, 2, 2, 2, 2, 2, 2, 2, 2, 2, 2, 2, 2, 2, 2, 2, 2, 2, 2, 2, 2, 2, 2, 2, 2, 2, 2, 2, 2, 2, 2, 2, 2, 2, 2, 2, 2, 2, 2, 2, 2, 3 ),
 ( 0.000000000000000000, 0.002173913043478260896, 0.004347826086956521792, 0.006521739130434782254, 0.008695652173913043584, 0.01086956521739130405, 0.01304347826086956451, 0.01521739130434782671, 0.01739130434782608717, 0.01956521739130434936, 0.02173913043478260809, 0.02391304347826087029, 0.02608695652173912902, 0.02826086956521739121, 0.03043478260869565341, 0.03260869565217391214, 0.03478260869565217434, 0.03695652173913043653, 0.03913043478260869873, 0.04130434782608695399, 0.04347826086956521618, 0.04565217391304347838, 0.04782608695652174058, 0.05000000000000000278, 0.05217391304347825803, 0.05434782608695652023, 0.05652173913043478243, 0.05869565217391304462, 0.06086956521739130682, 0.06304347826086956208, 0.06521739130434782428, 0.06739130434782608647, 0.06956521739130434867, 0.07173913043478261087, 0.07391304347826087306, 0.07608695652173913526, 0.07826086956521739746, 0.08043478260869564578, 0.08260869565217390798, 0.08478260869565217017, 0.08695652173913043237, 0.08913043478260869457, 0.09130434782608695676, 0.09347826086956521896, 0.09565217391304348116, 0.09782608695652174335, 0.1000000000000000056, 0.1021739130434782677, 0.1043478260869565161, 0.1065217391304347783, 0.1086956521739130405, 0.1108695652173913027, 0.1130434782608695649, 0.1152173913043478271, 0.1173913043478260892, 0.1195652173913043514, 0.1217391304347826136, 0.1239130434782608758, 0.1260869565217391242, 0.1282608695652174002, 0.1304347826086956486, 0.1326086956521739246, 0.1347826086956521729, 0.1369565217391304213, 0.1391304347826086973, 0.1413043478260869457, 0.1434782608695652217, 0.1456521739130434701, 0.1478260869565217461, 0.1499999999999999944, 0.1521739130434782705, 0.1543478260869565188, 0.1565217391304347949, 0.1586956521739130432, 0.1608695652173912916, 0.1630434782608695676, 0.1652173913043478160, 0.1673913043478260920, 0.1695652173913043403, 0.1717391304347826164, 0.1739130434782608647, 0.1760869565217391408, 0.1782608695652173891, 0.1804347826086956652, 0.1826086956521739135, 0.1847826086956521618, 0.1869565217391304379, 0.1891304347826086862, 0.1913043478260869623, 0.1934782608695652106, 0.1956521739130434867, 0.1978260869565217350, 0.2000000000000000111, 0.2021739130434782594, 0.2043478260869565355, 0.2065217391304347838, 0.2086956521739130321, 0.2108695652173913082, 0.2130434782608695565, 0.2152173913043478326, 0.2173913043478260809, 0.2195652173913043570, 0.2217391304347826053, 0.2239130434782608814, 0.2260869565217391297, 0.2282608695652173780, 0.2304347826086956541, 0.2326086956521739024, 0.2347826086956521785, 0.2369565217391304268, 0.2391304347826087029, 0.2413043478260869512, 0.2434782608695652273, 0.2456521739130434756, 0.2478260869565217517, 0.2500000000000000000, 0.2521739130434782483, 0.2543478260869564966, 0.2565217391304348005, 0.2586956521739130488, 0.2608695652173912971, 0.2630434782608695454, 0.2652173913043478493, 0.2673913043478260976, 0.2695652173913043459, 0.2717391304347825942, 0.2739130434782608425, 0.2760869565217391464, 0.2782608695652173947, 0.2804347826086956430, 0.2826086956521738913, 0.2847826086956521952, 0.2869565217391304435, 0.2891304347826086918, 0.2913043478260869401, 0.2934782608695652439, 0.2956521739130434923, 0.2978260869565217406, 0.2999999999999999889, 0.3021739130434782372, 0.3043478260869565410, 0.3065217391304347894, 0.3086956521739130377, 0.3108695652173912860, 0.3130434782608695898, 0.3152173913043478382, 0.3173913043478260865, 0.3195652173913043348, 0.3217391304347825831, 0.3239130434782608869, 0.3260869565217391353, 0.3282608695652173836, 0.3304347826086956319, 0.3326086956521739357, 0.3347826086956521840, 0.3369565217391304324, 0.3391304347826086807, 0.3413043478260869290, 0.3434782608695652328, 0.3456521739130434812, 0.3478260869565217295, 0.3499999999999999778, 0.3521739130434782816, 0.3543478260869565299, 0.3565217391304347783, 0.3586956521739130266, 0.3608695652173913304, 0.3630434782608695787, 0.3652173913043478271, 0.3673913043478260754, 0.3695652173913043237, 0.3717391304347826275, 0.3739130434782608758, 0.3760869565217391242, 0.3782608695652173725, 0.3804347826086956763, 0.3826086956521739246, 0.3847826086956521729, 0.3869565217391304213, 0.3891304347826086696, 0.3913043478260869734, 0.3934782608695652217, 0.3956521739130434701, 0.3978260869565217184, 0.4000000000000000222, 0.4021739130434782705, 0.4043478260869565188, 0.4065217391304347672, 0.4086956521739130710, 0.4108695652173913193, 0.4130434782608695676, 0.4152173913043478160, 0.4173913043478260643, 0.4195652173913043681, 0.4217391304347826164, 0.4239130434782608647, 0.4260869565217391131, 0.4282608695652174169, 0.4304347826086956652, 0.4326086956521739135, 0.4347826086956521618, 0.4369565217391304102, 0.4391304347826087140, 0.4413043478260869623, 0.4434782608695652106, 0.4456521739130434590, 0.4478260869565217628, 0.4500000000000000111, 0.4521739130434782594, 0.4543478260869565077, 0.4565217391304347561, 0.4586956521739130599, 0.4608695652173913082, 0.4630434782608695565, 0.4652173913043478048, 0.4673913043478261087, 0.4695652173913043570, 0.4717391304347826053, 0.4739130434782608536, 0.4760869565217391575, 0.4782608695652174058, 0.4804347826086956541, 0.4826086956521739024, 0.4847826086956521507, 0.4869565217391304546, 0.4891304347826087029, 0.4913043478260869512, 0.4934782608695651995, 0.4956521739130435034, 0.4978260869565217517, 0.5000000000000000000, 0.5021739130434782483, 0.5043478260869564966, 0.5065217391304347450, 0.5086956521739129933, 0.5108695652173913526, 0.5130434782608696009, 0.5152173913043478493, 0.5173913043478260976, 0.5195652173913043459, 0.5217391304347825942, 0.5239130434782608425, 0.5260869565217390909, 0.5282608695652173392, 0.5304347826086956985, 0.5326086956521739468, 0.5347826086956521952, 0.5369565217391304435, 0.5391304347826086918, 0.5413043478260869401, 0.5434782608695651884, 0.5456521739130434367, 0.5478260869565216851, 0.5500000000000000444, 0.5521739130434782927, 0.5543478260869565410, 0.5565217391304347894, 0.5586956521739130377, 0.5608695652173912860, 0.5630434782608695343, 0.5652173913043477826, 0.5673913043478261420, 0.5695652173913043903, 0.5717391304347826386, 0.5739130434782608869, 0.5760869565217391353, 0.5782608695652173836, 0.5804347826086956319, 0.5826086956521738802, 0.5847826086956521285, 0.5869565217391304879, 0.5891304347826087362, 0.5913043478260869845, 0.5934782608695652328, 0.5956521739130434812, 0.5978260869565217295, 0.5999999999999999778, 0.6021739130434782261, 0.6043478260869564744, 0.6065217391304348338, 0.6086956521739130821, 0.6108695652173913304, 0.6130434782608695787, 0.6152173913043478271, 0.6173913043478260754, 0.6195652173913043237, 0.6217391304347825720, 0.6239130434782608203, 0.6260869565217391797, 0.6282608695652174280, 0.6304347826086956763, 0.6326086956521739246, 0.6347826086956521729, 0.6369565217391304213, 0.6391304347826086696, 0.6413043478260869179, 0.6434782608695651662, 0.6456521739130435256, 0.6478260869565217739, 0.6500000000000000222, 0.6521739130434782705, 0.6543478260869565188, 0.6565217391304347672, 0.6586956521739130155, 0.6608695652173912638, 0.6630434782608695121, 0.6652173913043478715, 0.6673913043478261198, 0.6695652173913043681, 0.6717391304347826164, 0.6739130434782608647, 0.6760869565217391131, 0.6782608695652173614, 0.6804347826086956097, 0.6826086956521738580, 0.6847826086956522174, 0.6869565217391304657, 0.6891304347826087140, 0.6913043478260869623, 0.6934782608695652106, 0.6956521739130434590, 0.6978260869565217073, 0.6999999999999999556, 0.7021739130434783149, 0.7043478260869565633, 0.7065217391304348116, 0.7086956521739130599, 0.7108695652173913082, 0.7130434782608695565, 0.7152173913043478048, 0.7173913043478260532, 0.7195652173913043015, 0.7217391304347826608, 0.7239130434782609091, 0.7260869565217391575, 0.7282608695652174058, 0.7304347826086956541, 0.7326086956521739024, 0.7347826086956521507, 0.7369565217391303991, 0.7391304347826086474, 0.7413043478260870067, 0.7434782608695652550, 0.7456521739130435034, 0.7478260869565217517, 0.7500000000000000000, 0.7521739130434782483, 0.7543478260869564966, 0.7565217391304347450, 0.7586956521739129933, 0.7608695652173913526, 0.7630434782608696009, 0.7652173913043478493, 0.7673913043478260976, 0.7695652173913043459, 0.7717391304347825942, 0.7739130434782608425, 0.7760869565217390909, 0.7782608695652173392, 0.7804347826086956985, 0.7826086956521739468, 0.7847826086956521952, 0.7869565217391304435, 0.7891304347826086918, 0.7913043478260869401, 0.7934782608695651884, 0.7956521739130434367, 0.7978260869565216851, 0.8000000000000000444, 0.8021739130434782927, 0.8043478260869565410, 0.8065217391304347894, 0.8086956521739130377, 0.8108695652173912860, 0.8130434782608695343, 0.8152173913043477826, 0.8173913043478261420, 0.8195652173913043903, 0.8217391304347826386, 0.8239130434782608869, 0.8260869565217391353, 0.8282608695652173836, 0.8304347826086956319, 0.8326086956521738802, 0.8347826086956521285, 0.8369565217391304879, 0.8391304347826087362, 0.8413043478260869845, 0.8434782608695652328, 0.8456521739130434812, 0.8478260869565217295, 0.8499999999999999778, 0.8521739130434782261, 0.8543478260869564744, 0.8565217391304348338, 0.8586956521739130821, 0.8608695652173913304, 0.8630434782608695787, 0.8652173913043478271, 0.8673913043478260754, 0.8695652173913043237, 0.8717391304347825720, 0.8739130434782608203, 0.8760869565217391797, 0.8782608695652174280, 0.8804347826086956763, 0.8826086956521739246, 0.8847826086956521729, 0.8869565217391304213, 0.8891304347826086696, 0.8913043478260869179, 0.8934782608695651662, 0.8956521739130435256, 0.8978260869565217739, 0.9000000000000000222, 0.9021739130434782705, 0.9043478260869565188, 0.9065217391304347672, 0.9086956521739130155, 0.9108695652173912638, 0.9130434782608695121, 0.9152173913043478715, 0.9173913043478261198, 0.9195652173913043681, 0.9217391304347826164, 0.9239130434782608647, 0.9260869565217391131, 0.9282608695652173614, 0.9304347826086956097, 0.9326086956521738580, 0.9347826086956522174, 0.9369565217391304657, 0.9391304347826087140, 0.9413043478260869623, 0.9434782608695652106, 0.9456521739130434590, 0.9478260869565217073, 0.9499999999999999556, 0.9521739130434783149, 0.9543478260869565633, 0.9565217391304348116, 0.9586956521739130599, 0.9608695652173913082, 0.9630434782608695565, 0.9652173913043478048, 0.9673913043478260532, 0.9695652173913043015, 0.9717391304347826608, 0.9739130434782609091, 0.9760869565217391575, 0.9782608695652174058, 0.9804347826086956541, 0.9826086956521739024, 0.9847826086956521507, 0.9869565217391303991, 0.9891304347826086474, 0.9913043478260870067 ),
 .UNSPECIFIED. ) 
 CURVE ( )  GEOMETRIC_REPRESENTATION_ITEM ( )  RATIONAL_B_SPLINE_CURVE ( ( 1.000000000000000000, 0.9510565162951535312, 1.000000000000000000, 0.9510565162951535312, 1.000000000000000000, 0.9510565162951535312, 1.000000000000000000, 0.9510565162951535312, 1.000000000000000000, 0.9510565162951535312, 1.000000000000000000, 0.9510565162951535312, 1.000000000000000000, 0.9510565162951535312, 1.000000000000000000, 0.9510565162951535312, 1.000000000000000000, 0.9510565162951535312, 1.000000000000000000, 0.9510565162951535312, 1.000000000000000000, 0.9510565162951535312, 1.000000000000000000, 0.9510565162951535312, 1.000000000000000000, 0.9510565162951535312, 1.000000000000000000, 0.9510565162951535312, 1.000000000000000000, 0.9510565162951535312, 1.000000000000000000, 0.9510565162951535312, 1.000000000000000000, 0.9510565162951535312, 1.000000000000000000, 0.9510565162951535312, 1.000000000000000000, 0.9510565162951535312, 1.000000000000000000, 0.9510565162951535312, 1.000000000000000000, 0.9510565162951535312, 1.000000000000000000, 0.9510565162951535312, 1.000000000000000000, 0.9510565162951535312, 1.000000000000000000, 0.9510565162951535312, 1.000000000000000000, 0.9510565162951535312, 1.000000000000000000, 0.9510565162951535312, 1.000000000000000000, 0.9510565162951535312, 1.000000000000000000, 0.9510565162951535312, 1.000000000000000000, 0.9510565162951535312, 1.000000000000000000, 0.9510565162951535312, 1.000000000000000000, 0.9510565162951535312, 1.000000000000000000, 0.9510565162951535312, 1.000000000000000000, 0.9510565162951535312, 1.000000000000000000, 0.9510565162951535312, 1.000000000000000000, 0.9510565162951535312, 1.000000000000000000, 0.9510565162951535312, 1.000000000000000000, 0.9510565162951535312, 1.000000000000000000, 0.9510565162951535312, 1.000000000000000000, 0.9510565162951535312, 1.000000000000000000, 0.9510565162951535312, 1.000000000000000000, 0.9510565162951535312, 1.000000000000000000, 0.9510565162951535312, 1.000000000000000000, 0.9510565162951535312, 1.000000000000000000, 0.9510565162951535312, 1.000000000000000000, 0.9510565162951535312, 1.000000000000000000, 0.9510565162951535312, 1.000000000000000000, 0.9510565162951535312, 1.000000000000000000, 0.9510565162951535312, 1.000000000000000000, 0.9510565162951535312, 1.000000000000000000, 0.9510565162951535312, 1.000000000000000000, 0.9510565162951535312, 1.000000000000000000, 0.9510565162951535312, 1.000000000000000000, 0.9510565162951535312, 1.000000000000000000, 0.9510565162951535312, 1.000000000000000000, 0.9510565162951535312, 1.000000000000000000, 0.9510565162951535312, 1.000000000000000000, 0.9510565162951535312, 1.000000000000000000, 0.9510565162951535312, 1.000000000000000000, 0.9510565162951535312, 1.000000000000000000, 0.9510565162951535312, 1.000000000000000000, 0.9510565162951535312, 1.000000000000000000, 0.9510565162951535312, 1.000000000000000000, 0.9510565162951535312, 1.000000000000000000, 0.9510565162951535312, 1.000000000000000000, 0.9510565162951535312, 1.000000000000000000, 0.9510565162951535312, 1.000000000000000000, 0.9510565162951535312, 1.000000000000000000, 0.9510565162951535312, 1.000000000000000000, 0.9510565162951535312, 1.000000000000000000, 0.9510565162951535312, 1.000000000000000000, 0.9510565162951535312, 1.000000000000000000, 0.9510565162951535312, 1.000000000000000000, 0.9510565162951535312, 1.000000000000000000, 0.9510565162951535312, 1.000000000000000000, 0.9510565162951535312, 1.000000000000000000, 0.9510565162951535312, 1.000000000000000000, 0.9510565162951535312, 1.000000000000000000, 0.9510565162951535312, 1.000000000000000000, 0.9510565162951535312, 1.000000000000000000, 0.9510565162951535312, 1.000000000000000000, 0.9510565162951535312, 1.000000000000000000, 0.9510565162951535312, 1.000000000000000000, 0.9510565162951535312, 1.000000000000000000, 0.9510565162951535312, 1.000000000000000000, 0.9510565162951535312, 1.000000000000000000, 0.9510565162951535312, 1.000000000000000000, 0.9510565162951535312, 1.000000000000000000, 0.9510565162951535312, 1.000000000000000000, 0.9510565162951535312, 1.000000000000000000, 0.9510565162951535312, 1.000000000000000000, 0.9510565162951535312, 1.000000000000000000, 0.9510565162951535312, 1.000000000000000000, 0.9510565162951535312, 1.000000000000000000, 0.9510565162951535312, 1.000000000000000000, 0.9510565162951535312, 1.000000000000000000, 0.9510565162951535312, 1.000000000000000000, 0.9510565162951535312, 1.000000000000000000, 0.9510565162951535312, 1.000000000000000000, 0.9510565162951535312, 1.000000000000000000, 0.9510565162951535312, 1.000000000000000000, 0.9510565162951535312, 1.000000000000000000, 0.9510565162951535312, 1.000000000000000000, 0.9510565162951535312, 1.000000000000000000, 0.9510565162951535312, 1.000000000000000000, 0.9510565162951535312, 1.000000000000000000, 0.9510565162951535312, 1.000000000000000000, 0.9510565162951535312, 1.000000000000000000, 0.9510565162951535312, 1.000000000000000000, 0.9510565162951535312, 1.000000000000000000, 0.9510565162951535312, 1.000000000000000000, 0.9510565162951535312, 1.000000000000000000, 0.9510565162951535312, 1.000000000000000000, 0.9510565162951535312, 1.000000000000000000, 0.9510565162951535312, 1.000000000000000000, 0.9510565162951535312, 1.000000000000000000, 0.9510565162951535312, 1.000000000000000000, 0.9510565162951535312, 1.000000000000000000, 0.9510565162951535312, 1.000000000000000000, 0.9510565162951535312, 1.000000000000000000, 0.9510565162951535312, 1.000000000000000000, 0.9510565162951535312, 1.000000000000000000, 0.9510565162951535312, 1.000000000000000000, 0.9510565162951535312, 1.000000000000000000, 0.9510565162951535312, 1.000000000000000000, 0.9510565162951535312, 1.000000000000000000, 0.9510565162951535312, 1.000000000000000000, 0.9510565162951535312, 1.000000000000000000, 0.9510565162951535312, 1.000000000000000000, 0.9510565162951535312, 1.000000000000000000, 0.9510565162951535312, 1.000000000000000000, 0.9510565162951535312, 1.000000000000000000, 0.9510565162951535312, 1.000000000000000000, 0.9510565162951535312, 1.000000000000000000, 0.9510565162951535312, 1.000000000000000000, 0.9510565162951535312, 1.000000000000000000, 0.9510565162951535312, 1.000000000000000000, 0.9510565162951535312, 1.000000000000000000, 0.9510565162951535312, 1.000000000000000000, 0.9510565162951535312, 1.000000000000000000, 0.9510565162951535312, 1.000000000000000000, 0.9510565162951535312, 1.000000000000000000, 0.9510565162951535312, 1.000000000000000000, 0.9510565162951535312, 1.000000000000000000, 0.9510565162951535312, 1.000000000000000000, 0.9510565162951535312, 1.000000000000000000, 0.9510565162951535312, 1.000000000000000000, 0.9510565162951535312, 1.000000000000000000, 0.9510565162951535312, 1.000000000000000000, 0.9510565162951535312, 1.000000000000000000, 0.9510565162951535312, 1.000000000000000000, 0.9510565162951535312, 1.000000000000000000, 0.9510565162951535312, 1.000000000000000000, 0.9510565162951535312, 1.000000000000000000, 0.9510565162951535312, 1.000000000000000000, 0.9510565162951535312, 1.000000000000000000, 0.9510565162951535312, 1.000000000000000000, 0.9510565162951535312, 1.000000000000000000, 0.9510565162951535312, 1.000000000000000000, 0.9510565162951535312, 1.000000000000000000, 0.9510565162951535312, 1.000000000000000000, 0.9510565162951535312, 1.000000000000000000, 0.9510565162951535312, 1.000000000000000000, 0.9510565162951535312, 1.000000000000000000, 0.9510565162951535312, 1.000000000000000000, 0.9510565162951535312, 1.000000000000000000, 0.9510565162951535312, 1.000000000000000000, 0.9510565162951535312, 1.000000000000000000, 0.9510565162951535312, 1.000000000000000000, 0.9510565162951535312, 1.000000000000000000, 0.9510565162951535312, 1.000000000000000000, 0.9510565162951535312, 1.000000000000000000, 0.9510565162951535312, 1.000000000000000000, 0.9510565162951535312, 1.000000000000000000, 0.9510565162951535312, 1.000000000000000000, 0.9510565162951535312, 1.000000000000000000, 0.9510565162951535312, 1.000000000000000000, 0.9510565162951535312, 1.000000000000000000, 0.9510565162951535312, 1.000000000000000000, 0.9510565162951535312, 1.000000000000000000, 0.9510565162951535312, 1.000000000000000000, 0.9510565162951535312, 1.000000000000000000, 0.9510565162951535312, 1.000000000000000000, 0.9510565162951535312, 1.000000000000000000, 0.9510565162951535312, 1.000000000000000000, 0.9510565162951535312, 1.000000000000000000, 0.9510565162951535312, 1.000000000000000000, 0.9510565162951535312, 1.000000000000000000, 0.9510565162951535312, 1.000000000000000000, 0.9510565162951535312, 1.000000000000000000, 0.9510565162951535312, 1.000000000000000000, 0.9510565162951535312, 1.000000000000000000, 0.9510565162951535312, 1.000000000000000000, 0.9510565162951535312, 1.000000000000000000, 0.9510565162951535312, 1.000000000000000000, 0.9510565162951535312, 1.000000000000000000, 0.9510565162951535312, 1.000000000000000000, 0.9510565162951535312, 1.000000000000000000, 0.9510565162951535312, 1.000000000000000000, 0.9510565162951535312, 1.000000000000000000, 0.9510565162951535312, 1.000000000000000000, 0.9510565162951535312, 1.000000000000000000, 0.9510565162951535312, 1.000000000000000000, 0.9510565162951535312, 1.000000000000000000, 0.9510565162951535312, 1.000000000000000000, 0.9510565162951535312, 1.000000000000000000, 0.9510565162951535312, 1.000000000000000000, 0.9510565162951535312, 1.000000000000000000, 0.9510565162951535312, 1.000000000000000000, 0.9510565162951535312, 1.000000000000000000, 0.9510565162951535312, 1.000000000000000000, 0.9510565162951535312, 1.000000000000000000, 0.9510565162951535312, 1.000000000000000000, 0.9510565162951535312, 1.000000000000000000, 0.9510565162951535312, 1.000000000000000000, 0.9510565162951535312, 1.000000000000000000, 0.9510565162951535312, 1.000000000000000000, 0.9510565162951535312, 1.000000000000000000, 0.9510565162951535312, 1.000000000000000000, 0.9510565162951535312, 1.000000000000000000, 0.9510565162951535312, 1.000000000000000000, 0.9510565162951535312, 1.000000000000000000, 0.9510565162951535312, 1.000000000000000000, 0.9510565162951535312, 1.000000000000000000, 0.9510565162951535312, 1.000000000000000000, 0.9510565162951535312, 1.000000000000000000, 0.9510565162951535312, 1.000000000000000000, 0.9510565162951535312, 1.000000000000000000, 0.9510565162951535312, 1.000000000000000000, 0.9510565162951535312, 1.000000000000000000, 0.9510565162951535312, 1.000000000000000000, 0.9510565162951535312, 1.000000000000000000, 0.9510565162951535312, 1.000000000000000000, 0.9510565162951535312, 1.000000000000000000, 0.9510565162951535312, 1.000000000000000000, 0.9510565162951535312, 1.000000000000000000, 0.9510565162951535312, 1.000000000000000000, 0.9510565162951535312, 1.000000000000000000, 0.9510565162951535312, 1.000000000000000000, 0.9510565162951535312, 1.000000000000000000, 0.9510565162951535312, 1.000000000000000000, 0.9510565162951535312, 1.000000000000000000, 0.9510565162951535312, 1.000000000000000000, 0.9510565162951535312, 1.000000000000000000, 0.9510565162951535312, 1.000000000000000000, 0.9510565162951535312, 1.000000000000000000, 0.9510565162951535312, 1.000000000000000000, 0.9510565162951535312, 1.000000000000000000, 0.9510565162951535312, 1.000000000000000000, 0.9510565162951535312, 1.000000000000000000, 0.9510565162951535312, 1.000000000000000000, 0.9510565162951535312, 1.000000000000000000, 0.9510565162951535312, 1.000000000000000000, 0.9510565162951535312, 1.000000000000000000, 0.9510565162951535312, 1.000000000000000000, 0.9510565162951535312, 1.000000000000000000, 0.9510565162951535312, 1.000000000000000000, 0.9510565162951535312, 1.000000000000000000, 0.9510565162951535312, 1.000000000000000000, 0.9510565162951535312, 1.000000000000000000, 0.9510565162951535312, 1.000000000000000000, 0.9510565162951535312, 1.000000000000000000, 0.9510565162951535312, 1.000000000000000000, 0.9510565162951535312, 1.000000000000000000, 0.9510565162951535312, 1.000000000000000000, 0.9510565162951535312, 1.000000000000000000, 0.9510565162951535312, 1.000000000000000000, 0.9510565162951535312, 1.000000000000000000, 0.9510565162951535312, 1.000000000000000000, 0.9510565162951535312, 1.000000000000000000, 0.9510565162951535312, 1.000000000000000000, 0.9510565162951535312, 1.000000000000000000, 0.9510565162951535312, 1.000000000000000000, 0.9510565162951535312, 1.000000000000000000, 0.9510565162951535312, 1.000000000000000000, 0.9510565162951535312, 1.000000000000000000, 0.9510565162951535312, 1.000000000000000000, 0.9510565162951535312, 1.000000000000000000, 0.9510565162951535312, 1.000000000000000000, 0.9510565162951535312, 1.000000000000000000, 0.9510565162951535312, 1.000000000000000000, 0.9510565162951535312, 1.000000000000000000, 0.9510565162951535312, 1.000000000000000000, 0.9510565162951535312, 1.000000000000000000, 0.9510565162951535312, 1.000000000000000000, 0.9510565162951535312, 1.000000000000000000, 0.9510565162951535312, 1.000000000000000000, 0.9510565162951535312, 1.000000000000000000, 0.9510565162951535312, 1.000000000000000000, 0.9510565162951535312, 1.000000000000000000, 0.9510565162951535312, 1.000000000000000000, 0.9510565162951535312, 1.000000000000000000, 0.9510565162951535312, 1.000000000000000000, 0.9510565162951535312, 1.000000000000000000, 0.9510565162951535312, 1.000000000000000000, 0.9510565162951535312, 1.000000000000000000, 0.9510565162951535312, 1.000000000000000000, 0.9510565162951535312, 1.000000000000000000, 0.9510565162951535312, 1.000000000000000000, 0.9510565162951535312, 1.000000000000000000, 0.9510565162951535312, 1.000000000000000000, 0.9510565162951535312, 1.000000000000000000, 0.9510565162951535312, 1.000000000000000000, 0.9510565162951535312, 1.000000000000000000, 0.9510565162951535312, 1.000000000000000000, 0.9510565162951535312, 1.000000000000000000, 0.9510565162951535312, 1.000000000000000000, 0.9510565162951535312, 1.000000000000000000, 0.9510565162951535312, 1.000000000000000000, 0.9510565162951535312, 1.000000000000000000, 0.9510565162951535312, 1.000000000000000000, 0.9510565162951535312, 1.000000000000000000, 0.9510565162951535312, 1.000000000000000000, 0.9510565162951535312, 1.000000000000000000, 0.9510565162951535312, 1.000000000000000000, 0.9510565162951535312, 1.000000000000000000, 0.9510565162951535312, 1.000000000000000000, 0.9510565162951535312, 1.000000000000000000, 0.9510565162951535312, 1.000000000000000000, 0.9510565162951535312, 1.000000000000000000, 0.9510565162951535312, 1.000000000000000000, 0.9510565162951535312, 1.000000000000000000, 0.9510565162951535312, 1.000000000000000000, 0.9510565162951535312, 1.000000000000000000, 0.9510565162951535312, 1.000000000000000000, 0.9510565162951535312, 1.000000000000000000, 0.9510565162951535312, 1.000000000000000000, 0.9510565162951535312, 1.000000000000000000, 0.9510565162951535312, 1.000000000000000000, 0.9510565162951535312, 1.000000000000000000, 0.9510565162951535312, 1.000000000000000000, 0.9510565162951535312, 1.000000000000000000, 0.9510565162951535312, 1.000000000000000000, 0.9510565162951535312, 1.000000000000000000, 0.9510565162951535312, 1.000000000000000000, 0.9510565162951535312, 1.000000000000000000, 0.9510565162951535312, 1.000000000000000000, 0.9510565162951535312, 1.000000000000000000, 0.9510565162951535312, 1.000000000000000000, 0.9510565162951535312, 1.000000000000000000, 0.9510565162951535312, 1.000000000000000000, 0.9510565162951535312, 1.000000000000000000, 0.9510565162951535312, 1.000000000000000000, 0.9510565162951535312, 1.000000000000000000, 0.9510565162951535312, 1.000000000000000000, 0.9510565162951535312, 1.000000000000000000, 0.9510565162951535312, 1.000000000000000000, 0.9510565162951535312, 1.000000000000000000, 0.9510565162951535312, 1.000000000000000000, 0.9510565162951535312, 1.000000000000000000, 0.9510565162951535312, 1.000000000000000000, 0.9510565162951535312, 1.000000000000000000, 0.9510565162951535312, 1.000000000000000000, 0.9510565162951535312, 1.000000000000000000, 0.9510565162951535312, 1.000000000000000000, 0.9510565162951535312, 1.000000000000000000, 0.9510565162951535312, 1.000000000000000000, 0.9510565162951535312, 1.000000000000000000, 0.9510565162951535312, 1.000000000000000000, 0.9510565162951535312, 1.000000000000000000, 0.9510565162951535312, 1.000000000000000000, 0.9510565162951535312, 1.000000000000000000, 0.9510565162951535312, 1.000000000000000000, 0.9510565162951535312, 1.000000000000000000, 0.9510565162951535312, 1.000000000000000000, 0.9510565162951535312, 1.000000000000000000, 0.9510565162951535312, 1.000000000000000000, 0.9510565162951535312, 1.000000000000000000, 0.9510565162951535312, 1.000000000000000000, 0.9510565162951535312, 1.000000000000000000, 0.9510565162951535312, 1.000000000000000000, 0.9510565162951535312, 1.000000000000000000, 0.9510565162951535312, 1.000000000000000000, 0.9510565162951535312, 1.000000000000000000, 0.9510565162951535312, 1.000000000000000000, 0.9510565162951535312, 1.000000000000000000, 0.9510565162951535312, 1.000000000000000000, 0.9510565162951535312, 1.000000000000000000, 0.9510565162951535312, 1.000000000000000000, 0.9510565162951535312, 1.000000000000000000, 0.9510565162951535312, 1.000000000000000000, 0.9510565162951535312, 1.000000000000000000, 0.9510565162951535312, 1.000000000000000000, 0.9510565162951535312, 1.000000000000000000, 0.9510565162951535312, 1.000000000000000000, 0.9510565162951535312, 1.000000000000000000, 0.9510565162951535312, 1.000000000000000000, 0.9510565162951535312, 1.000000000000000000, 0.9510565162951535312, 1.000000000000000000, 0.9510565162951535312, 1.000000000000000000, 0.9510565162951535312, 1.000000000000000000, 0.9510565162951535312, 1.000000000000000000, 0.9510565162951535312, 1.000000000000000000, 0.9510565162951535312, 1.000000000000000000, 0.9510565162951535312, 1.000000000000000000, 0.9510565162951535312, 1.000000000000000000, 0.9510565162951535312, 1.000000000000000000, 0.9510565162951535312, 1.000000000000000000, 0.9510565162951535312, 1.000000000000000000, 0.9510565162951535312, 1.000000000000000000, 0.9510565162951535312, 1.000000000000000000, 0.9510565162951535312, 1.000000000000000000, 0.9510565162951535312, 1.000000000000000000, 0.9510565162951535312, 1.000000000000000000, 0.9510565162951535312, 1.000000000000000000, 0.9510565162951535312, 1.000000000000000000, 0.9510565162951535312, 1.000000000000000000, 0.9510565162951535312, 1.000000000000000000, 0.9510565162951535312, 1.000000000000000000, 0.9510565162951535312, 1.000000000000000000, 0.9510565162951535312, 1.000000000000000000, 0.9510565162951535312, 1.000000000000000000, 0.9510565162951535312, 1.000000000000000000, 0.9510565162951535312, 1.000000000000000000, 0.9510565162951535312, 1.000000000000000000, 0.9510565162951535312, 1.000000000000000000, 0.9510565162951535312, 1.000000000000000000, 0.9510565162951535312, 1.000000000000000000, 0.9510565162951535312, 1.000000000000000000, 0.9510565162951535312, 1.000000000000000000, 0.9510565162951535312, 1.000000000000000000, 0.9510565162951535312, 1.000000000000000000, 0.9510565162951535312, 1.000000000000000000, 0.9510565162951535312, 1.000000000000000000, 0.9510565162951535312, 1.000000000000000000, 0.9510565162951535312, 1.000000000000000000, 0.9510565162951535312, 1.000000000000000000, 0.9510565162951535312, 1.000000000000000000, 0.9510565162951535312, 1.000000000000000000, 0.9510565162951535312, 1.000000000000000000, 0.9510565162951535312, 1.000000000000000000, 0.9510565162951535312, 1.000000000000000000, 0.9510565162951535312, 1.000000000000000000, 0.9510565162951535312, 1.000000000000000000, 0.9510565162951535312, 1.000000000000000000, 0.9510565162951535312, 1.000000000000000000, 0.9510565162951535312, 1.000000000000000000, 0.9510565162951535312, 1.000000000000000000, 0.9510565162951535312, 1.000000000000000000, 0.9510565162951535312, 1.000000000000000000, 0.9510565162951535312, 1.000000000000000000, 0.9510565162951535312, 1.000000000000000000, 0.9510565162951535312, 1.000000000000000000, 0.9510565162951535312, 1.000000000000000000, 0.9510565162951535312, 1.000000000000000000, 0.9510565162951535312, 1.000000000000000000, 0.9510565162951535312, 1.000000000000000000, 0.9510565162951535312, 1.000000000000000000, 0.9510565162951535312, 1.000000000000000000, 0.9510565162951535312, 1.000000000000000000, 0.9510565162951535312, 1.000000000000000000, 0.9510565162951535312, 1.000000000000000000, 0.9510565162951535312, 1.000000000000000000, 0.9510565162951535312, 1.000000000000000000, 0.9510565162951535312, 1.000000000000000000, 0.9510565162951535312, 1.000000000000000000, 0.9510565162951535312, 1.000000000000000000 ) ) 
 REPRESENTATION_ITEM ( '' )  );
#38115=CARTESIAN_POINT ( 'NONE',  ( -89.60499999999997556, 6.826472737025113702, -4.959722759717902107 ) ) ;
#38122=CARTESIAN_POINT ( 'NONE',  ( -66.20707362346615810, 3.094860106618433360, 9.524999999999991473 ) ) ;
#38125=VERTEX_POINT ( 'NONE', #47242 ) ;
#38128=CARTESIAN_POINT ( 'NONE',  ( -102.8049999999999784, -8.437984349512085203, 5.166775262442717831E-16 ) ) ;
#38130=CARTESIAN_POINT ( 'NONE',  ( -111.8949999999999960, 6.826472737025116366, 4.959722759717898555 ) ) ;
#38134=CARTESIAN_POINT ( 'NONE',  ( -156.5929263765337964, -3.094860106618431139, -9.524999999999991473 ) ) ;
#38135=CARTESIAN_POINT ( 'NONE',  ( -172.9449999999999932, -9.827790563157499189E-16, -8.024999999999991473 ) ) ;
#38136=VECTOR ( 'NONE', #41388, 1000.000000000000000 ) ;
#38143=CARTESIAN_POINT ( 'NONE',  ( -80.54292637653379927, 9.058813317711329915, 2.943386871421369566 ) ) ;
#38150=EDGE_LOOP ( 'NONE', ( #38255, #54831, #66787, #61440 ) ) ;
#38151=CARTESIAN_POINT ( 'NONE',  ( -174.0549999999999784, -9.827790563157499189E-16, -8.024999999999991473 ) ) ;
#38158=CARTESIAN_POINT ( 'NONE',  ( -182.3070736234661808, -10.01517768586948698, 6.132527647946031529E-16 ) ) ;
#38164=CARTESIAN_POINT ( 'NONE',  ( -94.10499999999997556, -6.826472737025113702, 4.959722759717902107 ) ) ;
#38176=CARTESIAN_POINT ( 'NONE',  ( -64.64499999999998181, 4.716976649647091513, -6.492361379858946790 ) ) ;
#38186=CARTESIAN_POINT ( 'NONE',  ( -111.8049999999999784, -8.437984349512085203, 5.166775262442717831E-16 ) ) ;
#38194=CARTESIAN_POINT ( 'NONE',  ( -161.1570736234661751, -9.058813317711329915, -2.943386871421370898 ) ) ;
#38197=CARTESIAN_POINT ( 'NONE',  ( -96.05707362346618083, 0.000000000000000000, 9.524999999999991473 ) ) ;
#38205=CARTESIAN_POINT ( 'NONE',  ( -130.8549999999999898, 4.716976649647094177, 6.492361379858945902 ) ) ;
#38208=CARTESIAN_POINT ( 'NONE',  ( -143.9950000000000045, -6.826472737025115478, 4.959722759717900331 ) ) ;
#38210=CARTESIAN_POINT ( 'NONE',  ( -139.1949999999999932, 8.437984349512086979, -1.550032578732815448E-15 ) ) ;
#38214=CARTESIAN_POINT ( 'NONE',  ( -192.5249999999998636, 0.000000000000000000, 0.000000000000000000 ) ) ;
#38218=CARTESIAN_POINT ( 'NONE',  ( -58.55499999999999261, 0.000000000000000000, 8.024999999999991473 ) ) ;
#38221=CARTESIAN_POINT ( 'NONE',  ( -60.14499999999998892, -4.716976649647092401, 6.492361379858946790 ) ) ;
#38223=CARTESIAN_POINT ( 'NONE',  ( -102.5070736234661695, 8.102448949553176405, 5.886773742842740909 ) ) ;
#38228=CARTESIAN_POINT ( 'NONE',  ( -102.1429263765337936, 5.598654528085800663, -7.705886871421367523 ) ) ;
#38230=( BOUNDED_CURVE ( )  B_SPLINE_CURVE ( 2, ( #11147, #32594, #54058, #22066, #32972, #64956, #6545, #49501, #27994, #22761, #44260 ),
 .UNSPECIFIED., .F., .F. ) 
 B_SPLINE_CURVE_WITH_KNOTS ( ( 3, 2, 2, 2, 2, 3 ),
 ( 0.8369565217391304879, 0.8391304347826087362, 0.8413043478260869845, 0.8434782608695652328, 0.8456521739130434812, 0.8478260869565217295 ),
 .UNSPECIFIED. ) 
 CURVE ( )  GEOMETRIC_REPRESENTATION_ITEM ( )  RATIONAL_B_SPLINE_CURVE ( ( 1.000000000000000000, 0.9510565162951535312, 1.000000000000000000, 0.9510565162951535312, 1.000000000000000000, 0.9510565162951535312, 1.000000000000000000, 0.9510565162951535312, 1.000000000000000000, 0.9510565162951535312, 1.000000000000000000 ) ) 
 REPRESENTATION_ITEM ( '' )  );
#38231=CARTESIAN_POINT ( 'NONE',  ( -162.8070736234661808, 10.01517768586948698, -1.839758294383808966E-15 ) ) ;
#38252=CARTESIAN_POINT ( 'NONE',  ( -116.1570736234661751, -9.058813317711329915, -2.943386871421370898 ) ) ;
#38253=LINE ( 'NONE', #34568, #29741 ) ;
#38255=ORIENTED_EDGE ( 'NONE', *, *, #28165, .F. ) ;
#38256=CARTESIAN_POINT ( 'NONE',  ( -183.0769827045555473, 0.000000000000000000, 9.448017295444435248 ) ) ;
#38260=CARTESIAN_POINT ( 'NONE',  ( -90.74499999999999034, 4.716976649647094177, 6.492361379858945902 ) ) ;
#38261=ORIENTED_EDGE ( 'NONE', *, *, #36666, .F. ) ;
#38278=CYLINDRICAL_SURFACE ( 'NONE', #15898, 9.524999999999991473 ) ;
#38279=FACE_OUTER_BOUND ( 'NONE', #11716, .T. ) ;
#38288=CARTESIAN_POINT ( 'NONE',  ( -49.10707362346617089, 8.102448949553172852, -5.886773742842744461 ) ) ;
#38291=CARTESIAN_POINT ( 'NONE',  ( -167.6050000000000182, 6.826472737025113702, -4.959722759717902107 ) ) ;
#38292=FACE_OUTER_BOUND ( 'NONE', #46511, .T. ) ;
#38294=CARTESIAN_POINT ( 'NONE',  ( -177.8949999999999818, 6.826472737025116366, 4.959722759717898555 ) ) ;
#38296=CARTESIAN_POINT ( 'NONE',  ( -172.0450000000000159, 7.632228543268600340, 2.479861379858949277 ) ) ;
#38299=DIRECTION ( 'NONE',  ( 0.000000000000000000, 0.000000000000000000, 1.000000000000000000 ) ) ;
#38303=CARTESIAN_POINT ( 'NONE',  ( -87.05499999999999261, -9.827790563157499189E-16, -8.024999999999991473 ) ) ;
#38306=CARTESIAN_POINT ( 'NONE',  ( -81.14499999999998181, -4.716976649647092401, 6.492361379858946790 ) ) ;
#38330=DIRECTION ( 'NONE',  ( 0.000000000000000000, 0.000000000000000000, 1.000000000000000000 ) ) ;
#38335=CARTESIAN_POINT ( 'NONE',  ( -115.1049999999999756, -6.826472737025113702, 4.959722759717902107 ) ) ;
#38351=CARTESIAN_POINT ( 'NONE',  ( -118.1070736234661780, 8.102448949553172852, -5.886773742842744461 ) ) ;
#38366=CARTESIAN_POINT ( 'NONE',  ( -49.19292637653380496, -10.01517768586948698, 6.132527647946031529E-16 ) ) ;
#38370=CARTESIAN_POINT ( 'NONE',  ( -139.2549999999999955, -4.716976649647092401, 6.492361379858946790 ) ) ;
#38372=EDGE_CURVE ( 'NONE', #12708, #36632, #62006, .T. ) ;
#38383=CARTESIAN_POINT ( 'NONE',  ( -109.9429263765338050, 0.000000000000000000, 9.524999999999991473 ) ) ;
#38384=CARTESIAN_POINT ( 'NONE',  ( -60.65499999999998693, -7.632228543268600340, -2.479861379858950166 ) ) ;
#38393=EDGE_LOOP ( 'NONE', ( #28582, #56766, #15017, #22151 ) ) ;
#38396=CARTESIAN_POINT ( 'NONE',  ( -145.5570736234661808, -1.166476076187852838E-15, -9.524999999999991473 ) ) ;
#38400=CARTESIAN_POINT ( 'NONE',  ( -114.4449999999999932, 0.000000000000000000, 8.024999999999991473 ) ) ;
#38402=CARTESIAN_POINT ( 'NONE',  ( -90.74499999999999034, 4.716976649647094177, 6.492361379858945902 ) ) ;
#38413=CARTESIAN_POINT ( 'NONE',  ( -128.8429263765337964, 9.058813317711329915, -2.943386871421373119 ) ) ;
#38415=CARTESIAN_POINT ( 'NONE',  ( -151.9449999999999932, -9.827790563157499189E-16, -8.024999999999991473 ) ) ;
#38426=CARTESIAN_POINT ( 'NONE',  ( -60.29292637653380638, 3.094860106618428031, -9.524999999999993250 ) ) ;
#38429=LINE ( 'NONE', #44047, #31962 ) ;
#38432=CARTESIAN_POINT ( 'NONE',  ( -139.2549999999999955, -4.716976649647092401, 6.492361379858946790 ) ) ;
#38439=DIRECTION ( 'NONE',  ( 0.000000000000000000, 0.000000000000000000, 1.000000000000000000 ) ) ;
#38444=CARTESIAN_POINT ( 'NONE',  ( -95.00707362346616947, -8.102448949553174629, -5.886773742842741797 ) ) ;
#38447=CARTESIAN_POINT ( 'NONE',  ( -52.10499999999997556, -6.826472737025113702, 4.959722759717902107 ) ) ;
#38448=CARTESIAN_POINT ( 'NONE',  ( -116.3949999999999960, -6.826472737025115478, -4.959722759717899443 ) ) ;
#38456=CARTESIAN_POINT ( 'NONE',  ( 0.000000000000000000, 0.000000000000000000, 0.000000000000000000 ) ) ;
#38458=FACE_OUTER_BOUND ( 'NONE', #34336, .T. ) ;
#38461=CARTESIAN_POINT ( 'NONE',  ( -168.9549999999999841, -7.632228543268599452, 2.479861379858951054 ) ) ;
#38474=CARTESIAN_POINT ( 'NONE',  ( -85.70499999999999829, 2.607480562269073321, 8.024999999999991473 ) ) ;
#38475=EDGE_LOOP ( 'NONE', ( #11943, #59336, #57790, #41925 ) ) ;
#38480=CARTESIAN_POINT ( 'NONE',  ( -67.25707362346616947, 5.598654528085800663, -7.705886871421367523 ) ) ;
#38481=AXIS2_PLACEMENT_3D ( 'NONE', #51477, #66977, #18772 ) ;
#38488=CARTESIAN_POINT ( 'NONE',  ( -99.50499999999996703, -6.826472737025115478, -4.959722759717899443 ) ) ;
#38490=CARTESIAN_POINT ( 'NONE',  ( -115.6449999999999818, 4.716976649647091513, -6.492361379858946790 ) ) ;
#38495=CARTESIAN_POINT ( 'NONE',  ( -149.5429263765338135, 9.058813317711329915, 2.943386871421369566 ) ) ;
#38496=CARTESIAN_POINT ( 'NONE',  ( -177.8949999999999818, 6.826472737025116366, 4.959722759717898555 ) ) ;
#38506=CARTESIAN_POINT ( 'NONE',  ( -68.99292637653380211, 8.102448949553171076, -5.886773742842744461 ) ) ;
#38516=CARTESIAN_POINT ( 'NONE',  ( -171.0549999999999784, -9.827790563157499189E-16, -8.024999999999991473 ) ) ;
#38527=CARTESIAN_POINT ( 'NONE',  ( -80.30499999999999261, 8.437984349512086979, -1.550032578732815448E-15 ) ) ;
#38532=CARTESIAN_POINT ( 'NONE',  ( -168.4429263765337907, -1.166476076187852838E-15, -9.524999999999991473 ) ) ;
#38538=CARTESIAN_POINT ( 'NONE',  ( -61.79499999999998039, 2.607480562269068880, -8.024999999999993250 ) ) ;
#38548=CARTESIAN_POINT ( 'NONE',  ( -113.7549999999999955, 4.716976649647091513, -6.492361379858946790 ) ) ;
#38555=CARTESIAN_POINT ( 'NONE',  ( -147.3570736234661638, 5.598654528085804216, 7.705886871421366635 ) ) ;
#38558=CARTESIAN_POINT ( 'NONE',  ( -93.80707362346618083, 10.01517768586948698, -1.839758294383808571E-15 ) ) ;
#38565=CARTESIAN_POINT ( 'NONE',  ( -134.1550000000000011, 7.632228543268600340, 2.479861379858949277 ) ) ;
#38568=CARTESIAN_POINT ( 'NONE',  ( -55.04292637653379927, -9.058813317711329915, -2.943386871421370898 ) ) ;
#38569=CARTESIAN_POINT ( 'NONE',  ( -146.6949999999999932, -8.437984349512085203, 5.166775262442717831E-16 ) ) ;
#38570=EDGE_CURVE ( 'NONE', #13067, #37066, #16247, .T. ) ;
#38571=CARTESIAN_POINT ( 'NONE',  ( -133.0449999999999875, 7.632228543268600340, 2.479861379858949277 ) ) ;
#38574=EDGE_CURVE ( 'NONE', #41595, #52470, #40471, .T. ) ;
#38576=CARTESIAN_POINT ( 'NONE',  ( -48.20499999999999829, -2.607480562269071545, -8.024999999999991473 ) ) ;
#38579=CARTESIAN_POINT ( 'NONE',  ( -61.64499999999998892, 4.716976649647091513, -6.492361379858946790 ) ) ;
#38581=CARTESIAN_POINT ( 'NONE',  ( -139.0429263765338135, -9.058813317711329915, -2.943386871421370898 ) ) ;
#38582=CARTESIAN_POINT ( 'NONE',  ( -195.0000000000000000, 0.000000000000000000, 9.524999999999991473 ) ) ;
#38587=CARTESIAN_POINT ( 'NONE',  ( -76.55707362346616662, -1.166476076187852838E-15, -9.524999999999991473 ) ) ;
#38588=CARTESIAN_POINT ( 'NONE',  ( -92.99292637653381632, 8.102448949553171076, -5.886773742842744461 ) ) ;
#38590=CARTESIAN_POINT ( 'NONE',  ( -195.0000000000000000, 1.166476076187852838E-15, -9.524999999999991473 ) ) ;
#38608=ORIENTED_EDGE ( 'NONE', *, *, #69051, .F. ) ;
#38612=CARTESIAN_POINT ( 'NONE',  ( -91.64499999999999602, 4.716976649647091513, -6.492361379858946790 ) ) ;
#38617=CYLINDRICAL_SURFACE ( 'NONE', #1861, 9.524999999999991473 ) ;
#38628=AXIS2_PLACEMENT_3D ( 'NONE', #32308, #33693, #34719 ) ;
#38630=CARTESIAN_POINT ( 'NONE',  ( -183.0570736234661808, 0.000000000000000000, 9.524999999999991473 ) ) ;
#38636=CARTESIAN_POINT ( 'NONE',  ( -161.6929263765337907, 10.01517768586948698, -1.839758294383808966E-15 ) ) ;
#38643=CARTESIAN_POINT ( 'NONE',  ( -157.1049999999999898, -6.826472737025115478, 4.959722759717900331 ) ) ;
#38645=CARTESIAN_POINT ( 'NONE',  ( -195.0000000000000000, 0.000000000000000000, 0.000000000000000000 ) ) ;
#38647=CARTESIAN_POINT ( 'NONE',  ( -178.7949999999999875, 2.607480562269068880, -8.024999999999993250 ) ) ;
#38649=CARTESIAN_POINT ( 'NONE',  ( -158.2450000000000045, -4.716976649647093289, -6.492361379858945902 ) ) ;
#38650=EDGE_LOOP ( 'NONE', ( #25410, #53887, #45551, #68276 ) ) ;
#38657=CARTESIAN_POINT ( 'NONE',  ( -69.20499999999998408, -2.607480562269071545, -8.024999999999991473 ) ) ;
#38661=CARTESIAN_POINT ( 'NONE',  ( -84.74499999999999034, 4.716976649647094177, 6.492361379858945902 ) ) ;
#38682=EDGE_LOOP ( 'NONE', ( #50371, #20506, #36965, #53932 ) ) ;
#38683=CARTESIAN_POINT ( 'NONE',  ( -113.6049999999999898, 6.826472737025113702, -4.959722759717902107 ) ) ;
#38711=CARTESIAN_POINT ( 'NONE',  ( -48.44292637653380496, -1.166476076187852838E-15, -9.524999999999991473 ) ) ;
#38714=CARTESIAN_POINT ( 'NONE',  ( -138.5049999999999955, -6.826472737025115478, -4.959722759717899443 ) ) ;
#38720=CARTESIAN_POINT ( 'NONE',  ( -157.3429263765337964, -9.058813317711329915, 2.943386871421371787 ) ) ;
#38728=CARTESIAN_POINT ( 'NONE',  ( -58.40499999999997982, -2.607480562269069768, 8.024999999999991473 ) ) ;
#38739=CARTESIAN_POINT ( 'NONE',  ( -129.4429263765338192, -1.166476076187852838E-15, -9.524999999999991473 ) ) ;
#38743=CARTESIAN_POINT ( 'NONE',  ( -109.4949999999999619, 6.826472737025113702, -4.959722759717902107 ) ) ;
#38745=CARTESIAN_POINT ( 'NONE',  ( -75.29500000000000171, -2.607480562269069768, 8.024999999999991473 ) ) ;
#38752=CARTESIAN_POINT ( 'NONE',  ( -122.5429263765337993, 9.058813317711329915, 2.943386871421369566 ) ) ;
#38755=CARTESIAN_POINT ( 'NONE',  ( -147.8949999999999818, 6.826472737025116366, 4.959722759717898555 ) ) ;
#38766=CARTESIAN_POINT ( 'NONE',  ( -143.0049999999999955, 6.826472737025115478, 4.959722759717899443 ) ) ;
#38780=CARTESIAN_POINT ( 'NONE',  ( -195.0000000000000000, 0.000000000000000000, 9.524999999999991473 ) ) ;
#38782=CARTESIAN_POINT ( 'NONE',  ( -51.35499999999998266, -4.716976649647093289, -6.492361379858945902 ) ) ;
#38796=CARTESIAN_POINT ( 'NONE',  ( -167.1550000000000011, 7.632228543268600340, 2.479861379858949277 ) ) ;
#38804=CARTESIAN_POINT ( 'NONE',  ( -77.84292637653379643, 9.058813317711329915, -2.943386871421373119 ) ) ;
#38809=CARTESIAN_POINT ( 'NONE',  ( -84.95499999999998408, -7.632228543268599452, 2.479861379858951054 ) ) ;
#38814=CARTESIAN_POINT ( 'NONE',  ( -52.55707362346618083, -1.166476076187852838E-15, -9.524999999999991473 ) ) ;
#38822=ADVANCED_FACE ( 'NONE', ( #11379 ), #32843, .T. ) ;
#38825=CARTESIAN_POINT ( 'NONE',  ( -118.7950000000000017, 2.607480562269068880, -8.024999999999993250 ) ) ;
#38828=CARTESIAN_POINT ( 'NONE',  ( -78.44292637653380496, -1.166476076187852838E-15, -9.524999999999991473 ) ) ;
#38830=CARTESIAN_POINT ( 'NONE',  ( -16.62366585040244971, 11.02492648493062610, -4.740184257027916459 ) ) ;
#38831=CARTESIAN_POINT ( 'NONE',  ( -154.6429263765338078, -5.598654528085801552, 7.705886871421367523 ) ) ;
#38832=CARTESIAN_POINT ( 'NONE',  ( -179.8449999999999989, -7.632228543268599452, 2.479861379858951054 ) ) ;
#38840=CARTESIAN_POINT ( 'NONE',  ( -67.19292637653379074, -10.01517768586948698, 6.132527647946031529E-16 ) ) ;
#38850=CARTESIAN_POINT ( 'NONE',  ( -171.8049999999999784, -8.437984349512086979, 5.166775262442717831E-16 ) ) ;
#38860=CARTESIAN_POINT ( 'NONE',  ( -88.25499999999998124, -4.716976649647092401, 6.492361379858946790 ) ) ;
#38871=CARTESIAN_POINT ( 'NONE',  ( -140.3070736234661808, -10.01517768586948698, 6.132527647946031529E-16 ) ) ;
#38873=CARTESIAN_POINT ( 'NONE',  ( -64.49499999999997613, 6.826472737025113702, -4.959722759717902107 ) ) ;
#38880=ORIENTED_EDGE ( 'NONE', *, *, #37783, .T. ) ;
#38884=CARTESIAN_POINT ( 'NONE',  ( -112.8550000000000040, 4.716976649647094177, 6.492361379858945902 ) ) ;
#38892=CARTESIAN_POINT ( 'NONE',  ( -153.0570736234661808, 0.000000000000000000, 9.524999999999991473 ) ) ;
#38896=CARTESIAN_POINT ( 'NONE',  ( -86.75707362346616947, -5.598654528085801552, 7.705886871421367523 ) ) ;
#38904=CARTESIAN_POINT ( 'NONE',  ( -131.3050000000000068, 8.437984349512085203, -1.550032578732815448E-15 ) ) ;
#38907=CARTESIAN_POINT ( 'NONE',  ( -145.7950000000000443, 2.607480562269068880, -8.024999999999993250 ) ) ;
#38908=CARTESIAN_POINT ( 'NONE',  ( -130.1949999999999932, 8.437984349512086979, -1.550032578732815448E-15 ) ) ;
#38915=CARTESIAN_POINT ( 'NONE',  ( -183.5929263765338249, -3.094860106618431139, -9.524999999999991473 ) ) ;
#38917=CARTESIAN_POINT ( 'NONE',  ( -55.34499999999997755, 7.632228543268599452, -2.479861379858951942 ) ) ;
#38918=CARTESIAN_POINT ( 'NONE',  ( -103.1070736234661638, 8.102448949553172852, -5.886773742842744461 ) ) ;
#38923=CARTESIAN_POINT ( 'NONE',  ( -75.50707362346616947, 8.102448949553176405, 5.886773742842740909 ) ) ;
#38925=CARTESIAN_POINT ( 'NONE',  ( -98.54292637653381348, 9.058813317711329915, 2.943386871421369566 ) ) ;
#38949=CARTESIAN_POINT ( 'NONE',  ( -94.10707362346614957, 8.102448949553172852, -5.886773742842744461 ) ) ;
#38951=CARTESIAN_POINT ( 'NONE',  ( -95.09499999999999886, -2.607480562269071545, -8.024999999999991473 ) ) ;
#38956=FACE_OUTER_BOUND ( 'NONE', #14185, .T. ) ;
#38971=CARTESIAN_POINT ( 'NONE',  ( -137.3929263765337794, 8.102448949553176405, 5.886773742842740909 ) ) ;
#38975=CARTESIAN_POINT ( 'NONE',  ( -180.2070736234661865, 3.094860106618433360, 9.524999999999991473 ) ) ;
#38981=CARTESIAN_POINT ( 'NONE',  ( -115.6429263765338078, -5.598654528085801552, 7.705886871421367523 ) ) ;
#38989=CARTESIAN_POINT ( 'NONE',  ( -161.9050000000000011, 2.607480562269068880, -8.024999999999993250 ) ) ;
#38991=CARTESIAN_POINT ( 'NONE',  ( -183.5761998908936619, -4.982236208952005363, -7.440177628705773927 ) ) ;
#38992=CARTESIAN_POINT ( 'NONE',  ( -169.4949999999999761, 6.826472737025113702, -4.959722759717902107 ) ) ;
#38993=CARTESIAN_POINT ( 'NONE',  ( -154.4949999999999477, 6.826472737025113702, -4.959722759717902107 ) ) ;
#38997=CARTESIAN_POINT ( 'NONE',  ( -73.25499999999998124, -4.716976649647092401, 6.492361379858946790 ) ) ;
#39001=CARTESIAN_POINT ( 'NONE',  ( -71.69499999999997897, -8.437984349512086979, 5.166775262442717831E-16 ) ) ;
#39008=CARTESIAN_POINT ( 'NONE',  ( -195.0000000000000000, 0.000000000000000000, 9.524999999999991473 ) ) ;
#39019=CARTESIAN_POINT ( 'NONE',  ( -114.9549999999999841, -7.632228543268599452, 2.479861379858951054 ) ) ;
#39025=CARTESIAN_POINT ( 'NONE',  ( -56.54292637653379927, 9.058813317711329915, 2.943386871421369566 ) ) ;
#39031=ORIENTED_EDGE ( 'NONE', *, *, #60241, .F. ) ;
#39036=CARTESIAN_POINT ( 'NONE',  ( -152.1570736234661751, -9.058813317711329915, -2.943386871421370898 ) ) ;
#39042=CARTESIAN_POINT ( 'NONE',  ( -105.1429263765338078, 5.598654528085800663, -7.705886871421367523 ) ) ;
#39048=CARTESIAN_POINT ( 'NONE',  ( -49.04292637653379217, -9.058813317711329915, -2.943386871421370898 ) ) ;
#39052=CARTESIAN_POINT ( 'NONE',  ( -130.4050000000000011, -2.607480562269069768, 8.024999999999991473 ) ) ;
#39058=CARTESIAN_POINT ( 'NONE',  ( -106.7070736234671244, -3.094860106634161667, -9.524999999988564170 ) ) ;
#39065=CARTESIAN_POINT ( 'NONE',  ( -58.25499999999997414, -4.716976649647092401, 6.492361379858946790 ) ) ;
#39072=CARTESIAN_POINT ( 'NONE',  ( -183.4449999999999932, 0.000000000000000000, 8.024999999999991473 ) ) ;
#39079=VECTOR ( 'NONE', #28057, 1000.000000000000000 ) ;
#39080=CARTESIAN_POINT ( 'NONE',  ( -96.89499999999998181, 6.826472737025115478, 4.959722759717899443 ) ) ;
#39082=CARTESIAN_POINT ( 'NONE',  ( -77.69499999999999318, -8.437984349512085203, 5.166775262442717831E-16 ) ) ;
#39092=CARTESIAN_POINT ( 'NONE',  ( -126.8929263765338220, -8.102448949553172852, -5.886773742842741797 ) ) ;
#39094=CARTESIAN_POINT ( 'NONE',  ( -139.6449999999999818, 4.716976649647091513, -6.492361379858946790 ) ) ;
#39103=CARTESIAN_POINT ( 'NONE',  ( -132.0570736234661808, 0.000000000000000000, 9.524999999999991473 ) ) ;
#39105=CARTESIAN_POINT ( 'NONE',  ( -50.45707362346615810, -9.058813317711329915, 2.943386871421371787 ) ) ;
#39108=CARTESIAN_POINT ( 'NONE',  ( -139.8550000000000182, 4.716976649647094177, 6.492361379858945902 ) ) ;
#39123=CARTESIAN_POINT ( 'NONE',  ( -59.15499999999998693, 7.632228543268600340, 2.479861379858949277 ) ) ;
#39130=CARTESIAN_POINT ( 'NONE',  ( -88.94292637653380496, 0.000000000000000000, 9.524999999999991473 ) ) ;
#39131=EDGE_CURVE ( 'NONE', #2564, #58449, #23388, .T. ) ;
#39139=CARTESIAN_POINT ( 'NONE',  ( -173.6049999999999898, 6.826472737025113702, -4.959722759717902107 ) ) ;
#39151=CARTESIAN_POINT ( 'NONE',  ( -84.05499999999999261, -9.827790563157499189E-16, -8.024999999999991473 ) ) ;
#39153=( BOUNDED_CURVE ( )  B_SPLINE_CURVE ( 2, ( #2700, #24193, #45699, #46393, #9077, #19249, #67452, #36175, #25570, #40753, #62517 ),
 .UNSPECIFIED., .F., .F. ) 
 B_SPLINE_CURVE_WITH_KNOTS ( ( 3, 2, 2, 2, 2, 3 ),
 ( 0.02173913043478211890, 0.02391304347826033252, 0.02608695652173854268, 0.02826086956521675284, 0.03043478260869496993, 0.03260869565217317662 ),
 .UNSPECIFIED. ) 
 CURVE ( )  GEOMETRIC_REPRESENTATION_ITEM ( )  RATIONAL_B_SPLINE_CURVE ( ( 1.000000000000010880, 0.9510565162951424290, 1.000000000000000000, 0.9510565162951535312, 1.000000000000000000, 0.9510565162951535312, 1.000000000000000000, 0.9510565162951535312, 1.000000000000000000, 0.9510565162951700735, 0.9999999999999834577 ) ) 
 REPRESENTATION_ITEM ( '' )  );
#39162=CARTESIAN_POINT ( 'NONE',  ( -109.3449999999999847, 7.632228543268599452, -2.479861379858951942 ) ) ;
#39167=CARTESIAN_POINT ( 'NONE',  ( -157.3429263765337964, -9.058813317711329915, 2.943386871421371787 ) ) ;
#39168=CARTESIAN_POINT ( 'NONE',  ( -164.2450000000000045, -4.716976649647093289, -6.492361379858945902 ) ) ;
#39169=AXIS2_PLACEMENT_3D ( 'NONE', #21118, #38031, #44008 ) ;
#39174=ORIENTED_EDGE ( 'NONE', *, *, #52752, .F. ) ;
#39175=CARTESIAN_POINT ( 'NONE',  ( -64.19292637653380496, -10.01517768586948698, 6.132527647946031529E-16 ) ) ;
#39185=CARTESIAN_POINT ( 'NONE',  ( -168.9549999999999841, -7.632228543268599452, 2.479861379858951054 ) ) ;
#39196=CARTESIAN_POINT ( 'NONE',  ( -84.95499999999998408, -7.632228543268599452, 2.479861379858951054 ) ) ;
#39208=CARTESIAN_POINT ( 'NONE',  ( -58.34499999999997755, 7.632228543268599452, -2.479861379858951942 ) ) ;
#39211=CARTESIAN_POINT ( 'NONE',  ( -138.8070736234661524, 10.01517768586948698, -1.839758294383808966E-15 ) ) ;
#39214=CARTESIAN_POINT ( 'NONE',  ( -56.69499999999998607, -8.437984349512086979, 5.166775262442717831E-16 ) ) ;
#39219=CARTESIAN_POINT ( 'NONE',  ( -109.7049999999999699, 2.607480562269073321, 8.024999999999991473 ) ) ;
#39227=CARTESIAN_POINT ( 'NONE',  ( -151.7070736234662149, -3.094860106618431139, -9.524999999999991473 ) ) ;
#39231=CARTESIAN_POINT ( 'NONE',  ( -81.95707362346617231, 9.058813317711329915, -2.943386871421373119 ) ) ;
#39238=CARTESIAN_POINT ( 'NONE',  ( -130.4050000000000011, -2.607480562269069768, 8.024999999999991473 ) ) ;
#39239=CARTESIAN_POINT ( 'NONE',  ( -164.6929263765338476, 10.01517768586948698, -1.839758294383808966E-15 ) ) ;
#39240=CARTESIAN_POINT ( 'NONE',  ( -55.49292637653380211, -8.102448949553174629, 5.886773742842742685 ) ) ;
#39241=CARTESIAN_POINT ( 'NONE',  ( -133.0449999999999875, 7.632228543268600340, 2.479861379858949277 ) ) ;
#39244=CARTESIAN_POINT ( 'NONE',  ( -124.1949999999999932, 8.437984349512086979, -1.550032578732815448E-15 ) ) ;
#39250=CARTESIAN_POINT ( 'NONE',  ( -177.4429263765338192, -1.166476076187852838E-15, -9.524999999999991473 ) ) ;
#39251=CARTESIAN_POINT ( 'NONE',  ( -62.39499999999998181, -6.826472737025115478, -4.959722759717899443 ) ) ;
#39259=CARTESIAN_POINT ( 'NONE',  ( -100.1929263765337907, -10.01517768586948698, 6.132527647946031529E-16 ) ) ;
#39262=CARTESIAN_POINT ( 'NONE',  ( -162.5070736234661695, 8.102448949553176405, 5.886773742842740909 ) ) ;
#39265=CARTESIAN_POINT ( 'NONE',  ( -78.65707362346617515, 9.058813317711329915, 2.943386871421369566 ) ) ;
#39279=EDGE_CURVE ( 'NONE', #32568, #16179, #18322, .T. ) ;
#39283=CARTESIAN_POINT ( 'NONE',  ( -119.7570736234661695, -5.598654528085801552, 7.705886871421367523 ) ) ;
#39284=VECTOR ( 'NONE', #2195, 1000.000000000000000 ) ;
#39286=DIRECTION ( 'NONE',  ( -1.000000000000000000, -0.000000000000000000, -0.000000000000000000 ) ) ;
#39287=CARTESIAN_POINT ( 'NONE',  ( -92.99500000000000455, -6.826472737025115478, 4.959722759717900331 ) ) ;
#39308=CARTESIAN_POINT ( 'NONE',  ( -113.0070736234661695, -8.102448949553172852, -5.886773742842741797 ) ) ;
#39317=CARTESIAN_POINT ( 'NONE',  ( -164.0049999999999955, 6.826472737025116366, 4.959722759717898555 ) ) ;
#39320=CARTESIAN_POINT ( 'NONE',  ( -165.1449999999999818, -4.716976649647092401, 6.492361379858946790 ) ) ;
#39321=CARTESIAN_POINT ( 'NONE',  ( -153.8949999999999818, 6.826472737025115478, 4.959722759717899443 ) ) ;
#39328=CARTESIAN_POINT ( 'NONE',  ( -74.45499999999999829, 7.632228543268599452, -2.479861379858951942 ) ) ;
#39330=CARTESIAN_POINT ( 'NONE',  ( -74.99499999999999034, -6.826472737025113702, 4.959722759717902107 ) ) ;
#39353=CARTESIAN_POINT ( 'NONE',  ( -132.9570736234661865, 9.058813317711329915, -2.943386871421373119 ) ) ;
#39360=CARTESIAN_POINT ( 'NONE',  ( -107.3049999999999642, 8.437984349512086979, -1.550032578732815448E-15 ) ) ;
#39363=ORIENTED_EDGE ( 'NONE', *, *, #6923, .T. ) ;
#39372=CARTESIAN_POINT ( 'NONE',  ( -152.9070736234666015, -3.094860106612244977, 9.525000000004485656 ) ) ;
#39389=CARTESIAN_POINT ( 'NONE',  ( -128.9050000000000011, 2.607480562269068880, -8.024999999999993250 ) ) ;
#39401=CARTESIAN_POINT ( 'NONE',  ( -109.4929263765337737, -8.102448949553174629, 5.886773742842742685 ) ) ;
#39402=CARTESIAN_POINT ( 'NONE',  ( -49.55499999999998550, 0.000000000000000000, 8.024999999999991473 ) ) ;
#39412=ORIENTED_EDGE ( 'NONE', *, *, #59964, .F. ) ;
#39421=CARTESIAN_POINT ( 'NONE',  ( -101.2449999999999903, -4.716976649647093289, -6.492361379858945902 ) ) ;
#39423=CARTESIAN_POINT ( 'NONE',  ( -76.79499999999998749, 2.607480562269068880, -8.024999999999993250 ) ) ;
#39434=CARTESIAN_POINT ( 'NONE',  ( -126.1429263765337936, 5.598654528085800663, -7.705886871421367523 ) ) ;
#39436=CARTESIAN_POINT ( 'NONE',  ( -137.9950000000000045, -6.826472737025115478, 4.959722759717900331 ) ) ;
#39440=CARTESIAN_POINT ( 'NONE',  ( -173.8429263765338249, 9.058813317711329915, -2.943386871421373119 ) ) ;
#39441=ORIENTED_EDGE ( 'NONE', *, *, #42612, .T. ) ;
#39443=VECTOR ( 'NONE', #11109, 1000.000000000000000 ) ;
#39447=DIRECTION ( 'NONE',  ( 0.000000000000000000, 0.000000000000000000, 1.000000000000000000 ) ) ;
#39448=VECTOR ( 'NONE', #50746, 1000.000000000000000 ) ;
#39452=CARTESIAN_POINT ( 'NONE',  ( -140.4549999999999841, 7.632228543268599452, -2.479861379858951942 ) ) ;
#39453=ORIENTED_EDGE ( 'NONE', *, *, #64658, .F. ) ;
#39466=CARTESIAN_POINT ( 'NONE',  ( -55.10499999999998266, -6.826472737025113702, 4.959722759717902107 ) ) ;
#39475=VERTEX_POINT ( 'NONE', #51023 ) ;
#39477=CARTESIAN_POINT ( 'NONE',  ( -121.8570736234661780, -5.598654528085803328, -7.705886871421366635 ) ) ;
#39480=CARTESIAN_POINT ( 'NONE',  ( -157.8549999999999898, 4.716976649647094177, 6.492361379858945902 ) ) ;
#39490=CARTESIAN_POINT ( 'NONE',  ( -74.00499999999996703, 6.826472737025116366, 4.959722759717898555 ) ) ;
#39499=CARTESIAN_POINT ( 'NONE',  ( -53.75707362346618368, -5.598654528085801552, 7.705886871421367523 ) ) ;
#39504=CARTESIAN_POINT ( 'NONE',  ( -110.3949999999999818, -6.826472737025115478, -4.959722759717899443 ) ) ;
#39509=EDGE_CURVE ( 'NONE', #65525, #47886, #54406, .T. ) ;
#39510=CARTESIAN_POINT ( 'NONE',  ( -157.4929263765337737, -8.102448949553172852, 5.886773742842742685 ) ) ;
#39511=CARTESIAN_POINT ( 'NONE',  ( -168.8949999999999818, 6.826472737025116366, 4.959722759717898555 ) ) ;
#39517=CARTESIAN_POINT ( 'NONE',  ( -69.89292637653380780, -8.102448949553172852, -5.886773742842741797 ) ) ;
#39523=CARTESIAN_POINT ( 'NONE',  ( -141.5929263765343649, -3.094860106627439933, -9.524999999993450928 ) ) ;
#39528=CARTESIAN_POINT ( 'NONE',  ( -170.6050000000000182, 6.826472737025113702, -4.959722759717902107 ) ) ;
#39534=VECTOR ( 'NONE', #54292, 1000.000000000000000 ) ;
#39541=CARTESIAN_POINT ( 'NONE',  ( -81.65499999999998693, -7.632228543268600340, -2.479861379858950166 ) ) ;
#39547=CARTESIAN_POINT ( 'NONE',  ( -72.05707362346616662, 0.000000000000000000, 9.524999999999991473 ) ) ;
#39552=CARTESIAN_POINT ( 'NONE',  ( -139.7070736234666981, -3.094860106627305374, -9.524999999993545075 ) ) ;
#39554=CARTESIAN_POINT ( 'NONE',  ( -51.29499999999997328, -2.607480562269069768, 8.024999999999991473 ) ) ;
#39561=CARTESIAN_POINT ( 'NONE',  ( -138.5070736234661695, 8.102448949553176405, 5.886773742842740909 ) ) ;
#39565=CARTESIAN_POINT ( 'NONE',  ( -56.39499999999997470, -6.826472737025113702, -4.959722759717900331 ) ) ;
#39570=CARTESIAN_POINT ( 'NONE',  ( -118.5549999999999926, 0.000000000000000000, 8.024999999999991473 ) ) ;
#39571=VERTEX_POINT ( 'NONE', #5567 ) ;
#39573=DIRECTION ( 'NONE',  ( -1.000000000000000000, -0.000000000000000000, -0.000000000000000000 ) ) ;
#39574=CARTESIAN_POINT ( 'NONE',  ( -150.6570736234661751, 9.058813317711329915, 2.943386871421369566 ) ) ;
#39578=CARTESIAN_POINT ( 'NONE',  ( -82.10707362346616378, 8.102448949553171076, -5.886773742842744461 ) ) ;
#39584=CARTESIAN_POINT ( 'NONE',  ( -177.0570736234661808, 0.000000000000000000, 9.524999999999991473 ) ) ;
#39588=CARTESIAN_POINT ( 'NONE',  ( -130.7049999999999841, 2.607480562269073321, 8.024999999999991473 ) ) ;
#39592=CARTESIAN_POINT ( 'NONE',  ( -134.6950000000000216, -8.437984349512085203, 5.166775262442717831E-16 ) ) ;
#39593=CARTESIAN_POINT ( 'NONE',  ( -125.8449999999999847, -7.632228543268599452, 2.479861379858951054 ) ) ;
#39601=CARTESIAN_POINT ( 'NONE',  ( -121.7929263765346235, -3.094860106605321182, 9.525000000009514523 ) ) ;
#39602=CARTESIAN_POINT ( 'NONE',  ( -48.80499999999998550, -8.437984349512085203, 5.166775262442717831E-16 ) ) ;
#39604=CARTESIAN_POINT ( 'NONE',  ( -48.74499999999998323, 4.716976649647094177, 6.492361379858945902 ) ) ;
#39610=CARTESIAN_POINT ( 'NONE',  ( -95.09292637653381064, 3.094860106618433360, 9.524999999999991473 ) ) ;
#39630=CARTESIAN_POINT ( 'NONE',  ( -81.14499999999998181, -4.716976649647092401, 6.492361379858946790 ) ) ;
#39631=ORIENTED_EDGE ( 'NONE', *, *, #45497, .T. ) ;
#39635=ORIENTED_EDGE ( 'NONE', *, *, #52775, .F. ) ;
#39646=CARTESIAN_POINT ( 'NONE',  ( -175.8570736234661638, -5.598654528085803328, -7.705886871421366635 ) ) ;
#39649=( BOUNDED_CURVE ( )  B_SPLINE_CURVE ( 2, ( #19224, #35778, #56171, #24497, #8701, #51604, #1952, #29445, #3364, #61441, #18208 ),
 .UNSPECIFIED., .F., .F. ) 
 B_SPLINE_CURVE_WITH_KNOTS ( ( 3, 2, 2, 2, 2, 3 ),
 ( 0.8804347826086956763, 0.8826086956521739246, 0.8847826086956521729, 0.8869565217391304213, 0.8891304347826086696, 0.8913043478260869179 ),
 .UNSPECIFIED. ) 
 CURVE ( )  GEOMETRIC_REPRESENTATION_ITEM ( )  RATIONAL_B_SPLINE_CURVE ( ( 1.000000000000000000, 0.9510565162951535312, 1.000000000000000000, 0.9510565162951535312, 1.000000000000000000, 0.9510565162951535312, 1.000000000000000000, 0.9510565162951535312, 1.000000000000000000, 0.9510565162951535312, 1.000000000000000000 ) ) 
 REPRESENTATION_ITEM ( '' )  );
#39650=CARTESIAN_POINT ( 'NONE',  ( -108.9570736234661723, 9.058813317711329915, -2.943386871421373119 ) ) ;
#39659=CARTESIAN_POINT ( 'NONE',  ( -155.6049999999999329, 6.826472737025113702, -4.959722759717902107 ) ) ;
#39660=CARTESIAN_POINT ( 'NONE',  ( -184.0000000000000000, 0.000000000000000000, 0.000000000000000000 ) ) ;
#39662=CARTESIAN_POINT ( 'NONE',  ( -160.6449999999999818, 4.716976649647091513, -6.492361379858946790 ) ) ;
#39665=CARTESIAN_POINT ( 'NONE',  ( -154.6450000000000102, 4.716976649647091513, -6.492361379858946790 ) ) ;
#39671=CARTESIAN_POINT ( 'NONE',  ( -71.90499999999995850, 2.607480562269068880, -8.024999999999993250 ) ) ;
#39672=CARTESIAN_POINT ( 'NONE',  ( -70.55707362346616662, -1.166476076187852838E-15, -9.524999999999991473 ) ) ;
#39676=CARTESIAN_POINT ( 'NONE',  ( -68.99499999999999034, -6.826472737025113702, 4.959722759717902107 ) ) ;
#39689=CARTESIAN_POINT ( 'NONE',  ( -119.0929263765346064, 3.094860106632213004, 9.524999999989976374 ) ) ;
#39691=ORIENTED_EDGE ( 'NONE', *, *, #18289, .F. ) ;
#39694=CARTESIAN_POINT ( 'NONE',  ( -155.9929263765338021, 8.102448949553172852, -5.886773742842744461 ) ) ;
#39700=CARTESIAN_POINT ( 'NONE',  ( -98.30499999999997840, 8.437984349512086979, -1.550032578732815448E-15 ) ) ;
#39707=ORIENTED_EDGE ( 'NONE', *, *, #20080, .T. ) ;
#39713=CARTESIAN_POINT ( 'NONE',  ( -124.3449999999999847, 7.632228543268599452, -2.479861379858951942 ) ) ;
#39715=ORIENTED_EDGE ( 'NONE', *, *, #34163, .F. ) ;
#39716=APPLICATION_CONTEXT ( 'automotive_design' ) ;
#39733=CARTESIAN_POINT ( 'NONE',  ( -158.3070736234661808, -10.01517768586948698, 6.132527647946031529E-16 ) ) ;
#39734=CARTESIAN_POINT ( 'NONE',  ( -138.2049999999999272, -2.607480562269071545, -8.024999999999991473 ) ) ;
#39739=CONICAL_SURFACE ( 'NONE', #27325, 8.524999999999977263, 0.7853981633974552734 ) ;
#39741=CARTESIAN_POINT ( 'NONE',  ( -107.6070736234661638, -8.102448949553174629, 5.886773742842742685 ) ) ;
#39748=CARTESIAN_POINT ( 'NONE',  ( -51.80707362346617373, 10.01517768586948698, -1.839758294383808966E-15 ) ) ;
#39750=CARTESIAN_POINT ( 'NONE',  ( -47.90499999999997272, 2.607480562269068880, -8.024999999999993250 ) ) ;
#39755=DIRECTION ( 'NONE',  ( -1.000000000000000000, -0.000000000000000000, -0.000000000000000000 ) ) ;
#39763=CARTESIAN_POINT ( 'NONE',  ( -144.6570736234662036, 9.058813317711329915, 2.943386871421369566 ) ) ;
#39765=CARTESIAN_POINT ( 'NONE',  ( -103.7049999999999983, 2.607480562269073321, 8.024999999999991473 ) ) ;
#39770=AXIS2_PLACEMENT_3D ( 'NONE', #61195, #18953, #45749 ) ;
#39771=CARTESIAN_POINT ( 'NONE',  ( -97.04499999999998749, 7.632228543268600340, 2.479861379858949277 ) ) ;
#39773=CARTESIAN_POINT ( 'NONE',  ( -73.49499999999999034, 6.826472737025113702, -4.959722759717902107 ) ) ;
#39782=CARTESIAN_POINT ( 'NONE',  ( -110.2429263765338021, 5.598654528085804216, 7.705886871421366635 ) ) ;
#39784=CARTESIAN_POINT ( 'NONE',  ( -138.4449999999999932, 0.000000000000000000, 8.024999999999991473 ) ) ;
#39795=DIRECTION ( 'NONE',  ( -1.000000000000000000, -0.000000000000000000, -0.000000000000000000 ) ) ;
#39796=FACE_OUTER_BOUND ( 'NONE', #50835, .T. ) ;
#39800=CARTESIAN_POINT ( 'NONE',  ( -129.8050000000000068, -8.437984349512086979, 5.166775262442717831E-16 ) ) ;
#39813=DIRECTION ( 'NONE',  ( 0.000000000000000000, 0.000000000000000000, 1.000000000000000000 ) ) ;
#39815=CARTESIAN_POINT ( 'NONE',  ( -51.50499999999999545, -6.826472737025113702, -4.959722759717900331 ) ) ;
#39827=DIRECTION ( 'NONE',  ( 0.000000000000000000, 0.000000000000000000, 1.000000000000000000 ) ) ;
#39833=CARTESIAN_POINT ( 'NONE',  ( -162.6550000000000011, -7.632228543268600340, -2.479861379858950166 ) ) ;
#39836=EDGE_CURVE ( 'NONE', #42429, #57245, #61445, .T. ) ;
#39842=EDGE_LOOP ( 'NONE', ( #21064, #59050, #53840, #35993 ) ) ;
#39844=ORIENTED_EDGE ( 'NONE', *, *, #65536, .F. ) ;
#39846=FACE_OUTER_BOUND ( 'NONE', #38650, .T. ) ;
#39847=CARTESIAN_POINT ( 'NONE',  ( -76.85499999999998977, 4.716976649647094177, 6.492361379858945902 ) ) ;
#39860=CARTESIAN_POINT ( 'NONE',  ( -53.60707362346617089, -8.102448949553174629, 5.886773742842742685 ) ) ;
#39862=CONICAL_SURFACE ( 'NONE', #57806, 11.99999999999999645, 0.7853981633974552734 ) ;
#39864=CARTESIAN_POINT ( 'NONE',  ( -104.0949999999999989, -2.607480562269071545, -8.024999999999991473 ) ) ;
#39870=CARTESIAN_POINT ( 'NONE',  ( -142.1929263765337623, -10.01517768586948698, 6.132527647946031529E-16 ) ) ;
#39872=CARTESIAN_POINT ( 'NONE',  ( -170.5450000000000159, -7.632228543268600340, -2.479861379858950166 ) ) ;
#39885=EDGE_LOOP ( 'NONE', ( #9830, #8414, #7573, #48014 ) ) ;
#39886=CARTESIAN_POINT ( 'NONE',  ( -162.0550000000000068, -9.827790563157499189E-16, -8.024999999999991473 ) ) ;
#39888=CARTESIAN_POINT ( 'NONE',  ( -112.7929263765347088, -3.094860106603506189, 9.525000000010836132 ) ) ;
#39896=CARTESIAN_POINT ( 'NONE',  ( -82.70499999999998408, 2.607480562269072433, 8.024999999999991473 ) ) ;
#39903=EDGE_CURVE ( 'NONE', #55259, #24627, #32848, .T. ) ;
#39908=CARTESIAN_POINT ( 'NONE',  ( -55.64499999999997470, 4.716976649647091513, -6.492361379858946790 ) ) ;
#39918=CARTESIAN_POINT ( 'NONE',  ( -51.14499999999999602, -4.716976649647092401, 6.492361379858946790 ) ) ;
#39923=CARTESIAN_POINT ( 'NONE',  ( -107.1549999999999869, 7.632228543268600340, 2.479861379858949277 ) ) ;
#39928=CARTESIAN_POINT ( 'NONE',  ( -144.2070736234661865, 3.094860106618433360, 9.524999999999991473 ) ) ;
#39931=CARTESIAN_POINT ( 'NONE',  ( -86.15707362346617515, -9.058813317711329915, -2.943386871421370898 ) ) ;
#39932=EDGE_CURVE ( 'NONE', #36632, #31059, #57233, .T. ) ;
#39938=CARTESIAN_POINT ( 'NONE',  ( -119.4549999999999983, 7.632228543268599452, -2.479861379858951942 ) ) ;
#39939=CARTESIAN_POINT ( 'NONE',  ( -159.1429263765338078, 5.598654528085800663, -7.705886871421367523 ) ) ;
#39941=CARTESIAN_POINT ( 'NONE',  ( -131.6949999999999932, -8.437984349512085203, 5.166775262442717831E-16 ) ) ;
#39943=CARTESIAN_POINT ( 'NONE',  ( -128.0949999999999989, -2.607480562269071545, -8.024999999999991473 ) ) ;
#39947=CARTESIAN_POINT ( 'NONE',  ( -145.5570736234661808, -1.166476076187852838E-15, -9.524999999999991473 ) ) ;
#39951=CARTESIAN_POINT ( 'NONE',  ( -182.5429263765337851, 9.058813317711329915, 2.943386871421369566 ) ) ;
#39953=CARTESIAN_POINT ( 'NONE',  ( -53.84499999999997755, -7.632228543268599452, 2.479861379858951054 ) ) ;
#39956=CARTESIAN_POINT ( 'NONE',  ( -91.79292637653381348, -3.094860106618429807, 9.524999999999991473 ) ) ;
#39965=CYLINDRICAL_SURFACE ( 'NONE', #47134, 9.524999999999991473 ) ;
#39988=CARTESIAN_POINT ( 'NONE',  ( -80.99499999999999034, -6.826472737025115478, 4.959722759717900331 ) ) ;
#39997=CARTESIAN_POINT ( 'NONE',  ( -76.64292637653380780, -5.598654528085801552, 7.705886871421367523 ) ) ;
#40003=CARTESIAN_POINT ( 'NONE',  ( -137.8429263765337964, 9.058813317711329915, -2.943386871421373119 ) ) ;
#40008=CARTESIAN_POINT ( 'NONE',  ( -179.1570736234662036, -9.058813317711329915, -2.943386871421370898 ) ) ;
#40011=CARTESIAN_POINT ( 'NONE',  ( -115.1070736234661638, 8.102448949553171076, -5.886773742842744461 ) ) ;
#40013=CARTESIAN_POINT ( 'NONE',  ( -183.0295608176848532, 7.162088766832200193, -6.277019169650422725 ) ) ;
#40022=CARTESIAN_POINT ( 'NONE',  ( -163.1050000000000182, -6.826472737025115478, 4.959722759717900331 ) ) ;
#40024=CARTESIAN_POINT ( 'NONE',  ( -183.7236500287686738, -7.325335938885507048, -4.919193638985903227 ) ) ;
#40025=CARTESIAN_POINT ( 'NONE',  ( -163.4949999999999761, 6.826472737025113702, -4.959722759717902107 ) ) ;
#40029=CARTESIAN_POINT ( 'NONE',  ( -158.0949999999999989, -2.607480562269071545, -8.024999999999991473 ) ) ;
#40031=CARTESIAN_POINT ( 'NONE',  ( -67.49292637653380211, -8.102448949553174629, 5.886773742842742685 ) ) ;
#40032=CARTESIAN_POINT ( 'NONE',  ( -122.6929263765338050, 10.01517768586948698, -1.839758294383808966E-15 ) ) ;
#40033=CARTESIAN_POINT ( 'NONE',  ( -70.70499999999996987, 2.607480562269073321, 8.024999999999991473 ) ) ;
#40035=CARTESIAN_POINT ( 'NONE',  ( -69.59499999999998465, 2.607480562269072433, 8.024999999999991473 ) ) ;
#40039=CARTESIAN_POINT ( 'NONE',  ( -156.0570736234661808, 0.000000000000000000, 9.524999999999991473 ) ) ;
#40050=CARTESIAN_POINT ( 'NONE',  ( -154.9429263765338192, 0.000000000000000000, 9.524999999999991473 ) ) ;
#40060=EDGE_CURVE ( 'NONE', #57680, #65525, #57083, .T. ) ;
#40067=CARTESIAN_POINT ( 'NONE',  ( -83.45707362346617231, -9.058813317711329915, 2.943386871421371787 ) ) ;
#40069=CARTESIAN_POINT ( 'NONE',  ( -112.6449999999999960, 4.716976649647091513, -6.492361379858946790 ) ) ;
#40074=CARTESIAN_POINT ( 'NONE',  ( -54.44292637653380496, -1.166476076187852838E-15, -9.524999999999991473 ) ) ;
#40082=VERTEX_POINT ( 'NONE', #69198 ) ;
#40085=CARTESIAN_POINT ( 'NONE',  ( -135.9549999999999841, -7.632228543268599452, 2.479861379858951054 ) ) ;
#40088=ORIENTED_EDGE ( 'NONE', *, *, #59734, .F. ) ;
#40102=DIRECTION ( 'NONE',  ( 0.000000000000000000, 0.000000000000000000, 1.000000000000000000 ) ) ;
#40103=CARTESIAN_POINT ( 'NONE',  ( -53.60707362346617089, -8.102448949553172852, 5.886773742842742685 ) ) ;
#40104=CARTESIAN_POINT ( 'NONE',  ( -182.3950000000000102, -6.826472737025113702, -4.959722759717900331 ) ) ;
#40108=CARTESIAN_POINT ( 'NONE',  ( -161.0070736234661410, -8.102448949553174629, -5.886773742842741797 ) ) ;
#40110=CARTESIAN_POINT ( 'NONE',  ( -88.55707362346616662, -1.166476076187852838E-15, -9.524999999999991473 ) ) ;
#40111=CARTESIAN_POINT ( 'NONE',  ( -103.4049999999999869, -2.607480562269069768, 8.024999999999991473 ) ) ;
#40115=CIRCLE ( 'NONE', #24342, 8.525000000000000355 ) ;
#40116=CARTESIAN_POINT ( 'NONE',  ( -100.3449999999999847, 7.632228543268599452, -2.479861379858951942 ) ) ;
#40118=CARTESIAN_POINT ( 'NONE',  ( -77.24499999999997613, -4.716976649647093289, -6.492361379858945902 ) ) ;
#40125=CARTESIAN_POINT ( 'NONE',  ( -115.0429263765338135, -9.058813317711329915, -2.943386871421370898 ) ) ;
#40126=CARTESIAN_POINT ( 'NONE',  ( -138.8949999999999534, 6.826472737025116366, 4.959722759717898555 ) ) ;
#40129=DIRECTION ( 'NONE',  ( 0.000000000000000000, 0.000000000000000000, 1.000000000000000000 ) ) ;
#40135=CARTESIAN_POINT ( 'NONE',  ( -62.84292637653379643, 9.058813317711329915, -2.943386871421373119 ) ) ;
#40141=CARTESIAN_POINT ( 'NONE',  ( -135.6550000000000011, -7.632228543268600340, -2.479861379858950166 ) ) ;
#40142=ORIENTED_EDGE ( 'NONE', *, *, #47874, .F. ) ;
#40144=VERTEX_POINT ( 'NONE', #32241 ) ;
#40151=ORIENTED_EDGE ( 'NONE', *, *, #26984, .T. ) ;
#40154=CARTESIAN_POINT ( 'NONE',  ( -49.55499999999998550, 0.000000000000000000, 8.024999999999991473 ) ) ;
#40168=CARTESIAN_POINT ( 'NONE',  ( -158.9050000000000011, 2.607480562269068880, -8.024999999999993250 ) ) ;
#40177=CARTESIAN_POINT ( 'NONE',  ( -72.50499999999998124, -6.826472737025115478, -4.959722759717899443 ) ) ;
#40180=CARTESIAN_POINT ( 'NONE',  ( -63.95707362346617231, 9.058813317711329915, -2.943386871421373119 ) ) ;
#40187=CARTESIAN_POINT ( 'NONE',  ( -105.4449999999999790, 0.000000000000000000, 8.024999999999991473 ) ) ;
#40191=CARTESIAN_POINT ( 'NONE',  ( -145.9429263765337907, 0.000000000000000000, 9.524999999999991473 ) ) ;
#40193=CARTESIAN_POINT ( 'NONE',  ( -162.8949999999999534, 6.826472737025116366, 4.959722759717898555 ) ) ;
#40213=CARTESIAN_POINT ( 'NONE',  ( -158.7549999999999670, 4.716976649647091513, -6.492361379858946790 ) ) ;
#40226=CARTESIAN_POINT ( 'NONE',  ( -77.15499999999998693, 7.632228543268600340, 2.479861379858949277 ) ) ;
#40235=CARTESIAN_POINT ( 'NONE',  ( -51.44499999999999318, 0.000000000000000000, 8.024999999999991473 ) ) ;
#40238=CARTESIAN_POINT ( 'NONE',  ( -184.0000000000000000, 0.000000000000000000, -8.524999999999977263 ) ) ;
#40243=CARTESIAN_POINT ( 'NONE',  ( -49.49499999999997613, 6.826472737025113702, -4.959722759717902107 ) ) ;
#40247=CARTESIAN_POINT ( 'NONE',  ( -103.1049999999999756, -6.826472737025115478, 4.959722759717900331 ) ) ;
#40252=CARTESIAN_POINT ( 'NONE',  ( -143.4570736234661865, -9.058813317711329915, 2.943386871421371787 ) ) ;
#40255=CARTESIAN_POINT ( 'NONE',  ( -89.30707362346616662, -10.01517768586948698, 6.132527647946031529E-16 ) ) ;
#40259=LINE ( 'NONE', #55731, #62698 ) ;
#40261=CARTESIAN_POINT ( 'NONE',  ( -122.1549999999999869, 7.632228543268600340, 2.479861379858949277 ) ) ;
#40264=CARTESIAN_POINT ( 'NONE',  ( -132.4449999999999932, 0.000000000000000000, 8.024999999999991473 ) ) ;
#40265=CARTESIAN_POINT ( 'NONE',  ( -120.7449999999999903, 4.716976649647094177, 6.492361379858945902 ) ) ;
#40267=ORIENTED_EDGE ( 'NONE', *, *, #34163, .T. ) ;
#40272=CARTESIAN_POINT ( 'NONE',  ( -169.9429263765337907, 0.000000000000000000, 9.524999999999991473 ) ) ;
#40282=CARTESIAN_POINT ( 'NONE',  ( -89.54292637653379927, 9.058813317711329915, 2.943386871421369566 ) ) ;
#40290=CARTESIAN_POINT ( 'NONE',  ( -78.05707362346616662, 0.000000000000000000, 9.524999999999991473 ) ) ;
#40292=LINE ( 'NONE', #57133, #11183 ) ;
#40303=AXIS2_PLACEMENT_3D ( 'NONE', #60138, #23882, #40102 ) ;
#40306=CARTESIAN_POINT ( 'NONE',  ( -93.44292637653380496, -1.166476076187852838E-15, -9.524999999999991473 ) ) ;
#40310=CARTESIAN_POINT ( 'NONE',  ( -84.44499999999999318, 0.000000000000000000, 8.024999999999991473 ) ) ;
#40311=VERTEX_POINT ( 'NONE', #51537 ) ;
#40323=CARTESIAN_POINT ( 'NONE',  ( -195.0000000000000000, 0.000000000000000000, 0.000000000000000000 ) ) ;
#40328=CARTESIAN_POINT ( 'NONE',  ( -165.2070736234661865, 3.094860106618433360, 9.524999999999991473 ) ) ;
#40332=CARTESIAN_POINT ( 'NONE',  ( -113.7570736234661837, -5.598654528085801552, 7.705886871421367523 ) ) ;
#40335=ORIENTED_EDGE ( 'NONE', *, *, #28148, .F. ) ;
#40336=( BOUNDED_CURVE ( )  B_SPLINE_CURVE ( 2, ( #4765, #22002, #47758, #59610, #43503, #5433, #110, #21279, #21639, #69153, #10752 ),
 .UNSPECIFIED., .F., .F. ) 
 B_SPLINE_CURVE_WITH_KNOTS ( ( 3, 2, 2, 2, 2, 3 ),
 ( 0.6956521739130434590, 0.6978260869565217073, 0.6999999999999999556, 0.7021739130434783149, 0.7043478260869565633, 0.7065217391304348116 ),
 .UNSPECIFIED. ) 
 CURVE ( )  GEOMETRIC_REPRESENTATION_ITEM ( )  RATIONAL_B_SPLINE_CURVE ( ( 1.000000000000000000, 0.9510565162951535312, 1.000000000000000000, 0.9510565162951535312, 1.000000000000000000, 0.9510565162951535312, 1.000000000000000000, 0.9510565162951535312, 1.000000000000000000, 0.9510565162951535312, 1.000000000000000000 ) ) 
 REPRESENTATION_ITEM ( '' )  );
#40341=CARTESIAN_POINT ( 'NONE',  ( -149.9050000000000296, 2.607480562269068880, -8.024999999999993250 ) ) ;
#40344=CARTESIAN_POINT ( 'NONE',  ( -161.0949999999999420, -2.607480562269071545, -8.024999999999991473 ) ) ;
#40346=CARTESIAN_POINT ( 'NONE',  ( -146.2449999999999761, -4.716976649647093289, -6.492361379858945902 ) ) ;
#40350=CARTESIAN_POINT ( 'NONE',  ( -64.55499999999999261, 0.000000000000000000, 8.024999999999991473 ) ) ;
#40355=CARTESIAN_POINT ( 'NONE',  ( -76.04499999999998749, 7.632228543268600340, 2.479861379858949277 ) ) ;
#40360=UNCERTAINTY_MEASURE_WITH_UNIT (LENGTH_MEASURE( 1.000000000000000082E-05 ), #37, 'distance_accuracy_value', 'NONE');
#40369=CARTESIAN_POINT ( 'NONE',  ( -119.8429263765338106, 9.058813317711329915, -2.943386871421373119 ) ) ;
#40376=CARTESIAN_POINT ( 'NONE',  ( -88.94292637653380496, 0.000000000000000000, 9.524999999999991473 ) ) ;
#40391=CARTESIAN_POINT ( 'NONE',  ( -83.00707362346615525, -8.102448949553174629, -5.886773742842741797 ) ) ;
#40393=CARTESIAN_POINT ( 'NONE',  ( -109.9449999999999932, -9.827790563157499189E-16, -8.024999999999991473 ) ) ;
#40398=CARTESIAN_POINT ( 'NONE',  ( -11.69787818154473413, -11.39543851400849839, -3.768533683846105209 ) ) ;
#40412=CARTESIAN_POINT ( 'NONE',  ( -132.3549999999999898, -4.716976649647093289, -6.492361379858945902 ) ) ;
#40428=CARTESIAN_POINT ( 'NONE',  ( -48.80499999999998550, -8.437984349512085203, 5.166775262442717831E-16 ) ) ;
#40430=CARTESIAN_POINT ( 'NONE',  ( -177.8049999999999784, -8.437984349512085203, 5.166775262442717831E-16 ) ) ;
#40432=CARTESIAN_POINT ( 'NONE',  ( -60.50707362346616236, 8.102448949553176405, 5.886773742842740909 ) ) ;
#40435=CARTESIAN_POINT ( 'NONE',  ( -177.5070736234661695, 8.102448949553176405, 5.886773742842740909 ) ) ;
#40442=CARTESIAN_POINT ( 'NONE',  ( -99.05499999999999261, -9.827790563157499189E-16, -8.024999999999991473 ) ) ;
#40447=CARTESIAN_POINT ( 'NONE',  ( -103.4949999999999761, 6.826472737025113702, -4.959722759717902107 ) ) ;
#40450=CARTESIAN_POINT ( 'NONE',  ( -68.24499999999999034, -4.716976649647093289, -6.492361379858945902 ) ) ;
#40459=CARTESIAN_POINT ( 'NONE',  ( -111.2929263765337851, 3.094860106618428031, -9.524999999999993250 ) ) ;
#40460=CARTESIAN_POINT ( 'NONE',  ( -141.8950000000000102, 6.826472737025116366, 4.959722759717898555 ) ) ;
#40471=( BOUNDED_CURVE ( )  B_SPLINE_CURVE ( 2, ( #31615, #53093, #31249, #52419, #63291, #25302, #4884, #42565, #69597, #59047, #26328 ),
 .UNSPECIFIED., .F., .F. ) 
 B_SPLINE_CURVE_WITH_KNOTS ( ( 3, 2, 2, 2, 2, 3 ),
 ( 0.05434782608695529205, 0.05652173913043350567, 0.05869565217391171930, 0.06086956521738993292, 0.06304347826086814655, 0.06521739130434635323 ),
 .UNSPECIFIED. ) 
 CURVE ( )  GEOMETRIC_REPRESENTATION_ITEM ( )  RATIONAL_B_SPLINE_CURVE ( ( 1.000000000000027534, 0.9510565162951257756, 1.000000000000000000, 0.9510565162951535312, 1.000000000000000000, 0.9510565162951535312, 1.000000000000000000, 0.9510565162951535312, 1.000000000000000000, 0.9510565162951866158, 0.9999999999999669154 ) ) 
 REPRESENTATION_ITEM ( '' )  );
#40475=DIRECTION ( 'NONE',  ( 0.000000000000000000, 0.000000000000000000, 1.000000000000000000 ) ) ;
#40478=CARTESIAN_POINT ( 'NONE',  ( -129.9549999999999841, -7.632228543268599452, 2.479861379858951054 ) ) ;
#40479=ORIENTED_EDGE ( 'NONE', *, *, #45933, .T. ) ;
#40481=CARTESIAN_POINT ( 'NONE',  ( -124.2570736234661837, 5.598654528085800663, -7.705886871421367523 ) ) ;
#40485=CARTESIAN_POINT ( 'NONE',  ( -83.24292637653380211, 5.598654528085804216, 7.705886871421366635 ) ) ;
#40512=CARTESIAN_POINT ( 'NONE',  ( -167.0049999999999670, 6.826472737025116366, 4.959722759717898555 ) ) ;
#40522=DIRECTION ( 'NONE',  ( 0.000000000000000000, 0.000000000000000000, 1.000000000000000000 ) ) ;
#40525=CARTESIAN_POINT ( 'NONE',  ( -76.40499999999995850, -2.607480562269069768, 8.024999999999991473 ) ) ;
#40535=ORIENTED_EDGE ( 'NONE', *, *, #68560, .F. ) ;
#40540=CARTESIAN_POINT ( 'NONE',  ( -99.74499999999999034, 4.716976649647094177, 6.492361379858945902 ) ) ;
#40545=AXIS2_PLACEMENT_3D ( 'NONE', #6090, #48705, #60926 ) ;
#40548=CARTESIAN_POINT ( 'NONE',  ( -139.7929263765337851, -3.094860106618429807, 9.524999999999991473 ) ) ;
#40549=CARTESIAN_POINT ( 'NONE',  ( -166.1949999999999932, 8.437984349512085203, -1.550032578732815448E-15 ) ) ;
#40551=EDGE_CURVE ( 'NONE', #31165, #54295, #2066, .T. ) ;
#40564=ORIENTED_EDGE ( 'NONE', *, *, #45922, .F. ) ;
#40565=CARTESIAN_POINT ( 'NONE',  ( -160.5550000000000068, 0.000000000000000000, 8.024999999999991473 ) ) ;
#40577=CARTESIAN_POINT ( 'NONE',  ( -74.90500000000000114, 2.607480562269069324, -8.024999999999993250 ) ) ;
#40582=AXIS2_PLACEMENT_3D ( 'NONE', #47497, #36600, #10512 ) ;
#40583=CARTESIAN_POINT ( 'NONE',  ( -114.4429263765338050, -1.166476076187852838E-15, -9.524999999999991473 ) ) ;
#40589=CARTESIAN_POINT ( 'NONE',  ( -56.84499999999997755, -7.632228543268599452, 2.479861379858951054 ) ) ;
#40597=CARTESIAN_POINT ( 'NONE',  ( -57.74499999999999034, 4.716976649647094177, 6.492361379858945902 ) ) ;
#40600=CARTESIAN_POINT ( 'NONE',  ( -101.3050000000000068, 8.437984349512085203, -1.550032578732815448E-15 ) ) ;
#40605=CARTESIAN_POINT ( 'NONE',  ( -137.7570736234661695, -5.598654528085801552, 7.705886871421367523 ) ) ;
#40606=CARTESIAN_POINT ( 'NONE',  ( -59.45707362346616520, -9.058813317711329915, 2.943386871421371787 ) ) ;
#40609=CARTESIAN_POINT ( 'NONE',  ( -78.05707362346616662, 0.000000000000000000, 9.524999999999991473 ) ) ;
#40612=CARTESIAN_POINT ( 'NONE',  ( -16.77315986280488147, -11.05089483305399867, 4.677852893037058202 ) ) ;
#40614=CARTESIAN_POINT ( 'NONE',  ( -100.0429263765338135, -9.058813317711329915, -2.943386871421370898 ) ) ;
#40615=CARTESIAN_POINT ( 'NONE',  ( -120.3549999999999898, -4.716976649647093289, -6.492361379858945902 ) ) ;
#40618=CARTESIAN_POINT ( 'NONE',  ( -140.3950000000000102, -6.826472737025115478, -4.959722759717899443 ) ) ;
#40620=CARTESIAN_POINT ( 'NONE',  ( -123.4449999999999932, 0.000000000000000000, 8.024999999999991473 ) ) ;
#40629=CARTESIAN_POINT ( 'NONE',  ( -175.4929263765337737, -8.102448949553172852, 5.886773742842742685 ) ) ;
#40638=CARTESIAN_POINT ( 'NONE',  ( -89.69292637653380496, 10.01517768586948698, -1.839758294383808571E-15 ) ) ;
#40650=CARTESIAN_POINT ( 'NONE',  ( -136.1929263765337907, -10.01517768586948698, 6.132527647946031529E-16 ) ) ;
#40652=ORIENTED_EDGE ( 'NONE', *, *, #26584, .T. ) ;
#40653=CARTESIAN_POINT ( 'NONE',  ( -63.74292637653379501, -5.598654528085803328, -7.705886871421366635 ) ) ;
#40662=ORIENTED_EDGE ( 'NONE', *, *, #67824, .F. ) ;
#40668=CARTESIAN_POINT ( 'NONE',  ( -84.74499999999999034, 4.716976649647094177, 6.492361379858945902 ) ) ;
#40678=EDGE_LOOP ( 'NONE', ( #64281, #40564, #37516, #34516 ) ) ;
#40683=FACE_BOUND ( 'NONE', #14877, .T. ) ;
#40686=CARTESIAN_POINT ( 'NONE',  ( -169.1070736234662206, 8.102448949553171076, -5.886773742842744461 ) ) ;
#40691=CARTESIAN_POINT ( 'NONE',  ( -118.2570736234661695, 5.598654528085800663, -7.705886871421367523 ) ) ;
#40698=CARTESIAN_POINT ( 'NONE',  ( -82.04292637653379927, -9.058813317711329915, -2.943386871421370898 ) ) ;
#40700=CARTESIAN_POINT ( 'NONE',  ( -61.04292637653379927, -9.058813317711329915, -2.943386871421370898 ) ) ;
#40703=CARTESIAN_POINT ( 'NONE',  ( -154.4050000000000011, -2.607480562269069768, 8.024999999999991473 ) ) ;
#40705=CARTESIAN_POINT ( 'NONE',  ( -148.7929263765342398, -3.094860106610967776, 9.525000000005412915 ) ) ;
#40706=CARTESIAN_POINT ( 'NONE',  ( -163.0449999999999875, 7.632228543268600340, 2.479861379858949277 ) ) ;
#40708=CARTESIAN_POINT ( 'NONE',  ( -151.6450000000000102, 4.716976649647091513, -6.492361379858946790 ) ) ;
#40715=CARTESIAN_POINT ( 'NONE',  ( -67.40499999999997272, -2.607480562269069768, 8.024999999999991473 ) ) ;
#40718=CARTESIAN_POINT ( 'NONE',  ( -168.1429263765338078, 5.598654528085800663, -7.705886871421367523 ) ) ;
#40719=CARTESIAN_POINT ( 'NONE',  ( -63.74499999999998323, 4.716976649647094177, 6.492361379858945902 ) ) ;
#40721=CARTESIAN_POINT ( 'NONE',  ( -143.7570736234661695, -5.598654528085801552, 7.705886871421367523 ) ) ;
#40724=CARTESIAN_POINT ( 'NONE',  ( -159.9570736234661865, 9.058813317711329915, -2.943386871421373119 ) ) ;
#40733=ORIENTED_EDGE ( 'NONE', *, *, #10027, .F. ) ;
#40745=CARTESIAN_POINT ( 'NONE',  ( -144.8929263765338078, -8.102448949553174629, -5.886773742842741797 ) ) ;
#40750=CARTESIAN_POINT ( 'NONE',  ( -109.7950000000000017, 2.607480562269068880, -8.024999999999993250 ) ) ;
#40752=CARTESIAN_POINT ( 'NONE',  ( -163.5570736234661524, -1.166476076187852838E-15, -9.524999999999991473 ) ) ;
#40753=CARTESIAN_POINT ( 'NONE',  ( -178.7070736234662718, -3.094860106619322426, -9.524999999999344880 ) ) ;
#40757=( BOUNDED_CURVE ( )  B_SPLINE_CURVE ( 2, ( #49774, #7205, #27588, #60639, #23717, #39239, #28635, #1151, #6843, #2186, #793 ),
 .UNSPECIFIED., .F., .F. ) 
 B_SPLINE_CURVE_WITH_KNOTS ( ( 3, 2, 2, 2, 2, 3 ),
 ( 0.1413043478260836983, 0.1434782608695618911, 0.1456521739130400284, 0.1478260869565182212, 0.1499999999999963585, 0.1521739130434745513 ),
 .UNSPECIFIED. ) 
 CURVE ( )  GEOMETRIC_REPRESENTATION_ITEM ( )  RATIONAL_B_SPLINE_CURVE ( ( 1.000000000000073053, 0.9510565162950803675, 1.000000000000000000, 0.9510565162951535312, 1.000000000000000000, 0.9510565162951535312, 1.000000000000000000, 0.9510565162951535312, 1.000000000000000000, 0.9510565162952372420, 0.9999999999999162892 ) ) 
 REPRESENTATION_ITEM ( '' )  );
#40772=CARTESIAN_POINT ( 'NONE',  ( -123.9549999999999841, -7.632228543268599452, 2.479861379858951054 ) ) ;
#40777=CYLINDRICAL_SURFACE ( 'NONE', #64336, 9.524999999999991473 ) ;
#40784=CARTESIAN_POINT ( 'NONE',  ( -51.80499999999998550, -8.437984349512085203, 5.166775262442717831E-16 ) ) ;
#40786=CARTESIAN_POINT ( 'NONE',  ( -177.6550000000000011, -7.632228543268600340, -2.479861379858950166 ) ) ;
#40787=CARTESIAN_POINT ( 'NONE',  ( -90.44292637653379074, -1.166476076187852838E-15, -9.524999999999991473 ) ) ;
#40789=CARTESIAN_POINT ( 'NONE',  ( -57.80707362346616662, 10.01517768586948698, -1.839758294383808571E-15 ) ) ;
#40792=CARTESIAN_POINT ( 'NONE',  ( -178.4949999999999477, 6.826472737025113702, -4.959722759717902107 ) ) ;
#40795=AXIS2_PLACEMENT_3D ( 'NONE', #4999, #53877, #53547 ) ;
#40800=CARTESIAN_POINT ( 'NONE',  ( -92.90499999999997272, 2.607480562269068880, -8.024999999999993250 ) ) ;
#40805=CARTESIAN_POINT ( 'NONE',  ( -91.04499999999998749, 7.632228543268600340, 2.479861379858949277 ) ) ;
#40807=CARTESIAN_POINT ( 'NONE',  ( -70.04499999999998749, 7.632228543268600340, 2.479861379858949277 ) ) ;
#40810=CARTESIAN_POINT ( 'NONE',  ( -56.00707362346614815, -8.102448949553174629, -5.886773742842741797 ) ) ;
#40815=CARTESIAN_POINT ( 'NONE',  ( -115.4929263765338021, -8.102448949553172852, 5.886773742842742685 ) ) ;
#40816=CARTESIAN_POINT ( 'NONE',  ( -127.7949999999999875, 2.607480562269068880, -8.024999999999993250 ) ) ;
#40832=CARTESIAN_POINT ( 'NONE',  ( -133.4049999999999727, -2.607480562269069768, 8.024999999999991473 ) ) ;
#40833=VERTEX_POINT ( 'NONE', #8808 ) ;
#40834=CARTESIAN_POINT ( 'NONE',  ( -125.3070736234661808, -10.01517768586948698, 6.132527647946031529E-16 ) ) ;
#40847=CARTESIAN_POINT ( 'NONE',  ( -54.05707362346618083, 0.000000000000000000, 9.524999999999991473 ) ) ;
#40863=FACE_OUTER_BOUND ( 'NONE', #37393, .T. ) ;
#40866=CARTESIAN_POINT ( 'NONE',  ( -154.2549999999999955, -4.716976649647092401, 6.492361379858946790 ) ) ;
#40882=CARTESIAN_POINT ( 'NONE',  ( -78.95499999999998408, -7.632228543268599452, 2.479861379858951054 ) ) ;
#40885=CARTESIAN_POINT ( 'NONE',  ( -123.7429263765338021, -5.598654528085803328, -7.705886871421366635 ) ) ;
#40892=CARTESIAN_POINT ( 'NONE',  ( -93.44499999999999318, 0.000000000000000000, 8.024999999999991473 ) ) ;
#40900=CARTESIAN_POINT ( 'NONE',  ( -148.0429263765338135, -9.058813317711329915, -2.943386871421370898 ) ) ;
#40904=CARTESIAN_POINT ( 'NONE',  ( -157.1950000000000216, 8.437984349512085203, -1.550032578732815448E-15 ) ) ;
#40916=CARTESIAN_POINT ( 'NONE',  ( -172.5570736234661808, -1.166476076187852838E-15, -9.524999999999991473 ) ) ;
#40917=CARTESIAN_POINT ( 'NONE',  ( -181.5570736234661808, -1.166476076187852838E-15, -9.524999999999991473 ) ) ;
#40919=CARTESIAN_POINT ( 'NONE',  ( -156.2049999999999841, -2.607480562269071545, -8.024999999999991473 ) ) ;
#40933=CARTESIAN_POINT ( 'NONE',  ( -73.55499999999997840, 0.000000000000000000, 8.024999999999991473 ) ) ;
#40946=CARTESIAN_POINT ( 'NONE',  ( -55.04499999999998039, 7.632228543268600340, 2.479861379858949277 ) ) ;
#40955=ORIENTED_EDGE ( 'NONE', *, *, #63932, .T. ) ;
#40961=CARTESIAN_POINT ( 'NONE',  ( -100.7049999999999841, 2.607480562269073321, 8.024999999999991473 ) ) ;
#40965=CARTESIAN_POINT ( 'NONE',  ( -144.9570736234661865, 9.058813317711329915, -2.943386871421373119 ) ) ;
#40969=CARTESIAN_POINT ( 'NONE',  ( -77.90707362346617515, -3.094860106618429807, 9.524999999999991473 ) ) ;
#40974=CARTESIAN_POINT ( 'NONE',  ( -100.1929263765337907, -10.01517768586948698, 6.132527647946031529E-16 ) ) ;
#40976=CARTESIAN_POINT ( 'NONE',  ( -118.1049999999999898, -6.826472737025115478, 4.959722759717900331 ) ) ;
#40980=CARTESIAN_POINT ( 'NONE',  ( -128.6950000000000216, -8.437984349512085203, 5.166775262442717831E-16 ) ) ;
#40983=CARTESIAN_POINT ( 'NONE',  ( -120.4449999999999932, 0.000000000000000000, 8.024999999999991473 ) ) ;
#40989=CARTESIAN_POINT ( 'NONE',  ( -173.2429263765338305, 5.598654528085804216, 7.705886871421366635 ) ) ;
#40990=CARTESIAN_POINT ( 'NONE',  ( -47.99499999999998323, -6.826472737025115478, 4.959722759717900331 ) ) ;
#40995=ORIENTED_EDGE ( 'NONE', *, *, #34394, .T. ) ;
#40996=CARTESIAN_POINT ( 'NONE',  ( -83.24292637653380211, 5.598654528085804216, 7.705886871421366635 ) ) ;
#41003=CARTESIAN_POINT ( 'NONE',  ( -136.3429263765337964, -9.058813317711329915, 2.943386871421371787 ) ) ;
#41011=VECTOR ( 'NONE', #16500, 1000.000000000000000 ) ;
#41014=CARTESIAN_POINT ( 'NONE',  ( -106.4049999999999727, -2.607480562269069768, 8.024999999999991473 ) ) ;
#41025=CARTESIAN_POINT ( 'NONE',  ( -70.85707362346617799, -5.598654528085803328, -7.705886871421366635 ) ) ;
#41026=CARTESIAN_POINT ( 'NONE',  ( -78.74499999999997613, 4.716976649647094177, 6.492361379858945902 ) ) ;
#41034=EDGE_CURVE ( 'NONE', #38125, #7596, #52779, .T. ) ;
#41036=DIRECTION ( 'NONE',  ( -1.000000000000000000, -0.000000000000000000, -0.000000000000000000 ) ) ;
#41041=CARTESIAN_POINT ( 'NONE',  ( -149.9929263765338021, 8.102448949553172852, -5.886773742842744461 ) ) ;
#41042=CARTESIAN_POINT ( 'NONE',  ( -174.0570736234661808, 0.000000000000000000, 9.524999999999991473 ) ) ;
#41046=CARTESIAN_POINT ( 'NONE',  ( -105.8070736234661808, 10.01517768586948698, -1.839758294383808571E-15 ) ) ;
#41052=CARTESIAN_POINT ( 'NONE',  ( -152.0050000000000239, 6.826472737025116366, 4.959722759717898555 ) ) ;
#41055=CARTESIAN_POINT ( 'NONE',  ( -155.2450000000000045, -4.716976649647093289, -6.492361379858945902 ) ) ;
#41056=CARTESIAN_POINT ( 'NONE',  ( -149.2449999999999761, -4.716976649647093289, -6.492361379858945902 ) ) ;
#41063=CARTESIAN_POINT ( 'NONE',  ( -67.55499999999999261, 0.000000000000000000, 8.024999999999991473 ) ) ;
#41067=CARTESIAN_POINT ( 'NONE',  ( -64.19499999999999318, 8.437984349512086979, -1.550032578732815448E-15 ) ) ;
#41072=CARTESIAN_POINT ( 'NONE',  ( -155.6070736234661922, -8.102448949553174629, 5.886773742842742685 ) ) ;
#41087=EDGE_CURVE ( 'NONE', #3199, #57410, #58731, .T. ) ;
#41106=CARTESIAN_POINT ( 'NONE',  ( -106.4950000000000045, 6.826472737025113702, -4.959722759717902107 ) ) ;
#41109=CARTESIAN_POINT ( 'NONE',  ( -53.24292637653380211, 5.598654528085804216, 7.705886871421366635 ) ) ;
#41125=DIRECTION ( 'NONE',  ( -1.000000000000000000, -0.000000000000000000, -0.000000000000000000 ) ) ;
#41126=CARTESIAN_POINT ( 'NONE',  ( -121.1050000000000040, -6.826472737025115478, 4.959722759717900331 ) ) ;
#41129=LINE ( 'NONE', #62536, #54241 ) ;
#41139=CARTESIAN_POINT ( 'NONE',  ( -176.0049999999999670, 6.826472737025116366, 4.959722759717898555 ) ) ;
#41140=CARTESIAN_POINT ( 'NONE',  ( -91.34292637653381064, -9.058813317711329915, 2.943386871421371787 ) ) ;
#41143=CARTESIAN_POINT ( 'NONE',  ( -58.40707362346616094, 3.094860106618428031, -9.524999999999993250 ) ) ;
#41145=CARTESIAN_POINT ( 'NONE',  ( -179.8449999999999989, -7.632228543268599452, 2.479861379858951054 ) ) ;
#41151=CARTESIAN_POINT ( 'NONE',  ( -195.0000000000000000, 0.000000000000000000, 9.524999999999991473 ) ) ;
#41152=CARTESIAN_POINT ( 'NONE',  ( -96.95499999999998408, -7.632228543268599452, 2.479861379858951054 ) ) ;
#41156=CARTESIAN_POINT ( 'NONE',  ( -95.09499999999998465, -2.607480562269071545, -8.024999999999991473 ) ) ;
#41158=CARTESIAN_POINT ( 'NONE',  ( -64.79500000000000171, 2.607480562269068880, -8.024999999999993250 ) ) ;
#41160=CARTESIAN_POINT ( 'NONE',  ( -55.55707362346618083, -1.166476076187852838E-15, -9.524999999999991473 ) ) ;
#41166=CARTESIAN_POINT ( 'NONE',  ( -116.5429263765338135, 9.058813317711329915, 2.943386871421369566 ) ) ;
#41168=CARTESIAN_POINT ( 'NONE',  ( -128.9950000000000045, -6.826472737025115478, 4.959722759717900331 ) ) ;
#41170=AXIS2_PLACEMENT_3D ( 'NONE', #15763, #47095, #41823 ) ;
#41185=CARTESIAN_POINT ( 'NONE',  ( -131.3050000000000068, 8.437984349512086979, -1.550032578732815448E-15 ) ) ;
#41187=DIRECTION ( 'NONE',  ( 0.000000000000000000, 0.000000000000000000, -1.000000000000000000 ) ) ;
#41189=CARTESIAN_POINT ( 'NONE',  ( -118.5570736234661808, -1.166476076187852838E-15, -9.524999999999991473 ) ) ;
#41191=CARTESIAN_POINT ( 'NONE',  ( -172.4929263765338305, -8.102448949553174629, 5.886773742842742685 ) ) ;
#41193=ORIENTED_EDGE ( 'NONE', *, *, #3621, .T. ) ;
#41195=CARTESIAN_POINT ( 'NONE',  ( -195.0000000000000000, 0.000000000000000000, 9.524999999999991473 ) ) ;
#41200=CARTESIAN_POINT ( 'NONE',  ( -48.20499999999999829, -2.607480562269071545, -8.024999999999991473 ) ) ;
#41213=CARTESIAN_POINT ( 'NONE',  ( -57.74292637653380211, -5.598654528085803328, -7.705886871421366635 ) ) ;
#41215=CARTESIAN_POINT ( 'NONE',  ( -149.3049999999999500, 8.437984349512085203, -1.550032578732815448E-15 ) ) ;
#41226=CARTESIAN_POINT ( 'NONE',  ( -62.75499999999998835, 4.716976649647091513, -6.492361379858946790 ) ) ;
#41229=CARTESIAN_POINT ( 'NONE',  ( -90.35707362346617799, 5.598654528085804216, 7.705886871421366635 ) ) ;
#41230=CARTESIAN_POINT ( 'NONE',  ( -162.0570736234661808, 0.000000000000000000, 9.524999999999991473 ) ) ;
#41236=ADVANCED_FACE ( 'NONE', ( #34412 ), #44333, .T. ) ;
#41241=CARTESIAN_POINT ( 'NONE',  ( -96.44499999999999318, 0.000000000000000000, 8.024999999999991473 ) ) ;
#41248=CARTESIAN_POINT ( 'NONE',  ( -142.4929263765338590, -8.102448949553172852, 5.886773742842742685 ) ) ;
#41250=CARTESIAN_POINT ( 'NONE',  ( -160.7949999999999591, 2.607480562269068880, -8.024999999999993250 ) ) ;
#41267=CARTESIAN_POINT ( 'NONE',  ( -158.0049999999999670, 6.826472737025115478, 4.959722759717899443 ) ) ;
#41269=VERTEX_POINT ( 'NONE', #8391 ) ;
#41272=ORIENTED_EDGE ( 'NONE', *, *, #20766, .F. ) ;
#41279=CARTESIAN_POINT ( 'NONE',  ( -76.25499999999999545, -4.716976649647092401, 6.492361379858946790 ) ) ;
#41291=CARTESIAN_POINT ( 'NONE',  ( -181.4050000000000011, -2.607480562269069768, 8.024999999999991473 ) ) ;
#41292=ORIENTED_EDGE ( 'NONE', *, *, #65617, .T. ) ;
#41298=DIRECTION ( 'NONE',  ( -1.000000000000000000, -0.000000000000000000, -0.000000000000000000 ) ) ;
#41299=VERTEX_POINT ( 'NONE', #6866 ) ;
#41300=CARTESIAN_POINT ( 'NONE',  ( -100.5549999999999926, 0.000000000000000000, 8.024999999999991473 ) ) ;
#41303=CARTESIAN_POINT ( 'NONE',  ( -141.8070736234661808, 10.01517768586948698, -1.839758294383808571E-15 ) ) ;
#41306=CARTESIAN_POINT ( 'NONE',  ( -78.80707362346618083, 10.01517768586948698, -1.839758294383808571E-15 ) ) ;
#41311=CARTESIAN_POINT ( 'NONE',  ( -15.33043442081600638, -10.90871211463571022, 5.000000000000000000 ) ) ;
#41315=CARTESIAN_POINT ( 'NONE',  ( -123.0549999999999926, -9.827790563157499189E-16, -8.024999999999991473 ) ) ;
#41319=CARTESIAN_POINT ( 'NONE',  ( -124.3449999999999847, 7.632228543268599452, -2.479861379858951942 ) ) ;
#41326=CARTESIAN_POINT ( 'NONE',  ( -167.0070736234661695, -8.102448949553174629, -5.886773742842741797 ) ) ;
#41327=CARTESIAN_POINT ( 'NONE',  ( -169.4929263765338305, -8.102448949553172852, 5.886773742842742685 ) ) ;
#41338=CARTESIAN_POINT ( 'NONE',  ( -90.29292637653378506, 3.094860106618428031, -9.524999999999993250 ) ) ;
#41340=CARTESIAN_POINT ( 'NONE',  ( -166.9429263765337907, 0.000000000000000000, 9.524999999999991473 ) ) ;
#41341=CARTESIAN_POINT ( 'NONE',  ( -179.9929263765337737, 8.102448949553172852, -5.886773742842744461 ) ) ;
#41345=CARTESIAN_POINT ( 'NONE',  ( -156.0570736234661808, 0.000000000000000000, 9.524999999999991473 ) ) ;
#41347=CARTESIAN_POINT ( 'NONE',  ( -135.4429263765338192, -1.166476076187852838E-15, -9.524999999999991473 ) ) ;
#41350=CARTESIAN_POINT ( 'NONE',  ( -111.2929263765347088, 3.094860106603101180, -9.525000000011131007 ) ) ;
#41354=CARTESIAN_POINT ( 'NONE',  ( -101.3049999999999926, 8.437984349512086979, -1.550032578732815448E-15 ) ) ;
#41367=CARTESIAN_POINT ( 'NONE',  ( -68.84499999999998465, -7.632228543268599452, 2.479861379858951054 ) ) ;
#41368=ORIENTED_EDGE ( 'NONE', *, *, #35986, .F. ) ;
#41378=ORIENTED_EDGE ( 'NONE', *, *, #36046, .T. ) ;
#41384=CARTESIAN_POINT ( 'NONE',  ( -166.8570736234661922, -5.598654528085803328, -7.705886871421366635 ) ) ;
#41386=CARTESIAN_POINT ( 'NONE',  ( -101.0070736234661695, -8.102448949553172852, -5.886773742842741797 ) ) ;
#41388=DIRECTION ( 'NONE',  ( -1.000000000000000000, -0.000000000000000000, -0.000000000000000000 ) ) ;
#41390=CARTESIAN_POINT ( 'NONE',  ( -195.0000000000000000, 0.000000000000000000, 0.000000000000000000 ) ) ;
#41391=CARTESIAN_POINT ( 'NONE',  ( -105.5070736234661553, 8.102448949553176405, 5.886773742842740909 ) ) ;
#41395=CARTESIAN_POINT ( 'NONE',  ( -146.9049999999999727, 2.607480562269068880, -8.024999999999993250 ) ) ;
#41400=CARTESIAN_POINT ( 'NONE',  ( -150.4449999999999932, 0.000000000000000000, 8.024999999999991473 ) ) ;
#41402=CARTESIAN_POINT ( 'NONE',  ( -151.0449999999999875, 7.632228543268600340, 2.479861379858949277 ) ) ;
#41403=( BOUNDED_CURVE ( )  B_SPLINE_CURVE ( 2, ( #46353, #45660, #19572, #54608, #5714, #48695, #398, #57560, #58865, #32127, #9389 ),
 .UNSPECIFIED., .F., .F. ) 
 B_SPLINE_CURVE_WITH_KNOTS ( ( 3, 2, 2, 2, 2, 3 ),
 ( 0.2065217391304298988, 0.2086956521739080916, 0.2108695652173863400, 0.2130434782608645328, 0.2152173913043427811, 0.2173913043478209739 ),
 .UNSPECIFIED. ) 
 CURVE ( )  GEOMETRIC_REPRESENTATION_ITEM ( )  RATIONAL_B_SPLINE_CURVE ( ( 1.000000000000109912, 0.9510565162950435081, 1.000000000000000000, 0.9510565162951535312, 1.000000000000000000, 0.9510565162951535312, 1.000000000000000000, 0.9510565162951535312, 1.000000000000000000, 0.9510565162952685503, 0.9999999999998849809 ) ) 
 REPRESENTATION_ITEM ( '' )  );
#41407=EDGE_CURVE ( 'NONE', #64348, #21270, #15025, .T. ) ;
#41408=CARTESIAN_POINT ( 'NONE',  ( -61.25499999999998835, -4.716976649647092401, 6.492361379858946790 ) ) ;
#41414=CARTESIAN_POINT ( 'NONE',  ( -60.29499999999998749, -2.607480562269069768, 8.024999999999991473 ) ) ;
#41427=ORIENTED_EDGE ( 'NONE', *, *, #51973, .F. ) ;
#41431=DIRECTION ( 'NONE',  ( 0.000000000000000000, 0.000000000000000000, 1.000000000000000000 ) ) ;
#41443=CARTESIAN_POINT ( 'NONE',  ( -105.8949999999999676, 6.826472737025116366, 4.959722759717898555 ) ) ;
#41461=CARTESIAN_POINT ( 'NONE',  ( -125.1549999999999869, 7.632228543268600340, 2.479861379858949277 ) ) ;
#41472=CARTESIAN_POINT ( 'NONE',  ( -174.8050000000000068, -8.437984349512085203, 5.166775262442717831E-16 ) ) ;
#41473=EDGE_CURVE ( 'NONE', #68888, #12986, #19534, .T. ) ;
#41474=CARTESIAN_POINT ( 'NONE',  ( -50.00707362346616947, -8.102448949553172852, -5.886773742842741797 ) ) ;
#41475=CARTESIAN_POINT ( 'NONE',  ( -175.9449999999999932, -9.827790563157499189E-16, -8.024999999999991473 ) ) ;
#41481=CARTESIAN_POINT ( 'NONE',  ( -10.66861100029810316, 11.73594037587654171, 2.518823584575576646 ) ) ;
#41482=CARTESIAN_POINT ( 'NONE',  ( -95.00499999999998124, 6.826472737025116366, 4.959722759717898555 ) ) ;
#41487=CARTESIAN_POINT ( 'NONE',  ( -94.49499999999997613, 6.826472737025113702, -4.959722759717902107 ) ) ;
#41489=CARTESIAN_POINT ( 'NONE',  ( -67.79499999999998749, 2.607480562269068880, -8.024999999999993250 ) ) ;
#41494=CARTESIAN_POINT ( 'NONE',  ( -57.05707362346618083, 0.000000000000000000, 9.524999999999991473 ) ) ;
#41495=EDGE_CURVE ( 'NONE', #40311, #34254, #64180, .T. ) ;
#41499=( BOUNDED_CURVE ( )  B_SPLINE_CURVE ( 2, ( #53667, #20978, #5454, #47409, #48444, #135, #53348, #42473, #9752, #58604, #5815 ),
 .UNSPECIFIED., .F., .F. ) 
 B_SPLINE_CURVE_WITH_KNOTS ( ( 3, 2, 2, 2, 2, 3 ),
 ( 0.6739130434782450996, 0.6760869565217264565, 0.6782608695652079245, 0.6804347826086892814, 0.6826086956521707494, 0.6847826086956522174 ),
 .UNSPECIFIED. ) 
 CURVE ( )  GEOMETRIC_REPRESENTATION_ITEM ( )  RATIONAL_B_SPLINE_CURVE ( ( 1.000000000000354827, 0.9510565162947985929, 1.000000000000000000, 0.9510565162951535312, 1.000000000000000000, 0.9510565162951535312, 1.000000000000000000, 0.9510565162951535312, 1.000000000000000000, 0.9510565162951535312, 1.000000000000000000 ) ) 
 REPRESENTATION_ITEM ( '' )  );
#41503=CARTESIAN_POINT ( 'NONE',  ( -105.4429263765338050, -1.166476076187852838E-15, -9.524999999999991473 ) ) ;
#41504=CARTESIAN_POINT ( 'NONE',  ( -131.8449999999999989, -7.632228543268599452, 2.479861379858951054 ) ) ;
#41513=CARTESIAN_POINT ( 'NONE',  ( -135.4429263765338192, -1.166476076187852838E-15, -9.524999999999991473 ) ) ;
#41518=CARTESIAN_POINT ( 'NONE',  ( -118.5549999999999926, 0.000000000000000000, 8.024999999999991473 ) ) ;
#41520=CARTESIAN_POINT ( 'NONE',  ( -123.5070736234661837, 8.102448949553176405, 5.886773742842740909 ) ) ;
#41533=EDGE_LOOP ( 'NONE', ( #39412, #28166, #34339, #36949 ) ) ;
#41541=CARTESIAN_POINT ( 'NONE',  ( -93.44292637653380496, -1.166476076187852838E-15, -9.524999999999991473 ) ) ;
#41543=CARTESIAN_POINT ( 'NONE',  ( -62.24292637653379501, 5.598654528085804216, 7.705886871421366635 ) ) ;
#41547=CARTESIAN_POINT ( 'NONE',  ( -154.5550000000000068, 0.000000000000000000, 8.024999999999991473 ) ) ;
#41561=DIRECTION ( 'NONE',  ( -1.000000000000000000, -0.000000000000000000, -0.000000000000000000 ) ) ;
#41563=CARTESIAN_POINT ( 'NONE',  ( -61.70499999999997698, 2.607480562269073321, 8.024999999999991473 ) ) ;
#41577=CARTESIAN_POINT ( 'NONE',  ( -99.14499999999998181, -4.716976649647092401, 6.492361379858946790 ) ) ;
#41586=CARTESIAN_POINT ( 'NONE',  ( -137.0929263765338249, 3.094860106618433360, 9.524999999999991473 ) ) ;
#41588=CARTESIAN_POINT ( 'NONE',  ( -159.1449999999999818, -4.716976649647092401, 6.492361379858946790 ) ) ;
#41595=VERTEX_POINT ( 'NONE', #26197 ) ;
#41602=DIRECTION ( 'NONE',  ( -1.000000000000000000, -0.000000000000000000, -0.000000000000000000 ) ) ;
#41606=CARTESIAN_POINT ( 'NONE',  ( -154.1049999999999898, -6.826472737025113702, 4.959722759717902107 ) ) ;
#41621=CARTESIAN_POINT ( 'NONE',  ( -75.95499999999998408, -7.632228543268599452, 2.479861379858951054 ) ) ;
#41627=CARTESIAN_POINT ( 'NONE',  ( -195.0000000000000000, 0.000000000000000000, 0.000000000000000000 ) ) ;
#41636=CARTESIAN_POINT ( 'NONE',  ( -184.2549999999999955, -4.716976649647092401, 6.492361379858946790 ) ) ;
#41647=CARTESIAN_POINT ( 'NONE',  ( -90.80499999999996419, -8.437984349512085203, 5.166775262442717831E-16 ) ) ;
#41654=CARTESIAN_POINT ( 'NONE',  ( -131.6070736234661922, -8.102448949553172852, 5.886773742842742685 ) ) ;
#41658=CARTESIAN_POINT ( 'NONE',  ( -71.30707362346616662, -10.01517768586948698, 6.132527647946031529E-16 ) ) ;
#41666=CARTESIAN_POINT ( 'NONE',  ( -115.8549999999999898, 4.716976649647094177, 6.492361379858945902 ) ) ;
#41669=CARTESIAN_POINT ( 'NONE',  ( -125.8449999999999847, -7.632228543268599452, 2.479861379858951054 ) ) ;
#41679=CARTESIAN_POINT ( 'NONE',  ( -167.6070736234661638, -8.102448949553174629, 5.886773742842742685 ) ) ;
#41681=CARTESIAN_POINT ( 'NONE',  ( -175.7929263765337851, -3.094860106618429807, 9.524999999999991473 ) ) ;
#41688=CARTESIAN_POINT ( 'NONE',  ( -90.14292637653380780, 5.598654528085800663, -7.705886871421367523 ) ) ;
#41699=CARTESIAN_POINT ( 'NONE',  ( -103.1929263765338050, -10.01517768586948698, 6.132527647946031529E-16 ) ) ;
#41703=CIRCLE ( 'NONE', #15836, 11.99999999999999467 ) ;
#41706=CARTESIAN_POINT ( 'NONE',  ( -99.65499999999998693, -7.632228543268600340, -2.479861379858950166 ) ) ;
#41715=CARTESIAN_POINT ( 'NONE',  ( -67.49499999999999034, 6.826472737025113702, -4.959722759717902107 ) ) ;
#41729=CARTESIAN_POINT ( 'NONE',  ( -195.0000000000000000, 0.000000000000000000, 9.524999999999991473 ) ) ;
#41735=CARTESIAN_POINT ( 'NONE',  ( -149.6929263765338192, 10.01517768586948698, -1.839758294383808966E-15 ) ) ;
#41737=CARTESIAN_POINT ( 'NONE',  ( -173.3070736234661808, -10.01517768586948698, 6.132527647946031529E-16 ) ) ;
#41740=CARTESIAN_POINT ( 'NONE',  ( -106.2570736234661695, 5.598654528085800663, -7.705886871421367523 ) ) ;
#41749=CYLINDRICAL_SURFACE ( 'NONE', #68304, 9.524999999999991473 ) ;
#41750=CARTESIAN_POINT ( 'NONE',  ( -115.4070736234669994, 3.094860106604512495, -9.525000000010106049 ) ) ;
#41753=CARTESIAN_POINT ( 'NONE',  ( -151.4049999999999443, -2.607480562269069768, 8.024999999999991473 ) ) ;
#41756=CARTESIAN_POINT ( 'NONE',  ( -154.3449999999999704, 7.632228543268599452, -2.479861379858951942 ) ) ;
#41757=CARTESIAN_POINT ( 'NONE',  ( -144.7449999999999761, 4.716976649647094177, 6.492361379858945902 ) ) ;
#41764=CARTESIAN_POINT ( 'NONE',  ( -68.45499999999998408, 7.632228543268599452, -2.479861379858951942 ) ) ;
#41766=CARTESIAN_POINT ( 'NONE',  ( -62.09499999999998465, -2.607480562269071545, -8.024999999999991473 ) ) ;
#41775=CARTESIAN_POINT ( 'NONE',  ( -152.3929263765338078, 8.102448949553176405, 5.886773742842740909 ) ) ;
#41796=CYLINDRICAL_SURFACE ( 'NONE', #33117, 9.524999999999991473 ) ;
#41800=CARTESIAN_POINT ( 'NONE',  ( -84.89292637653377938, -8.102448949553174629, -5.886773742842741797 ) ) ;
#41805=CARTESIAN_POINT ( 'NONE',  ( -96.44499999999999318, 0.000000000000000000, 8.024999999999991473 ) ) ;
#41816=EDGE_CURVE ( 'NONE', #13211, #24116, #21268, .T. ) ;
#41823=DIRECTION ( 'NONE',  ( 0.000000000000000000, 0.000000000000000000, 1.000000000000000000 ) ) ;
#41824=CARTESIAN_POINT ( 'NONE',  ( -119.6049999999999756, 6.826472737025113702, -4.959722759717902107 ) ) ;
#41839=CARTESIAN_POINT ( 'NONE',  ( -180.3549999999999898, -4.716976649647093289, -6.492361379858945902 ) ) ;
#41842=CARTESIAN_POINT ( 'NONE',  ( -182.0949999999999989, -2.607480562269071545, -8.024999999999991473 ) ) ;
#41844=CARTESIAN_POINT ( 'NONE',  ( -174.5949999999999989, 2.607480562269072433, 8.024999999999991473 ) ) ;
#41848=CARTESIAN_POINT ( 'NONE',  ( -10.03355964668487843, 11.98590840856550344, -0.6655800929182279502 ) ) ;
#41849=CARTESIAN_POINT ( 'NONE',  ( -89.60499999999997556, 6.826472737025113702, -4.959722759717902107 ) ) ;
#41851=CARTESIAN_POINT ( 'NONE',  ( -91.94499999999997897, -9.827790563157499189E-16, -8.024999999999991473 ) ) ;
#41853=CARTESIAN_POINT ( 'NONE',  ( -72.74499999999999034, 4.716976649647094177, 6.492361379858945902 ) ) ;
#41856=CARTESIAN_POINT ( 'NONE',  ( -56.30707362346618794, -10.01517768586948698, 6.132527647946031529E-16 ) ) ;
#41862=CARTESIAN_POINT ( 'NONE',  ( -105.7429263765338021, -5.598654528085803328, -7.705886871421366635 ) ) ;
#41863=CARTESIAN_POINT ( 'NONE',  ( -130.3449999999999989, 7.632228543268599452, -2.479861379858951942 ) ) ;
#41880=CARTESIAN_POINT ( 'NONE',  ( -121.2549999999999812, -4.716976649647092401, 6.492361379858946790 ) ) ;
#41882=CARTESIAN_POINT ( 'NONE',  ( -137.6070736234661922, -8.102448949553174629, 5.886773742842742685 ) ) ;
#41883=CARTESIAN_POINT ( 'NONE',  ( -126.2070736234661723, 3.094860106618433360, 9.524999999999991473 ) ) ;
#41898=EDGE_LOOP ( 'NONE', ( #55214, #3108, #16003, #40088 ) ) ;
#41904=CARTESIAN_POINT ( 'NONE',  ( -98.54292637653381348, 9.058813317711329915, 2.943386871421369566 ) ) ;
#41911=CARTESIAN_POINT ( 'NONE',  ( -56.09292637653378222, 3.094860106618433360, 9.524999999999991473 ) ) ;
#41914=CARTESIAN_POINT ( 'NONE',  ( -152.4550000000000125, 7.632228543268599452, -2.479861379858951942 ) ) ;
#41925=ORIENTED_EDGE ( 'NONE', *, *, #54574, .T. ) ;
#41930=CARTESIAN_POINT ( 'NONE',  ( -66.80499999999999261, -8.437984349512085203, 5.166775262442717831E-16 ) ) ;
#41936=FACE_OUTER_BOUND ( 'NONE', #27891, .T. ) ;
#41939=( BOUNDED_CURVE ( )  B_SPLINE_CURVE ( 2, ( #16365, #59571, #54296, #23003, #5747, #17049, #44496, #435, #17399, #17730, #6118 ),
 .UNSPECIFIED., .F., .F. ) 
 B_SPLINE_CURVE_WITH_KNOTS ( ( 3, 2, 2, 2, 2, 3 ),
 ( 0.6521739130434630605, 0.6543478260869413088, 0.6565217391304194461, 0.6586956521738976944, 0.6608695652173758317, 0.6630434782608540800 ),
 .UNSPECIFIED. ) 
 CURVE ( )  GEOMETRIC_REPRESENTATION_ITEM ( )  RATIONAL_B_SPLINE_CURVE ( ( 1.000000000000342393, 0.9510565162948111384, 1.000000000000000000, 0.9510565162951535312, 1.000000000000000000, 0.9510565162951535312, 1.000000000000000000, 0.9510565162951535312, 1.000000000000000000, 0.9510565162955009200, 0.9999999999996526112 ) ) 
 REPRESENTATION_ITEM ( '' )  );
#41947=CARTESIAN_POINT ( 'NONE',  ( -95.09499999999999886, -2.607480562269071545, -8.024999999999991473 ) ) ;
#41955=CARTESIAN_POINT ( 'NONE',  ( -135.5929263765337964, -3.094860106618431139, -9.524999999999991473 ) ) ;
#41957=CARTESIAN_POINT ( 'NONE',  ( -154.9449999999999932, -9.827790563157499189E-16, -8.024999999999991473 ) ) ;
#41970=CARTESIAN_POINT ( 'NONE',  ( -110.0070736234661979, -8.102448949553174629, -5.886773742842741797 ) ) ;
#41973=CARTESIAN_POINT ( 'NONE',  ( -146.3049999999999784, 8.437984349512086979, -1.550032578732815448E-15 ) ) ;
#41984=ADVANCED_FACE ( 'NONE', ( #709 ), #55973, .T. ) ;
#41990=CARTESIAN_POINT ( 'NONE',  ( -69.05499999999999261, -9.827790563157499189E-16, -8.024999999999991473 ) ) ;
#41991=CARTESIAN_POINT ( 'NONE',  ( -79.85707362346616378, -5.598654528085803328, -7.705886871421366635 ) ) ;
#41992=VERTEX_POINT ( 'NONE', #12355 ) ;
#41996=CARTESIAN_POINT ( 'NONE',  ( -183.0516217685573679, -0.3847981879420483420, 9.473378231442628916 ) ) ;
#41999=ADVANCED_FACE ( 'NONE', ( #39846 ), #1769, .T. ) ;
#42006=CARTESIAN_POINT ( 'NONE',  ( -177.3549999999999898, -4.716976649647093289, -6.492361379858945902 ) ) ;
#42018=CARTESIAN_POINT ( 'NONE',  ( -97.55499999999999261, 0.000000000000000000, 8.024999999999991473 ) ) ;
#42022=CARTESIAN_POINT ( 'NONE',  ( -134.7570736234661695, -5.598654528085801552, 7.705886871421367523 ) ) ;
#42026=CARTESIAN_POINT ( 'NONE',  ( -71.60707362346616378, -8.102448949553172852, 5.886773742842742685 ) ) ;
#42028=CARTESIAN_POINT ( 'NONE',  ( -93.14292637653380780, 5.598654528085800663, -7.705886871421367523 ) ) ;
#42032=CARTESIAN_POINT ( 'NONE',  ( -19.83596493880951428, -11.93243626797339907, 1.312027138233742285 ) ) ;
#42036=CARTESIAN_POINT ( 'NONE',  ( -107.0049999999999955, 6.826472737025116366, 4.959722759717898555 ) ) ;
#42038=CARTESIAN_POINT ( 'NONE',  ( -122.6949999999999790, -8.437984349512085203, 5.166775262442717831E-16 ) ) ;
#42045=CARTESIAN_POINT ( 'NONE',  ( -163.3429263765337964, -9.058813317711329915, 2.943386871421371787 ) ) ;
#42046=CARTESIAN_POINT ( 'NONE',  ( -182.5449999999999875, -7.632228543268600340, -2.479861379858950166 ) ) ;
#42054=CARTESIAN_POINT ( 'NONE',  ( -77.99292637653380211, 8.102448949553171076, -5.886773742842744461 ) ) ;
#42056=DIRECTION ( 'NONE',  ( 0.000000000000000000, 0.000000000000000000, 1.000000000000000000 ) ) ;
#42062=CARTESIAN_POINT ( 'NONE',  ( -183.9550000000000125, -7.632228543268599452, 2.479861379858951054 ) ) ;
#42068=CARTESIAN_POINT ( 'NONE',  ( -74.30707362346616662, -10.01517768586948698, 6.132527647946031529E-16 ) ) ;
#42070=CARTESIAN_POINT ( 'NONE',  ( -110.0929263765347343, 3.094860106634028885, 9.524999999988660093 ) ) ;
#42078=CARTESIAN_POINT ( 'NONE',  ( -92.45499999999998408, 7.632228543268599452, -2.479861379858951942 ) ) ;
#42092=CARTESIAN_POINT ( 'NONE',  ( -75.14499999999999602, -4.716976649647092401, 6.492361379858946790 ) ) ;
#42104=VERTEX_POINT ( 'NONE', #20325 ) ;
#42110=CARTESIAN_POINT ( 'NONE',  ( -163.7070736234661297, -3.094860106618431139, -9.524999999999991473 ) ) ;
#42112=CARTESIAN_POINT ( 'NONE',  ( -107.3070736234661666, -10.01517768586948698, 6.132527647946031529E-16 ) ) ;
#42120=CARTESIAN_POINT ( 'NONE',  ( -139.4050000000000296, -2.607480562269069768, 8.024999999999991473 ) ) ;
#42122=CARTESIAN_POINT ( 'NONE',  ( -156.5949999999999704, 2.607480562269073321, 8.024999999999991473 ) ) ;
#42124=CARTESIAN_POINT ( 'NONE',  ( -138.4449999999999932, 0.000000000000000000, 8.024999999999991473 ) ) ;
#42131=CARTESIAN_POINT ( 'NONE',  ( -49.85499999999998266, 4.716976649647094177, 6.492361379858945902 ) ) ;
#42135=CARTESIAN_POINT ( 'NONE',  ( -51.59292637653378932, -3.094860106618431139, -9.524999999999991473 ) ) ;
#42142=CARTESIAN_POINT ( 'NONE',  ( -82.10707362346614957, 8.102448949553172852, -5.886773742842744461 ) ) ;
#42174=CARTESIAN_POINT ( 'NONE',  ( -100.3449999999999847, 7.632228543268599452, -2.479861379858951942 ) ) ;
#42193=CIRCLE ( 'NONE', #65675, 7.499999999999984901 ) ;
#42207=CARTESIAN_POINT ( 'NONE',  ( -170.7549999999999955, 4.716976649647091513, -6.492361379858946790 ) ) ;
#42208=CARTESIAN_POINT ( 'NONE',  ( -91.19292637653379074, -10.01517768586948698, 6.132527647946031529E-16 ) ) ;
#42209=CARTESIAN_POINT ( 'NONE',  ( -147.0570736234661808, 0.000000000000000000, 9.524999999999991473 ) ) ;
#42210=CARTESIAN_POINT ( 'NONE',  ( -46.25707362346617657, 5.598654528085800663, -7.705886871421367523 ) ) ;
#42213=CARTESIAN_POINT ( 'NONE',  ( -170.5450000000000159, -7.632228543268600340, -2.479861379858950166 ) ) ;
#42217=CARTESIAN_POINT ( 'NONE',  ( -11.23577065669009478, 11.53784018821510848, 3.306942921224938825 ) ) ;
#42218=CARTESIAN_POINT ( 'NONE',  ( -92.00499999999998124, 6.826472737025116366, 4.959722759717898555 ) ) ;
#42220=CARTESIAN_POINT ( 'NONE',  ( -169.4070736234663173, 3.094860106615739515, -9.525000000001949019 ) ) ;
#42223=CARTESIAN_POINT ( 'NONE',  ( -92.24499999999999034, -4.716976649647093289, -6.492361379858945902 ) ) ;
#42230=CARTESIAN_POINT ( 'NONE',  ( -74.09292637653381064, 3.094860106618433360, 9.524999999999991473 ) ) ;
#42232=ORIENTED_EDGE ( 'NONE', *, *, #18449, .F. ) ;
#42244=CARTESIAN_POINT ( 'NONE',  ( -135.2929263765344388, 3.094860106608008810, -9.525000000007565859 ) ) ;
#42252=CARTESIAN_POINT ( 'NONE',  ( -119.4549999999999983, 7.632228543268599452, -2.479861379858951942 ) ) ;
#42259=AXIS2_PLACEMENT_3D ( 'NONE', #6194, #23081, #44576 ) ;
#42264=CARTESIAN_POINT ( 'NONE',  ( -55.10707362346616378, 8.102448949553172852, -5.886773742842744461 ) ) ;
#42279=ORIENTED_EDGE ( 'NONE', *, *, #43429, .T. ) ;
#42280=CARTESIAN_POINT ( 'NONE',  ( -55.19292637653379785, -10.01517768586948698, 6.132527647946031529E-16 ) ) ;
#42283=CARTESIAN_POINT ( 'NONE',  ( -151.4049999999999443, -2.607480562269069768, 8.024999999999991473 ) ) ;
#42286=CARTESIAN_POINT ( 'NONE',  ( -87.05707362346618083, 0.000000000000000000, 9.524999999999991473 ) ) ;
#42294=CARTESIAN_POINT ( 'NONE',  ( -69.95499999999998408, -7.632228543268599452, 2.479861379858951054 ) ) ;
#42307=CARTESIAN_POINT ( 'NONE',  ( -116.9949999999999761, -6.826472737025113702, 4.959722759717902107 ) ) ;
#42309=CARTESIAN_POINT ( 'NONE',  ( -88.04499999999998749, 7.632228543268600340, 2.479861379858949277 ) ) ;
#42310=EDGE_CURVE ( 'NONE', #40082, #62431, #57504, .T. ) ;
#42316=CARTESIAN_POINT ( 'NONE',  ( -129.2929263765338135, 3.094860106618428031, -9.524999999999993250 ) ) ;
#42318=CARTESIAN_POINT ( 'NONE',  ( -153.8949999999999818, 6.826472737025116366, 4.959722759717898555 ) ) ;
#42333=CARTESIAN_POINT ( 'NONE',  ( -154.2549999999999955, -4.716976649647092401, 6.492361379858946790 ) ) ;
#42336=LINE ( 'NONE', #9244, #18053 ) ;
#42343=CARTESIAN_POINT ( 'NONE',  ( -65.30499999999999261, 8.437984349512086979, -1.550032578732815448E-15 ) ) ;
#42358=CARTESIAN_POINT ( 'NONE',  ( -46.64499999999998892, 4.716976649647091513, -6.492361379858946790 ) ) ;
#42367=CARTESIAN_POINT ( 'NONE',  ( -128.0070736234661979, -8.102448949553174629, -5.886773742842741797 ) ) ;
#42369=CARTESIAN_POINT ( 'NONE',  ( -97.40499999999997272, -2.607480562269069768, 8.024999999999991473 ) ) ;
#42373=CARTESIAN_POINT ( 'NONE',  ( -135.8070736234661808, 10.01517768586948698, -1.839758294383808571E-15 ) ) ;
#42375=CARTESIAN_POINT ( 'NONE',  ( -68.15707362346616094, -9.058813317711329915, -2.943386871421370898 ) ) ;
#42382=CARTESIAN_POINT ( 'NONE',  ( -115.1049999999999756, -6.826472737025115478, 4.959722759717900331 ) ) ;
#42384=CARTESIAN_POINT ( 'NONE',  ( -122.2449999999999903, -4.716976649647093289, -6.492361379858945902 ) ) ;
#42385=EDGE_CURVE ( 'NONE', #8699, #63234, #49914, .T. ) ;
#42391=CARTESIAN_POINT ( 'NONE',  ( -167.3929263765338078, 8.102448949553176405, 5.886773742842740909 ) ) ;
#42402=CARTESIAN_POINT ( 'NONE',  ( -80.99292637653380211, 8.102448949553171076, -5.886773742842744461 ) ) ;
#42411=CARTESIAN_POINT ( 'NONE',  ( -179.0049999999999955, 6.826472737025115478, 4.959722759717899443 ) ) ;
#42415=CARTESIAN_POINT ( 'NONE',  ( -182.4570736234661865, -9.058813317711329915, 2.943386871421371787 ) ) ;
#42419=CARTESIAN_POINT ( 'NONE',  ( -89.15499999999998693, 7.632228543268600340, 2.479861379858949277 ) ) ;
#42428=CARTESIAN_POINT ( 'NONE',  ( -69.89499999999999602, 6.826472737025116366, 4.959722759717898555 ) ) ;
#42429=VERTEX_POINT ( 'NONE', #56490 ) ;
#42432=ORIENTED_EDGE ( 'NONE', *, *, #26438, .T. ) ;
#42444=CARTESIAN_POINT ( 'NONE',  ( -156.3570736234661922, 5.598654528085804216, 7.705886871421366635 ) ) ;
#42446=CARTESIAN_POINT ( 'NONE',  ( -105.9570736234661865, 9.058813317711329915, -2.943386871421373119 ) ) ;
#42453=CARTESIAN_POINT ( 'NONE',  ( -143.0050000000000239, 6.826472737025116366, 4.959722759717898555 ) ) ;
#42456=CARTESIAN_POINT ( 'NONE',  ( -157.7950000000000159, 2.607480562269068880, -8.024999999999993250 ) ) ;
#42458=CARTESIAN_POINT ( 'NONE',  ( -137.5449999999999875, -7.632228543268600340, -2.479861379858950166 ) ) ;
#42465=CARTESIAN_POINT ( 'NONE',  ( -56.60499999999998266, 6.826472737025113702, -4.959722759717902107 ) ) ;
#42473=CARTESIAN_POINT ( 'NONE',  ( -89.00707362346618368, -8.102448949553174629, -5.886773742842741797 ) ) ;
#42481=ORIENTED_EDGE ( 'NONE', *, *, #25803, .F. ) ;
#42494=CARTESIAN_POINT ( 'NONE',  ( -101.8429263765338106, 9.058813317711329915, -2.943386871421373119 ) ) ;
#42498=CARTESIAN_POINT ( 'NONE',  ( -105.1449999999999818, -4.716976649647092401, 6.492361379858946790 ) ) ;
#42499=VERTEX_POINT ( 'NONE', #35041 ) ;
#42514=CARTESIAN_POINT ( 'NONE',  ( -126.2929263765345524, 3.094860106606193817, -9.525000000008883916 ) ) ;
#42520=ORIENTED_EDGE ( 'NONE', *, *, #54329, .T. ) ;
#42528=CARTESIAN_POINT ( 'NONE',  ( -153.4429263765338192, -1.166476076187852838E-15, -9.524999999999991473 ) ) ;
#42529=CARTESIAN_POINT ( 'NONE',  ( -165.2050000000000125, -2.607480562269071545, -8.024999999999991473 ) ) ;
#42531=CARTESIAN_POINT ( 'NONE',  ( -195.0000000000000000, 0.000000000000000000, 9.524999999999991473 ) ) ;
#42533=CARTESIAN_POINT ( 'NONE',  ( -50.30707362346617373, -10.01517768586948698, 6.132527647946031529E-16 ) ) ;
#42535=CARTESIAN_POINT ( 'NONE',  ( -167.8449999999999989, -7.632228543268599452, 2.479861379858951054 ) ) ;
#42540=CARTESIAN_POINT ( 'NONE',  ( -10.03217797797695354, 11.98647912738839239, 0.6570571964558979960 ) ) ;
#42541=CARTESIAN_POINT ( 'NONE',  ( -79.70499999999995566, 2.607480562269073321, 8.024999999999991473 ) ) ;
#42545=CARTESIAN_POINT ( 'NONE',  ( -79.79499999999998749, 2.607480562269069324, -8.024999999999993250 ) ) ;
#42565=CARTESIAN_POINT ( 'NONE',  ( -174.5070736234661410, 8.102448949553176405, 5.886773742842740909 ) ) ;
#42572=CARTESIAN_POINT ( 'NONE',  ( -124.8549999999999898, 4.716976649647094177, 6.492361379858945902 ) ) ;
#42584=LINE ( 'NONE', #5932, #54629 ) ;
#42597=CARTESIAN_POINT ( 'NONE',  ( -61.04292637653379927, -9.058813317711329915, -2.943386871421370898 ) ) ;
#42600=CARTESIAN_POINT ( 'NONE',  ( -147.5049999999999955, -6.826472737025115478, -4.959722759717899443 ) ) ;
#42601=CARTESIAN_POINT ( 'NONE',  ( -177.0570736234661808, 0.000000000000000000, 9.524999999999991473 ) ) ;
#42612=EDGE_CURVE ( 'NONE', #2500, #32796, #28291, .T. ) ;
#42613=CARTESIAN_POINT ( 'NONE',  ( -64.25499999999998124, -4.716976649647092401, 6.492361379858946790 ) ) ;
#42617=EDGE_CURVE ( 'NONE', #43509, #18673, #51929, .T. ) ;
#42626=( BOUNDED_CURVE ( )  B_SPLINE_CURVE ( 2, ( #31946, #5894, #37278, #43594, #54431, #60061, #889, #32289, #43255, #11177, #48867 ),
 .UNSPECIFIED., .F., .F. ) 
 B_SPLINE_CURVE_WITH_KNOTS ( ( 3, 2, 2, 2, 2, 3 ),
 ( 0.3478260869565134583, 0.3499999999999916511, 0.3521739130434698994, 0.3543478260869481478, 0.3565217391304263406, 0.3586956521739045334 ),
 .UNSPECIFIED. ) 
 CURVE ( )  GEOMETRIC_REPRESENTATION_ITEM ( )  RATIONAL_B_SPLINE_CURVE ( ( 1.000000000000186295, 0.9510565162949673468, 1.000000000000000000, 0.9510565162951535312, 1.000000000000000000, 0.9510565162951535312, 1.000000000000000000, 0.9510565162951535312, 1.000000000000000000, 0.9510565162953447116, 0.9999999999998088196 ) ) 
 REPRESENTATION_ITEM ( '' )  );
#42631=CARTESIAN_POINT ( 'NONE',  ( -123.1449999999999960, -4.716976649647092401, 6.492361379858946790 ) ) ;
#42633=CARTESIAN_POINT ( 'NONE',  ( -83.69499999999997897, -8.437984349512085203, 5.166775262442717831E-16 ) ) ;
#42639=CARTESIAN_POINT ( 'NONE',  ( -133.9429263765338192, 0.000000000000000000, 9.524999999999991473 ) ) ;
#42641=CARTESIAN_POINT ( 'NONE',  ( -146.6949999999999932, -8.437984349512085203, 5.166775262442717831E-16 ) ) ;
#42658=CARTESIAN_POINT ( 'NONE',  ( -150.0550000000000068, -9.827790563157499189E-16, -8.024999999999991473 ) ) ;
#42675=CARTESIAN_POINT ( 'NONE',  ( -66.50499999999998124, -6.826472737025113702, -4.959722759717900331 ) ) ;
#42676=CARTESIAN_POINT ( 'NONE',  ( -117.4449999999999932, 0.000000000000000000, 8.024999999999991473 ) ) ;
#42683=CARTESIAN_POINT ( 'NONE',  ( -183.0769827045555473, 0.000000000000000000, 9.448017295444435248 ) ) ;
#42693=CARTESIAN_POINT ( 'NONE',  ( -47.24499999999998323, -4.716976649647093289, -6.492361379858945902 ) ) ;
#42702=ORIENTED_EDGE ( 'NONE', *, *, #52562, .T. ) ;
#42706=CARTESIAN_POINT ( 'NONE',  ( -99.80499999999997840, -8.437984349512085203, 5.166775262442717831E-16 ) ) ;
#42709=CARTESIAN_POINT ( 'NONE',  ( -135.9570736234661865, 9.058813317711329915, -2.943386871421373119 ) ) ;
#42714=CARTESIAN_POINT ( 'NONE',  ( -66.05707362346618083, 0.000000000000000000, 9.524999999999991473 ) ) ;
#42716=CARTESIAN_POINT ( 'NONE',  ( -80.69292637653380496, 10.01517768586948698, -1.839758294383808966E-15 ) ) ;
#42718=LINE ( 'NONE', #64116, #22631 ) ;
#42723=CARTESIAN_POINT ( 'NONE',  ( -113.4549999999999841, 7.632228543268599452, -2.479861379858951942 ) ) ;
#42725=CARTESIAN_POINT ( 'NONE',  ( -119.6950000000000074, -8.437984349512085203, 5.166775262442717831E-16 ) ) ;
#42730=CARTESIAN_POINT ( 'NONE',  ( -117.4429263765338050, -1.166476076187852838E-15, -9.524999999999991473 ) ) ;
#42733=CARTESIAN_POINT ( 'NONE',  ( -165.4429263765337907, -1.166476076187852838E-15, -9.524999999999991473 ) ) ;
#42734=CARTESIAN_POINT ( 'NONE',  ( -174.7449999999999761, 4.716976649647094177, 6.492361379858945902 ) ) ;
#42741=CARTESIAN_POINT ( 'NONE',  ( -76.34292637653379643, -9.058813317711329915, 2.943386871421371787 ) ) ;
#42748=CARTESIAN_POINT ( 'NONE',  ( -47.75499999999999545, 4.716976649647091513, -6.492361379858946790 ) ) ;
#42750=CARTESIAN_POINT ( 'NONE',  ( -177.3549999999999898, -4.716976649647093289, -6.492361379858945902 ) ) ;
#42759=( BOUNDED_CURVE ( )  B_SPLINE_CURVE ( 2, ( #36448, #57869, #69113, #5068, #16361, #25482, #37836, #9330, #20919, #31100, #4014 ),
 .UNSPECIFIED., .F., .F. ) 
 B_SPLINE_CURVE_WITH_KNOTS ( ( 3, 2, 2, 2, 2, 3 ),
 ( 0.5869565217391166101, 0.5891304347825948584, 0.5913043478260731067, 0.5934782608695512440, 0.5956521739130294923, 0.5978260869565077407 ),
 .UNSPECIFIED. ) 
 CURVE ( )  GEOMETRIC_REPRESENTATION_ITEM ( )  RATIONAL_B_SPLINE_CURVE ( ( 1.000000000000312417, 0.9510565162948411144, 1.000000000000000000, 0.9510565162951535312, 1.000000000000000000, 0.9510565162951535312, 1.000000000000000000, 0.9510565162951535312, 1.000000000000000000, 0.9510565162954685015, 0.9999999999996850297 ) ) 
 REPRESENTATION_ITEM ( '' )  );
#42763=CARTESIAN_POINT ( 'NONE',  ( -92.60499999999998977, 6.826472737025113702, -4.959722759717902107 ) ) ;
#42776=CARTESIAN_POINT ( 'NONE',  ( -69.44499999999999318, 0.000000000000000000, 8.024999999999991473 ) ) ;
#42783=DIRECTION ( 'NONE',  ( 1.000000000000000000, 0.000000000000000000, 0.000000000000000000 ) ) ;
#42797=CARTESIAN_POINT ( 'NONE',  ( -155.6070736234661922, -8.102448949553172852, 5.886773742842742685 ) ) ;
#42801=CARTESIAN_POINT ( 'NONE',  ( -98.45707362346617231, -9.058813317711329915, 2.943386871421371787 ) ) ;
#42807=FACE_OUTER_BOUND ( 'NONE', #4129, .T. ) ;
#42810=CARTESIAN_POINT ( 'NONE',  ( -138.6550000000000011, -7.632228543268600340, -2.479861379858950166 ) ) ;
#42814=CARTESIAN_POINT ( 'NONE',  ( -149.8449999999999989, -7.632228543268599452, 2.479861379858951054 ) ) ;
#42815=CARTESIAN_POINT ( 'NONE',  ( -140.8449999999999989, -7.632228543268599452, 2.479861379858951054 ) ) ;
#42820=CARTESIAN_POINT ( 'NONE',  ( -57.20499999999996987, -2.607480562269071545, -8.024999999999991473 ) ) ;
#42835=AXIS2_PLACEMENT_3D ( 'NONE', #60329, #33601, #6867 ) ;
#42840=AXIS2_PLACEMENT_3D ( 'NONE', #59977, #7217, #49786 ) ;
#42850=ORIENTED_EDGE ( 'NONE', *, *, #28148, .T. ) ;
#42854=CARTESIAN_POINT ( 'NONE',  ( -97.49499999999999034, 6.826472737025113702, -4.959722759717902107 ) ) ;
#42864=EDGE_CURVE ( 'NONE', #37240, #43509, #35532, .T. ) ;
#42871=CARTESIAN_POINT ( 'NONE',  ( -195.0000000000000000, 1.166476076187852838E-15, -9.524999999999991473 ) ) ;
#42879=CARTESIAN_POINT ( 'NONE',  ( -59.90707362346617515, -3.094860106618429807, 9.524999999999991473 ) ) ;
#42886=CARTESIAN_POINT ( 'NONE',  ( -170.9070736234663173, -3.094860106616059703, 9.525000000001714540 ) ) ;
#42889=CARTESIAN_POINT ( 'NONE',  ( -154.3429263765337964, -9.058813317711329915, 2.943386871421371787 ) ) ;
#42890=CARTESIAN_POINT ( 'NONE',  ( -168.2050000000000125, -2.607480562269071545, -8.024999999999991473 ) ) ;
#42891=LINE ( 'NONE', #42531, #8258 ) ;
#42893=CARTESIAN_POINT ( 'NONE',  ( -49.70707362346615810, -3.094860106618431139, -9.524999999999991473 ) ) ;
#42894=CARTESIAN_POINT ( 'NONE',  ( -170.6949999999999932, -8.437984349512086979, 5.166775262442717831E-16 ) ) ;
#42899=CARTESIAN_POINT ( 'NONE',  ( -82.25499999999998124, -4.716976649647092401, 6.492361379858946790 ) ) ;
#42904=CARTESIAN_POINT ( 'NONE',  ( -83.39499999999998181, -6.826472737025113702, -4.959722759717900331 ) ) ;
#42907=CARTESIAN_POINT ( 'NONE',  ( -170.5429263765338135, 9.058813317711329915, 2.943386871421369566 ) ) ;
#42909=EDGE_CURVE ( 'NONE', #55165, #30878, #9024, .T. ) ;
#42911=ORIENTED_EDGE ( 'NONE', *, *, #37222, .T. ) ;
#42918=VERTEX_POINT ( 'NONE', #35320 ) ;
#42927=CARTESIAN_POINT ( 'NONE',  ( -69.50707362346615525, 8.102448949553176405, 5.886773742842740909 ) ) ;
#42929=CARTESIAN_POINT ( 'NONE',  ( -122.3049999999999926, 8.437984349512086979, -1.550032578732815448E-15 ) ) ;
#42934=EDGE_CURVE ( 'NONE', #149, #12986, #63435, .T. ) ;
#42940=VERTEX_POINT ( 'NONE', #9642 ) ;
#42959=CARTESIAN_POINT ( 'NONE',  ( -142.8550000000000182, 4.716976649647094177, 6.492361379858945902 ) ) ;
#42962=( BOUNDED_CURVE ( )  B_SPLINE_CURVE ( 2, ( #9988, #4687, #68737, #21204, #52568, #63778, #15624, #10334, #31767, #4311, #42730 ),
 .UNSPECIFIED., .F., .F. ) 
 B_SPLINE_CURVE_WITH_KNOTS ( ( 3, 2, 2, 2, 2, 3 ),
 ( 0.4782608695652060260, 0.4804347826086842188, 0.4826086956521624116, 0.4847826086956406044, 0.4869565217391188527, 0.4891304347825970456 ),
 .UNSPECIFIED. ) 
 CURVE ( )  GEOMETRIC_REPRESENTATION_ITEM ( )  RATIONAL_B_SPLINE_CURVE ( ( 1.000000000000256239, 0.9510565162948972917, 1.000000000000000000, 0.9510565162951535312, 1.000000000000000000, 0.9510565162951535312, 1.000000000000000000, 0.9510565162951535312, 1.000000000000000000, 0.9510565162954159879, 0.9999999999997375433 ) ) 
 REPRESENTATION_ITEM ( '' )  );
#42972=CARTESIAN_POINT ( 'NONE',  ( -59.90499999999997982, 2.607480562269068880, -8.024999999999993250 ) ) ;
#42980=CARTESIAN_POINT ( 'NONE',  ( -111.4429263765338050, -1.166476076187852838E-15, -9.524999999999991473 ) ) ;
#42986=CARTESIAN_POINT ( 'NONE',  ( -107.5449999999999875, -7.632228543268600340, -2.479861379858950166 ) ) ;
#42988=CARTESIAN_POINT ( 'NONE',  ( -87.14499999999998181, -4.716976649647092401, 6.492361379858946790 ) ) ;
#42989=CIRCLE ( 'NONE', #56379, 7.499999999999985789 ) ;
#42991=DIRECTION ( 'NONE',  ( 1.000000000000000000, 0.000000000000000000, 0.000000000000000000 ) ) ;
#42997=CARTESIAN_POINT ( 'NONE',  ( -136.1929263765337907, -10.01517768586948698, 6.132527647946031529E-16 ) ) ;
#42998=CARTESIAN_POINT ( 'NONE',  ( -145.0449999999999875, 7.632228543268600340, 2.479861379858949277 ) ) ;
#43017=CARTESIAN_POINT ( 'NONE',  ( -147.5049999999999955, -6.826472737025113702, -4.959722759717900331 ) ) ;
#43033=CARTESIAN_POINT ( 'NONE',  ( -66.05499999999999261, -9.827790563157499189E-16, -8.024999999999991473 ) ) ;
#43034=CARTESIAN_POINT ( 'NONE',  ( -121.1949999999999790, 8.437984349512085203, -1.550032578732815448E-15 ) ) ;
#43036=EDGE_LOOP ( 'NONE', ( #4194, #244, #57833, #7533, #13270, #26325, #20450, #24099, #60530, #16701, #23769, #27208, #49562, #63841, #64866, #58127, #15433, #47950, #11206, #48616, #59580, #24890, #6623, #5586, #35226, #21400, #21015, #44975, #46746, #5144, #58082, #61407, #41427, #46333, #13729, #65796, #2880, #40662, #16956, #16225, #13708, #66476, #64602, #53435, #16301, #49156, #9710, #60218, #33638, #16158, #53194, #34256, #22164, #55556, #67742, #762, #47580, #45925, #39691, #52163, #56745, #39174, #26181, #59383, #19385, #65148, #15776, #9543, #52903, #54016, #65918, #2624, #11937, #63306, #8481, #25546, #35344, #3827, #39453, #68544, #6264, #36088, #58124, #45800, #3642, #45469, #25748, #8912, #54626, #48032, #1923, #11992, #48980, #43070, #18420, #61157 ) ) ;
#43044=ORIENTED_EDGE ( 'NONE', *, *, #38574, .T. ) ;
#43046=CARTESIAN_POINT ( 'NONE',  ( -168.8049999999999500, -8.437984349512085203, 5.166775262442717831E-16 ) ) ;
#43048=CARTESIAN_POINT ( 'NONE',  ( -88.40707362346616094, 3.094860106618428031, -9.524999999999993250 ) ) ;
#43058=CARTESIAN_POINT ( 'NONE',  ( -86.15499999999998693, 7.632228543268600340, 2.479861379858949277 ) ) ;
#43062=CARTESIAN_POINT ( 'NONE',  ( -135.0570736234661808, 0.000000000000000000, 9.524999999999991473 ) ) ;
#43067=CARTESIAN_POINT ( 'NONE',  ( -69.95707362346617231, 9.058813317711329915, -2.943386871421373119 ) ) ;
#43070=ORIENTED_EDGE ( 'NONE', *, *, #20260, .F. ) ;
#43074=CARTESIAN_POINT ( 'NONE',  ( -108.0549999999999784, -9.827790563157499189E-16, -8.024999999999991473 ) ) ;
#43077=CARTESIAN_POINT ( 'NONE',  ( -112.6449999999999960, 4.716976649647091513, -6.492361379858946790 ) ) ;
#43083=CARTESIAN_POINT ( 'NONE',  ( -158.0929263765338249, 3.094860106618433360, 9.524999999999991473 ) ) ;
#43085=CARTESIAN_POINT ( 'NONE',  ( -171.5949999999999704, 2.607480562269073321, 8.024999999999991473 ) ) ;
#43088=CARTESIAN_POINT ( 'NONE',  ( -61.94292637653379785, 0.000000000000000000, 9.524999999999991473 ) ) ;
#43091=CARTESIAN_POINT ( 'NONE',  ( -77.24292637653380211, 5.598654528085804216, 7.705886871421366635 ) ) ;
#43098=CARTESIAN_POINT ( 'NONE',  ( -178.4050000000000011, -2.607480562269069768, 8.024999999999991473 ) ) ;
#43111=CARTESIAN_POINT ( 'NONE',  ( -96.95499999999998408, -7.632228543268599452, 2.479861379858951054 ) ) ;
#43114=EDGE_CURVE ( 'NONE', #45514, #17985, #68686, .T. ) ;
#43122=CARTESIAN_POINT ( 'NONE',  ( -61.34499999999998465, 7.632228543268599452, -2.479861379858951942 ) ) ;
#43130=ORIENTED_EDGE ( 'NONE', *, *, #41473, .T. ) ;
#43134=CARTESIAN_POINT ( 'NONE',  ( -120.0549999999999926, -9.827790563157499189E-16, -8.024999999999991473 ) ) ;
#43142=CARTESIAN_POINT ( 'NONE',  ( -164.4570736234661865, -9.058813317711329915, 2.943386871421371787 ) ) ;
#43145=CARTESIAN_POINT ( 'NONE',  ( -93.35707362346617799, 5.598654528085804216, 7.705886871421366635 ) ) ;
#43155=CARTESIAN_POINT ( 'NONE',  ( -136.2549999999999955, -4.716976649647092401, 6.492361379858946790 ) ) ;
#43158=CARTESIAN_POINT ( 'NONE',  ( -145.0449999999999875, 7.632228543268600340, 2.479861379858949277 ) ) ;
#43161=CARTESIAN_POINT ( 'NONE',  ( -137.9949999999999477, -6.826472737025113702, 4.959722759717902107 ) ) ;
#43169=CARTESIAN_POINT ( 'NONE',  ( -58.85499999999998977, 4.716976649647094177, 6.492361379858945902 ) ) ;
#43171=CARTESIAN_POINT ( 'NONE',  ( -62.24499999999998323, -4.716976649647093289, -6.492361379858945902 ) ) ;
#43177=CARTESIAN_POINT ( 'NONE',  ( -109.1929263765337907, -10.01517768586948698, 6.132527647946031529E-16 ) ) ;
#43208=CYLINDRICAL_SURFACE ( 'NONE', #26029, 9.524999999999991473 ) ;
#43209=CARTESIAN_POINT ( 'NONE',  ( -102.7449999999999903, 4.716976649647094177, 6.492361379858945902 ) ) ;
#43233=CARTESIAN_POINT ( 'NONE',  ( -48.05707362346617373, 0.000000000000000000, 9.524999999999991473 ) ) ;
#43238=CARTESIAN_POINT ( 'NONE',  ( -172.2549999999999955, -4.716976649647092401, 6.492361379858946790 ) ) ;
#43241=CARTESIAN_POINT ( 'NONE',  ( -175.9449999999999932, -9.827790563157499189E-16, -8.024999999999991473 ) ) ;
#43242=CARTESIAN_POINT ( 'NONE',  ( -164.0949999999999989, -2.607480562269071545, -8.024999999999991473 ) ) ;
#43248=CARTESIAN_POINT ( 'NONE',  ( -80.60499999999996135, 6.826472737025113702, -4.959722759717902107 ) ) ;
#43253=CARTESIAN_POINT ( 'NONE',  ( -76.64499999999999602, 4.716976649647091513, -6.492361379858946790 ) ) ;
#43255=CARTESIAN_POINT ( 'NONE',  ( -133.8570736234661638, -5.598654528085803328, -7.705886871421366635 ) ) ;
#43257=CARTESIAN_POINT ( 'NONE',  ( -171.1429263765338078, 5.598654528085800663, -7.705886871421367523 ) ) ;
#43287=CARTESIAN_POINT ( 'NONE',  ( -109.2549999999999955, -4.716976649647092401, 6.492361379858946790 ) ) ;
#43304=CARTESIAN_POINT ( 'NONE',  ( -181.1929263765338192, -10.01517768586948698, 6.132527647946031529E-16 ) ) ;
#43320=CARTESIAN_POINT ( 'NONE',  ( -142.1049999999999613, -6.826472737025115478, 4.959722759717900331 ) ) ;
#43330=CARTESIAN_POINT ( 'NONE',  ( -54.95499999999997698, -7.632228543268599452, 2.479861379858951054 ) ) ;
#43331=ORIENTED_EDGE ( 'NONE', *, *, #49812, .T. ) ;
#43335=CARTESIAN_POINT ( 'NONE',  ( -60.44292637653379785, -1.166476076187852838E-15, -9.524999999999991473 ) ) ;
#43345=EDGE_CURVE ( 'NONE', #19358, #61162, #15534, .T. ) ;
#43346=CARTESIAN_POINT ( 'NONE',  ( -112.9449999999999932, -9.827790563157499189E-16, -8.024999999999991473 ) ) ;
#43348=CARTESIAN_POINT ( 'NONE',  ( -89.39499999999996760, -6.826472737025115478, -4.959722759717899443 ) ) ;
#43359=CARTESIAN_POINT ( 'NONE',  ( -123.2929263765337993, 3.094860106618428031, -9.524999999999993250 ) ) ;
#43361=CARTESIAN_POINT ( 'NONE',  ( -150.1450000000000102, -4.716976649647092401, 6.492361379858946790 ) ) ;
#43364=CARTESIAN_POINT ( 'NONE',  ( -66.35707362346616378, 5.598654528085804216, 7.705886871421366635 ) ) ;
#43365=CARTESIAN_POINT ( 'NONE',  ( -195.0000000000000000, 0.000000000000000000, 9.524999999999991473 ) ) ;
#43373=CARTESIAN_POINT ( 'NONE',  ( -129.2070736234668402, 3.094860106629659491, 9.524999999991834443 ) ) ;
#43376=CARTESIAN_POINT ( 'NONE',  ( -137.9049999999999727, 2.607480562269069324, -8.024999999999993250 ) ) ;
#43377=ORIENTED_EDGE ( 'NONE', *, *, #6677, .T. ) ;
#43380=CARTESIAN_POINT ( 'NONE',  ( -142.4070736234666583, 3.094860106610092920, -9.525000000006050627 ) ) ;
#43390=CARTESIAN_POINT ( 'NONE',  ( -66.35499999999998977, -4.716976649647093289, -6.492361379858945902 ) ) ;
#43392=CARTESIAN_POINT ( 'NONE',  ( -118.6449999999999818, 4.716976649647091513, -6.492361379858946790 ) ) ;
#43403=CARTESIAN_POINT ( 'NONE',  ( -174.3549999999999898, -4.716976649647093289, -6.492361379858945902 ) ) ;
#43409=CARTESIAN_POINT ( 'NONE',  ( -195.0000000000000000, 0.000000000000000000, 0.000000000000000000 ) ) ;
#43411=CARTESIAN_POINT ( 'NONE',  ( -77.54292637653379927, 9.058813317711329915, 2.943386871421369566 ) ) ;
#43416=CARTESIAN_POINT ( 'NONE',  ( -80.75499999999999545, 4.716976649647091513, -6.492361379858946790 ) ) ;
#43422=CARTESIAN_POINT ( 'NONE',  ( -67.55707362346618083, -1.166476076187852838E-15, -9.524999999999991473 ) ) ;
#43429=EDGE_CURVE ( 'NONE', #53864, #1748, #6214, .T. ) ;
#43431=CARTESIAN_POINT ( 'NONE',  ( -101.0049999999999812, 6.826472737025116366, 4.959722759717898555 ) ) ;
#43434=CARTESIAN_POINT ( 'NONE',  ( -112.4949999999999761, 6.826472737025113702, -4.959722759717902107 ) ) ;
#43440=CARTESIAN_POINT ( 'NONE',  ( -162.4429263765338192, -1.166476076187852838E-15, -9.524999999999991473 ) ) ;
#43441=CARTESIAN_POINT ( 'NONE',  ( -173.9949999999999761, -6.826472737025115478, 4.959722759717900331 ) ) ;
#43449=CARTESIAN_POINT ( 'NONE',  ( -79.19292637653379074, -10.01517768586948698, 6.132527647946031529E-16 ) ) ;
#43458=CARTESIAN_POINT ( 'NONE',  ( -176.7549999999999955, 4.716976649647091513, -6.492361379858946790 ) ) ;
#43467=CARTESIAN_POINT ( 'NONE',  ( -89.90499999999997272, 2.607480562269069324, -8.024999999999993250 ) ) ;
#43477=ORIENTED_EDGE ( 'NONE', *, *, #44645, .T. ) ;
#43478=CARTESIAN_POINT ( 'NONE',  ( -62.84499999999998465, -7.632228543268599452, 2.479861379858951054 ) ) ;
#43487=CARTESIAN_POINT ( 'NONE',  ( -117.9549999999999841, -7.632228543268599452, 2.479861379858951054 ) ) ;
#43494=CARTESIAN_POINT ( 'NONE',  ( -158.0070736234661695, -8.102448949553172852, -5.886773742842741797 ) ) ;
#43496=CARTESIAN_POINT ( 'NONE',  ( -94.85707362346616378, -5.598654528085803328, -7.705886871421366635 ) ) ;
#43502=CARTESIAN_POINT ( 'NONE',  ( -133.5549999999999784, 0.000000000000000000, 8.024999999999991473 ) ) ;
#43503=CARTESIAN_POINT ( 'NONE',  ( -86.45707362346617231, -9.058813317711329915, 2.943386871421371787 ) ) ;
#43507=CARTESIAN_POINT ( 'NONE',  ( -147.2949999999999591, -2.607480562269069768, 8.024999999999991473 ) ) ;
#43508=CARTESIAN_POINT ( 'NONE',  ( -135.4449999999999932, 0.000000000000000000, 8.024999999999991473 ) ) ;
#43509=VERTEX_POINT ( 'NONE', #23889 ) ;
#43514=CARTESIAN_POINT ( 'NONE',  ( -51.50499999999999545, -6.826472737025115478, -4.959722759717899443 ) ) ;
#43515=CARTESIAN_POINT ( 'NONE',  ( -57.89499999999996760, 6.826472737025116366, 4.959722759717898555 ) ) ;
#43519=CARTESIAN_POINT ( 'NONE',  ( -102.9570736234661723, 9.058813317711329915, -2.943386871421373119 ) ) ;
#43522=CARTESIAN_POINT ( 'NONE',  ( -102.7429263765338021, -5.598654528085803328, -7.705886871421366635 ) ) ;
#43539=VERTEX_POINT ( 'NONE', #62215 ) ;
#43546=CARTESIAN_POINT ( 'NONE',  ( -119.1570736234661751, -9.058813317711329915, -2.943386871421370898 ) ) ;
#43547=CARTESIAN_POINT ( 'NONE',  ( -195.0000000000000000, 0.000000000000000000, 0.000000000000000000 ) ) ;
#43548=CARTESIAN_POINT ( 'NONE',  ( -94.79499999999997328, 2.607480562269068880, -8.024999999999993250 ) ) ;
#43561=DIRECTION ( 'NONE',  ( -1.000000000000000000, -0.000000000000000000, -0.000000000000000000 ) ) ;
#43563=CARTESIAN_POINT ( 'NONE',  ( -165.9570736234661865, 9.058813317711329915, -2.943386871421373119 ) ) ;
#43565=DIRECTION ( 'NONE',  ( 0.000000000000000000, 0.000000000000000000, 1.000000000000000000 ) ) ;
#43575=CARTESIAN_POINT ( 'NONE',  ( -169.4049999999999727, -2.607480562269069768, 8.024999999999991473 ) ) ;
#43576=DIRECTION ( 'NONE',  ( 0.000000000000000000, 0.000000000000000000, 1.000000000000000000 ) ) ;
#43578=CARTESIAN_POINT ( 'NONE',  ( -177.5950000000000273, 2.607480562269073321, 8.024999999999991473 ) ) ;
#43579=CARTESIAN_POINT ( 'NONE',  ( -171.2950000000000159, -2.607480562269069768, 8.024999999999991473 ) ) ;
#43585=CARTESIAN_POINT ( 'NONE',  ( -78.50499999999996703, -6.826472737025115478, -4.959722759717899443 ) ) ;
#43591=CARTESIAN_POINT ( 'NONE',  ( -84.44499999999999318, 0.000000000000000000, 8.024999999999991473 ) ) ;
#43594=CARTESIAN_POINT ( 'NONE',  ( -134.6070736234661638, -8.102448949553174629, 5.886773742842742685 ) ) ;
#43607=DIRECTION ( 'NONE',  ( -1.000000000000000000, -0.000000000000000000, -0.000000000000000000 ) ) ;
#43610=CARTESIAN_POINT ( 'NONE',  ( -116.3049999999999784, 8.437984349512086979, -1.550032578732815448E-15 ) ) ;
#43624=CARTESIAN_POINT ( 'NONE',  ( -151.8570736234661638, -5.598654528085803328, -7.705886871421366635 ) ) ;
#43632=CARTESIAN_POINT ( 'NONE',  ( -105.2929263765348082, 3.094860106601757366, -9.525000000012106227 ) ) ;
#43636=ORIENTED_EDGE ( 'NONE', *, *, #16908, .T. ) ;
#43637=CARTESIAN_POINT ( 'NONE',  ( -49.94292637653380496, 0.000000000000000000, 9.524999999999991473 ) ) ;
#43641=CARTESIAN_POINT ( 'NONE',  ( -140.7549999999999955, 4.716976649647091513, -6.492361379858946790 ) ) ;
#43654=CARTESIAN_POINT ( 'NONE',  ( -61.10499999999997556, -6.826472737025115478, 4.959722759717900331 ) ) ;
#43663=CARTESIAN_POINT ( 'NONE',  ( -128.6929263765337907, 10.01517768586948698, -1.839758294383808966E-15 ) ) ;
#43668=LINE ( 'NONE', #9983, #22455 ) ;
#43670=CARTESIAN_POINT ( 'NONE',  ( -110.3949999999999818, -6.826472737025113702, -4.959722759717900331 ) ) ;
#43672=CARTESIAN_POINT ( 'NONE',  ( -90.59499999999999886, 2.607480562269073321, 8.024999999999991473 ) ) ;
#43677=( BOUNDED_CURVE ( )  B_SPLINE_CURVE ( 2, ( #17498, #55789, #56125, #18516, #40003, #61398, #44596, #38971, #13213, #1578, #34669 ),
 .UNSPECIFIED., .F., .F. ) 
 B_SPLINE_CURVE_WITH_KNOTS ( ( 3, 2, 2, 2, 2, 3 ),
 ( 0.3369565217391224943, 0.3391304347826006316, 0.3413043478260788244, 0.3434782608695570172, 0.3456521739130352100, 0.3478260869565133473 ),
 .UNSPECIFIED. ) 
 CURVE ( )  GEOMETRIC_REPRESENTATION_ITEM ( )  RATIONAL_B_SPLINE_CURVE ( ( 1.000000000000178746, 0.9510565162949747853, 1.000000000000000000, 0.9510565162951535312, 1.000000000000000000, 0.9510565162951535312, 1.000000000000000000, 0.9510565162951535312, 1.000000000000000000, 0.9510565162953422691, 0.9999999999998112621 ) ) 
 REPRESENTATION_ITEM ( '' )  );
#43682=CARTESIAN_POINT ( 'NONE',  ( -121.0429263765337993, -9.058813317711329915, -2.943386871421370898 ) ) ;
#43683=CARTESIAN_POINT ( 'NONE',  ( -148.4950000000000045, 6.826472737025113702, -4.959722759717902107 ) ) ;
#43690=ORIENTED_EDGE ( 'NONE', *, *, #69308, .F. ) ;
#43698=ORIENTED_EDGE ( 'NONE', *, *, #57703, .T. ) ;
#43699=CARTESIAN_POINT ( 'NONE',  ( -136.8550000000000182, 4.716976649647094177, 6.492361379858945902 ) ) ;
#43700=ORIENTED_EDGE ( 'NONE', *, *, #23920, .T. ) ;
#43711=CARTESIAN_POINT ( 'NONE',  ( -53.15499999999997982, 7.632228543268600340, 2.479861379858949277 ) ) ;
#43712=CARTESIAN_POINT ( 'NONE',  ( -119.8449999999999989, -7.632228543268599452, 2.479861379858951054 ) ) ;
#43724=CARTESIAN_POINT ( 'NONE',  ( -169.1049999999999613, -6.826472737025115478, 4.959722759717900331 ) ) ;
#43728=FACE_OUTER_BOUND ( 'NONE', #53013, .T. ) ;
#43735=CARTESIAN_POINT ( 'NONE',  ( -89.90499999999998693, 2.607480562269068880, -8.024999999999993250 ) ) ;
#43743=CARTESIAN_POINT ( 'NONE',  ( -64.85707362346616378, -5.598654528085803328, -7.705886871421366635 ) ) ;
#43750=CARTESIAN_POINT ( 'NONE',  ( -99.80499999999997840, -8.437984349512085203, 5.166775262442717831E-16 ) ) ;
#43752=CARTESIAN_POINT ( 'NONE',  ( -119.9949999999999903, -6.826472737025115478, 4.959722759717900331 ) ) ;
#43755=DIRECTION ( 'NONE',  ( -1.000000000000000000, -0.000000000000000000, -0.000000000000000000 ) ) ;
#43756=CARTESIAN_POINT ( 'NONE',  ( -152.9929263765337737, 8.102448949553171076, -5.886773742842744461 ) ) ;
#43758=CARTESIAN_POINT ( 'NONE',  ( -180.5949999999999704, 2.607480562269073321, 8.024999999999991473 ) ) ;
#43768=CARTESIAN_POINT ( 'NONE',  ( -67.94292637653380496, 0.000000000000000000, 9.524999999999991473 ) ) ;
#43778=CARTESIAN_POINT ( 'NONE',  ( -165.8049999999999784, -8.437984349512086979, 5.166775262442717831E-16 ) ) ;
#43790=CARTESIAN_POINT ( 'NONE',  ( -81.20499999999998408, -2.607480562269071545, -8.024999999999991473 ) ) ;
#43794=CARTESIAN_POINT ( 'NONE',  ( -113.9070736234670278, -3.094860106604178096, 9.525000000010345858 ) ) ;
#43798=CARTESIAN_POINT ( 'NONE',  ( -65.09499999999998465, -2.607480562269071545, -8.024999999999991473 ) ) ;
#43810=CARTESIAN_POINT ( 'NONE',  ( -116.3049999999999784, 8.437984349512085203, -1.550032578732815448E-15 ) ) ;
#43811=EDGE_LOOP ( 'NONE', ( #21964, #9131, #65838, #46123 ) ) ;
#43815=CARTESIAN_POINT ( 'NONE',  ( -159.8929263765337794, -8.102448949553174629, -5.886773742842741797 ) ) ;
#43819=CARTESIAN_POINT ( 'NONE',  ( -151.4070736234661751, 3.094860106618428031, -9.524999999999993250 ) ) ;
#43823=CARTESIAN_POINT ( 'NONE',  ( -97.55707362346618083, -1.166476076187852838E-15, -9.524999999999991473 ) ) ;
#43831=CARTESIAN_POINT ( 'NONE',  ( -127.5550000000000068, 0.000000000000000000, 8.024999999999991473 ) ) ;
#43834=CARTESIAN_POINT ( 'NONE',  ( -140.6949999999999363, -8.437984349512085203, 5.166775262442717831E-16 ) ) ;
#43836=CARTESIAN_POINT ( 'NONE',  ( -132.5949999999999989, 2.607480562269072433, 8.024999999999991473 ) ) ;
#43842=CARTESIAN_POINT ( 'NONE',  ( -183.1429263765338078, 5.598654528085800663, -7.705886871421367523 ) ) ;
#43844=CARTESIAN_POINT ( 'NONE',  ( -58.34499999999997755, 7.632228543268599452, -2.479861379858951942 ) ) ;
#43846=CARTESIAN_POINT ( 'NONE',  ( -178.5570736234661808, -1.166476076187852838E-15, -9.524999999999991473 ) ) ;
#43851=CARTESIAN_POINT ( 'NONE',  ( -102.8929263765338078, -8.102448949553172852, -5.886773742842741797 ) ) ;
#43864=ORIENTED_EDGE ( 'NONE', *, *, #63932, .F. ) ;
#43874=ORIENTED_EDGE ( 'NONE', *, *, #13104, .T. ) ;
#43885=CARTESIAN_POINT ( 'NONE',  ( -91.34499999999998465, 7.632228543268599452, -2.479861379858951942 ) ) ;
#43897=ORIENTED_EDGE ( 'NONE', *, *, #56861, .F. ) ;
#43908=CARTESIAN_POINT ( 'NONE',  ( -114.8929263765337936, -8.102448949553174629, -5.886773742842741797 ) ) ;
#43914=CARTESIAN_POINT ( 'NONE',  ( -158.3049999999999500, 8.437984349512085203, -1.550032578732815448E-15 ) ) ;
#43916=CARTESIAN_POINT ( 'NONE',  ( -183.8457661644624750, -8.375912622596889179, -2.295903050784204869 ) ) ;
#43918=CARTESIAN_POINT ( 'NONE',  ( -174.7449999999999761, 4.716976649647094177, 6.492361379858945902 ) ) ;
#43919=CARTESIAN_POINT ( 'NONE',  ( -161.9950000000000045, -6.826472737025113702, 4.959722759717902107 ) ) ;
#43925=CARTESIAN_POINT ( 'NONE',  ( -85.70499999999999829, 2.607480562269073321, 8.024999999999991473 ) ) ;
#43929=CARTESIAN_POINT ( 'NONE',  ( -82.64499999999998181, 4.716976649647091513, -6.492361379858946790 ) ) ;
#43933=VECTOR ( 'NONE', #6500, 1000.000000000000000 ) ;
#43953=CARTESIAN_POINT ( 'NONE',  ( -70.40707362346617515, 3.094860106618428031, -9.524999999999993250 ) ) ;
#43956=CARTESIAN_POINT ( 'NONE',  ( -113.4549999999999841, 7.632228543268599452, -2.479861379858951942 ) ) ;
#43962=CARTESIAN_POINT ( 'NONE',  ( -68.60707362346616378, -8.102448949553174629, 5.886773742842742685 ) ) ;
#43971=CYLINDRICAL_SURFACE ( 'NONE', #6330, 9.524999999999991473 ) ;
#43977=DIRECTION ( 'NONE',  ( -1.000000000000000000, -0.000000000000000000, -0.000000000000000000 ) ) ;
#43981=ORIENTED_EDGE ( 'NONE', *, *, #53310, .T. ) ;
#43984=CARTESIAN_POINT ( 'NONE',  ( -48.74292637653379501, -5.598654528085803328, -7.705886871421366635 ) ) ;
#43986=DIRECTION ( 'NONE',  ( 0.000000000000000000, 0.000000000000000000, 1.000000000000000000 ) ) ;
#43987=CARTESIAN_POINT ( 'NONE',  ( -145.2549999999999955, -4.716976649647092401, 6.492361379858946790 ) ) ;
#44002=CARTESIAN_POINT ( 'NONE',  ( -51.20707362346615099, 3.094860106618433360, 9.524999999999991473 ) ) ;
#44003=CARTESIAN_POINT ( 'NONE',  ( -52.40499999999998693, -2.607480562269069768, 8.024999999999991473 ) ) ;
#44008=DIRECTION ( 'NONE',  ( 0.000000000000000000, 0.000000000000000000, 1.000000000000000000 ) ) ;
#44010=EDGE_CURVE ( 'NONE', #60379, #41992, #68820, .T. ) ;
#44011=CARTESIAN_POINT ( 'NONE',  ( -129.1429263765338078, 5.598654528085800663, -7.705886871421367523 ) ) ;
#44020=CARTESIAN_POINT ( 'NONE',  ( -105.2949999999999875, -2.607480562269069768, 8.024999999999991473 ) ) ;
#44022=CARTESIAN_POINT ( 'NONE',  ( -77.84499999999998465, -7.632228543268599452, 2.479861379858951054 ) ) ;
#44032=CARTESIAN_POINT ( 'NONE',  ( -122.2429263765338021, 5.598654528085804216, 7.705886871421366635 ) ) ;
#44034=CARTESIAN_POINT ( 'NONE',  ( -149.5449999999999875, -7.632228543268600340, -2.479861379858950166 ) ) ;
#44046=CARTESIAN_POINT ( 'NONE',  ( -116.8429263765338106, 9.058813317711329915, -2.943386871421373119 ) ) ;
#44047=CARTESIAN_POINT ( 'NONE',  ( -195.0000000000000000, 0.000000000000000000, 9.524999999999991473 ) ) ;
#44049=CARTESIAN_POINT ( 'NONE',  ( -141.8050000000000068, -8.437984349512086979, 5.166775262442717831E-16 ) ) ;
#44055=ORIENTED_EDGE ( 'NONE', *, *, #62089, .F. ) ;
#44066=CARTESIAN_POINT ( 'NONE',  ( -54.50499999999998835, -6.826472737025113702, -4.959722759717900331 ) ) ;
#44081=CARTESIAN_POINT ( 'NONE',  ( -167.6050000000000182, 6.826472737025113702, -4.959722759717902107 ) ) ;
#44089=CARTESIAN_POINT ( 'NONE',  ( -102.0570736234661808, 0.000000000000000000, 9.524999999999991473 ) ) ;
#44090=CARTESIAN_POINT ( 'NONE',  ( -78.29292637653377085, 3.094860106618428031, -9.524999999999993250 ) ) ;
#44095=CARTESIAN_POINT ( 'NONE',  ( -85.55499999999999261, 0.000000000000000000, 8.024999999999991473 ) ) ;
#44102=CARTESIAN_POINT ( 'NONE',  ( -53.15707362346616804, -9.058813317711329915, -2.943386871421370898 ) ) ;
#44109=CARTESIAN_POINT ( 'NONE',  ( -104.0049999999999812, 6.826472737025116366, 4.959722759717898555 ) ) ;
#44111=CARTESIAN_POINT ( 'NONE',  ( -115.4949999999999903, 6.826472737025113702, -4.959722759717902107 ) ) ;
#44115=CARTESIAN_POINT ( 'NONE',  ( -17.64912285177511819, 11.22500550600073588, -4.243648409907320840 ) ) ;
#44116=CARTESIAN_POINT ( 'NONE',  ( -152.3929263765338078, 8.102448949553176405, 5.886773742842740909 ) ) ;
#44117=CARTESIAN_POINT ( 'NONE',  ( -179.5450000000000159, -7.632228543268600340, -2.479861379858950166 ) ) ;
#44125=CARTESIAN_POINT ( 'NONE',  ( -70.19292637653380496, -10.01517768586948698, 6.132527647946031529E-16 ) ) ;
#44136=CARTESIAN_POINT ( 'NONE',  ( -167.3049999999999784, 8.437984349512086979, -1.550032578732815448E-15 ) ) ;
#44139=VECTOR ( 'NONE', #67064, 1000.000000000000000 ) ;
#44150=CARTESIAN_POINT ( 'NONE',  ( -79.40499999999998693, -2.607480562269069768, 8.024999999999991473 ) ) ;
#44152=CARTESIAN_POINT ( 'NONE',  ( -45.99999999999999289, 0.000000000000000000, 9.525000000000000355 ) ) ;
#44158=VERTEX_POINT ( 'NONE', #38828 ) ;
#44161=CARTESIAN_POINT ( 'NONE',  ( -58.94499999999998607, -9.827790563157499189E-16, -8.024999999999991473 ) ) ;
#44167=ORIENTED_EDGE ( 'NONE', *, *, #12464, .T. ) ;
#44171=CARTESIAN_POINT ( 'NONE',  ( -112.2549999999999955, -4.716976649647092401, 6.492361379858946790 ) ) ;
#44176=CARTESIAN_POINT ( 'NONE',  ( -195.0000000000000000, 0.000000000000000000, 0.000000000000000000 ) ) ;
#44177=CARTESIAN_POINT ( 'NONE',  ( -153.6570736234661751, 9.058813317711329915, 2.943386871421369566 ) ) ;
#44180=CARTESIAN_POINT ( 'NONE',  ( -94.25707362346618368, 5.598654528085800663, -7.705886871421367523 ) ) ;
#44181=EDGE_CURVE ( 'NONE', #29534, #66538, #53846, .T. ) ;
#44188=CARTESIAN_POINT ( 'NONE',  ( -134.4549999999999841, 7.632228543268599452, -2.479861379858951942 ) ) ;
#44192=CARTESIAN_POINT ( 'NONE',  ( -146.0949999999999989, -2.607480562269071545, -8.024999999999991473 ) ) ;
#44193=CARTESIAN_POINT ( 'NONE',  ( -127.9449999999999790, -9.827790563157499189E-16, -8.024999999999991473 ) ) ;
#44197=CARTESIAN_POINT ( 'NONE',  ( -179.6929263765337907, 10.01517768586948698, -1.839758294383808571E-15 ) ) ;
#44199=CARTESIAN_POINT ( 'NONE',  ( -56.54499999999998749, -7.632228543268600340, -2.479861379858950166 ) ) ;
#44205=CARTESIAN_POINT ( 'NONE',  ( -91.49292637653378790, -8.102448949553172852, 5.886773742842742685 ) ) ;
#44235=CARTESIAN_POINT ( 'NONE',  ( -94.40707362346725517, 3.094860106600277661, -9.525000000013180923 ) ) ;
#44237=CARTESIAN_POINT ( 'NONE',  ( -86.69499999999999318, -8.437984349512085203, 5.166775262442717831E-16 ) ) ;
#44254=CARTESIAN_POINT ( 'NONE',  ( -182.0070736234661979, -8.102448949553172852, -5.886773742842741797 ) ) ;
#44255=CARTESIAN_POINT ( 'NONE',  ( -195.0000000000000000, 0.000000000000000000, 0.000000000000000000 ) ) ;
#44260=CARTESIAN_POINT ( 'NONE',  ( -67.94292637653380496, 0.000000000000000000, 9.524999999999991473 ) ) ;
#44269=CARTESIAN_POINT ( 'NONE',  ( -164.1550000000000011, 7.632228543268600340, 2.479861379858949277 ) ) ;
#44270=FACE_OUTER_BOUND ( 'NONE', #34056, .T. ) ;
#44271=CARTESIAN_POINT ( 'NONE',  ( -183.6019133891463468, -5.474665737238584740, -7.053184183476749247 ) ) ;
#44272=CARTESIAN_POINT ( 'NONE',  ( -175.7950000000000159, 2.607480562269068880, -8.024999999999993250 ) ) ;
#44274=CARTESIAN_POINT ( 'NONE',  ( -155.5449999999999875, -7.632228543268600340, -2.479861379858950166 ) ) ;
#44280=CARTESIAN_POINT ( 'NONE',  ( -70.55499999999999261, 0.000000000000000000, 8.024999999999991473 ) ) ;
#44286=CARTESIAN_POINT ( 'NONE',  ( -67.04499999999997328, 7.632228543268600340, 2.479861379858949277 ) ) ;
#44293=LINE ( 'NONE', #39008, #5724 ) ;
#44297=CARTESIAN_POINT ( 'NONE',  ( -50.69292637653379785, 10.01517768586948698, -1.839758294383808966E-15 ) ) ;
#44313=CARTESIAN_POINT ( 'NONE',  ( -108.5049999999999812, -6.826472737025113702, -4.959722759717900331 ) ) ;
#44327=ORIENTED_EDGE ( 'NONE', *, *, #36989, .F. ) ;
#44333=CYLINDRICAL_SURFACE ( 'NONE', #52527, 9.524999999999991473 ) ;
#44339=ORIENTED_EDGE ( 'NONE', *, *, #7937, .F. ) ;
#44340=CARTESIAN_POINT ( 'NONE',  ( -52.04292637653379217, -9.058813317711329915, -2.943386871421370898 ) ) ;
#44342=DIRECTION ( 'NONE',  ( -1.000000000000000000, -0.000000000000000000, -0.000000000000000000 ) ) ;
#44343=CARTESIAN_POINT ( 'NONE',  ( -132.9549999999999841, -7.632228543268599452, 2.479861379858951054 ) ) ;
#44349=CARTESIAN_POINT ( 'NONE',  ( -107.3070736234661524, -10.01517768586948698, 6.132527647946031529E-16 ) ) ;
#44355=CARTESIAN_POINT ( 'NONE',  ( -52.70499999999996277, 2.607480562269073321, 8.024999999999991473 ) ) ;
#44373=CARTESIAN_POINT ( 'NONE',  ( -103.0449999999999875, 7.632228543268600340, 2.479861379858949277 ) ) ;
#44375=CARTESIAN_POINT ( 'NONE',  ( -82.79499999999998749, 2.607480562269068880, -8.024999999999993250 ) ) ;
#44385=CARTESIAN_POINT ( 'NONE',  ( -125.3929263765338220, 8.102448949553176405, 5.886773742842740909 ) ) ;
#44388=CARTESIAN_POINT ( 'NONE',  ( -133.4950000000000045, 6.826472737025113702, -4.959722759717902107 ) ) ;
#44392=CARTESIAN_POINT ( 'NONE',  ( -172.9429263765337907, 0.000000000000000000, 9.524999999999991473 ) ) ;
#44394=VERTEX_POINT ( 'NONE', #9214 ) ;
#44401=CARTESIAN_POINT ( 'NONE',  ( -50.00707362346617657, -8.102448949553174629, -5.886773742842741797 ) ) ;
#44402=CARTESIAN_POINT ( 'NONE',  ( -150.4429263765338192, -1.166476076187852838E-15, -9.524999999999991473 ) ) ;
#44404=CARTESIAN_POINT ( 'NONE',  ( -146.0049999999999955, 6.826472737025115478, 4.959722759717899443 ) ) ;
#44421=CARTESIAN_POINT ( 'NONE',  ( -53.75499999999999545, 4.716976649647091513, -6.492361379858946790 ) ) ;
#44427=CARTESIAN_POINT ( 'NONE',  ( -87.59292637653381064, -3.094860106618431139, -9.524999999999991473 ) ) ;
#44433=CYLINDRICAL_SURFACE ( 'NONE', #46433, 5.000000000000000000 ) ;
#44436=CARTESIAN_POINT ( 'NONE',  ( -173.9049999999999727, 2.607480562269068880, -8.024999999999993250 ) ) ;
#44444=CARTESIAN_POINT ( 'NONE',  ( -88.55499999999999261, 0.000000000000000000, 8.024999999999991473 ) ) ;
#44460=CARTESIAN_POINT ( 'NONE',  ( -102.2949999999999733, -2.607480562269069768, 8.024999999999991473 ) ) ;
#44464=CARTESIAN_POINT ( 'NONE',  ( -155.2429263765338021, 5.598654528085804216, 7.705886871421366635 ) ) ;
#44466=CARTESIAN_POINT ( 'NONE',  ( -168.7450000000000045, 4.716976649647094177, 6.492361379858945902 ) ) ;
#44470=AXIS2_PLACEMENT_3D ( 'NONE', #38456, #6380, #69383 ) ;
#44474=ORIENTED_EDGE ( 'NONE', *, *, #13911, .T. ) ;
#44475=CARTESIAN_POINT ( 'NONE',  ( -66.89292637653377938, -8.102448949553172852, -5.886773742842741797 ) ) ;
#44479=CARTESIAN_POINT ( 'NONE',  ( -142.6429263765338078, -5.598654528085801552, 7.705886871421367523 ) ) ;
#44483=CARTESIAN_POINT ( 'NONE',  ( -173.4549999999999841, 7.632228543268599452, -2.479861379858951942 ) ) ;
#44487=DIRECTION ( 'NONE',  ( -1.000000000000000000, -0.000000000000000000, -0.000000000000000000 ) ) ;
#44494=CARTESIAN_POINT ( 'NONE',  ( -79.25499999999999545, -4.716976649647092401, 6.492361379858946790 ) ) ;
#44496=CARTESIAN_POINT ( 'NONE',  ( -92.15707362346617515, -9.058813317711329915, -2.943386871421370898 ) ) ;
#44498=CARTESIAN_POINT ( 'NONE',  ( -113.8429263765337964, 9.058813317711329915, -2.943386871421373119 ) ) ;
#44505=CARTESIAN_POINT ( 'NONE',  ( -58.04499999999998749, 7.632228543268600340, 2.479861379858949277 ) ) ;
#44512=CARTESIAN_POINT ( 'NONE',  ( -51.89499999999998892, 6.826472737025115478, 4.959722759717899443 ) ) ;
#44517=CARTESIAN_POINT ( 'NONE',  ( -114.9549999999999841, -7.632228543268599452, 2.479861379858951054 ) ) ;
#44520=ADVANCED_FACE ( 'NONE', ( #63699 ), #26730, .T. ) ;
#44521=CARTESIAN_POINT ( 'NONE',  ( -96.44292637653380496, -1.166476076187852838E-15, -9.524999999999991473 ) ) ;
#44523=CARTESIAN_POINT ( 'NONE',  ( -146.0070736234661410, -8.102448949553172852, -5.886773742842741797 ) ) ;
#44527=CARTESIAN_POINT ( 'NONE',  ( -87.35707362346617799, 5.598654528085804216, 7.705886871421366635 ) ) ;
#44534=CARTESIAN_POINT ( 'NONE',  ( -127.1050000000000040, -6.826472737025115478, 4.959722759717900331 ) ) ;
#44537=CARTESIAN_POINT ( 'NONE',  ( -82.55707362346618083, -1.166476076187852838E-15, -9.524999999999991473 ) ) ;
#44538=CARTESIAN_POINT ( 'NONE',  ( -133.4950000000000045, 6.826472737025113702, -4.959722759717902107 ) ) ;
#44540=CARTESIAN_POINT ( 'NONE',  ( -131.3949999999999818, -6.826472737025113702, -4.959722759717900331 ) ) ;
#44549=CARTESIAN_POINT ( 'NONE',  ( -182.3929263765338078, 8.102448949553176405, 5.886773742842740909 ) ) ;
#44550=CARTESIAN_POINT ( 'NONE',  ( -56.39499999999997470, -6.826472737025115478, -4.959722759717899443 ) ) ;
#44557=CARTESIAN_POINT ( 'NONE',  ( -95.39292637653380780, 8.102448949553176405, 5.886773742842740909 ) ) ;
#44563=CARTESIAN_POINT ( 'NONE',  ( -163.9429263765338192, 0.000000000000000000, 9.524999999999991473 ) ) ;
#44576=DIRECTION ( 'NONE',  ( 0.000000000000000000, 0.000000000000000000, 1.000000000000000000 ) ) ;
#44579=CARTESIAN_POINT ( 'NONE',  ( -93.65707362346617515, 9.058813317711329915, 2.943386871421369566 ) ) ;
#44581=CARTESIAN_POINT ( 'NONE',  ( -93.89499999999998181, 6.826472737025116366, 4.959722759717898555 ) ) ;
#44591=EDGE_LOOP ( 'NONE', ( #25310, #48828, #61258, #11900 ) ) ;
#44596=CARTESIAN_POINT ( 'NONE',  ( -137.5429263765338135, 9.058813317711329915, 2.943386871421369566 ) ) ;
#44601=FACE_OUTER_BOUND ( 'NONE', #43036, .T. ) ;
#44605=( BOUNDED_CURVE ( )  B_SPLINE_CURVE ( 2, ( #40583, #61999, #33544, #28227, #44498, #65902, #17733, #33877, #55341, #50091, #1821 ),
 .UNSPECIFIED., .F., .F. ) 
 B_SPLINE_CURVE_WITH_KNOTS ( ( 3, 2, 2, 2, 2, 3 ),
 ( 0.5108695652173792512, 0.5130434782608574995, 0.5152173913043356368, 0.5173913043478138851, 0.5195652173912920224, 0.5217391304347702707 ),
 .UNSPECIFIED. ) 
 CURVE ( )  GEOMETRIC_REPRESENTATION_ITEM ( )  RATIONAL_B_SPLINE_CURVE ( ( 1.000000000000272449, 0.9510565162948810825, 1.000000000000000000, 0.9510565162951535312, 1.000000000000000000, 0.9510565162951535312, 1.000000000000000000, 0.9510565162951535312, 1.000000000000000000, 0.9510565162954309759, 0.9999999999997225553 ) ) 
 REPRESENTATION_ITEM ( '' )  );
#44606=CARTESIAN_POINT ( 'NONE',  ( -110.7570736234661837, -5.598654528085801552, 7.705886871421367523 ) ) ;
#44615=CARTESIAN_POINT ( 'NONE',  ( -156.8050000000000068, -8.437984349512085203, 5.166775262442717831E-16 ) ) ;
#44617=CARTESIAN_POINT ( 'NONE',  ( -174.4449999999999932, 0.000000000000000000, 8.024999999999991473 ) ) ;
#44619=CARTESIAN_POINT ( 'NONE',  ( -155.8449999999999704, -7.632228543268599452, 2.479861379858951054 ) ) ;
#44625=CARTESIAN_POINT ( 'NONE',  ( -71.30499999999997840, 8.437984349512085203, -1.550032578732815448E-15 ) ) ;
#44628=CARTESIAN_POINT ( 'NONE',  ( -73.34499999999999886, 7.632228543268599452, -2.479861379858951942 ) ) ;
#44639=CARTESIAN_POINT ( 'NONE',  ( -120.4429263765338050, -1.166476076187852838E-15, -9.524999999999991473 ) ) ;
#44640=VECTOR ( 'NONE', #46133, 1000.000000000000000 ) ;
#44645=EDGE_CURVE ( 'NONE', #62912, #12986, #994, .T. ) ;
#44647=DIRECTION ( 'NONE',  ( -1.000000000000000000, -0.000000000000000000, -0.000000000000000000 ) ) ;
#44651=CARTESIAN_POINT ( 'NONE',  ( -108.9549999999999983, -7.632228543268599452, 2.479861379858951054 ) ) ;
#44670=CARTESIAN_POINT ( 'NONE',  ( -195.0000000000000000, 1.166476076187852838E-15, -9.524999999999991473 ) ) ;
#44681=CARTESIAN_POINT ( 'NONE',  ( -129.3549999999999898, -4.716976649647093289, -6.492361379858945902 ) ) ;
#44682=FACE_OUTER_BOUND ( 'NONE', #66943, .T. ) ;
#44687=CARTESIAN_POINT ( 'NONE',  ( -106.4929263765338021, -8.102448949553174629, 5.886773742842742685 ) ) ;
#44688=CARTESIAN_POINT ( 'NONE',  ( -108.0570736234661666, 0.000000000000000000, 9.524999999999991473 ) ) ;
#44695=CARTESIAN_POINT ( 'NONE',  ( -50.60499999999996845, 6.826472737025113702, -4.959722759717902107 ) ) ;
#44703=CARTESIAN_POINT ( 'NONE',  ( -182.9949999999999761, -6.826472737025113702, 4.959722759717902107 ) ) ;
#44712=CARTESIAN_POINT ( 'NONE',  ( -95.54499999999998749, -7.632228543268600340, -2.479861379858950166 ) ) ;
#44714=CARTESIAN_POINT ( 'NONE',  ( -80.84499999999998465, -7.632228543268599452, 2.479861379858951054 ) ) ;
#44722=CARTESIAN_POINT ( 'NONE',  ( -128.9929263765338305, 8.102448949553171076, -5.886773742842744461 ) ) ;
#44724=CARTESIAN_POINT ( 'NONE',  ( -140.0949999999999989, -2.607480562269071545, -8.024999999999991473 ) ) ;
#44727=CARTESIAN_POINT ( 'NONE',  ( -173.5429263765338135, 9.058813317711329915, 2.943386871421369566 ) ) ;
#44732=EDGE_CURVE ( 'NONE', #12986, #28296, #60663, .T. ) ;
#44739=CARTESIAN_POINT ( 'NONE',  ( -143.1549999999999727, 7.632228543268600340, 2.479861379858949277 ) ) ;
#44747=DIRECTION ( 'NONE',  ( -1.000000000000000000, -0.000000000000000000, -0.000000000000000000 ) ) ;
#44750=ORIENTED_EDGE ( 'NONE', *, *, #10624, .F. ) ;
#44753=CARTESIAN_POINT ( 'NONE',  ( -55.40499999999997272, -2.607480562269069768, 8.024999999999991473 ) ) ;
#44755=ORIENTED_EDGE ( 'NONE', *, *, #65927, .T. ) ;
#44760=VECTOR ( 'NONE', #41036, 1000.000000000000000 ) ;
#44767=CARTESIAN_POINT ( 'NONE',  ( -158.6050000000000182, 6.826472737025113702, -4.959722759717902107 ) ) ;
#44779=CARTESIAN_POINT ( 'NONE',  ( -74.90499999999997272, 2.607480562269068880, -8.024999999999993250 ) ) ;
#44787=CARTESIAN_POINT ( 'NONE',  ( -53.90707362346616094, -3.094860106618429807, 9.524999999999991473 ) ) ;
#44790=EDGE_CURVE ( 'NONE', #58402, #66309, #37833, .T. ) ;
#44792=CARTESIAN_POINT ( 'NONE',  ( -102.7449999999999903, 4.716976649647094177, 6.492361379858945902 ) ) ;
#44799=CARTESIAN_POINT ( 'NONE',  ( -149.9929263765338021, 8.102448949553171076, -5.886773742842744461 ) ) ;
#44800=CARTESIAN_POINT ( 'NONE',  ( -170.9950000000000330, -6.826472737025115478, 4.959722759717900331 ) ) ;
#44803=CARTESIAN_POINT ( 'NONE',  ( -195.0000000000000000, 0.000000000000000000, 0.000000000000000000 ) ) ;
#44806=CARTESIAN_POINT ( 'NONE',  ( -63.44292637653379785, -1.166476076187852838E-15, -9.524999999999991473 ) ) ;
#44810=CARTESIAN_POINT ( 'NONE',  ( -78.89292637653380780, -8.102448949553174629, -5.886773742842741797 ) ) ;
#44813=CARTESIAN_POINT ( 'NONE',  ( -174.2050000000000125, -2.607480562269071545, -8.024999999999991473 ) ) ;
#44826=CARTESIAN_POINT ( 'NONE',  ( -84.20499999999995566, -2.607480562269071545, -8.024999999999991473 ) ) ;
#44830=AXIS2_PLACEMENT_3D ( 'NONE', #47400, #64582, #36504 ) ;
#44833=CARTESIAN_POINT ( 'NONE',  ( -169.3429263765337964, -9.058813317711329915, 2.943386871421371787 ) ) ;
#44839=CARTESIAN_POINT ( 'NONE',  ( -52.04499999999998039, 7.632228543268600340, 2.479861379858949277 ) ) ;
#44843=CARTESIAN_POINT ( 'NONE',  ( -138.9570736234661865, 9.058813317711329915, -2.943386871421373119 ) ) ;
#44847=CARTESIAN_POINT ( 'NONE',  ( -58.19499999999999318, 8.437984349512086979, -1.550032578732815448E-15 ) ) ;
#44853=CARTESIAN_POINT ( 'NONE',  ( -113.6049999999999898, 6.826472737025113702, -4.959722759717902107 ) ) ;
#44857=CARTESIAN_POINT ( 'NONE',  ( -152.4570736234661581, -9.058813317711329915, 2.943386871421371787 ) ) ;
#44860=CARTESIAN_POINT ( 'NONE',  ( -87.05707362346618083, 0.000000000000000000, 9.524999999999991473 ) ) ;
#44867=CARTESIAN_POINT ( 'NONE',  ( -126.2049999999999841, -2.607480562269071545, -8.024999999999991473 ) ) ;
#44870=CARTESIAN_POINT ( 'NONE',  ( -137.0949999999999989, -2.607480562269071545, -8.024999999999991473 ) ) ;
#44872=CARTESIAN_POINT ( 'NONE',  ( -133.4950000000000045, 6.826472737025113702, -4.959722759717902107 ) ) ;
#44878=CARTESIAN_POINT ( 'NONE',  ( -135.4429263765338192, -1.166476076187852838E-15, -9.524999999999991473 ) ) ;
#44879=CARTESIAN_POINT ( 'NONE',  ( -179.2429263765338021, 5.598654528085804216, 7.705886871421366635 ) ) ;
#44880=( BOUNDED_CURVE ( )  B_SPLINE_CURVE ( 2, ( #44563, #34993, #65959, #8278, #17790, #33945, #55404, #25133, #19144, #62420, #14952 ),
 .UNSPECIFIED., .F., .F. ) 
 B_SPLINE_CURVE_WITH_KNOTS ( ( 3, 2, 2, 2, 2, 3 ),
 ( 0.1521739130434745513, 0.1543478260869527441, 0.1565217391304309924, 0.1586956521739091852, 0.1608695652173874058, 0.1630434782608656263 ),
 .UNSPECIFIED. ) 
 CURVE ( )  GEOMETRIC_REPRESENTATION_ITEM ( )  RATIONAL_B_SPLINE_CURVE ( ( 1.000000000000083711, 0.9510565162950698204, 1.000000000000000000, 0.9510565162951535312, 1.000000000000000000, 0.9510565162951535312, 1.000000000000000000, 0.9510565162951535312, 1.000000000000000000, 0.9510565162952422380, 0.9999999999999112932 ) ) 
 REPRESENTATION_ITEM ( '' )  );
#44882=CARTESIAN_POINT ( 'NONE',  ( -52.79499999999997328, 2.607480562269068880, -8.024999999999993250 ) ) ;
#44889=CARTESIAN_POINT ( 'NONE',  ( -97.19292637653379074, -10.01517768586948698, 6.132527647946031529E-16 ) ) ;
#44892=CARTESIAN_POINT ( 'NONE',  ( -162.9570736234661865, 9.058813317711329915, -2.943386871421373119 ) ) ;
#44901=ORIENTED_EDGE ( 'NONE', *, *, #218, .T. ) ;
#44902=DIRECTION ( 'NONE',  ( -1.000000000000000000, -0.000000000000000000, -0.000000000000000000 ) ) ;
#44919=CARTESIAN_POINT ( 'NONE',  ( -93.14499999999999602, -4.716976649647092401, 6.492361379858946790 ) ) ;
#44930=EDGE_CURVE ( 'NONE', #40311, #12077, #27754, .T. ) ;
#44931=ORIENTED_EDGE ( 'NONE', *, *, #63526, .F. ) ;
#44933=ORIENTED_EDGE ( 'NONE', *, *, #9635, .T. ) ;
#44938=CARTESIAN_POINT ( 'NONE',  ( -176.1570736234662036, -9.058813317711329915, -2.943386871421370898 ) ) ;
#44939=FACE_OUTER_BOUND ( 'NONE', #24987, .T. ) ;
#44940=TOROIDAL_SURFACE ( 'NONE', #14576, 9.525000000000000355, 1.000000000000000888 ) ;
#44941=CARTESIAN_POINT ( 'NONE',  ( -112.4070736234661894, 3.094860106618428031, -9.524999999999993250 ) ) ;
#44948=CARTESIAN_POINT ( 'NONE',  ( -162.2049999999999557, -2.607480562269071545, -8.024999999999991473 ) ) ;
#44951=CARTESIAN_POINT ( 'NONE',  ( -166.9450000000000216, -9.827790563157499189E-16, -8.024999999999991473 ) ) ;
#44952=CARTESIAN_POINT ( 'NONE',  ( -160.3449999999999989, 7.632228543268599452, -2.479861379858951942 ) ) ;
#44959=CARTESIAN_POINT ( 'NONE',  ( -76.25499999999999545, -4.716976649647092401, 6.492361379858946790 ) ) ;
#44962=CARTESIAN_POINT ( 'NONE',  ( -71.39499999999998181, -6.826472737025113702, -4.959722759717900331 ) ) ;
#44975=ORIENTED_EDGE ( 'NONE', *, *, #52033, .F. ) ;
#44978=CARTESIAN_POINT ( 'NONE',  ( -132.3570736234661922, 5.598654528085804216, 7.705886871421366635 ) ) ;
#44982=CARTESIAN_POINT ( 'NONE',  ( -195.0000000000000000, 0.000000000000000000, 9.524999999999991473 ) ) ;
#44988=CARTESIAN_POINT ( 'NONE',  ( -98.60499999999997556, 6.826472737025113702, -4.959722759717902107 ) ) ;
#44992=EDGE_CURVE ( 'NONE', #34254, #63927, #6336, .T. ) ;
#44994=CARTESIAN_POINT ( 'NONE',  ( -66.44292637653380496, -1.166476076187852838E-15, -9.524999999999991473 ) ) ;
#44999=CARTESIAN_POINT ( 'NONE',  ( -67.55707362346618083, -1.166476076187852838E-15, -9.524999999999991473 ) ) ;
#45001=CARTESIAN_POINT ( 'NONE',  ( -121.7949999999999875, 2.607480562269068880, -8.024999999999993250 ) ) ;
#45006=CARTESIAN_POINT ( 'NONE',  ( -10.44927233264747102, -11.81971797664088442, -2.077929409079531720 ) ) ;
#45023=CARTESIAN_POINT ( 'NONE',  ( -137.6049999999999329, 6.826472737025113702, -4.959722759717902107 ) ) ;
#45034=CARTESIAN_POINT ( 'NONE',  ( -52.25707362346618368, 5.598654528085800663, -7.705886871421367523 ) ) ;
#45037=CARTESIAN_POINT ( 'NONE',  ( -123.8070736234661666, 10.01517768586948698, -1.839758294383808966E-15 ) ) ;
#45039=FACE_OUTER_BOUND ( 'NONE', #32146, .T. ) ;
#45042=CARTESIAN_POINT ( 'NONE',  ( -181.7949999999999875, 2.607480562269069324, -8.024999999999993250 ) ) ;
#45046=ADVANCED_FACE ( 'NONE', ( #8198 ), #51807, .T. ) ;
#45052=CARTESIAN_POINT ( 'NONE',  ( -98.24499999999999034, -4.716976649647093289, -6.492361379858945902 ) ) ;
#45054=CARTESIAN_POINT ( 'NONE',  ( -75.89499999999998181, 6.826472737025116366, 4.959722759717898555 ) ) ;
#45063=CARTESIAN_POINT ( 'NONE',  ( -114.5929263765337822, -3.094860106618431139, -9.524999999999991473 ) ) ;
#45066=CARTESIAN_POINT ( 'NONE',  ( -137.0949999999999989, -2.607480562269071545, -8.024999999999991473 ) ) ;
#45077=CARTESIAN_POINT ( 'NONE',  ( -63.44292637653379785, -1.166476076187852838E-15, -9.524999999999991473 ) ) ;
#45081=CARTESIAN_POINT ( 'NONE',  ( -131.3070736234661524, -10.01517768586948698, 6.132527647946031529E-16 ) ) ;
#45086=CARTESIAN_POINT ( 'NONE',  ( -130.1049999999999898, -6.826472737025113702, 4.959722759717902107 ) ) ;
#45100=CARTESIAN_POINT ( 'NONE',  ( -56.60499999999998266, 6.826472737025113702, -4.959722759717902107 ) ) ;
#45109=ORIENTED_EDGE ( 'NONE', *, *, #48644, .T. ) ;
#45113=CARTESIAN_POINT ( 'NONE',  ( -160.8549999999999898, 4.716976649647094177, 6.492361379858945902 ) ) ;
#45124=CARTESIAN_POINT ( 'NONE',  ( -80.45499999999998408, 7.632228543268599452, -2.479861379858951942 ) ) ;
#45137=CARTESIAN_POINT ( 'NONE',  ( -110.0949999999999704, -2.607480562269071545, -8.024999999999991473 ) ) ;
#45143=CARTESIAN_POINT ( 'NONE',  ( -149.8429263765337964, 9.058813317711329915, -2.943386871421373119 ) ) ;
#45144=CARTESIAN_POINT ( 'NONE',  ( -168.4449999999999932, 0.000000000000000000, 8.024999999999991473 ) ) ;
#45149=EDGE_LOOP ( 'NONE', ( #8284, #48354, #21167, #47164, #42702 ) ) ;
#45161=CARTESIAN_POINT ( 'NONE',  ( -172.5549999999999784, 0.000000000000000000, 8.024999999999991473 ) ) ;
#45172=ORIENTED_EDGE ( 'NONE', *, *, #36989, .T. ) ;
#45174=CARTESIAN_POINT ( 'NONE',  ( -88.10499999999998977, -6.826472737025113702, 4.959722759717902107 ) ) ;
#45185=CARTESIAN_POINT ( 'NONE',  ( -56.99499999999999034, -6.826472737025115478, 4.959722759717900331 ) ) ;
#45190=CARTESIAN_POINT ( 'NONE',  ( -86.09292637653378222, 3.094860106618433360, 9.524999999999991473 ) ) ;
#45194=CARTESIAN_POINT ( 'NONE',  ( -51.74499999999998323, 4.716976649647094177, 6.492361379858945902 ) ) ;
#45199=CARTESIAN_POINT ( 'NONE',  ( -102.2049999999999983, -2.607480562269071545, -8.024999999999991473 ) ) ;
#45204=CARTESIAN_POINT ( 'NONE',  ( -151.1070736234661638, 8.102448949553171076, -5.886773742842744461 ) ) ;
#45208=CARTESIAN_POINT ( 'NONE',  ( -82.70707362346617231, -3.094860106618431139, -9.524999999999991473 ) ) ;
#45210=EDGE_LOOP ( 'NONE', ( #68142, #8866, #2854, #49062 ) ) ;
#45214=CARTESIAN_POINT ( 'NONE',  ( -125.1549999999999869, 7.632228543268600340, 2.479861379858949277 ) ) ;
#45218=CARTESIAN_POINT ( 'NONE',  ( -131.8449999999999989, -7.632228543268599452, 2.479861379858951054 ) ) ;
#45219=CARTESIAN_POINT ( 'NONE',  ( -131.0949999999999989, -2.607480562269071545, -8.024999999999991473 ) ) ;
#45226=CARTESIAN_POINT ( 'NONE',  ( -184.3429263765338249, -9.058813317711329915, 2.943386871421371787 ) ) ;
#45227=CARTESIAN_POINT ( 'NONE',  ( -48.59499999999997755, 2.607480562269073321, 8.024999999999991473 ) ) ;
#45228=EDGE_CURVE ( 'NONE', #62431, #23874, #42336, .T. ) ;
#45233=CARTESIAN_POINT ( 'NONE',  ( -92.24292637653380211, 5.598654528085804216, 7.705886871421366635 ) ) ;
#45265=VECTOR ( 'NONE', #60208, 1000.000000000000000 ) ;
#45268=CARTESIAN_POINT ( 'NONE',  ( -81.59499999999997044, 2.607480562269073321, 8.024999999999991473 ) ) ;
#45286=CARTESIAN_POINT ( 'NONE',  ( -174.9570736234661865, 9.058813317711329915, -2.943386871421373119 ) ) ;
#45289=CARTESIAN_POINT ( 'NONE',  ( -109.5570736234661666, -1.166476076187852838E-15, -9.524999999999991473 ) ) ;
#45298=CARTESIAN_POINT ( 'NONE',  ( -161.4549999999999841, 7.632228543268599452, -2.479861379858951942 ) ) ;
#45301=CARTESIAN_POINT ( 'NONE',  ( -165.2949999999999591, -2.607480562269069768, 8.024999999999991473 ) ) ;
#45303=CARTESIAN_POINT ( 'NONE',  ( -162.1449999999999818, -4.716976649647092401, 6.492361379858946790 ) ) ;
#45308=CARTESIAN_POINT ( 'NONE',  ( -123.2929263765345667, 3.094860106605588967, -9.525000000009322676 ) ) ;
#45309=CARTESIAN_POINT ( 'NONE',  ( -71.60499999999997556, 6.826472737025113702, -4.959722759717902107 ) ) ;
#45313=CARTESIAN_POINT ( 'NONE',  ( -70.94499999999997897, -9.827790563157499189E-16, -8.024999999999991473 ) ) ;
#45322=CARTESIAN_POINT ( 'NONE',  ( -159.5070736234661979, 8.102448949553176405, 5.886773742842740909 ) ) ;
#45329=AXIS2_PLACEMENT_3D ( 'NONE', #987, #53512, #28117 ) ;
#45336=CARTESIAN_POINT ( 'NONE',  ( -155.2429263765338021, 5.598654528085804216, 7.705886871421366635 ) ) ;
#45348=CARTESIAN_POINT ( 'NONE',  ( -84.05707362346618083, 0.000000000000000000, 9.524999999999991473 ) ) ;
#45349=DIRECTION ( 'NONE',  ( -1.000000000000000000, -0.000000000000000000, -0.000000000000000000 ) ) ;
#45350=CARTESIAN_POINT ( 'NONE',  ( -110.0949999999999704, -2.607480562269071545, -8.024999999999991473 ) ) ;
#45352=ORIENTED_EDGE ( 'NONE', *, *, #47735, .F. ) ;
#45356=CARTESIAN_POINT ( 'NONE',  ( -10.52052679316176587, -11.79239196812588553, -2.227343248702441159 ) ) ;
#45357=CARTESIAN_POINT ( 'NONE',  ( -180.8929263765338078, -8.102448949553174629, -5.886773742842741797 ) ) ;
#45361=CARTESIAN_POINT ( 'NONE',  ( -195.0000000000000000, 0.000000000000000000, 0.000000000000000000 ) ) ;
#45372=CARTESIAN_POINT ( 'NONE',  ( -129.9549999999999841, -7.632228543268599452, 2.479861379858951054 ) ) ;
#45375=FACE_OUTER_BOUND ( 'NONE', #59478, .T. ) ;
#45378=( NAMED_UNIT ( * ) SI_UNIT ( $, .STERADIAN. ) SOLID_ANGLE_UNIT ( ) );
#45392=CARTESIAN_POINT ( 'NONE',  ( -59.45707362346616520, -9.058813317711329915, 2.943386871421371787 ) ) ;
#45393=CIRCLE ( 'NONE', #19522, 7.499999999999984901 ) ;
#45399=CARTESIAN_POINT ( 'NONE',  ( -161.7570736234661695, -5.598654528085801552, 7.705886871421367523 ) ) ;
#45401=LINE ( 'NONE', #41151, #55132 ) ;
#45402=CARTESIAN_POINT ( 'NONE',  ( -98.15499999999998693, 7.632228543268600340, 2.479861379858949277 ) ) ;
#45408=CARTESIAN_POINT ( 'NONE',  ( -96.29499999999998749, -2.607480562269069768, 8.024999999999991473 ) ) ;
#45410=CARTESIAN_POINT ( 'NONE',  ( -74.09499999999998465, -2.607480562269071545, -8.024999999999991473 ) ) ;
#45417=CIRCLE ( 'NONE', #9429, 9.525000000000000355 ) ;
#45421=CARTESIAN_POINT ( 'NONE',  ( -111.4429263765338050, -1.166476076187852838E-15, -9.524999999999991473 ) ) ;
#45422=CARTESIAN_POINT ( 'NONE',  ( -137.2450000000000045, -4.716976649647093289, -6.492361379858945902 ) ) ;
#45437=CARTESIAN_POINT ( 'NONE',  ( -133.2549999999999955, -4.716976649647092401, 6.492361379858946790 ) ) ;
#45442=CARTESIAN_POINT ( 'NONE',  ( -84.29292637653381348, 3.094860106618428031, -9.524999999999993250 ) ) ;
#45452=CARTESIAN_POINT ( 'NONE',  ( -49.25499999999999545, -4.716976649647092401, 6.492361379858946790 ) ) ;
#45457=CARTESIAN_POINT ( 'NONE',  ( -88.04292637653379927, -9.058813317711329915, -2.943386871421370898 ) ) ;
#45466=CARTESIAN_POINT ( 'NONE',  ( -122.9070736234668999, -3.094860106606060590, 9.525000000008979839 ) ) ;
#45468=CARTESIAN_POINT ( 'NONE',  ( -162.5049999999999386, -6.826472737025115478, -4.959722759717899443 ) ) ;
#45469=ORIENTED_EDGE ( 'NONE', *, *, #69300, .F. ) ;
#45478=CARTESIAN_POINT ( 'NONE',  ( -76.10500000000000398, -6.826472737025115478, 4.959722759717900331 ) ) ;
#45496=CARTESIAN_POINT ( 'NONE',  ( -108.2949999999999733, -2.607480562269069768, 8.024999999999991473 ) ) ;
#45497=EDGE_CURVE ( 'NONE', #49292, #57697, #23804, .T. ) ;
#45501=CARTESIAN_POINT ( 'NONE',  ( -96.05707362346618083, 0.000000000000000000, 9.524999999999991473 ) ) ;
#45502=CARTESIAN_POINT ( 'NONE',  ( -19.48602968775583832, 11.79452023969822250, -2.232621730279843675 ) ) ;
#45505=CARTESIAN_POINT ( 'NONE',  ( -138.7429263765338021, -5.598654528085803328, -7.705886871421366635 ) ) ;
#45506=CARTESIAN_POINT ( 'NONE',  ( -167.0949999999999704, -2.607480562269071545, -8.024999999999991473 ) ) ;
#45514=VERTEX_POINT ( 'NONE', #32567 ) ;
#45519=EDGE_LOOP ( 'NONE', ( #27743, #42432, #57971, #67907 ) ) ;
#45520=CARTESIAN_POINT ( 'NONE',  ( -160.7049999999999841, 2.607480562269072433, 8.024999999999991473 ) ) ;
#45531=CARTESIAN_POINT ( 'NONE',  ( -73.10499999999997556, -6.826472737025113702, 4.959722759717902107 ) ) ;
#45541=CARTESIAN_POINT ( 'NONE',  ( -52.94499999999999318, -9.827790563157499189E-16, -8.024999999999991473 ) ) ;
#45547=ORIENTED_EDGE ( 'NONE', *, *, #10415, .F. ) ;
#45549=CARTESIAN_POINT ( 'NONE',  ( -50.39499999999999602, -6.826472737025113702, -4.959722759717900331 ) ) ;
#45551=ORIENTED_EDGE ( 'NONE', *, *, #32247, .T. ) ;
#45555=CARTESIAN_POINT ( 'NONE',  ( -107.0049999999999955, 6.826472737025116366, 4.959722759717898555 ) ) ;
#45561=CARTESIAN_POINT ( 'NONE',  ( -143.1570736234662036, -9.058813317711329915, -2.943386871421370898 ) ) ;
#45564=CARTESIAN_POINT ( 'NONE',  ( -80.00707362346618368, -8.102448949553172852, -5.886773742842741797 ) ) ;
#45570=CARTESIAN_POINT ( 'NONE',  ( -120.8049999999999784, -8.437984349512085203, 5.166775262442717831E-16 ) ) ;
#45573=CARTESIAN_POINT ( 'NONE',  ( -135.8949999999999818, 6.826472737025116366, 4.959722759717898555 ) ) ;
#45576=CARTESIAN_POINT ( 'NONE',  ( -116.6949999999999790, -8.437984349512086979, 5.166775262442717831E-16 ) ) ;
#45583=CARTESIAN_POINT ( 'NONE',  ( -171.1429263765338078, 5.598654528085800663, -7.705886871421367523 ) ) ;
#45585=CARTESIAN_POINT ( 'NONE',  ( -50.39499999999999602, -6.826472737025115478, -4.959722759717899443 ) ) ;
#45587=CARTESIAN_POINT ( 'NONE',  ( -195.0000000000000000, 1.166476076187852838E-15, -9.524999999999991473 ) ) ;
#45591=CARTESIAN_POINT ( 'NONE',  ( -97.04292637653379927, -9.058813317711329915, -2.943386871421370898 ) ) ;
#45600=CARTESIAN_POINT ( 'NONE',  ( -78.80707362346618083, 10.01517768586948698, -1.839758294383808966E-15 ) ) ;
#45607=CARTESIAN_POINT ( 'NONE',  ( -64.49292637653380211, -8.102448949553174629, 5.886773742842742685 ) ) ;
#45619=CARTESIAN_POINT ( 'NONE',  ( -80.84499999999998465, -7.632228543268599452, 2.479861379858951054 ) ) ;
#45633=FACE_OUTER_BOUND ( 'NONE', #22035, .T. ) ;
#45637=CARTESIAN_POINT ( 'NONE',  ( -166.5570736234661808, -1.166476076187852838E-15, -9.524999999999991473 ) ) ;
#45640=CARTESIAN_POINT ( 'NONE',  ( -115.5570736234661808, -1.166476076187852838E-15, -9.524999999999991473 ) ) ;
#45644=CARTESIAN_POINT ( 'NONE',  ( -84.65707362346616094, 9.058813317711329915, 2.943386871421369566 ) ) ;
#45649=CARTESIAN_POINT ( 'NONE',  ( -150.8050000000000068, -8.437984349512085203, 5.166775262442717831E-16 ) ) ;
#45652=CARTESIAN_POINT ( 'NONE',  ( -161.5449999999999875, -7.632228543268600340, -2.479861379858950166 ) ) ;
#45654=CARTESIAN_POINT ( 'NONE',  ( -151.9449999999999932, -9.827790563157499189E-16, -8.024999999999991473 ) ) ;
#45656=CARTESIAN_POINT ( 'NONE',  ( -66.74292637653380211, -5.598654528085803328, -7.705886871421366635 ) ) ;
#45658=CARTESIAN_POINT ( 'NONE',  ( -65.60499999999997556, 6.826472737025113702, -4.959722759717902107 ) ) ;
#45660=CARTESIAN_POINT ( 'NONE',  ( -154.4070736234665162, 3.094860106612512762, -9.525000000004292033 ) ) ;
#45661=CARTESIAN_POINT ( 'NONE',  ( -67.34499999999998465, 7.632228543268599452, -2.479861379858951942 ) ) ;
#45674=CARTESIAN_POINT ( 'NONE',  ( -118.9429263765338050, 0.000000000000000000, 9.524999999999991473 ) ) ;
#45677=ORIENTED_EDGE ( 'NONE', *, *, #60357, .F. ) ;
#45678=CARTESIAN_POINT ( 'NONE',  ( -156.4429263765338192, -1.166476076187852838E-15, -9.524999999999991473 ) ) ;
#45681=ORIENTED_EDGE ( 'NONE', *, *, #7630, .T. ) ;
#45685=CARTESIAN_POINT ( 'NONE',  ( -65.69292637653380496, 10.01517768586948698, -1.839758294383808966E-15 ) ) ;
#45691=CARTESIAN_POINT ( 'NONE',  ( -83.30707362346619504, -10.01517768586948698, 6.132527647946031529E-16 ) ) ;
#45693=CARTESIAN_POINT ( 'NONE',  ( -114.7449999999999903, 4.716976649647094177, 6.492361379858945902 ) ) ;
#45696=CARTESIAN_POINT ( 'NONE',  ( -183.2510368117331154, 0.000000000000000000, 8.774999999999991473 ) ) ;
#45697=CARTESIAN_POINT ( 'NONE',  ( -13.68947831298332218, -10.98244867573161443, -4.836413723188878855 ) ) ;
#45699=CARTESIAN_POINT ( 'NONE',  ( -179.7570736234661979, -5.598654528085801552, 7.705886871421367523 ) ) ;
#45714=CARTESIAN_POINT ( 'NONE',  ( -134.0049999999999955, 6.826472737025116366, 4.959722759717898555 ) ) ;
#45727=ORIENTED_EDGE ( 'NONE', *, *, #50588, .F. ) ;
#45729=CARTESIAN_POINT ( 'NONE',  ( -180.5049999999999670, -6.826472737025115478, -4.959722759717899443 ) ) ;
#45732=CARTESIAN_POINT ( 'NONE',  ( -59.60707362346616378, -8.102448949553172852, 5.886773742842742685 ) ) ;
#45738=CARTESIAN_POINT ( 'NONE',  ( -104.7549999999999812, 4.716976649647091513, -6.492361379858946790 ) ) ;
#45739=DIRECTION ( 'NONE',  ( -1.000000000000000000, -0.000000000000000000, -0.000000000000000000 ) ) ;
#45742=CARTESIAN_POINT ( 'NONE',  ( -102.8949999999999818, 6.826472737025115478, 4.959722759717899443 ) ) ;
#45745=CARTESIAN_POINT ( 'NONE',  ( -67.94499999999999318, -9.827790563157499189E-16, -8.024999999999991473 ) ) ;
#45749=DIRECTION ( 'NONE',  ( 0.000000000000000000, 0.000000000000000000, 1.000000000000000000 ) ) ;
#45751=CARTESIAN_POINT ( 'NONE',  ( -113.8429263765337964, 9.058813317711329915, -2.943386871421373119 ) ) ;
#45752=CARTESIAN_POINT ( 'NONE',  ( -137.8449999999999989, -7.632228543268599452, 2.479861379858951054 ) ) ;
#45762=CARTESIAN_POINT ( 'NONE',  ( -195.0000000000000000, 0.000000000000000000, 0.000000000000000000 ) ) ;
#45763=CARTESIAN_POINT ( 'NONE',  ( -127.2570736234661695, 5.598654528085800663, -7.705886871421367523 ) ) ;
#45765=CARTESIAN_POINT ( 'NONE',  ( -127.8549999999999898, 4.716976649647094177, 6.492361379858945902 ) ) ;
#45767=CARTESIAN_POINT ( 'NONE',  ( -127.1070736234661922, 8.102448949553171076, -5.886773742842744461 ) ) ;
#45769=CARTESIAN_POINT ( 'NONE',  ( -171.8929263765338078, -8.102448949553174629, -5.886773742842741797 ) ) ;
#45770=CARTESIAN_POINT ( 'NONE',  ( -84.14292637653379359, 5.598654528085800663, -7.705886871421367523 ) ) ;
#45795=CARTESIAN_POINT ( 'NONE',  ( -165.2050000000000125, -2.607480562269071545, -8.024999999999991473 ) ) ;
#45796=EDGE_CURVE ( 'NONE', #55073, #41299, #66546, .T. ) ;
#45800=ORIENTED_EDGE ( 'NONE', *, *, #18026, .F. ) ;
#45808=CARTESIAN_POINT ( 'NONE',  ( -74.75499999999998124, 4.716976649647091513, -6.492361379858946790 ) ) ;
#45818=CARTESIAN_POINT ( 'NONE',  ( -107.0949999999999847, -2.607480562269071545, -8.024999999999991473 ) ) ;
#45822=CARTESIAN_POINT ( 'NONE',  ( -71.84292637653381064, 9.058813317711329915, -2.943386871421373119 ) ) ;
#45824=CARTESIAN_POINT ( 'NONE',  ( -146.6929263765337623, 10.01517768586948698, -1.839758294383808571E-15 ) ) ;
#45826=CARTESIAN_POINT ( 'NONE',  ( -166.0449999999999875, 7.632228543268600340, 2.479861379858949277 ) ) ;
#45835=CYLINDRICAL_SURFACE ( 'NONE', #37190, 9.524999999999991473 ) ;
#45840=CARTESIAN_POINT ( 'NONE',  ( -162.2049999999999557, -2.607480562269071545, -8.024999999999991473 ) ) ;
#45851=CARTESIAN_POINT ( 'NONE',  ( -77.30499999999996419, 8.437984349512086979, -1.550032578732815448E-15 ) ) ;
#45861=VERTEX_POINT ( 'NONE', #16367 ) ;
#45863=CARTESIAN_POINT ( 'NONE',  ( -49.19499999999999318, 8.437984349512085203, -1.550032578732815448E-15 ) ) ;
#45871=CARTESIAN_POINT ( 'NONE',  ( -55.94499999999999318, -9.827790563157499189E-16, -8.024999999999991473 ) ) ;
#45877=CARTESIAN_POINT ( 'NONE',  ( -104.9049999999999869, 2.607480562269068880, -8.024999999999993250 ) ) ;
#45881=CARTESIAN_POINT ( 'NONE',  ( -141.9570736234661865, 9.058813317711329915, -2.943386871421373119 ) ) ;
#45885=CARTESIAN_POINT ( 'NONE',  ( -83.90707362346614673, -3.094860106618429807, 9.524999999999991473 ) ) ;
#45886=CARTESIAN_POINT ( 'NONE',  ( -92.99292637653380211, 8.102448949553172852, -5.886773742842744461 ) ) ;
#45891=CARTESIAN_POINT ( 'NONE',  ( -100.9429263765338050, 0.000000000000000000, 9.524999999999991473 ) ) ;
#45892=CARTESIAN_POINT ( 'NONE',  ( -119.0049999999999955, 6.826472737025116366, 4.959722759717898555 ) ) ;
#45893=CARTESIAN_POINT ( 'NONE',  ( -158.9929263765338021, 8.102448949553172852, -5.886773742842744461 ) ) ;
#45895=CARTESIAN_POINT ( 'NONE',  ( -137.8449999999999989, -7.632228543268599452, 2.479861379858951054 ) ) ;
#45896=CARTESIAN_POINT ( 'NONE',  ( -121.4949999999999761, 6.826472737025113702, -4.959722759717902107 ) ) ;
#45904=CARTESIAN_POINT ( 'NONE',  ( -174.5929263765337964, -3.094860106618431139, -9.524999999999991473 ) ) ;
#45905=CARTESIAN_POINT ( 'NONE',  ( -48.29499999999997328, -2.607480562269069768, 8.024999999999991473 ) ) ;
#45913=CARTESIAN_POINT ( 'NONE',  ( -86.69292637653380496, 10.01517768586948698, -1.839758294383808571E-15 ) ) ;
#45919=DIRECTION ( 'NONE',  ( 0.000000000000000000, 0.000000000000000000, 1.000000000000000000 ) ) ;
#45922=EDGE_CURVE ( 'NONE', #30865, #62777, #64268, .T. ) ;
#45925=ORIENTED_EDGE ( 'NONE', *, *, #61507, .F. ) ;
#45926=CARTESIAN_POINT ( 'NONE',  ( -106.9429263765337907, 0.000000000000000000, 9.524999999999991473 ) ) ;
#45933=EDGE_CURVE ( 'NONE', #12077, #64678, #30993, .T. ) ;
#45943=EDGE_CURVE ( 'NONE', #23561, #7596, #13521, .T. ) ;
#45945=CARTESIAN_POINT ( 'NONE',  ( -79.34499999999998465, 7.632228543268599452, -2.479861379858951942 ) ) ;
#45962=CARTESIAN_POINT ( 'NONE',  ( -171.3570736234661922, 5.598654528085804216, 7.705886871421366635 ) ) ;
#45966=CARTESIAN_POINT ( 'NONE',  ( -113.4570736234661723, -9.058813317711329915, 2.943386871421371787 ) ) ;
#45976=CARTESIAN_POINT ( 'NONE',  ( -154.7049999999999841, 2.607480562269073321, 8.024999999999991473 ) ) ;
#45977=CARTESIAN_POINT ( 'NONE',  ( -166.1949999999999932, 8.437984349512085203, -1.550032578732815448E-15 ) ) ;
#45979=CARTESIAN_POINT ( 'NONE',  ( -144.1449999999999818, -4.716976649647092401, 6.492361379858946790 ) ) ;
#45983=CARTESIAN_POINT ( 'NONE',  ( -66.59292637653379643, -3.094860106618431139, -9.524999999999991473 ) ) ;
#45986=CARTESIAN_POINT ( 'NONE',  ( -65.75499999999998124, 4.716976649647091513, -6.492361379858946790 ) ) ;
#45989=CARTESIAN_POINT ( 'NONE',  ( -65.84499999999998465, -7.632228543268599452, 2.479861379858951054 ) ) ;
#45991=CARTESIAN_POINT ( 'NONE',  ( -143.3070736234661524, -10.01517768586948698, 6.132527647946031529E-16 ) ) ;
#45995=PRODUCT_DEFINITION ( 'UNKNOWN', '', #31526, #64216 ) ;
#46023=ORIENTED_EDGE ( 'NONE', *, *, #24005, .F. ) ;
#46027=CARTESIAN_POINT ( 'NONE',  ( -65.99292637653378790, 8.102448949553172852, -5.886773742842744461 ) ) ;
#46028=CARTESIAN_POINT ( 'NONE',  ( -144.7429263765338021, -5.598654528085803328, -7.705886871421366635 ) ) ;
#46033=CARTESIAN_POINT ( 'NONE',  ( -112.4949999999999761, 6.826472737025113702, -4.959722759717902107 ) ) ;
#46037=CARTESIAN_POINT ( 'NONE',  ( -10.51797786690659109, -11.79336193633089636, 2.222196116146513134 ) ) ;
#46041=CYLINDRICAL_SURFACE ( 'NONE', #46768, 9.524999999999991473 ) ;
#46044=ORIENTED_EDGE ( 'NONE', *, *, #55680, .T. ) ;
#46049=DIRECTION ( 'NONE',  ( 0.000000000000000000, 0.000000000000000000, 1.000000000000000000 ) ) ;
#46050=CARTESIAN_POINT ( 'NONE',  ( -120.6549999999999869, -7.632228543268600340, -2.479861379858950166 ) ) ;
#46062=LINE ( 'NONE', #61838, #68030 ) ;
#46064=CARTESIAN_POINT ( 'NONE',  ( -47.75499999999999545, 4.716976649647091513, -6.492361379858946790 ) ) ;
#46066=CARTESIAN_POINT ( 'NONE',  ( -179.3049999999999784, 8.437984349512085203, -1.550032578732815448E-15 ) ) ;
#46069=CARTESIAN_POINT ( 'NONE',  ( -58.70707362346615810, -3.094860106618431139, -9.524999999999991473 ) ) ;
#46071=CARTESIAN_POINT ( 'NONE',  ( -180.1450000000000102, -4.716976649647092401, 6.492361379858946790 ) ) ;
#46076=CARTESIAN_POINT ( 'NONE',  ( -94.70499999999999829, 2.607480562269073321, 8.024999999999991473 ) ) ;
#46081=CARTESIAN_POINT ( 'NONE',  ( -93.59499999999997044, 2.607480562269072433, 8.024999999999991473 ) ) ;
#46083=CARTESIAN_POINT ( 'NONE',  ( -72.44499999999997897, 0.000000000000000000, 8.024999999999991473 ) ) ;
#46092=CARTESIAN_POINT ( 'NONE',  ( -112.1929263765338050, -10.01517768586948698, 6.132527647946031529E-16 ) ) ;
#46093=CARTESIAN_POINT ( 'NONE',  ( -129.4449999999999648, 0.000000000000000000, 8.024999999999991473 ) ) ;
#46098=CARTESIAN_POINT ( 'NONE',  ( -131.5429263765338135, 9.058813317711329915, 2.943386871421369566 ) ) ;
#46111=CARTESIAN_POINT ( 'NONE',  ( -127.5550000000000068, 0.000000000000000000, 8.024999999999991473 ) ) ;
#46114=CARTESIAN_POINT ( 'NONE',  ( -119.1570736234661751, -9.058813317711329915, -2.943386871421370898 ) ) ;
#46123=ORIENTED_EDGE ( 'NONE', *, *, #19914, .T. ) ;
#46133=DIRECTION ( 'NONE',  ( -1.000000000000000000, -0.000000000000000000, -0.000000000000000000 ) ) ;
#46140=PLANE ( 'NONE',  #6422 ) ;
#46142=CARTESIAN_POINT ( 'NONE',  ( -164.0049999999999955, 6.826472737025116366, 4.959722759717898555 ) ) ;
#46156=CARTESIAN_POINT ( 'NONE',  ( -78.50499999999996703, -6.826472737025115478, -4.959722759717899443 ) ) ;
#46161=CARTESIAN_POINT ( 'NONE',  ( -150.3570736234661638, 5.598654528085804216, 7.705886871421366635 ) ) ;
#46170=CARTESIAN_POINT ( 'NONE',  ( -94.19499999999999318, 8.437984349512085203, -1.550032578732815448E-15 ) ) ;
#46177=CARTESIAN_POINT ( 'NONE',  ( -96.95707362346617231, 9.058813317711329915, -2.943386871421373119 ) ) ;
#46179=CARTESIAN_POINT ( 'NONE',  ( -142.7929263765337851, -3.094860106618429807, 9.524999999999991473 ) ) ;
#46182=CARTESIAN_POINT ( 'NONE',  ( -158.0949999999999704, -2.607480562269071545, -8.024999999999991473 ) ) ;
#46202=CARTESIAN_POINT ( 'NONE',  ( -156.9549999999999841, -7.632228543268599452, 2.479861379858951054 ) ) ;
#46204=CARTESIAN_POINT ( 'NONE',  ( -46.25707362346617657, 5.598654528085800663, -7.705886871421367523 ) ) ;
#46207=CARTESIAN_POINT ( 'NONE',  ( -58.10707362346617799, 8.102448949553172852, -5.886773742842744461 ) ) ;
#46214=CARTESIAN_POINT ( 'NONE',  ( -71.30499999999997840, 8.437984349512086979, -1.550032578732815448E-15 ) ) ;
#46225=CARTESIAN_POINT ( 'NONE',  ( -184.0000000000000000, 0.000000000000000000, 0.000000000000000000 ) ) ;
#46227=CARTESIAN_POINT ( 'NONE',  ( -56.69499999999998607, -8.437984349512085203, 5.166775262442717831E-16 ) ) ;
#46239=CARTESIAN_POINT ( 'NONE',  ( -106.7049999999999983, 2.607480562269073321, 8.024999999999991473 ) ) ;
#46243=CARTESIAN_POINT ( 'NONE',  ( -142.4070736234661751, 3.094860106618428031, -9.524999999999993250 ) ) ;
#46246=CARTESIAN_POINT ( 'NONE',  ( -70.55707362346616662, -1.166476076187852838E-15, -9.524999999999991473 ) ) ;
#46252=CARTESIAN_POINT ( 'NONE',  ( -100.7929263765348509, -3.094860106600816341, 9.525000000012788348 ) ) ;
#46253=CARTESIAN_POINT ( 'NONE',  ( -116.9050000000000011, 2.607480562269068880, -8.024999999999993250 ) ) ;
#46255=CARTESIAN_POINT ( 'NONE',  ( -122.9950000000000045, -6.826472737025115478, 4.959722759717900331 ) ) ;
#46257=CARTESIAN_POINT ( 'NONE',  ( -116.3949999999999818, -6.826472737025113702, -4.959722759717900331 ) ) ;
#46266=VECTOR ( 'NONE', #33332, 1000.000000000000000 ) ;
#46267=CARTESIAN_POINT ( 'NONE',  ( -172.9429263765337907, 0.000000000000000000, 9.524999999999991473 ) ) ;
#46269=CARTESIAN_POINT ( 'NONE',  ( -52.49499999999999034, 6.826472737025113702, -4.959722759717902107 ) ) ;
#46280=CARTESIAN_POINT ( 'NONE',  ( -88.94292637653380496, 0.000000000000000000, 9.524999999999991473 ) ) ;
#46292=FACE_OUTER_BOUND ( 'NONE', #11312, .T. ) ;
#46297=CARTESIAN_POINT ( 'NONE',  ( -102.9549999999999841, -7.632228543268599452, 2.479861379858951054 ) ) ;
#46306=CARTESIAN_POINT ( 'NONE',  ( -79.79500000000000171, 2.607480562269068880, -8.024999999999993250 ) ) ;
#46321=CARTESIAN_POINT ( 'NONE',  ( -97.55707362346618083, -1.166476076187852838E-15, -9.524999999999991473 ) ) ;
#46325=CARTESIAN_POINT ( 'NONE',  ( -166.4070736234662036, 3.094860106618428031, -9.524999999999993250 ) ) ;
#46329=CARTESIAN_POINT ( 'NONE',  ( -105.5070736234661695, 8.102448949553176405, 5.886773742842740909 ) ) ;
#46333=ORIENTED_EDGE ( 'NONE', *, *, #29035, .F. ) ;
#46334=CARTESIAN_POINT ( 'NONE',  ( -82.49292637653378790, -8.102448949553174629, 5.886773742842742685 ) ) ;
#46337=CARTESIAN_POINT ( 'NONE',  ( -147.6549999999999727, -7.632228543268600340, -2.479861379858950166 ) ) ;
#46342=CARTESIAN_POINT ( 'NONE',  ( -169.1949999999999932, 8.437984349512085203, -1.550032578732815448E-15 ) ) ;
#46343=CARTESIAN_POINT ( 'NONE',  ( -144.2950000000000159, -2.607480562269069768, 8.024999999999991473 ) ) ;
#46344=( BOUNDED_CURVE ( )  B_SPLINE_CURVE ( 2, ( #32326, #11566, #64347, #63991, #48209, #53117, #58728, #48911, #54124, #68949, #33037 ),
 .UNSPECIFIED., .F., .F. ) 
 B_SPLINE_CURVE_WITH_KNOTS ( ( 3, 2, 2, 2, 2, 3 ),
 ( 0.3913043478260775365, 0.3934782608695557293, 0.3956521739130339221, 0.3978260869565121705, 0.3999999999999904188, 0.4021739130434686116 ),
 .UNSPECIFIED. ) 
 CURVE ( )  GEOMETRIC_REPRESENTATION_ITEM ( )  RATIONAL_B_SPLINE_CURVE ( ( 1.000000000000212497, 0.9510565162949410345, 1.000000000000000000, 0.9510565162951535312, 1.000000000000000000, 0.9510565162951535312, 1.000000000000000000, 0.9510565162951535312, 1.000000000000000000, 0.9510565162953710239, 0.9999999999997825073 ) ) 
 REPRESENTATION_ITEM ( '' )  );
#46349=CARTESIAN_POINT ( 'NONE',  ( -195.0000000000000000, 0.000000000000000000, 0.000000000000000000 ) ) ;
#46350=CARTESIAN_POINT ( 'NONE',  ( -63.50499999999998124, -6.826472737025115478, -4.959722759717899443 ) ) ;
#46353=CARTESIAN_POINT ( 'NONE',  ( -154.5570736234661808, -1.166476076187852838E-15, -9.524999999999991473 ) ) ;
#46354=CARTESIAN_POINT ( 'NONE',  ( -65.69499999999999318, -8.437984349512086979, 5.166775262442717831E-16 ) ) ;
#46386=CARTESIAN_POINT ( 'NONE',  ( -107.5449999999999875, -7.632228543268600340, -2.479861379858950166 ) ) ;
#46387=ORIENTED_EDGE ( 'NONE', *, *, #12073, .T. ) ;
#46392=VECTOR ( 'NONE', #27277, 1000.000000000000000 ) ;
#46393=CARTESIAN_POINT ( 'NONE',  ( -179.6070736234661638, -8.102448949553174629, 5.886773742842742685 ) ) ;
#46404=FACE_OUTER_BOUND ( 'NONE', #6186, .T. ) ;
#46407=CARTESIAN_POINT ( 'NONE',  ( -122.9049999999999727, 2.607480562269068880, -8.024999999999993250 ) ) ;
#46418=CARTESIAN_POINT ( 'NONE',  ( -109.9429263765338050, 0.000000000000000000, 9.524999999999991473 ) ) ;
#46424=CARTESIAN_POINT ( 'NONE',  ( -179.4550000000000125, 7.632228543268599452, -2.479861379858951942 ) ) ;
#46429=CARTESIAN_POINT ( 'NONE',  ( -56.45707362346616520, -9.058813317711329915, 2.943386871421371787 ) ) ;
#46431=CARTESIAN_POINT ( 'NONE',  ( -172.1949999999999648, 8.437984349512086979, -1.550032578732815448E-15 ) ) ;
#46433=AXIS2_PLACEMENT_3D ( 'NONE', #65480, #18346, #39827 ) ;
#46437=CARTESIAN_POINT ( 'NONE',  ( -93.05499999999997840, -9.827790563157499189E-16, -8.024999999999991473 ) ) ;
#46442=CARTESIAN_POINT ( 'NONE',  ( -87.89499999999996760, 6.826472737025115478, 4.959722759717899443 ) ) ;
#46444=CARTESIAN_POINT ( 'NONE',  ( -65.39499999999998181, -6.826472737025115478, -4.959722759717899443 ) ) ;
#46446=EDGE_CURVE ( 'NONE', #61370, #65704, #59317, .T. ) ;
#46449=( BOUNDED_CURVE ( )  B_SPLINE_CURVE ( 2, ( #68273, #52462, #14816, #31300, #36296, #30965, #3866, #52799, #63332, #4571, #20055 ),
 .UNSPECIFIED., .F., .F. ) 
 B_SPLINE_CURVE_WITH_KNOTS ( ( 3, 2, 2, 2, 2, 3 ),
 ( 0.8260869565217391353, 0.8282608695652173836, 0.8304347826086956319, 0.8326086956521738802, 0.8347826086956521285, 0.8369565217391304879 ),
 .UNSPECIFIED. ) 
 CURVE ( )  GEOMETRIC_REPRESENTATION_ITEM ( )  RATIONAL_B_SPLINE_CURVE ( ( 1.000000000000000000, 0.9510565162951535312, 1.000000000000000000, 0.9510565162951535312, 1.000000000000000000, 0.9510565162951535312, 1.000000000000000000, 0.9510565162951535312, 1.000000000000000000, 0.9510565162951535312, 1.000000000000000000 ) ) 
 REPRESENTATION_ITEM ( '' )  );
#46453=CARTESIAN_POINT ( 'NONE',  ( -118.7929263765338135, -3.094860106618429807, 9.524999999999991473 ) ) ;
#46455=CARTESIAN_POINT ( 'NONE',  ( -131.3949999999999818, -6.826472737025115478, -4.959722759717899443 ) ) ;
#46469=CARTESIAN_POINT ( 'NONE',  ( -134.0049999999999955, 6.826472737025115478, 4.959722759717899443 ) ) ;
#46472=CARTESIAN_POINT ( 'NONE',  ( -119.4570736234661723, -9.058813317711329915, 2.943386871421371787 ) ) ;
#46499=CARTESIAN_POINT ( 'NONE',  ( -55.79292637653379217, -3.094860106618429807, 9.524999999999991473 ) ) ;
#46502=CARTESIAN_POINT ( 'NONE',  ( -152.6050000000000182, 6.826472737025113702, -4.959722759717902107 ) ) ;
#46511=EDGE_LOOP ( 'NONE', ( #16818, #1883, #5637, #29130 ) ) ;
#46518=CARTESIAN_POINT ( 'NONE',  ( -68.90499999999997272, 2.607480562269068880, -8.024999999999993250 ) ) ;
#46535=CARTESIAN_POINT ( 'NONE',  ( -94.64499999999999602, 4.716976649647091513, -6.492361379858946790 ) ) ;
#46536=AXIS2_PLACEMENT_3D ( 'NONE', #54053, #1225, #43565 ) ;
#46541=CARTESIAN_POINT ( 'NONE',  ( -148.1929263765337907, -10.01517768586948698, 6.132527647946031529E-16 ) ) ;
#46545=CARTESIAN_POINT ( 'NONE',  ( -161.5449999999999875, -7.632228543268600340, -2.479861379858950166 ) ) ;
#46563=CARTESIAN_POINT ( 'NONE',  ( -160.1049999999999613, -6.826472737025113702, 4.959722759717902107 ) ) ;
#46575=CARTESIAN_POINT ( 'NONE',  ( -78.05499999999997840, -9.827790563157499189E-16, -8.024999999999991473 ) ) ;
#46588=CARTESIAN_POINT ( 'NONE',  ( -159.4429263765338192, -1.166476076187852838E-15, -9.524999999999991473 ) ) ;
#46589=CARTESIAN_POINT ( 'NONE',  ( -183.2050000000000125, -2.607480562269071545, -8.024999999999991473 ) ) ;
#46606=CARTESIAN_POINT ( 'NONE',  ( -107.7549999999999955, 4.716976649647091513, -6.492361379858946790 ) ) ;
#46610=CARTESIAN_POINT ( 'NONE',  ( -142.8570736234661638, -5.598654528085803328, -7.705886871421366635 ) ) ;
#46612=CARTESIAN_POINT ( 'NONE',  ( -75.05707362346616662, 0.000000000000000000, 9.524999999999991473 ) ) ;
#46617=CARTESIAN_POINT ( 'NONE',  ( -17.22738557021654415, -11.12983653794787742, -4.488350797354065946 ) ) ;
#46622=CARTESIAN_POINT ( 'NONE',  ( -124.5549999999999926, 0.000000000000000000, 8.024999999999991473 ) ) ;
#46625=CARTESIAN_POINT ( 'NONE',  ( -130.7950000000000159, 2.607480562269068880, -8.024999999999993250 ) ) ;
#46631=CARTESIAN_POINT ( 'NONE',  ( -176.8429263765338249, 9.058813317711329915, -2.943386871421373119 ) ) ;
#46639=CARTESIAN_POINT ( 'NONE',  ( -82.49292637653378790, -8.102448949553172852, 5.886773742842742685 ) ) ;
#46647=CARTESIAN_POINT ( 'NONE',  ( -156.6570736234661751, 9.058813317711329915, 2.943386871421369566 ) ) ;
#46660=CARTESIAN_POINT ( 'NONE',  ( -103.7049999999999983, 2.607480562269072433, 8.024999999999991473 ) ) ;
#46662=ORIENTED_EDGE ( 'NONE', *, *, #35986, .T. ) ;
#46671=CARTESIAN_POINT ( 'NONE',  ( -80.54499999999998749, -7.632228543268600340, -2.479861379858950166 ) ) ;
#46682=ADVANCED_FACE ( 'NONE', ( #69211 ), #36550, .T. ) ;
#46691=CARTESIAN_POINT ( 'NONE',  ( -172.2570736234661695, 5.598654528085800663, -7.705886871421367523 ) ) ;
#46694=CARTESIAN_POINT ( 'NONE',  ( -102.6570736234661751, 9.058813317711329915, 2.943386871421369566 ) ) ;
#46700=CARTESIAN_POINT ( 'NONE',  ( -105.9570736234661865, 9.058813317711329915, -2.943386871421373119 ) ) ;
#46702=CARTESIAN_POINT ( 'NONE',  ( -60.59292637653378932, -3.094860106618431139, -9.524999999999991473 ) ) ;
#46704=CARTESIAN_POINT ( 'NONE',  ( -154.2549999999999955, -4.716976649647092401, 6.492361379858946790 ) ) ;
#46707=CARTESIAN_POINT ( 'NONE',  ( -155.8449999999999704, -7.632228543268599452, 2.479861379858951054 ) ) ;
#46708=CARTESIAN_POINT ( 'NONE',  ( -151.3449999999999989, 7.632228543268599452, -2.479861379858951942 ) ) ;
#46715=CARTESIAN_POINT ( 'NONE',  ( -62.75499999999998835, 4.716976649647091513, -6.492361379858946790 ) ) ;
#46719=CARTESIAN_POINT ( 'NONE',  ( -61.04499999999998749, 7.632228543268600340, 2.479861379858949277 ) ) ;
#46726=LINE ( 'NONE', #68136, #64127 ) ;
#46741=CARTESIAN_POINT ( 'NONE',  ( -43.99999999999998579, 0.000000000000000000, 0.000000000000000000 ) ) ;
#46746=ORIENTED_EDGE ( 'NONE', *, *, #57361, .F. ) ;
#46752=CARTESIAN_POINT ( 'NONE',  ( -108.2949999999999733, -2.607480562269069768, 8.024999999999991473 ) ) ;
#46768=AXIS2_PLACEMENT_3D ( 'NONE', #45361, #56554, #66780 ) ;
#46773=CARTESIAN_POINT ( 'NONE',  ( -125.4549999999999841, 7.632228543268599452, -2.479861379858951942 ) ) ;
#46774=CARTESIAN_POINT ( 'NONE',  ( -184.0000000000000000, 0.000000000000000000, 8.024999999999991473 ) ) ;
#46778=CARTESIAN_POINT ( 'NONE',  ( -124.9429263765338192, 0.000000000000000000, 9.524999999999991473 ) ) ;
#46790=CARTESIAN_POINT ( 'NONE',  ( -175.2549999999999955, -4.716976649647092401, 6.492361379858946790 ) ) ;
#46793=CARTESIAN_POINT ( 'NONE',  ( -50.60707362346615668, -8.102448949553172852, 5.886773742842742685 ) ) ;
#46795=CARTESIAN_POINT ( 'NONE',  ( -179.0949999999999704, -2.607480562269071545, -8.024999999999991473 ) ) ;
#46801=CARTESIAN_POINT ( 'NONE',  ( -95.30499999999997840, 8.437984349512085203, -1.550032578732815448E-15 ) ) ;
#46805=CARTESIAN_POINT ( 'NONE',  ( -92.84499999999998465, -7.632228543268599452, 2.479861379858951054 ) ) ;
#46807=CARTESIAN_POINT ( 'NONE',  ( -71.24499999999999034, -4.716976649647093289, -6.492361379858945902 ) ) ;
#46817=CARTESIAN_POINT ( 'NONE',  ( -108.2929263765337851, 3.094860106618428031, -9.524999999999993250 ) ) ;
#46818=CARTESIAN_POINT ( 'NONE',  ( -132.1449999999999818, -4.716976649647092401, 6.492361379858946790 ) ) ;
#46830=DIRECTION ( 'NONE',  ( -1.000000000000000000, -0.000000000000000000, -0.000000000000000000 ) ) ;
#46832=CARTESIAN_POINT ( 'NONE',  ( -118.7049999999999841, 2.607480562269072433, 8.024999999999991473 ) ) ;
#46836=CARTESIAN_POINT ( 'NONE',  ( -127.4070736234661751, 3.094860106618428031, -9.524999999999993250 ) ) ;
#46860=CARTESIAN_POINT ( 'NONE',  ( -57.14292637653378648, 5.598654528085800663, -7.705886871421367523 ) ) ;
#46863=CARTESIAN_POINT ( 'NONE',  ( -153.8049999999999784, -8.437984349512085203, 5.166775262442717831E-16 ) ) ;
#46876=CARTESIAN_POINT ( 'NONE',  ( -62.15499999999998693, 7.632228543268600340, 2.479861379858949277 ) ) ;
#46884=( BOUNDED_CURVE ( )  B_SPLINE_CURVE ( 2, ( #27025, #58374, #48559, #52773, #58727, #31637, #26355, #47893, #15496, #4548, #20758 ),
 .UNSPECIFIED., .F., .F. ) 
 B_SPLINE_CURVE_WITH_KNOTS ( ( 3, 2, 2, 2, 2, 3 ),
 ( 0.3369565217391226053, 0.3391304347826007426, 0.3413043478260789354, 0.3434782608695571282, 0.3456521739130353210, 0.3478260869565134583 ),
 .UNSPECIFIED. ) 
 CURVE ( )  GEOMETRIC_REPRESENTATION_ITEM ( )  RATIONAL_B_SPLINE_CURVE ( ( 1.000000000000176303, 0.9510565162949773388, 1.000000000000000000, 0.9510565162951535312, 1.000000000000000000, 0.9510565162951535312, 1.000000000000000000, 0.9510565162951535312, 1.000000000000000000, 0.9510565162953397156, 0.9999999999998138156 ) ) 
 REPRESENTATION_ITEM ( '' )  );
#46890=CARTESIAN_POINT ( 'NONE',  ( -96.14499999999999602, -4.716976649647092401, 6.492361379858946790 ) ) ;
#46896=CARTESIAN_POINT ( 'NONE',  ( -131.2429263765338021, 5.598654528085804216, 7.705886871421366635 ) ) ;
#46897=CARTESIAN_POINT ( 'NONE',  ( -155.5449999999999875, -7.632228543268600340, -2.479861379858950166 ) ) ;
#46899=CARTESIAN_POINT ( 'NONE',  ( -133.3429263765337964, -9.058813317711329915, 2.943386871421371787 ) ) ;
#46907=CARTESIAN_POINT ( 'NONE',  ( -173.0070736234661695, -8.102448949553174629, -5.886773742842741797 ) ) ;
#46909=ORIENTED_EDGE ( 'NONE', *, *, #39903, .F. ) ;
#46910=CARTESIAN_POINT ( 'NONE',  ( -164.6049999999999613, 6.826472737025113702, -4.959722759717902107 ) ) ;
#46917=CARTESIAN_POINT ( 'NONE',  ( -58.55707362346616662, -1.166476076187852838E-15, -9.524999999999991473 ) ) ;
#46923=CARTESIAN_POINT ( 'NONE',  ( -69.80499999999997840, -8.437984349512086979, 5.166775262442717831E-16 ) ) ;
#46937=CARTESIAN_POINT ( 'NONE',  ( -177.6550000000000011, -7.632228543268600340, -2.479861379858950166 ) ) ;
#46938=ORIENTED_EDGE ( 'NONE', *, *, #14636, .T. ) ;
#46945=ORIENTED_EDGE ( 'NONE', *, *, #19217, .T. ) ;
#46947=CARTESIAN_POINT ( 'NONE',  ( -91.85499999999998977, 4.716976649647094177, 6.492361379858945902 ) ) ;
#46950=CARTESIAN_POINT ( 'NONE',  ( -139.5570736234661808, -1.166476076187852838E-15, -9.524999999999991473 ) ) ;
#46954=CARTESIAN_POINT ( 'NONE',  ( -73.25707362346616947, 5.598654528085800663, -7.705886871421367523 ) ) ;
#46961=CARTESIAN_POINT ( 'NONE',  ( -107.7549999999999955, 4.716976649647091513, -6.492361379858946790 ) ) ;
#46965=CARTESIAN_POINT ( 'NONE',  ( -128.5449999999999875, -7.632228543268600340, -2.479861379858950166 ) ) ;
#46970=CARTESIAN_POINT ( 'NONE',  ( -172.7929263765337851, -3.094860106618429807, 9.524999999999991473 ) ) ;
#46979=CARTESIAN_POINT ( 'NONE',  ( -81.44292637653380496, -1.166476076187852838E-15, -9.524999999999991473 ) ) ;
#46997=CARTESIAN_POINT ( 'NONE',  ( -105.0549999999999926, -9.827790563157499189E-16, -8.024999999999991473 ) ) ;
#47008=CARTESIAN_POINT ( 'NONE',  ( -75.29500000000000171, -2.607480562269069768, 8.024999999999991473 ) ) ;
#47023=CARTESIAN_POINT ( 'NONE',  ( -45.00000000000000000, 0.000000000000000000, 0.000000000000000000 ) ) ;
#47024=CARTESIAN_POINT ( 'NONE',  ( -165.8070736234661524, 10.01517768586948698, -1.839758294383808571E-15 ) ) ;
#47027=CARTESIAN_POINT ( 'NONE',  ( -106.7070736234661865, -3.094860106618431139, -9.524999999999991473 ) ) ;
#47033=CARTESIAN_POINT ( 'NONE',  ( -114.9570736234661723, 9.058813317711329915, -2.943386871421373119 ) ) ;
#47035=CARTESIAN_POINT ( 'NONE',  ( -148.4050000000000296, -2.607480562269069768, 8.024999999999991473 ) ) ;
#47037=CARTESIAN_POINT ( 'NONE',  ( -155.5449999999999875, -7.632228543268600340, -2.479861379858950166 ) ) ;
#47039=CARTESIAN_POINT ( 'NONE',  ( -149.6949999999999648, -8.437984349512086979, 5.166775262442717831E-16 ) ) ;
#47044=CYLINDRICAL_SURFACE ( 'NONE', #32708, 7.499999999999985789 ) ;
#47045=CARTESIAN_POINT ( 'NONE',  ( -59.00499999999998124, 6.826472737025116366, 4.959722759717898555 ) ) ;
#47046=CARTESIAN_POINT ( 'NONE',  ( -59.24499999999999034, -4.716976649647093289, -6.492361379858945902 ) ) ;
#47067=DIRECTION ( 'NONE',  ( -1.000000000000000000, -0.000000000000000000, -0.000000000000000000 ) ) ;
#47071=ADVANCED_FACE ( 'NONE', ( #50028 ), #59503, .T. ) ;
#47078=CARTESIAN_POINT ( 'NONE',  ( -96.74499999999999034, 4.716976649647094177, 6.492361379858945902 ) ) ;
#47084=ORIENTED_EDGE ( 'NONE', *, *, #9816, .T. ) ;
#47091=CARTESIAN_POINT ( 'NONE',  ( -62.00707362346617657, -8.102448949553174629, -5.886773742842741797 ) ) ;
#47095=DIRECTION ( 'NONE',  ( -1.000000000000000000, -0.000000000000000000, -0.000000000000000000 ) ) ;
#47097=CARTESIAN_POINT ( 'NONE',  ( -121.2549999999999812, -4.716976649647092401, 6.492361379858946790 ) ) ;
#47098=CARTESIAN_POINT ( 'NONE',  ( -184.0000000000000284, -7.203081035975417379, 3.559358198943581630 ) ) ;
#47110=CARTESIAN_POINT ( 'NONE',  ( -182.6929263765338192, 10.01517768586948698, -1.839758294383808966E-15 ) ) ;
#47114=CARTESIAN_POINT ( 'NONE',  ( -181.1049999999999898, -6.826472737025115478, 4.959722759717900331 ) ) ;
#47117=CARTESIAN_POINT ( 'NONE',  ( -46.40707362346616094, 3.094860106618428031, -9.524999999999993250 ) ) ;
#47118=CARTESIAN_POINT ( 'NONE',  ( -173.9949999999999761, -6.826472737025113702, 4.959722759717902107 ) ) ;
#47121=CARTESIAN_POINT ( 'NONE',  ( -14.33318179684024862, 10.92439180899981999, 4.966154840202036347 ) ) ;
#47122=CARTESIAN_POINT ( 'NONE',  ( -94.55499999999999261, 0.000000000000000000, 8.024999999999991473 ) ) ;
#47126=CARTESIAN_POINT ( 'NONE',  ( -87.44499999999999318, 0.000000000000000000, 8.024999999999991473 ) ) ;
#47128=CARTESIAN_POINT ( 'NONE',  ( -73.19499999999999318, 8.437984349512085203, -1.550032578732815448E-15 ) ) ;
#47134=AXIS2_PLACEMENT_3D ( 'NONE', #13177, #55046, #45919 ) ;
#47138=CARTESIAN_POINT ( 'NONE',  ( -48.14292637653380780, 5.598654528085800663, -7.705886871421367523 ) ) ;
#47139=EDGE_CURVE ( 'NONE', #40144, #24888, #66626, .T. ) ;
#47141=CARTESIAN_POINT ( 'NONE',  ( -103.0429263765337993, -9.058813317711329915, -2.943386871421370898 ) ) ;
#47142=( BOUNDED_CURVE ( )  B_SPLINE_CURVE ( 2, ( #18265, #61171, #34439, #2732, #41140, #42208, #68196, #47474, #20696, #19281, #40787 ),
 .UNSPECIFIED., .F., .F. ) 
 B_SPLINE_CURVE_WITH_KNOTS ( ( 3, 2, 2, 2, 2, 3 ),
 ( 0.6739130434782448775, 0.6760869565217263455, 0.6782608695652078135, 0.6804347826086891704, 0.6826086956521706384, 0.6847826086956522174 ),
 .UNSPECIFIED. ) 
 CURVE ( )  GEOMETRIC_REPRESENTATION_ITEM ( )  RATIONAL_B_SPLINE_CURVE ( ( 1.000000000000359934, 0.9510565162947935969, 1.000000000000000000, 0.9510565162951535312, 1.000000000000000000, 0.9510565162951535312, 1.000000000000000000, 0.9510565162951535312, 1.000000000000000000, 0.9510565162951535312, 1.000000000000000000 ) ) 
 REPRESENTATION_ITEM ( '' )  );
#47143=CARTESIAN_POINT ( 'NONE',  ( -130.7950000000000159, 2.607480562269068880, -8.024999999999993250 ) ) ;
#47149=CARTESIAN_POINT ( 'NONE',  ( -43.99999999999999289, 1.166476076187854022E-15, -9.525000000000000355 ) ) ;
#47163=CARTESIAN_POINT ( 'NONE',  ( -123.0549999999999926, -9.827790563157499189E-16, -8.024999999999991473 ) ) ;
#47164=ORIENTED_EDGE ( 'NONE', *, *, #29335, .F. ) ;
#47166=CARTESIAN_POINT ( 'NONE',  ( -122.9070736234661609, -3.094860106618429807, 9.524999999999991473 ) ) ;
#47183=CARTESIAN_POINT ( 'NONE',  ( -47.30707362346616662, -10.01517768586948698, 6.132527647946031529E-16 ) ) ;
#47190=CARTESIAN_POINT ( 'NONE',  ( -60.44292637653379785, -1.166476076187852838E-15, -9.524999999999991473 ) ) ;
#47194=CARTESIAN_POINT ( 'NONE',  ( -152.9049999999999727, 2.607480562269068880, -8.024999999999993250 ) ) ;
#47207=CARTESIAN_POINT ( 'NONE',  ( -65.90499999999998693, 2.607480562269068880, -8.024999999999993250 ) ) ;
#47212=CARTESIAN_POINT ( 'NONE',  ( -124.1929263765338192, -10.01517768586948698, 6.132527647946031529E-16 ) ) ;
#47222=CARTESIAN_POINT ( 'NONE',  ( -95.39499999999999602, -6.826472737025115478, -4.959722759717899443 ) ) ;
#47230=CARTESIAN_POINT ( 'NONE',  ( -130.6429263765338078, -5.598654528085801552, 7.705886871421367523 ) ) ;
#47233=CARTESIAN_POINT ( 'NONE',  ( -161.2450000000000045, -4.716976649647093289, -6.492361379858945902 ) ) ;
#47235=CARTESIAN_POINT ( 'NONE',  ( -51.14292637653380780, 5.598654528085800663, -7.705886871421367523 ) ) ;
#47242=CARTESIAN_POINT ( 'NONE',  ( -70.94292637653380496, 0.000000000000000000, 9.524999999999991473 ) ) ;
#47251=CARTESIAN_POINT ( 'NONE',  ( -150.6549999999999727, -7.632228543268600340, -2.479861379858950166 ) ) ;
#47261=VERTEX_POINT ( 'NONE', #42286 ) ;
#47263=CARTESIAN_POINT ( 'NONE',  ( -67.40499999999997272, -2.607480562269069768, 8.024999999999991473 ) ) ;
#47276=CARTESIAN_POINT ( 'NONE',  ( -180.2049999999999841, -2.607480562269071545, -8.024999999999991473 ) ) ;
#47279=( BOUNDED_CURVE ( )  B_SPLINE_CURVE ( 2, ( #40074, #61462, #24191, #61805, #35099, #29819, #52682, #24880, #41109, #20667, #57962 ),
 .UNSPECIFIED., .F., .F. ) 
 B_SPLINE_CURVE_WITH_KNOTS ( ( 3, 2, 2, 2, 2, 3 ),
 ( 0.9456521739130434590, 0.9478260869565217073, 0.9499999999999999556, 0.9521739130434783149, 0.9543478260869565633, 0.9565217391304348116 ),
 .UNSPECIFIED. ) 
 CURVE ( )  GEOMETRIC_REPRESENTATION_ITEM ( )  RATIONAL_B_SPLINE_CURVE ( ( 1.000000000000000000, 0.9510565162951535312, 1.000000000000000000, 0.9510565162951535312, 1.000000000000000000, 0.9510565162951535312, 1.000000000000000000, 0.9510565162951535312, 1.000000000000000000, 0.9510565162951535312, 1.000000000000000000 ) ) 
 REPRESENTATION_ITEM ( '' )  );
#47285=CARTESIAN_POINT ( 'NONE',  ( -94.70499999999999829, 2.607480562269073321, 8.024999999999991473 ) ) ;
#47289=CARTESIAN_POINT ( 'NONE',  ( -129.0570736234661808, 0.000000000000000000, 9.524999999999991473 ) ) ;
#47293=CARTESIAN_POINT ( 'NONE',  ( -74.75707362346616947, -5.598654528085801552, 7.705886871421367523 ) ) ;
#47294=EDGE_CURVE ( 'NONE', #52329, #62435, #45417, .T. ) ;
#47296=CARTESIAN_POINT ( 'NONE',  ( -92.24292637653380211, 5.598654528085804216, 7.705886871421366635 ) ) ;
#47300=CARTESIAN_POINT ( 'NONE',  ( -19.74219527431328203, -11.89431361296820988, -1.618896920497846059 ) ) ;
#47303=CARTESIAN_POINT ( 'NONE',  ( -108.9549999999999983, -7.632228543268599452, 2.479861379858951054 ) ) ;
#47307=CARTESIAN_POINT ( 'NONE',  ( -125.5449999999999875, -7.632228543268600340, -2.479861379858950166 ) ) ;
#47315=CARTESIAN_POINT ( 'NONE',  ( -165.1429263765338078, 5.598654528085800663, -7.705886871421367523 ) ) ;
#47320=CARTESIAN_POINT ( 'NONE',  ( -159.0570736234661808, 0.000000000000000000, 9.524999999999991473 ) ) ;
#47323=CARTESIAN_POINT ( 'NONE',  ( -90.44292637653379074, -1.166476076187852838E-15, -9.524999999999991473 ) ) ;
#47324=CYLINDRICAL_SURFACE ( 'NONE', #3708, 9.524999999999991473 ) ;
#47330=CARTESIAN_POINT ( 'NONE',  ( -183.9772050269406236, -7.512949680700584665, 2.846963971517519010 ) ) ;
#47336=CARTESIAN_POINT ( 'NONE',  ( -110.3929263765337936, 8.102448949553176405, 5.886773742842740909 ) ) ;
#47342=CARTESIAN_POINT ( 'NONE',  ( -104.3049999999999784, 8.437984349512086979, -1.550032578732815448E-15 ) ) ;
#47345=ORIENTED_EDGE ( 'NONE', *, *, #26438, .F. ) ;
#47351=CARTESIAN_POINT ( 'NONE',  ( -71.54499999999998749, -7.632228543268600340, -2.479861379858950166 ) ) ;
#47355=CARTESIAN_POINT ( 'NONE',  ( -120.5070736234661553, 8.102448949553176405, 5.886773742842740909 ) ) ;
#47356=CARTESIAN_POINT ( 'NONE',  ( -125.7570736234661695, -5.598654528085801552, 7.705886871421367523 ) ) ;
#47358=DIRECTION ( 'NONE',  ( 0.000000000000000000, 0.000000000000000000, -1.000000000000000000 ) ) ;
#47359=CARTESIAN_POINT ( 'NONE',  ( -175.9429263765337907, 0.000000000000000000, 9.524999999999991473 ) ) ;
#47365=DIRECTION ( 'NONE',  ( 0.000000000000000000, 0.000000000000000000, -1.000000000000000000 ) ) ;
#47368=CARTESIAN_POINT ( 'NONE',  ( -158.7570736234661979, -5.598654528085801552, 7.705886871421367523 ) ) ;
#47370=CARTESIAN_POINT ( 'NONE',  ( -99.80707362346616662, 10.01517768586948698, -1.839758294383808571E-15 ) ) ;
#47377=CYLINDRICAL_SURFACE ( 'NONE', #3622, 9.524999999999991473 ) ;
#47384=CARTESIAN_POINT ( 'NONE',  ( -144.2050000000000125, -2.607480562269071545, -8.024999999999991473 ) ) ;
#47388=CARTESIAN_POINT ( 'NONE',  ( -151.1950000000000216, 8.437984349512085203, -1.550032578732815448E-15 ) ) ;
#47389=CARTESIAN_POINT ( 'NONE',  ( -135.7450000000000045, 4.716976649647094177, 6.492361379858945902 ) ) ;
#47396=CARTESIAN_POINT ( 'NONE',  ( -50.60499999999996845, 6.826472737025113702, -4.959722759717902107 ) ) ;
#47398=EDGE_CURVE ( 'NONE', #9325, #61370, #4062, .T. ) ;
#47400=CARTESIAN_POINT ( 'NONE',  ( -195.0000000000000000, 0.000000000000000000, 0.000000000000000000 ) ) ;
#47409=CARTESIAN_POINT ( 'NONE',  ( -89.60707362346616378, -8.102448949553174629, 5.886773742842742685 ) ) ;
#47411=STYLED_ITEM ( 'NONE', ( #5599 ), #28116 ) ;
#47426=CARTESIAN_POINT ( 'NONE',  ( -77.75707362346618368, -5.598654528085801552, 7.705886871421367523 ) ) ;
#47439=CARTESIAN_POINT ( 'NONE',  ( -105.2949999999999875, -2.607480562269069768, 8.024999999999991473 ) ) ;
#47443=CARTESIAN_POINT ( 'NONE',  ( -164.0070736234661695, -8.102448949553174629, -5.886773742842741797 ) ) ;
#47464=CARTESIAN_POINT ( 'NONE',  ( -195.0000000000000000, 1.166476076187852838E-15, -9.524999999999991473 ) ) ;
#47470=CARTESIAN_POINT ( 'NONE',  ( -195.0000000000000000, 0.000000000000000000, 0.000000000000000000 ) ) ;
#47473=CARTESIAN_POINT ( 'NONE',  ( -172.4050000000000296, -2.607480562269069768, 8.024999999999991473 ) ) ;
#47474=CARTESIAN_POINT ( 'NONE',  ( -90.89292637653380780, -8.102448949553174629, -5.886773742842741797 ) ) ;
#47476=CARTESIAN_POINT ( 'NONE',  ( -182.2450000000000045, -4.716976649647093289, -6.492361379858945902 ) ) ;
#47478=CARTESIAN_POINT ( 'NONE',  ( -177.2950000000000159, -2.607480562269069768, 8.024999999999991473 ) ) ;
#47481=AXIS2_PLACEMENT_3D ( 'NONE', #50644, #2023, #23548 ) ;
#47483=CARTESIAN_POINT ( 'NONE',  ( -96.20499999999996987, -2.607480562269071545, -8.024999999999991473 ) ) ;
#47489=CARTESIAN_POINT ( 'NONE',  ( -93.74499999999999034, 4.716976649647094177, 6.492361379858945902 ) ) ;
#47491=CARTESIAN_POINT ( 'NONE',  ( -56.84499999999997755, -7.632228543268599452, 2.479861379858951054 ) ) ;
#47494=CARTESIAN_POINT ( 'NONE',  ( -170.0929263765340238, 3.094860106621441176, 9.524999999997808331 ) ) ;
#47497=CARTESIAN_POINT ( 'NONE',  ( -195.0000000000000000, 0.000000000000000000, 0.000000000000000000 ) ) ;
#47520=CARTESIAN_POINT ( 'NONE',  ( -117.5049999999999670, -6.826472737025113702, -4.959722759717900331 ) ) ;
#47550=CARTESIAN_POINT ( 'NONE',  ( -56.69292637653379785, 10.01517768586948698, -1.839758294383808571E-15 ) ) ;
#47553=CARTESIAN_POINT ( 'NONE',  ( -153.9550000000000125, -7.632228543268599452, 2.479861379858951054 ) ) ;
#47567=ORIENTED_EDGE ( 'NONE', *, *, #44732, .F. ) ;
#47571=CARTESIAN_POINT ( 'NONE',  ( -63.35499999999998266, -4.716976649647093289, -6.492361379858945902 ) ) ;
#47576=ADVANCED_FACE ( 'NONE', ( #23870 ), #40777, .T. ) ;
#47578=CARTESIAN_POINT ( 'NONE',  ( -90.65707362346617515, 9.058813317711329915, 2.943386871421369566 ) ) ;
#47580=ORIENTED_EDGE ( 'NONE', *, *, #7350, .F. ) ;
#47583=CYLINDRICAL_SURFACE ( 'NONE', #2718, 9.524999999999991473 ) ;
#47587=CARTESIAN_POINT ( 'NONE',  ( -117.1449999999999818, -4.716976649647092401, 6.492361379858946790 ) ) ;
#47589=CARTESIAN_POINT ( 'NONE',  ( -96.89499999999998181, 6.826472737025116366, 4.959722759717898555 ) ) ;
#47597=CARTESIAN_POINT ( 'NONE',  ( -131.6929263765338192, 10.01517768586948698, -1.839758294383808571E-15 ) ) ;
#47599=CARTESIAN_POINT ( 'NONE',  ( -160.6449999999999818, 4.716976649647091513, -6.492361379858946790 ) ) ;
#47608=CARTESIAN_POINT ( 'NONE',  ( -143.9929263765337737, 8.102448949553172852, -5.886773742842744461 ) ) ;
#47610=CARTESIAN_POINT ( 'NONE',  ( -129.0570736234661808, 0.000000000000000000, 9.524999999999991473 ) ) ;
#47613=CARTESIAN_POINT ( 'NONE',  ( -150.2049999999999841, -2.607480562269071545, -8.024999999999991473 ) ) ;
#47616=LINE ( 'NONE', #53192, #32364 ) ;
#47626=CARTESIAN_POINT ( 'NONE',  ( -62.60499999999998266, 6.826472737025113702, -4.959722759717902107 ) ) ;
#47639=CARTESIAN_POINT ( 'NONE',  ( -47.54499999999997328, -7.632228543268600340, -2.479861379858950166 ) ) ;
#47647=VERTEX_POINT ( 'NONE', #30167 ) ;
#47649=CARTESIAN_POINT ( 'NONE',  ( -132.0570736234661808, 0.000000000000000000, 9.524999999999991473 ) ) ;
#47652=CARTESIAN_POINT ( 'NONE',  ( -92.15499999999998693, 7.632228543268600340, 2.479861379858949277 ) ) ;
#47654=ORIENTED_EDGE ( 'NONE', *, *, #5529, .T. ) ;
#47656=EDGE_CURVE ( 'NONE', #62435, #56584, #41129, .T. ) ;
#47658=CARTESIAN_POINT ( 'NONE',  ( -132.9570736234661865, 9.058813317711329915, -2.943386871421373119 ) ) ;
#47662=CARTESIAN_POINT ( 'NONE',  ( -68.75707362346616947, -5.598654528085801552, 7.705886871421367523 ) ) ;
#47671=CARTESIAN_POINT ( 'NONE',  ( -110.7549999999999955, 4.716976649647091513, -6.492361379858946790 ) ) ;
#47674=CARTESIAN_POINT ( 'NONE',  ( -129.7450000000000045, 4.716976649647094177, 6.492361379858945902 ) ) ;
#47680=CARTESIAN_POINT ( 'NONE',  ( -163.4929263765338305, -8.102448949553172852, 5.886773742842742685 ) ) ;
#47681=PRESENTATION_STYLE_ASSIGNMENT (( #5044 ) ) ;
#47689=CARTESIAN_POINT ( 'NONE',  ( -73.49292637653380211, -8.102448949553172852, 5.886773742842742685 ) ) ;
#47697=CARTESIAN_POINT ( 'NONE',  ( -174.9550000000000125, -7.632228543268599452, 2.479861379858951054 ) ) ;
#47711=CARTESIAN_POINT ( 'NONE',  ( -89.75499999999998124, 4.716976649647091513, -6.492361379858946790 ) ) ;
#47725=CARTESIAN_POINT ( 'NONE',  ( -70.49499999999996191, 6.826472737025113702, -4.959722759717902107 ) ) ;
#47735=EDGE_CURVE ( 'NONE', #62777, #64020, #27874, .T. ) ;
#47747=CARTESIAN_POINT ( 'NONE',  ( -156.6570736234661751, 9.058813317711329915, 2.943386871421369566 ) ) ;
#47749=CARTESIAN_POINT ( 'NONE',  ( -101.6070736234661780, -8.102448949553172852, 5.886773742842742685 ) ) ;
#47750=EDGE_CURVE ( 'NONE', #40082, #36469, #53043, .T. ) ;
#47757=CARTESIAN_POINT ( 'NONE',  ( -140.0049999999999386, 6.826472737025116366, 4.959722759717898555 ) ) ;
#47758=CARTESIAN_POINT ( 'NONE',  ( -86.75707362346616947, -5.598654528085801552, 7.705886871421367523 ) ) ;
#47760=CARTESIAN_POINT ( 'NONE',  ( -150.1450000000000102, -4.716976649647092401, 6.492361379858946790 ) ) ;
#47761=CARTESIAN_POINT ( 'NONE',  ( -142.1949999999999932, 8.437984349512086979, -1.550032578732815448E-15 ) ) ;
#47767=CARTESIAN_POINT ( 'NONE',  ( -57.65499999999998693, -7.632228543268600340, -2.479861379858950166 ) ) ;
#47802=CARTESIAN_POINT ( 'NONE',  ( -103.3449999999999989, 7.632228543268599452, -2.479861379858951942 ) ) ;
#47818=DIRECTION ( 'NONE',  ( -1.000000000000000000, -0.000000000000000000, -0.000000000000000000 ) ) ;
#47832=CARTESIAN_POINT ( 'NONE',  ( -170.3070736234661524, -10.01517768586948698, 6.132527647946031529E-16 ) ) ;
#47837=CARTESIAN_POINT ( 'NONE',  ( -170.9049999999999727, 2.607480562269068880, -8.024999999999993250 ) ) ;
#47839=EDGE_CURVE ( 'NONE', #56906, #58710, #38230, .T. ) ;
#47841=CARTESIAN_POINT ( 'NONE',  ( -47.30707362346615952, -10.01517768586948698, 6.132527647946031529E-16 ) ) ;
#47844=CARTESIAN_POINT ( 'NONE',  ( -171.5949999999999704, 2.607480562269072433, 8.024999999999991473 ) ) ;
#47848=CARTESIAN_POINT ( 'NONE',  ( -12.77386173820650583, 11.13265356232346903, -4.480059943853192728 ) ) ;
#47849=CARTESIAN_POINT ( 'NONE',  ( -81.35499999999998977, -4.716976649647093289, -6.492361379858945902 ) ) ;
#47854=CARTESIAN_POINT ( 'NONE',  ( -82.34499999999998465, 7.632228543268599452, -2.479861379858951942 ) ) ;
#47874=EDGE_CURVE ( 'NONE', #54371, #65805, #3324, .T. ) ;
#47879=CARTESIAN_POINT ( 'NONE',  ( -125.1549999999999869, 7.632228543268600340, 2.479861379858949277 ) ) ;
#47880=ORIENTED_EDGE ( 'NONE', *, *, #12073, .F. ) ;
#47882=CARTESIAN_POINT ( 'NONE',  ( -137.4570736234661865, -9.058813317711329915, 2.943386871421371787 ) ) ;
#47886=VERTEX_POINT ( 'NONE', #56851 ) ;
#47893=CARTESIAN_POINT ( 'NONE',  ( -135.5070736234661695, 8.102448949553176405, 5.886773742842740909 ) ) ;
#47894=CARTESIAN_POINT ( 'NONE',  ( -181.6429263765338078, -5.598654528085801552, 7.705886871421367523 ) ) ;
#47906=CARTESIAN_POINT ( 'NONE',  ( -53.69292637653380496, 10.01517768586948698, -1.839758294383808571E-15 ) ) ;
#47908=CARTESIAN_POINT ( 'NONE',  ( -150.5049999999999955, -6.826472737025115478, -4.959722759717899443 ) ) ;
#47909=CARTESIAN_POINT ( 'NONE',  ( -176.4570736234661865, -9.058813317711329915, 2.943386871421371787 ) ) ;
#47919=CARTESIAN_POINT ( 'NONE',  ( -65.00499999999998124, 6.826472737025116366, 4.959722759717898555 ) ) ;
#47932=CARTESIAN_POINT ( 'NONE',  ( -122.0949999999999847, -2.607480562269071545, -8.024999999999991473 ) ) ;
#47934=CARTESIAN_POINT ( 'NONE',  ( -88.64499999999998181, 4.716976649647091513, -6.492361379858946790 ) ) ;
#47936=AXIS2_PLACEMENT_3D ( 'NONE', #31030, #25752, #63734 ) ;
#47942=CARTESIAN_POINT ( 'NONE',  ( -130.0429263765338135, -9.058813317711329915, -2.943386871421370898 ) ) ;
#47945=CARTESIAN_POINT ( 'NONE',  ( -150.4449999999999932, 0.000000000000000000, 8.024999999999991473 ) ) ;
#47950=ORIENTED_EDGE ( 'NONE', *, *, #29370, .F. ) ;
#47956=CARTESIAN_POINT ( 'NONE',  ( -130.5570736234661808, -1.166476076187852838E-15, -9.524999999999991473 ) ) ;
#47958=CARTESIAN_POINT ( 'NONE',  ( -153.2049999999999841, -2.607480562269071545, -8.024999999999991473 ) ) ;
#47962=CARTESIAN_POINT ( 'NONE',  ( -141.5070736234661410, 8.102448949553176405, 5.886773742842740909 ) ) ;
#47966=EDGE_CURVE ( 'NONE', #62912, #50010, #60739, .T. ) ;
#47974=CARTESIAN_POINT ( 'NONE',  ( -61.55499999999998550, 0.000000000000000000, 8.024999999999991473 ) ) ;
#47975=CARTESIAN_POINT ( 'NONE',  ( -117.5949999999999989, 2.607480562269073321, 8.024999999999991473 ) ) ;
#47985=CARTESIAN_POINT ( 'NONE',  ( -46.25707362346617657, 5.598654528085800663, -7.705886871421367523 ) ) ;
#47986=CARTESIAN_POINT ( 'NONE',  ( -182.0049999999999670, 6.826472737025116366, 4.959722759717898555 ) ) ;
#47997=CARTESIAN_POINT ( 'NONE',  ( -90.65499999999998693, -7.632228543268600340, -2.479861379858950166 ) ) ;
#48000=CARTESIAN_POINT ( 'NONE',  ( -133.1070736234661922, 8.102448949553171076, -5.886773742842744461 ) ) ;
#48002=CARTESIAN_POINT ( 'NONE',  ( -67.40707362346614673, 3.094860106618428031, -9.524999999999993250 ) ) ;
#48009=CARTESIAN_POINT ( 'NONE',  ( -108.6549999999999869, -7.632228543268600340, -2.479861379858950166 ) ) ;
#48011=CARTESIAN_POINT ( 'NONE',  ( -116.3949999999999960, -6.826472737025115478, -4.959722759717899443 ) ) ;
#48012=( BOUNDED_CURVE ( )  B_SPLINE_CURVE ( 2, ( #1205, #44235, #65637, #38949, #28317, #60349, #44579, #33621, #1563, #59295, #12500 ),
 .UNSPECIFIED., .F., .F. ) 
 B_SPLINE_CURVE_WITH_KNOTS ( ( 3, 2, 2, 2, 2, 3 ),
 ( 0.6413043478260719299, 0.6434782608695501782, 0.6456521739130284265, 0.6478260869565066749, 0.6499999999999848121, 0.6521739130434630605 ),
 .UNSPECIFIED. ) 
 CURVE ( )  GEOMETRIC_REPRESENTATION_ITEM ( )  RATIONAL_B_SPLINE_CURVE ( ( 1.000000000000337508, 0.9510565162948161344, 1.000000000000000000, 0.9510565162951535312, 1.000000000000000000, 0.9510565162951535312, 1.000000000000000000, 0.9510565162951535312, 1.000000000000000000, 0.9510565162954959240, 0.9999999999996576072 ) ) 
 REPRESENTATION_ITEM ( '' )  );
#48014=ORIENTED_EDGE ( 'NONE', *, *, #39836, .T. ) ;
#48015=CARTESIAN_POINT ( 'NONE',  ( -165.7429263765338305, -5.598654528085803328, -7.705886871421366635 ) ) ;
#48024=CARTESIAN_POINT ( 'NONE',  ( -72.59292637653379643, -3.094860106618431139, -9.524999999999991473 ) ) ;
#48031=CARTESIAN_POINT ( 'NONE',  ( -179.3049999999999784, 8.437984349512086979, -1.550032578732815448E-15 ) ) ;
#48032=ORIENTED_EDGE ( 'NONE', *, *, #38574, .F. ) ;
#48043=CARTESIAN_POINT ( 'NONE',  ( -95.15499999999998693, 7.632228543268600340, 2.479861379858949277 ) ) ;
#48052=CARTESIAN_POINT ( 'NONE',  ( -73.34499999999999886, 7.632228543268599452, -2.479861379858951942 ) ) ;
#48055=CARTESIAN_POINT ( 'NONE',  ( -120.6570736234661751, 9.058813317711329915, 2.943386871421369566 ) ) ;
#48068=CARTESIAN_POINT ( 'NONE',  ( -155.9070736234662036, -3.094860106618429807, 9.524999999999991473 ) ) ;
#48071=CARTESIAN_POINT ( 'NONE',  ( -90.05707362346616662, 0.000000000000000000, 9.524999999999991473 ) ) ;
#48074=VERTEX_POINT ( 'NONE', #53092 ) ;
#48078=CARTESIAN_POINT ( 'NONE',  ( -85.55707362346618083, -1.166476076187852838E-15, -9.524999999999991473 ) ) ;
#48080=CARTESIAN_POINT ( 'NONE',  ( -143.7549999999999955, 4.716976649647091513, -6.492361379858946790 ) ) ;
#48082=CARTESIAN_POINT ( 'NONE',  ( -154.1949999999999648, 8.437984349512085203, -1.550032578732815448E-15 ) ) ;
#48083=CARTESIAN_POINT ( 'NONE',  ( -137.2450000000000045, -4.716976649647093289, -6.492361379858945902 ) ) ;
#48089=CARTESIAN_POINT ( 'NONE',  ( -54.50499999999998835, -6.826472737025115478, -4.959722759717899443 ) ) ;
#48107=VECTOR ( 'NONE', #8351, 1000.000000000000000 ) ;
#48114=VERTEX_POINT ( 'NONE', #55494 ) ;
#48115=CARTESIAN_POINT ( 'NONE',  ( -109.1070736234661780, 8.102448949553172852, -5.886773742842744461 ) ) ;
#48120=CARTESIAN_POINT ( 'NONE',  ( -85.49292637653380211, -8.102448949553174629, 5.886773742842742685 ) ) ;
#48123=CARTESIAN_POINT ( 'NONE',  ( -98.39499999999999602, -6.826472737025115478, -4.959722759717899443 ) ) ;
#48152=CARTESIAN_POINT ( 'NONE',  ( -164.7549999999999955, 4.716976649647091513, -6.492361379858946790 ) ) ;
#48155=CARTESIAN_POINT ( 'NONE',  ( -179.6949999999999932, -8.437984349512085203, 5.166775262442717831E-16 ) ) ;
#48156=CARTESIAN_POINT ( 'NONE',  ( -164.8449999999999989, -7.632228543268599452, 2.479861379858951054 ) ) ;
#48163=CARTESIAN_POINT ( 'NONE',  ( -85.10499999999997556, -6.826472737025115478, 4.959722759717900331 ) ) ;
#48164=DIRECTION ( 'NONE',  ( -1.000000000000000000, -0.000000000000000000, -0.000000000000000000 ) ) ;
#48168=CARTESIAN_POINT ( 'NONE',  ( -80.09499999999998465, -2.607480562269071545, -8.024999999999991473 ) ) ;
#48172=CARTESIAN_POINT ( 'NONE',  ( -170.9929263765338021, 8.102448949553172852, -5.886773742842744461 ) ) ;
#48175=CARTESIAN_POINT ( 'NONE',  ( -75.14292637653380780, 5.598654528085800663, -7.705886871421367523 ) ) ;
#48185=ORIENTED_EDGE ( 'NONE', *, *, #34768, .F. ) ;
#48187=CARTESIAN_POINT ( 'NONE',  ( -134.8429263765337964, 9.058813317711329915, -2.943386871421373119 ) ) ;
#48196=CARTESIAN_POINT ( 'NONE',  ( -119.6049999999999756, 6.826472737025113702, -4.959722759717902107 ) ) ;
#48198=CARTESIAN_POINT ( 'NONE',  ( -136.8570736234661638, -5.598654528085803328, -7.705886871421366635 ) ) ;
#48209=CARTESIAN_POINT ( 'NONE',  ( -130.3429263765337964, -9.058813317711329915, 2.943386871421371787 ) ) ;
#48221=CARTESIAN_POINT ( 'NONE',  ( -142.2549999999999955, -4.716976649647092401, 6.492361379858946790 ) ) ;
#48233=CARTESIAN_POINT ( 'NONE',  ( -57.50499999999997414, -6.826472737025115478, -4.959722759717899443 ) ) ;
#48247=CARTESIAN_POINT ( 'NONE',  ( -110.8449999999999847, -7.632228543268599452, 2.479861379858951054 ) ) ;
#48249=CARTESIAN_POINT ( 'NONE',  ( -88.34499999999999886, 7.632228543268599452, -2.479861379858951942 ) ) ;
#48258=CARTESIAN_POINT ( 'NONE',  ( -138.5929263765338249, -3.094860106618431139, -9.524999999999991473 ) ) ;
#48259=CARTESIAN_POINT ( 'NONE',  ( -145.7950000000000443, 2.607480562269068880, -8.024999999999993250 ) ) ;
#48262=CARTESIAN_POINT ( 'NONE',  ( -66.05707362346618083, 0.000000000000000000, 9.524999999999991473 ) ) ;
#48264=ORIENTED_EDGE ( 'NONE', *, *, #52231, .T. ) ;
#48270=CARTESIAN_POINT ( 'NONE',  ( -130.4070736234668573, 3.094860106607471018, -9.525000000007956658 ) ) ;
#48273=CARTESIAN_POINT ( 'NONE',  ( -147.9550000000000125, -7.632228543268599452, 2.479861379858951054 ) ) ;
#48281=EDGE_CURVE ( 'NONE', #26061, #68565, #39649, .T. ) ;
#48282=DIRECTION ( 'NONE',  ( 1.000000000000000000, 0.000000000000000000, 0.000000000000000000 ) ) ;
#48287=( BOUNDED_CURVE ( )  B_SPLINE_CURVE ( 2, ( #11897, #43953, #33358, #11546, #33017, #54786, #65369, #42927, #6597, #53763, #28039 ),
 .UNSPECIFIED., .F., .F. ) 
 B_SPLINE_CURVE_WITH_KNOTS ( ( 3, 2, 2, 2, 2, 3 ),
 ( 0.8152173913043477826, 0.8173913043478261420, 0.8195652173913043903, 0.8217391304347826386, 0.8239130434782608869, 0.8260869565217391353 ),
 .UNSPECIFIED. ) 
 CURVE ( )  GEOMETRIC_REPRESENTATION_ITEM ( )  RATIONAL_B_SPLINE_CURVE ( ( 1.000000000000000000, 0.9510565162951535312, 1.000000000000000000, 0.9510565162951535312, 1.000000000000000000, 0.9510565162951535312, 1.000000000000000000, 0.9510565162951535312, 1.000000000000000000, 0.9510565162951535312, 1.000000000000000000 ) ) 
 REPRESENTATION_ITEM ( '' )  );
#48291=CARTESIAN_POINT ( 'NONE',  ( -63.65499999999998693, -7.632228543268600340, -2.479861379858950166 ) ) ;
#48292=CARTESIAN_POINT ( 'NONE',  ( -117.1449999999999818, -4.716976649647092401, 6.492361379858946790 ) ) ;
#48306=CARTESIAN_POINT ( 'NONE',  ( -169.4049999999999727, -2.607480562269069768, 8.024999999999991473 ) ) ;
#48318=CARTESIAN_POINT ( 'NONE',  ( -95.60499999999998977, 6.826472737025113702, -4.959722759717902107 ) ) ;
#48320=CARTESIAN_POINT ( 'NONE',  ( -46.64499999999998892, 4.716976649647091513, -6.492361379858946790 ) ) ;
#48322=CARTESIAN_POINT ( 'NONE',  ( -134.4570736234661865, -9.058813317711329915, 2.943386871421371787 ) ) ;
#48327=CARTESIAN_POINT ( 'NONE',  ( -68.45707362346617231, -9.058813317711329915, 2.943386871421371787 ) ) ;
#48334=CARTESIAN_POINT ( 'NONE',  ( -108.2049999999999983, -2.607480562269071545, -8.024999999999991473 ) ) ;
#48337=CARTESIAN_POINT ( 'NONE',  ( -112.9449999999999932, -9.827790563157499189E-16, -8.024999999999991473 ) ) ;
#48341=AXIS2_PLACEMENT_3D ( 'NONE', #17302, #39795, #39447 ) ;
#48345=CARTESIAN_POINT ( 'NONE',  ( -164.9929263765338305, 8.102448949553171076, -5.886773742842744461 ) ) ;
#48346=CARTESIAN_POINT ( 'NONE',  ( -181.0449999999999875, 7.632228543268600340, 2.479861379858949277 ) ) ;
#48354=ORIENTED_EDGE ( 'NONE', *, *, #54378, .T. ) ;
#48355=CARTESIAN_POINT ( 'NONE',  ( -72.44292637653379074, -1.166476076187852838E-15, -9.524999999999991473 ) ) ;
#48364=CARTESIAN_POINT ( 'NONE',  ( -182.3049999999999784, 8.437984349512086979, -1.550032578732815448E-15 ) ) ;
#48366=CARTESIAN_POINT ( 'NONE',  ( -195.0000000000000000, 0.000000000000000000, 0.000000000000000000 ) ) ;
#48375=CARTESIAN_POINT ( 'NONE',  ( -96.05499999999999261, -9.827790563157499189E-16, -8.024999999999991473 ) ) ;
#48386=CARTESIAN_POINT ( 'NONE',  ( -75.89499999999998181, 6.826472737025116366, 4.959722759717898555 ) ) ;
#48397=CARTESIAN_POINT ( 'NONE',  ( -127.7049999999999699, 2.607480562269073321, 8.024999999999991473 ) ) ;
#48400=CIRCLE ( 'NONE', #33735, 1.000000000000000888 ) ;
#48405=CARTESIAN_POINT ( 'NONE',  ( -162.8070736234661808, 10.01517768586948698, -1.839758294383808571E-15 ) ) ;
#48409=CARTESIAN_POINT ( 'NONE',  ( -91.10707362346619220, 8.102448949553171076, -5.886773742842744461 ) ) ;
#48418=CARTESIAN_POINT ( 'NONE',  ( -138.0549999999999784, -9.827790563157499189E-16, -8.024999999999991473 ) ) ;
#48422=CARTESIAN_POINT ( 'NONE',  ( -149.2449999999999761, -4.716976649647093289, -6.492361379858945902 ) ) ;
#48424=CARTESIAN_POINT ( 'NONE',  ( -134.8449999999999989, -7.632228543268599452, 2.479861379858951054 ) ) ;
#48434=CARTESIAN_POINT ( 'NONE',  ( -55.70499999999998408, 2.607480562269073321, 8.024999999999991473 ) ) ;
#48441=CARTESIAN_POINT ( 'NONE',  ( -103.6429263765337936, -5.598654528085801552, 7.705886871421367523 ) ) ;
#48444=CARTESIAN_POINT ( 'NONE',  ( -89.45707362346618652, -9.058813317711329915, 2.943386871421371787 ) ) ;
#48458=CARTESIAN_POINT ( 'NONE',  ( -102.4429263765338050, -1.166476076187852838E-15, -9.524999999999991473 ) ) ;
#48465=CARTESIAN_POINT ( 'NONE',  ( -96.59499999999998465, 2.607480562269073321, 8.024999999999991473 ) ) ;
#48480=DIRECTION ( 'NONE',  ( -1.000000000000000000, -0.000000000000000000, -0.000000000000000000 ) ) ;
#48481=DIRECTION ( 'NONE',  ( 0.000000000000000000, 0.000000000000000000, 1.000000000000000000 ) ) ;
#48491=ORIENTED_EDGE ( 'NONE', *, *, #2994, .F. ) ;
#48500=CARTESIAN_POINT ( 'NONE',  ( -169.2549999999999955, -4.716976649647092401, 6.492361379858946790 ) ) ;
#48502=CARTESIAN_POINT ( 'NONE',  ( -147.8070736234661524, 10.01517768586948698, -1.839758294383808966E-15 ) ) ;
#48503=CARTESIAN_POINT ( 'NONE',  ( -173.9949999999999761, -6.826472737025115478, 4.959722759717900331 ) ) ;
#48505=CARTESIAN_POINT ( 'NONE',  ( -163.0449999999999875, 7.632228543268600340, 2.479861379858949277 ) ) ;
#48508=EDGE_CURVE ( 'NONE', #20383, #12708, #63463, .T. ) ;
#48509=CARTESIAN_POINT ( 'NONE',  ( -14.67070496082497577, 10.91243640479189025, -4.991899053143842302 ) ) ;
#48510=CARTESIAN_POINT ( 'NONE',  ( -79.55499999999999261, 0.000000000000000000, 8.024999999999991473 ) ) ;
#48511=DIRECTION ( 'NONE',  ( 0.000000000000000000, 0.000000000000000000, 1.000000000000000000 ) ) ;
#48514=CARTESIAN_POINT ( 'NONE',  ( -77.09499999999997044, -2.607480562269071545, -8.024999999999991473 ) ) ;
#48526=CARTESIAN_POINT ( 'NONE',  ( -50.24292637653379501, 5.598654528085804216, 7.705886871421366635 ) ) ;
#48535=ADVANCED_FACE ( 'NONE', ( #46292 ), #62063, .T. ) ;
#48541=ADVANCED_FACE ( 'NONE', ( #56816 ), #30785, .F. ) ;
#48544=CARTESIAN_POINT ( 'NONE',  ( -109.4049999999999727, -2.607480562269069768, 8.024999999999991473 ) ) ;
#48545=VERTEX_POINT ( 'NONE', #67712 ) ;
#48546=CARTESIAN_POINT ( 'NONE',  ( -137.1570736234661751, -9.058813317711329915, -2.943386871421370898 ) ) ;
#48559=CARTESIAN_POINT ( 'NONE',  ( -136.2570736234661695, 5.598654528085800663, -7.705886871421367523 ) ) ;
#48563=CARTESIAN_POINT ( 'NONE',  ( -47.90707362346616094, -3.094860106618429807, 9.524999999999991473 ) ) ;
#48571=CARTESIAN_POINT ( 'NONE',  ( -51.74292637653380211, -5.598654528085803328, -7.705886871421366635 ) ) ;
#48573=CARTESIAN_POINT ( 'NONE',  ( -117.0570736234661808, 0.000000000000000000, 9.524999999999991473 ) ) ;
#48575=CARTESIAN_POINT ( 'NONE',  ( -142.7049999999999557, 2.607480562269073321, 8.024999999999991473 ) ) ;
#48588=CARTESIAN_POINT ( 'NONE',  ( -55.70499999999998408, 2.607480562269073321, 8.024999999999991473 ) ) ;
#48594=EDGE_CURVE ( 'NONE', #16969, #24888, #22971, .T. ) ;
#48603=CARTESIAN_POINT ( 'NONE',  ( -94.55707362346616662, -1.166476076187852838E-15, -9.524999999999991473 ) ) ;
#48607=CARTESIAN_POINT ( 'NONE',  ( -112.3449999999999847, 7.632228543268599452, -2.479861379858951942 ) ) ;
#48609=CARTESIAN_POINT ( 'NONE',  ( -83.39499999999998181, -6.826472737025115478, -4.959722759717899443 ) ) ;
#48613=( BOUNDED_CURVE ( )  B_SPLINE_CURVE ( 2, ( #2369, #23888, #45399, #62213, #66819, #18630, #61854, #40108, #35141, #8060, #56596 ),
 .UNSPECIFIED., .F., .F. ) 
 B_SPLINE_CURVE_WITH_KNOTS ( ( 3, 2, 2, 2, 2, 3 ),
 ( 0.1521739130434746068, 0.1543478260869527996, 0.1565217391304310479, 0.1586956521739092407, 0.1608695652173874613, 0.1630434782608656819 ),
 .UNSPECIFIED. ) 
 CURVE ( )  GEOMETRIC_REPRESENTATION_ITEM ( )  RATIONAL_B_SPLINE_CURVE ( ( 1.000000000000082379, 0.9510565162950710416, 1.000000000000000000, 0.9510565162951535312, 1.000000000000000000, 0.9510565162951535312, 1.000000000000000000, 0.9510565162951535312, 1.000000000000000000, 0.9510565162952410168, 0.9999999999999125144 ) ) 
 REPRESENTATION_ITEM ( '' )  );
#48614=CARTESIAN_POINT ( 'NONE',  ( -167.4570736234661865, -9.058813317711329915, 2.943386871421371787 ) ) ;
#48616=ORIENTED_EDGE ( 'NONE', *, *, #61722, .F. ) ;
#48617=CARTESIAN_POINT ( 'NONE',  ( -128.2429263765338021, 5.598654528085804216, 7.705886871421366635 ) ) ;
#48619=CARTESIAN_POINT ( 'NONE',  ( -152.2450000000000045, -4.716976649647093289, -6.492361379858945902 ) ) ;
#48622=CARTESIAN_POINT ( 'NONE',  ( -48.44499999999998607, 0.000000000000000000, 8.024999999999991473 ) ) ;
#48628=EDGE_CURVE ( 'NONE', #65704, #49292, #27063, .T. ) ;
#48633=CARTESIAN_POINT ( 'NONE',  ( -142.2549999999999955, -4.716976649647092401, 6.492361379858946790 ) ) ;
#48644=EDGE_CURVE ( 'NONE', #63556, #19085, #30144, .T. ) ;
#48647=CARTESIAN_POINT ( 'NONE',  ( -60.80499999999998550, -8.437984349512086979, 5.166775262442717831E-16 ) ) ;
#48648=CARTESIAN_POINT ( 'NONE',  ( -119.3949999999999676, -6.826472737025115478, -4.959722759717899443 ) ) ;
#48664=CARTESIAN_POINT ( 'NONE',  ( -171.0549999999999784, -9.827790563157499189E-16, -8.024999999999991473 ) ) ;
#48675=CARTESIAN_POINT ( 'NONE',  ( -81.20499999999999829, -2.607480562269071545, -8.024999999999991473 ) ) ;
#48681=CARTESIAN_POINT ( 'NONE',  ( -67.10707362346616378, 8.102448949553171076, -5.886773742842744461 ) ) ;
#48685=CARTESIAN_POINT ( 'NONE',  ( -101.3050000000000068, 8.437984349512085203, -1.550032578732815448E-15 ) ) ;
#48689=CARTESIAN_POINT ( 'NONE',  ( -120.7449999999999903, 4.716976649647094177, 6.492361379858945902 ) ) ;
#48695=CARTESIAN_POINT ( 'NONE',  ( -153.8070736234661808, 10.01517768586948698, -1.839758294383808966E-15 ) ) ;
#48696=CARTESIAN_POINT ( 'NONE',  ( -166.6429263765338078, -5.598654528085801552, 7.705886871421367523 ) ) ;
#48698=CARTESIAN_POINT ( 'NONE',  ( -176.2449999999999761, -4.716976649647093289, -6.492361379858945902 ) ) ;
#48705=DIRECTION ( 'NONE',  ( 1.000000000000000000, 0.000000000000000000, 0.000000000000000000 ) ) ;
#48707=CARTESIAN_POINT ( 'NONE',  ( -71.69292637653380496, 10.01517768586948698, -1.839758294383808571E-15 ) ) ;
#48710=( BOUNDED_CURVE ( )  B_SPLINE_CURVE ( 2, ( #50848, #50503, #12856, #7581, #67365, #19162, #51533, #29736, #29369, #34322, #40306 ),
 .UNSPECIFIED., .F., .F. ) 
 B_SPLINE_CURVE_WITH_KNOTS ( ( 3, 2, 2, 2, 2, 3 ),
 ( 0.6521739130434628384, 0.6543478260869410867, 0.6565217391304192240, 0.6586956521738974724, 0.6608695652173756097, 0.6630434782608538580 ),
 .UNSPECIFIED. ) 
 CURVE ( )  GEOMETRIC_REPRESENTATION_ITEM ( )  RATIONAL_B_SPLINE_CURVE ( ( 1.000000000000347500, 0.9510565162948061424, 1.000000000000000000, 0.9510565162951535312, 1.000000000000000000, 0.9510565162951535312, 1.000000000000000000, 0.9510565162951535312, 1.000000000000000000, 0.9510565162955059160, 0.9999999999996476152 ) ) 
 REPRESENTATION_ITEM ( '' )  );
#48711=CARTESIAN_POINT ( 'NONE',  ( -184.0000000000000000, 0.000000000000000000, 8.524999999999984368 ) ) ;
#48712=CARTESIAN_POINT ( 'NONE',  ( -154.5570736234661808, -1.166476076187852838E-15, -9.524999999999991473 ) ) ;
#48716=CARTESIAN_POINT ( 'NONE',  ( -179.4550000000000125, 7.632228543268599452, -2.479861379858951942 ) ) ;
#48729=CARTESIAN_POINT ( 'NONE',  ( -180.4429263765338192, -1.166476076187852838E-15, -9.524999999999991473 ) ) ;
#48730=CARTESIAN_POINT ( 'NONE',  ( -90.05499999999997840, -9.827790563157499189E-16, -8.024999999999991473 ) ) ;
#48731=ORIENTED_EDGE ( 'NONE', *, *, #37783, .F. ) ;
#48740=CARTESIAN_POINT ( 'NONE',  ( -67.04499999999997328, 7.632228543268600340, 2.479861379858949277 ) ) ;
#48743=CARTESIAN_POINT ( 'NONE',  ( -48.44292637653380496, -1.166476076187852838E-15, -9.524999999999991473 ) ) ;
#48754=CARTESIAN_POINT ( 'NONE',  ( -112.7049999999999699, 2.607480562269073321, 8.024999999999991473 ) ) ;
#48758=FACE_OUTER_BOUND ( 'NONE', #25642, .T. ) ;
#48759=CARTESIAN_POINT ( 'NONE',  ( -164.1570736234661751, -9.058813317711329915, -2.943386871421370898 ) ) ;
#48761=CARTESIAN_POINT ( 'NONE',  ( -93.05707362346616662, 0.000000000000000000, 9.524999999999991473 ) ) ;
#48770=CARTESIAN_POINT ( 'NONE',  ( -139.7049999999999841, 2.607480562269073321, 8.024999999999991473 ) ) ;
#48772=CARTESIAN_POINT ( 'NONE',  ( -141.2949999999999875, -2.607480562269069768, 8.024999999999991473 ) ) ;
#48774=CARTESIAN_POINT ( 'NONE',  ( -133.9449999999999932, -9.827790563157499189E-16, -8.024999999999991473 ) ) ;
#48780=CARTESIAN_POINT ( 'NONE',  ( -54.20499999999997698, -2.607480562269071545, -8.024999999999991473 ) ) ;
#48781=CARTESIAN_POINT ( 'NONE',  ( -60.44499999999998607, 0.000000000000000000, 8.024999999999991473 ) ) ;
#48784=AXIS2_PLACEMENT_3D ( 'NONE', #33641, #33987, #49839 ) ;
#48786=CARTESIAN_POINT ( 'NONE',  ( -106.6429263765338078, -5.598654528085801552, 7.705886871421367523 ) ) ;
#48796=ORIENTED_EDGE ( 'NONE', *, *, #27401, .T. ) ;
#48814=ORIENTED_EDGE ( 'NONE', *, *, #59623, .T. ) ;
#48816=CARTESIAN_POINT ( 'NONE',  ( -119.4570736234661723, -9.058813317711329915, 2.943386871421371787 ) ) ;
#48820=ADVANCED_FACE ( 'NONE', ( #1462, #55327 ), #36257, .F. ) ;
#48822=CARTESIAN_POINT ( 'NONE',  ( -94.49499999999999034, 6.826472737025113702, -4.959722759717902107 ) ) ;
#48828=ORIENTED_EDGE ( 'NONE', *, *, #5075, .T. ) ;
#48843=CARTESIAN_POINT ( 'NONE',  ( -161.9929263765337737, 8.102448949553172852, -5.886773742842744461 ) ) ;
#48850=CARTESIAN_POINT ( 'NONE',  ( -171.5049999999999386, -6.826472737025115478, -4.959722759717899443 ) ) ;
#48853=CARTESIAN_POINT ( 'NONE',  ( -171.7450000000000045, 4.716976649647094177, 6.492361379858945902 ) ) ;
#48854=CARTESIAN_POINT ( 'NONE',  ( -169.0449999999999875, 7.632228543268600340, 2.479861379858949277 ) ) ;
#48860=CARTESIAN_POINT ( 'NONE',  ( -80.75499999999999545, 4.716976649647091513, -6.492361379858946790 ) ) ;
#48861=LINE ( 'NONE', #26306, #41011 ) ;
#48865=CARTESIAN_POINT ( 'NONE',  ( -80.99499999999999034, -6.826472737025113702, 4.959722759717902107 ) ) ;
#48867=CARTESIAN_POINT ( 'NONE',  ( -133.5570736234661808, -1.166476076187852838E-15, -9.524999999999991473 ) ) ;
#48874=ORIENTED_EDGE ( 'NONE', *, *, #21403, .F. ) ;
#48893=CARTESIAN_POINT ( 'NONE',  ( -110.3049999999999926, 8.437984349512086979, -1.550032578732815448E-15 ) ) ;
#48896=CARTESIAN_POINT ( 'NONE',  ( -105.3570736234661780, 5.598654528085804216, 7.705886871421366635 ) ) ;
#48898=CARTESIAN_POINT ( 'NONE',  ( -57.44292637653381206, -1.166476076187852838E-15, -9.524999999999991473 ) ) ;
#48900=ORIENTED_EDGE ( 'NONE', *, *, #17591, .T. ) ;
#48911=CARTESIAN_POINT ( 'NONE',  ( -129.8929263765338362, -8.102448949553174629, -5.886773742842741797 ) ) ;
#48920=CARTESIAN_POINT ( 'NONE',  ( -52.34292637653378932, -9.058813317711329915, 2.943386871421371787 ) ) ;
#48926=CARTESIAN_POINT ( 'NONE',  ( -141.3550000000000182, -4.716976649647093289, -6.492361379858945902 ) ) ;
#48935=CARTESIAN_POINT ( 'NONE',  ( -58.70499999999997698, 2.607480562269073321, 8.024999999999991473 ) ) ;
#48949=CARTESIAN_POINT ( 'NONE',  ( -106.4949999999999903, 6.826472737025113702, -4.959722759717902107 ) ) ;
#48951=CARTESIAN_POINT ( 'NONE',  ( -82.94499999999999318, -9.827790563157499189E-16, -8.024999999999991473 ) ) ;
#48954=DIRECTION ( 'NONE',  ( -1.000000000000000000, -0.000000000000000000, -0.000000000000000000 ) ) ;
#48959=CARTESIAN_POINT ( 'NONE',  ( -120.5929263765337822, -3.094860106618431139, -9.524999999999991473 ) ) ;
#48961=CARTESIAN_POINT ( 'NONE',  ( -149.8449999999999989, -7.632228543268599452, 2.479861379858951054 ) ) ;
#48967=CARTESIAN_POINT ( 'NONE',  ( -112.5570736234661808, -1.166476076187852838E-15, -9.524999999999991473 ) ) ;
#48971=EDGE_CURVE ( 'NONE', #39571, #36987, #19887, .T. ) ;
#48972=CARTESIAN_POINT ( 'NONE',  ( -153.4429263765338192, -1.166476076187852838E-15, -9.524999999999991473 ) ) ;
#48979=CARTESIAN_POINT ( 'NONE',  ( -141.2050000000000125, -2.607480562269071545, -8.024999999999991473 ) ) ;
#48980=ORIENTED_EDGE ( 'NONE', *, *, #6923, .F. ) ;
#48993=CARTESIAN_POINT ( 'NONE',  ( -58.25499999999997414, -4.716976649647092401, 6.492361379858946790 ) ) ;
#48994=VECTOR ( 'NONE', #34543, 1000.000000000000000 ) ;
#48995=CARTESIAN_POINT ( 'NONE',  ( -122.5449999999999875, -7.632228543268600340, -2.479861379858950166 ) ) ;
#49004=CARTESIAN_POINT ( 'NONE',  ( -175.1050000000000182, -6.826472737025115478, 4.959722759717900331 ) ) ;
#49015=CARTESIAN_POINT ( 'NONE',  ( -85.40499999999998693, -2.607480562269069768, 8.024999999999991473 ) ) ;
#49022=( BOUNDED_CURVE ( )  B_SPLINE_CURVE ( 2, ( #24797, #18507, #39997, #51213, #34661, #13555, #7943, #29385, #35022, #56475, #35385 ),
 .UNSPECIFIED., .F., .F. ) 
 B_SPLINE_CURVE_WITH_KNOTS ( ( 3, 2, 2, 2, 2, 3 ),
 ( 0.7826086956521739468, 0.7847826086956521952, 0.7869565217391304435, 0.7891304347826086918, 0.7913043478260869401, 0.7934782608695651884 ),
 .UNSPECIFIED. ) 
 CURVE ( )  GEOMETRIC_REPRESENTATION_ITEM ( )  RATIONAL_B_SPLINE_CURVE ( ( 1.000000000000000000, 0.9510565162951535312, 1.000000000000000000, 0.9510565162951535312, 1.000000000000000000, 0.9510565162951535312, 1.000000000000000000, 0.9510565162951535312, 1.000000000000000000, 0.9510565162951535312, 1.000000000000000000 ) ) 
 REPRESENTATION_ITEM ( '' )  );
#49025=CARTESIAN_POINT ( 'NONE',  ( -64.10707362346616378, 8.102448949553171076, -5.886773742842744461 ) ) ;
#49033=CARTESIAN_POINT ( 'NONE',  ( -103.1049999999999756, -6.826472737025115478, 4.959722759717900331 ) ) ;
#49035=CARTESIAN_POINT ( 'NONE',  ( -118.1949999999999790, 8.437984349512085203, -1.550032578732815448E-15 ) ) ;
#49040=CARTESIAN_POINT ( 'NONE',  ( -154.9429263765338192, 0.000000000000000000, 9.524999999999991473 ) ) ;
#49041=CARTESIAN_POINT ( 'NONE',  ( -172.3449999999999989, 7.632228543268599452, -2.479861379858951942 ) ) ;
#49050=CARTESIAN_POINT ( 'NONE',  ( -64.04292637653379927, -9.058813317711329915, -2.943386871421370898 ) ) ;
#49052=DIRECTION ( 'NONE',  ( -1.000000000000000000, -0.000000000000000000, -0.000000000000000000 ) ) ;
#49061=CARTESIAN_POINT ( 'NONE',  ( -166.4049999999999727, -2.607480562269069768, 8.024999999999991473 ) ) ;
#49062=ORIENTED_EDGE ( 'NONE', *, *, #30072, .F. ) ;
#49070=CARTESIAN_POINT ( 'NONE',  ( -95.00499999999998124, 6.826472737025115478, 4.959722759717899443 ) ) ;
#49079=CARTESIAN_POINT ( 'NONE',  ( -60.44499999999998607, 0.000000000000000000, 8.024999999999991473 ) ) ;
#49088=CARTESIAN_POINT ( 'NONE',  ( -117.6550000000000011, -7.632228543268600340, -2.479861379858950166 ) ) ;
#49091=CARTESIAN_POINT ( 'NONE',  ( -73.94292637653379074, 0.000000000000000000, 9.524999999999991473 ) ) ;
#49095=CARTESIAN_POINT ( 'NONE',  ( -147.6570736234662036, 9.058813317711329915, 2.943386871421369566 ) ) ;
#49097=CARTESIAN_POINT ( 'NONE',  ( -92.30707362346618083, -10.01517768586948698, 6.132527647946031529E-16 ) ) ;
#49105=CARTESIAN_POINT ( 'NONE',  ( -128.3050000000000068, 8.437984349512085203, -1.550032578732815448E-15 ) ) ;
#49109=CARTESIAN_POINT ( 'NONE',  ( -54.59292637653378222, -3.094860106618431139, -9.524999999999991473 ) ) ;
#49111=CARTESIAN_POINT ( 'NONE',  ( -140.8449999999999989, -7.632228543268599452, 2.479861379858951054 ) ) ;
#49112=CARTESIAN_POINT ( 'NONE',  ( -131.8449999999999989, -7.632228543268599452, 2.479861379858951054 ) ) ;
#49118=CARTESIAN_POINT ( 'NONE',  ( -182.9929263765338021, 8.102448949553171076, -5.886773742842744461 ) ) ;
#49119=CARTESIAN_POINT ( 'NONE',  ( -62.09499999999998465, -2.607480562269071545, -8.024999999999991473 ) ) ;
#49122=CARTESIAN_POINT ( 'NONE',  ( -139.7929263765343535, -3.094860106609085726, 9.525000000006778933 ) ) ;
#49125=CARTESIAN_POINT ( 'NONE',  ( -108.5929263765338106, -3.094860106618431139, -9.524999999999991473 ) ) ;
#49129=CARTESIAN_POINT ( 'NONE',  ( -99.05707362346618083, 0.000000000000000000, 9.524999999999991473 ) ) ;
#49134=ORIENTED_EDGE ( 'NONE', *, *, #735, .F. ) ;
#49138=ORIENTED_EDGE ( 'NONE', *, *, #20160, .T. ) ;
#49142=CARTESIAN_POINT ( 'NONE',  ( -119.9070736234669567, -3.094860106605456185, 9.525000000009420376 ) ) ;
#49145=CARTESIAN_POINT ( 'NONE',  ( -93.29499999999998749, -2.607480562269069768, 8.024999999999991473 ) ) ;
#49155=CARTESIAN_POINT ( 'NONE',  ( -195.0000000000000000, 0.000000000000000000, 0.000000000000000000 ) ) ;
#49156=ORIENTED_EDGE ( 'NONE', *, *, #49300, .F. ) ;
#49157=CARTESIAN_POINT ( 'NONE',  ( -165.2070736234663855, 3.094860106621995399, 9.524999999997403322 ) ) ;
#49160=CARTESIAN_POINT ( 'NONE',  ( -182.9070736234661751, -3.094860106618429807, 9.524999999999991473 ) ) ;
#49171=CARTESIAN_POINT ( 'NONE',  ( -158.7549999999999670, 4.716976649647091513, -6.492361379858946790 ) ) ;
#49173=CARTESIAN_POINT ( 'NONE',  ( -183.8059463088887640, -8.116739841473526340, -3.200022323834349702 ) ) ;
#49174=EDGE_CURVE ( 'NONE', #59012, #24116, #3733, .T. ) ;
#49175=CARTESIAN_POINT ( 'NONE',  ( -175.1949999999999932, 8.437984349512085203, -1.550032578732815448E-15 ) ) ;
#49176=CARTESIAN_POINT ( 'NONE',  ( -171.7450000000000045, 4.716976649647094177, 6.492361379858945902 ) ) ;
#49180=CARTESIAN_POINT ( 'NONE',  ( -86.75499999999998124, 4.716976649647091513, -6.492361379858946790 ) ) ;
#49181=CARTESIAN_POINT ( 'NONE',  ( -195.0000000000000000, 0.000000000000000000, 0.000000000000000000 ) ) ;
#49185=CARTESIAN_POINT ( 'NONE',  ( -77.54499999999998749, -7.632228543268600340, -2.479861379858950166 ) ) ;
#49195=VECTOR ( 'NONE', #16385, 1000.000000000000000 ) ;
#49205=CARTESIAN_POINT ( 'NONE',  ( -116.6049999999999898, 6.826472737025113702, -4.959722759717902107 ) ) ;
#49213=VERTEX_POINT ( 'NONE', #37213 ) ;
#49221=CARTESIAN_POINT ( 'NONE',  ( -195.0000000000000000, 0.000000000000000000, 0.000000000000000000 ) ) ;
#49232=CARTESIAN_POINT ( 'NONE',  ( -195.0000000000000000, 0.000000000000000000, 0.000000000000000000 ) ) ;
#49234=CARTESIAN_POINT ( 'NONE',  ( -139.5549999999999784, 0.000000000000000000, 8.024999999999991473 ) ) ;
#49239=DIRECTION ( 'NONE',  ( 0.000000000000000000, 0.000000000000000000, 1.000000000000000000 ) ) ;
#49246=CARTESIAN_POINT ( 'NONE',  ( -53.90499999999997272, 2.607480562269068880, -8.024999999999993250 ) ) ;
#49263=CARTESIAN_POINT ( 'NONE',  ( -112.7949999999999733, 2.607480562269069324, -8.024999999999993250 ) ) ;
#49265=CARTESIAN_POINT ( 'NONE',  ( -86.99499999999997613, -6.826472737025115478, 4.959722759717900331 ) ) ;
#49268=CARTESIAN_POINT ( 'NONE',  ( -1.000000000000028644, 0.000000000000000000, 11.99999999999999645 ) ) ;
#49274=CARTESIAN_POINT ( 'NONE',  ( -127.3429263765337964, -9.058813317711329915, 2.943386871421371787 ) ) ;
#49275=CARTESIAN_POINT ( 'NONE',  ( -142.9449999999999932, -9.827790563157499189E-16, -8.024999999999991473 ) ) ;
#49276=FACE_OUTER_BOUND ( 'NONE', #21595, .T. ) ;
#49278=CARTESIAN_POINT ( 'NONE',  ( -48.74499999999998323, 4.716976649647094177, 6.492361379858945902 ) ) ;
#49291=CARTESIAN_POINT ( 'NONE',  ( -144.8049999999999500, -8.437984349512086979, 5.166775262442717831E-16 ) ) ;
#49292=VERTEX_POINT ( 'NONE', #48458 ) ;
#49300=EDGE_CURVE ( 'NONE', #32584, #16622, #32421, .T. ) ;
#49304=CARTESIAN_POINT ( 'NONE',  ( -57.35499999999998977, -4.716976649647093289, -6.492361379858945902 ) ) ;
#49306=CARTESIAN_POINT ( 'NONE',  ( -121.4949999999999761, 6.826472737025113702, -4.959722759717902107 ) ) ;
#49312=AXIS2_PLACEMENT_3D ( 'NONE', #49327, #28167, #60896 ) ;
#49319=CARTESIAN_POINT ( 'NONE',  ( -167.7549999999999955, 4.716976649647091513, -6.492361379858946790 ) ) ;
#49320=VERTEX_POINT ( 'NONE', #21324 ) ;
#49327=CARTESIAN_POINT ( 'NONE',  ( -195.0000000000000000, 0.000000000000000000, 0.000000000000000000 ) ) ;
#49328=CARTESIAN_POINT ( 'NONE',  ( -82.85499999999998977, 4.716976649647094177, 6.492361379858945902 ) ) ;
#49329=ORIENTED_EDGE ( 'NONE', *, *, #38570, .T. ) ;
#49334=CARTESIAN_POINT ( 'NONE',  ( -56.60707362346616378, -8.102448949553172852, 5.886773742842742685 ) ) ;
#49342=CARTESIAN_POINT ( 'NONE',  ( -103.2549999999999812, -4.716976649647092401, 6.492361379858946790 ) ) ;
#49344=CARTESIAN_POINT ( 'NONE',  ( -117.1449999999999818, -4.716976649647092401, 6.492361379858946790 ) ) ;
#49347=CARTESIAN_POINT ( 'NONE',  ( -18.96980255412093896, 11.60735904872732149, -3.057087346036348130 ) ) ;
#49350=CARTESIAN_POINT ( 'NONE',  ( -153.1429263765338078, 5.598654528085800663, -7.705886871421367523 ) ) ;
#49352=CARTESIAN_POINT ( 'NONE',  ( -172.6449999999999818, 4.716976649647091513, -6.492361379858946790 ) ) ;
#49362=CARTESIAN_POINT ( 'NONE',  ( -71.39292637653379359, 8.102448949553176405, 5.886773742842740909 ) ) ;
#49373=CARTESIAN_POINT ( 'NONE',  ( -171.9549999999999841, -7.632228543268599452, 2.479861379858951054 ) ) ;
#49382=CARTESIAN_POINT ( 'NONE',  ( -86.45499999999998408, 7.632228543268599452, -2.479861379858951942 ) ) ;
#49384=DIRECTION ( 'NONE',  ( -1.000000000000000000, -0.000000000000000000, -0.000000000000000000 ) ) ;
#49386=CARTESIAN_POINT ( 'NONE',  ( -169.6429263765338078, -5.598654528085801552, 7.705886871421367523 ) ) ;
#49393=CARTESIAN_POINT ( 'NONE',  ( -59.54499999999998749, -7.632228543268600340, -2.479861379858950166 ) ) ;
#49395=( BOUNDED_CURVE ( )  B_SPLINE_CURVE ( 2, ( #16244, #57834, #38046, #41679, #48614, #36034, #53505, #41326, #5988, #3987, #68050 ),
 .UNSPECIFIED., .F., .F. ) 
 B_SPLINE_CURVE_WITH_KNOTS ( ( 3, 2, 2, 2, 2, 3 ),
 ( 0.1086956521739105841, 0.1108695652173887908, 0.1130434782608669975, 0.1152173913043452180, 0.1173913043478234247, 0.1195652173913016314 ),
 .UNSPECIFIED. ) 
 CURVE ( )  GEOMETRIC_REPRESENTATION_ITEM ( )  RATIONAL_B_SPLINE_CURVE ( ( 1.000000000000055289, 0.9510565162950983531, 1.000000000000000000, 0.9510565162951535312, 1.000000000000000000, 0.9510565162951535312, 1.000000000000000000, 0.9510565162951535312, 1.000000000000000000, 0.9510565162952148155, 0.9999999999999387157 ) ) 
 REPRESENTATION_ITEM ( '' )  );
#49397=EDGE_CURVE ( 'NONE', #36469, #23874, #22581, .T. ) ;
#49400=AXIS2_PLACEMENT_3D ( 'NONE', #15885, #42991, #32722 ) ;
#49406=ADVANCED_FACE ( 'NONE', ( #49818 ), #11116, .T. ) ;
#49409=CARTESIAN_POINT ( 'NONE',  ( -113.0049999999999812, 6.826472737025116366, 4.959722759717898555 ) ) ;
#49418=CARTESIAN_POINT ( 'NONE',  ( -154.2570736234661979, 5.598654528085800663, -7.705886871421367523 ) ) ;
#49420=CARTESIAN_POINT ( 'NONE',  ( -90.20707362346618652, 3.094860106618433360, 9.524999999999991473 ) ) ;
#49429=CARTESIAN_POINT ( 'NONE',  ( -133.1050000000000182, -6.826472737025115478, 4.959722759717900331 ) ) ;
#49433=CARTESIAN_POINT ( 'NONE',  ( -145.1949999999999648, 8.437984349512085203, -1.550032578732815448E-15 ) ) ;
#49435=CARTESIAN_POINT ( 'NONE',  ( -124.9450000000000074, -9.827790563157499189E-16, -8.024999999999991473 ) ) ;
#49444=CARTESIAN_POINT ( 'NONE',  ( -180.1429263765338078, 5.598654528085800663, -7.705886871421367523 ) ) ;
#49447=CARTESIAN_POINT ( 'NONE',  ( -54.89499999999997470, 6.826472737025116366, 4.959722759717898555 ) ) ;
#49452=CARTESIAN_POINT ( 'NONE',  ( -94.04292637653379927, -9.058813317711329915, -2.943386871421370898 ) ) ;
#49477=CARTESIAN_POINT ( 'NONE',  ( -88.19499999999996476, 8.437984349512085203, -1.550032578732815448E-15 ) ) ;
#49489=EDGE_CURVE ( 'NONE', #43509, #55165, #48710, .T. ) ;
#49499=( BOUNDED_CURVE ( )  B_SPLINE_CURVE ( 2, ( #20190, #62057, #13888, #24765, #24094, #50833, #46647, #30378, #51882, #19851, #41345 ),
 .UNSPECIFIED., .F., .F. ) 
 B_SPLINE_CURVE_WITH_KNOTS ( ( 3, 2, 2, 2, 2, 3 ),
 ( 0.1847826086956478042, 0.1869565217391260248, 0.1891304347826042176, 0.1913043478260824382, 0.1934782608695606310, 0.1956521739130388515 ),
 .UNSPECIFIED. ) 
 CURVE ( )  GEOMETRIC_REPRESENTATION_ITEM ( )  RATIONAL_B_SPLINE_CURVE ( ( 1.000000000000097922, 0.9510565162950552764, 1.000000000000000000, 0.9510565162951535312, 1.000000000000000000, 0.9510565162951535312, 1.000000000000000000, 0.9510565162951535312, 1.000000000000000000, 0.9510565162952578921, 0.9999999999998956390 ) ) 
 REPRESENTATION_ITEM ( '' )  );
#49501=CARTESIAN_POINT ( 'NONE',  ( -68.39292637653379359, 8.102448949553176405, 5.886773742842740909 ) ) ;
#49510=ORIENTED_EDGE ( 'NONE', *, *, #7843, .F. ) ;
#49511=CARTESIAN_POINT ( 'NONE',  ( -157.8549999999999898, 4.716976649647094177, 6.492361379858945902 ) ) ;
#49515=CARTESIAN_POINT ( 'NONE',  ( -173.2449999999999761, -4.716976649647093289, -6.492361379858945902 ) ) ;
#49517=CARTESIAN_POINT ( 'NONE',  ( -156.8950000000000387, 6.826472737025115478, 4.959722759717899443 ) ) ;
#49523=CARTESIAN_POINT ( 'NONE',  ( -71.00499999999996703, 6.826472737025116366, 4.959722759717898555 ) ) ;
#49526=CARTESIAN_POINT ( 'NONE',  ( -69.14499999999998181, -4.716976649647092401, 6.492361379858946790 ) ) ;
#49538=CYLINDRICAL_SURFACE ( 'NONE', #13906, 9.524999999999991473 ) ;
#49549=CARTESIAN_POINT ( 'NONE',  ( -115.4049999999999727, -2.607480562269069768, 8.024999999999991473 ) ) ;
#49562=ORIENTED_EDGE ( 'NONE', *, *, #28578, .F. ) ;
#49581=CARTESIAN_POINT ( 'NONE',  ( -140.9050000000000011, 2.607480562269068880, -8.024999999999993250 ) ) ;
#49596=CARTESIAN_POINT ( 'NONE',  ( -61.25499999999998835, -4.716976649647092401, 6.492361379858946790 ) ) ;
#49609=CARTESIAN_POINT ( 'NONE',  ( -108.1449999999999960, -4.716976649647092401, 6.492361379858946790 ) ) ;
#49611=CARTESIAN_POINT ( 'NONE',  ( -76.19499999999999318, 8.437984349512085203, -1.550032578732815448E-15 ) ) ;
#49620=CARTESIAN_POINT ( 'NONE',  ( -124.0429263765337993, -9.058813317711329915, -2.943386871421370898 ) ) ;
#49621=CARTESIAN_POINT ( 'NONE',  ( -136.0449999999999875, 7.632228543268600340, 2.479861379858949277 ) ) ;
#49624=AXIS2_PLACEMENT_3D ( 'NONE', #29588, #66539, #40522 ) ;
#49625=CARTESIAN_POINT ( 'NONE',  ( -67.40707362346614673, 3.094860106618428031, -9.524999999999993250 ) ) ;
#49632=CARTESIAN_POINT ( 'NONE',  ( -49.85707362346617089, -5.598654528085803328, -7.705886871421366635 ) ) ;
#49635=CARTESIAN_POINT ( 'NONE',  ( -143.9050000000000011, 2.607480562269069324, -8.024999999999993250 ) ) ;
#49640=ORIENTED_EDGE ( 'NONE', *, *, #12094, .F. ) ;
#49650=CARTESIAN_POINT ( 'NONE',  ( -59.45499999999997698, 7.632228543268599452, -2.479861379858951942 ) ) ;
#49666=CARTESIAN_POINT ( 'NONE',  ( -171.3550000000000182, -4.716976649647093289, -6.492361379858945902 ) ) ;
#49678=CARTESIAN_POINT ( 'NONE',  ( -77.39292637653380780, 8.102448949553176405, 5.886773742842740909 ) ) ;
#49684=CARTESIAN_POINT ( 'NONE',  ( -82.10499999999998977, -6.826472737025115478, 4.959722759717900331 ) ) ;
#49691=ORIENTED_EDGE ( 'NONE', *, *, #20080, .F. ) ;
#49695=CARTESIAN_POINT ( 'NONE',  ( -110.9950000000000045, -6.826472737025115478, 4.959722759717900331 ) ) ;
#49697=CARTESIAN_POINT ( 'NONE',  ( -15.65902202074856397, 10.92377308316372897, -4.967528286585814357 ) ) ;
#49699=CARTESIAN_POINT ( 'NONE',  ( -153.5929263765338249, -3.094860106618431139, -9.524999999999991473 ) ) ;
#49700=CARTESIAN_POINT ( 'NONE',  ( -175.6449999999999818, 4.716976649647091513, -6.492361379858946790 ) ) ;
#49705=ORIENTED_EDGE ( 'NONE', *, *, #59147, .T. ) ;
#49708=CARTESIAN_POINT ( 'NONE',  ( -70.34292637653381064, -9.058813317711329915, 2.943386871421371787 ) ) ;
#49716=CARTESIAN_POINT ( 'NONE',  ( -168.2049999999999841, -2.607480562269071545, -8.024999999999991473 ) ) ;
#49718=ORIENTED_EDGE ( 'NONE', *, *, #13085, .F. ) ;
#49729=LINE ( 'NONE', #1470, #39534 ) ;
#49730=CARTESIAN_POINT ( 'NONE',  ( -86.60500000000000398, 6.826472737025113702, -4.959722759717902107 ) ) ;
#49733=CARTESIAN_POINT ( 'NONE',  ( -127.4929263765338163, -8.102448949553174629, 5.886773742842742685 ) ) ;
#49741=CARTESIAN_POINT ( 'NONE',  ( -62.99499999999996902, -6.826472737025115478, 4.959722759717900331 ) ) ;
#49745=CARTESIAN_POINT ( 'NONE',  ( -49.79292637653379217, -3.094860106618429807, 9.524999999999991473 ) ) ;
#49749=CARTESIAN_POINT ( 'NONE',  ( -55.19499999999998607, 8.437984349512086979, -1.550032578732815448E-15 ) ) ;
#49754=CARTESIAN_POINT ( 'NONE',  ( -110.1549999999999869, 7.632228543268600340, 2.479861379858949277 ) ) ;
#49762=CARTESIAN_POINT ( 'NONE',  ( -146.4570736234661865, -9.058813317711329915, 2.943386871421371787 ) ) ;
#49765=CARTESIAN_POINT ( 'NONE',  ( -86.00707362346616947, -8.102448949553172852, -5.886773742842741797 ) ) ;
#49773=CARTESIAN_POINT ( 'NONE',  ( -135.2050000000000125, -2.607480562269071545, -8.024999999999991473 ) ) ;
#49774=CARTESIAN_POINT ( 'NONE',  ( -165.4429263765337907, -1.166476076187852838E-15, -9.524999999999991473 ) ) ;
#49776=CARTESIAN_POINT ( 'NONE',  ( -55.79292637653379927, -3.094860106618429807, 9.524999999999991473 ) ) ;
#49777=CARTESIAN_POINT ( 'NONE',  ( -133.6449999999999818, 4.716976649647091513, -6.492361379858946790 ) ) ;
#49778=CARTESIAN_POINT ( 'NONE',  ( -129.2949999999999875, -2.607480562269069768, 8.024999999999991473 ) ) ;
#49779=ORIENTED_EDGE ( 'NONE', *, *, #50250, .T. ) ;
#49784=CARTESIAN_POINT ( 'NONE',  ( -178.4929263765338021, -8.102448949553172852, 5.886773742842742685 ) ) ;
#49785=( BOUNDED_CURVE ( )  B_SPLINE_CURVE ( 2, ( #51960, #26245, #57570, #36138, #69175, #9404, #63540, #57936, #57212, #30824, #52323 ),
 .UNSPECIFIED., .F., .F. ) 
 B_SPLINE_CURVE_WITH_KNOTS ( ( 3, 2, 2, 2, 2, 3 ),
 ( 0.04347826086956422392, 0.04565217391304243755, 0.04782608695652065117, 0.04999999999999885786, 0.05217391304347706454, 0.05434782608695527817 ),
 .UNSPECIFIED. ) 
 CURVE ( )  GEOMETRIC_REPRESENTATION_ITEM ( )  RATIONAL_B_SPLINE_CURVE ( ( 1.000000000000022427, 0.9510565162951313267, 1.000000000000000000, 0.9510565162951535312, 1.000000000000000000, 0.9510565162951535312, 1.000000000000000000, 0.9510565162951535312, 1.000000000000000000, 0.9510565162951815088, 0.9999999999999720224 ) ) 
 REPRESENTATION_ITEM ( '' )  );
#49786=DIRECTION ( 'NONE',  ( 1.000000000000000000, 0.000000000000000000, 0.000000000000000000 ) ) ;
#49787=CARTESIAN_POINT ( 'NONE',  ( -63.29499999999998749, -2.607480562269069768, 8.024999999999991473 ) ) ;
#49792=CARTESIAN_POINT ( 'NONE',  ( -90.74292637653380211, -5.598654528085803328, -7.705886871421366635 ) ) ;
#49809=CIRCLE ( 'NONE', #16139, 5.499999999999984901 ) ;
#49812=EDGE_CURVE ( 'NONE', #65754, #54235, #41939, .T. ) ;
#49818=FACE_OUTER_BOUND ( 'NONE', #28934, .T. ) ;
#49824=CARTESIAN_POINT ( 'NONE',  ( -94.04499999999998749, 7.632228543268600340, 2.479861379858949277 ) ) ;
#49839=DIRECTION ( 'NONE',  ( 0.000000000000000000, 0.000000000000000000, 1.000000000000000000 ) ) ;
#49843=CARTESIAN_POINT ( 'NONE',  ( -177.3570736234661638, 5.598654528085804216, 7.705886871421366635 ) ) ;
#49847=CARTESIAN_POINT ( 'NONE',  ( -114.5070736234661979, 8.102448949553176405, 5.886773742842740909 ) ) ;
#49855=CARTESIAN_POINT ( 'NONE',  ( -149.4570736234661581, -9.058813317711329915, 2.943386871421371787 ) ) ;
#49858=CARTESIAN_POINT ( 'NONE',  ( -156.6550000000000011, -7.632228543268600340, -2.479861379858950166 ) ) ;
#49859=FACE_OUTER_BOUND ( 'NONE', #19938, .T. ) ;
#49861=CARTESIAN_POINT ( 'NONE',  ( -170.0949999999999704, -2.607480562269071545, -8.024999999999991473 ) ) ;
#49863=CARTESIAN_POINT ( 'NONE',  ( -156.1450000000000102, -4.716976649647092401, 6.492361379858946790 ) ) ;
#49864=ORIENTED_EDGE ( 'NONE', *, *, #18178, .F. ) ;
#49866=CARTESIAN_POINT ( 'NONE',  ( -90.14292637653380780, 5.598654528085800663, -7.705886871421367523 ) ) ;
#49869=CARTESIAN_POINT ( 'NONE',  ( -75.35499999999998977, -4.716976649647093289, -6.492361379858945902 ) ) ;
#49873=CARTESIAN_POINT ( 'NONE',  ( -75.44499999999997897, 0.000000000000000000, 8.024999999999991473 ) ) ;
#49875=CYLINDRICAL_SURFACE ( 'NONE', #32033, 9.524999999999991473 ) ;
#49876=VECTOR ( 'NONE', #11307, 1000.000000000000000 ) ;
#49890=CARTESIAN_POINT ( 'NONE',  ( -119.9929263765338021, 8.102448949553172852, -5.886773742842744461 ) ) ;
#49896=CARTESIAN_POINT ( 'NONE',  ( -195.0000000000000000, 0.000000000000000000, 7.499999999999985789 ) ) ;
#49900=ADVANCED_FACE ( 'NONE', ( #58135 ), #62681, .T. ) ;
#49902=CARTESIAN_POINT ( 'NONE',  ( -114.0549999999999926, -9.827790563157499189E-16, -8.024999999999991473 ) ) ;
#49914=( BOUNDED_CURVE ( )  B_SPLINE_CURVE ( 2, ( #28705, #7279, #34351, #55800, #12528, #7962, #45644, #29405, #60374, #12176, #50879 ),
 .UNSPECIFIED., .F., .F. ) 
 B_SPLINE_CURVE_WITH_KNOTS ( ( 3, 2, 2, 2, 2, 3 ),
 ( 0.7065217391304348116, 0.7086956521739130599, 0.7108695652173913082, 0.7130434782608695565, 0.7152173913043478048, 0.7173913043478260532 ),
 .UNSPECIFIED. ) 
 CURVE ( )  GEOMETRIC_REPRESENTATION_ITEM ( )  RATIONAL_B_SPLINE_CURVE ( ( 1.000000000000000000, 0.9510565162951535312, 1.000000000000000000, 0.9510565162951535312, 1.000000000000000000, 0.9510565162951535312, 1.000000000000000000, 0.9510565162951535312, 1.000000000000000000, 0.9510565162951535312, 1.000000000000000000 ) ) 
 REPRESENTATION_ITEM ( '' )  );
#49918=CARTESIAN_POINT ( 'NONE',  ( -152.7570736234661979, -5.598654528085801552, 7.705886871421367523 ) ) ;
#49927=ADVANCED_FACE ( 'NONE', ( #30318 ), #9614, .T. ) ;
#49933=CARTESIAN_POINT ( 'NONE',  ( -130.1049999999999898, -6.826472737025115478, 4.959722759717900331 ) ) ;
#49940=CARTESIAN_POINT ( 'NONE',  ( -156.5929263765341375, -3.094860106624447660, -9.524999999995621636 ) ) ;
#49956=ORIENTED_EDGE ( 'NONE', *, *, #51160, .T. ) ;
#49958=CARTESIAN_POINT ( 'NONE',  ( -144.0570736234661808, 0.000000000000000000, 9.524999999999991473 ) ) ;
#49962=DIRECTION ( 'NONE',  ( 0.000000000000000000, 0.000000000000000000, 1.000000000000000000 ) ) ;
#49964=CARTESIAN_POINT ( 'NONE',  ( -101.6949999999999648, -8.437984349512086979, 5.166775262442717831E-16 ) ) ;
#49966=CARTESIAN_POINT ( 'NONE',  ( -78.44499999999999318, 0.000000000000000000, 8.024999999999991473 ) ) ;
#49976=CARTESIAN_POINT ( 'NONE',  ( -128.3929263765338078, 8.102448949553176405, 5.886773742842740909 ) ) ;
#49979=CARTESIAN_POINT ( 'NONE',  ( -142.6449999999999818, 4.716976649647091513, -6.492361379858946790 ) ) ;
#49981=EDGE_CURVE ( 'NONE', #149, #28296, #68123, .T. ) ;
#49989=CARTESIAN_POINT ( 'NONE',  ( -131.9070736234668004, -3.094860106607875583, 9.525000000007660006 ) ) ;
#49994=CARTESIAN_POINT ( 'NONE',  ( -140.9050000000000011, 2.607480562269069324, -8.024999999999993250 ) ) ;
#49995=ORIENTED_EDGE ( 'NONE', *, *, #54623, .F. ) ;
#49997=EDGE_LOOP ( 'NONE', ( #40142, #62615, #40652, #56886 ) ) ;
#50008=CARTESIAN_POINT ( 'NONE',  ( -56.45499999999997698, 7.632228543268599452, -2.479861379858951942 ) ) ;
#50010=VERTEX_POINT ( 'NONE', #30676 ) ;
#50023=CARTESIAN_POINT ( 'NONE',  ( -158.3049999999999500, 8.437984349512085203, -1.550032578732815448E-15 ) ) ;
#50028=FACE_OUTER_BOUND ( 'NONE', #22300, .T. ) ;
#50030=CARTESIAN_POINT ( 'NONE',  ( -144.0570736234661808, 0.000000000000000000, 9.524999999999991473 ) ) ;
#50035=CARTESIAN_POINT ( 'NONE',  ( -83.30500000000000682, 8.437984349512085203, -1.550032578732815448E-15 ) ) ;
#50043=ORIENTED_EDGE ( 'NONE', *, *, #45228, .T. ) ;
#50049=CARTESIAN_POINT ( 'NONE',  ( -107.5449999999999875, -7.632228543268600340, -2.479861379858950166 ) ) ;
#50055=CARTESIAN_POINT ( 'NONE',  ( -18.30771561979323891, 11.39710497969720571, 3.763356312794146508 ) ) ;
#50056=CARTESIAN_POINT ( 'NONE',  ( -152.5429263765338135, 9.058813317711329915, 2.943386871421369566 ) ) ;
#50058=CARTESIAN_POINT ( 'NONE',  ( -164.0949999999999989, -2.607480562269071545, -8.024999999999991473 ) ) ;
#50063=ORIENTED_EDGE ( 'NONE', *, *, #36998, .F. ) ;
#50066=CARTESIAN_POINT ( 'NONE',  ( -63.74292637653379501, -5.598654528085803328, -7.705886871421366635 ) ) ;
#50075=ORIENTED_EDGE ( 'NONE', *, *, #45796, .T. ) ;
#50076=CARTESIAN_POINT ( 'NONE',  ( -174.6550000000000011, -7.632228543268600340, -2.479861379858950166 ) ) ;
#50085=CARTESIAN_POINT ( 'NONE',  ( -83.90499999999998693, 2.607480562269069324, -8.024999999999993250 ) ) ;
#50088=CARTESIAN_POINT ( 'NONE',  ( -118.9429263765338050, 0.000000000000000000, 9.524999999999991473 ) ) ;
#50090=CARTESIAN_POINT ( 'NONE',  ( -72.35707362346617799, 5.598654528085804216, 7.705886871421366635 ) ) ;
#50091=CARTESIAN_POINT ( 'NONE',  ( -113.0929263765346917, 3.094860106633356978, 9.524999999989150368 ) ) ;
#50093=CARTESIAN_POINT ( 'NONE',  ( -113.0070736234661695, -8.102448949553174629, -5.886773742842741797 ) ) ;
#50098=CARTESIAN_POINT ( 'NONE',  ( -52.79499999999997328, 2.607480562269068880, -8.024999999999993250 ) ) ;
#50102=CARTESIAN_POINT ( 'NONE',  ( -138.2070736234667550, 3.094860106627642882, 9.524999999993303490 ) ) ;
#50106=CARTESIAN_POINT ( 'NONE',  ( -49.64499999999999602, 4.716976649647091513, -6.492361379858946790 ) ) ;
#50111=CARTESIAN_POINT ( 'NONE',  ( -116.4549999999999841, 7.632228543268599452, -2.479861379858951942 ) ) ;
#50118=CARTESIAN_POINT ( 'NONE',  ( -153.2070736234662149, 3.094860106618433360, 9.524999999999991473 ) ) ;
#50121=CARTESIAN_POINT ( 'NONE',  ( -81.80707362346615241, 10.01517768586948698, -1.839758294383808571E-15 ) ) ;
#50122=CARTESIAN_POINT ( 'NONE',  ( -95.09292637653494751, 3.094860106637121522, 9.524999999986416555 ) ) ;
#50126=CARTESIAN_POINT ( 'NONE',  ( -126.8050000000000068, -8.437984349512085203, 5.166775262442717831E-16 ) ) ;
#50130=CARTESIAN_POINT ( 'NONE',  ( -133.1950000000000216, 8.437984349512085203, -1.550032578732815448E-15 ) ) ;
#50132=CARTESIAN_POINT ( 'NONE',  ( -132.7450000000000045, 4.716976649647094177, 6.492361379858945902 ) ) ;
#50139=CARTESIAN_POINT ( 'NONE',  ( -179.3929263765337794, 8.102448949553176405, 5.886773742842740909 ) ) ;
#50140=CARTESIAN_POINT ( 'NONE',  ( -49.94499999999998607, -9.827790563157499189E-16, -8.024999999999991473 ) ) ;
#50149=CARTESIAN_POINT ( 'NONE',  ( -97.94292637653380496, 0.000000000000000000, 9.524999999999991473 ) ) ;
#50152=CARTESIAN_POINT ( 'NONE',  ( -162.0570736234661808, 0.000000000000000000, 9.524999999999991473 ) ) ;
#50163=DIRECTION ( 'NONE',  ( 0.000000000000000000, 0.000000000000000000, 1.000000000000000000 ) ) ;
#50169=CARTESIAN_POINT ( 'NONE',  ( -115.7070736234670250, -3.094860106632346675, -9.524999999989880450 ) ) ;
#50174=CARTESIAN_POINT ( 'NONE',  ( -95.39499999999999602, -6.826472737025115478, -4.959722759717899443 ) ) ;
#50186=LINE ( 'NONE', #13925, #2649 ) ;
#50188=CARTESIAN_POINT ( 'NONE',  ( -178.7070736234661581, -3.094860106618431139, -9.524999999999991473 ) ) ;
#50190=LINE ( 'NONE', #66344, #2622 ) ;
#50191=CARTESIAN_POINT ( 'NONE',  ( -117.3570736234661780, 5.598654528085804216, 7.705886871421366635 ) ) ;
#50198=ADVANCED_FACE ( 'NONE', ( #24287 ), #60518, .T. ) ;
#50202=CARTESIAN_POINT ( 'NONE',  ( -160.7049999999999841, 2.607480562269073321, 8.024999999999991473 ) ) ;
#50206=CARTESIAN_POINT ( 'NONE',  ( -160.4949999999999761, 6.826472737025113702, -4.959722759717902107 ) ) ;
#50207=CARTESIAN_POINT ( 'NONE',  ( -155.6949999999999932, -8.437984349512086979, 5.166775262442717831E-16 ) ) ;
#50208=EDGE_LOOP ( 'NONE', ( #62295, #48900, #43044, #11243 ) ) ;
#50213=CARTESIAN_POINT ( 'NONE',  ( -162.4429263765338192, -1.166476076187852838E-15, -9.524999999999991473 ) ) ;
#50214=CARTESIAN_POINT ( 'NONE',  ( -78.05499999999997840, -9.827790563157499189E-16, -8.024999999999991473 ) ) ;
#50217=CARTESIAN_POINT ( 'NONE',  ( -70.04499999999998749, 7.632228543268600340, 2.479861379858949277 ) ) ;
#50219=EDGE_CURVE ( 'NONE', #52874, #31166, #3630, .T. ) ;
#50239=CARTESIAN_POINT ( 'NONE',  ( -101.4549999999999841, 7.632228543268599452, -2.479861379858951942 ) ) ;
#50250=EDGE_CURVE ( 'NONE', #45861, #2564, #3482, .T. ) ;
#50251=VERTEX_POINT ( 'NONE', #30592 ) ;
#50255=ORIENTED_EDGE ( 'NONE', *, *, #57023, .F. ) ;
#50267=CARTESIAN_POINT ( 'NONE',  ( -137.0049999999999670, 6.826472737025116366, 4.959722759717898555 ) ) ;
#50273=EDGE_CURVE ( 'NONE', #54371, #39475, #29764, .T. ) ;
#50274=CARTESIAN_POINT ( 'NONE',  ( -156.4429263765338192, -1.166476076187852838E-15, -9.524999999999991473 ) ) ;
#50280=CARTESIAN_POINT ( 'NONE',  ( -50.30499999999999261, 8.437984349512085203, -1.550032578732815448E-15 ) ) ;
#50286=CARTESIAN_POINT ( 'NONE',  ( -182.6949999999999648, -8.437984349512086979, 5.166775262442717831E-16 ) ) ;
#50298=CARTESIAN_POINT ( 'NONE',  ( -104.5449999999999875, -7.632228543268600340, -2.479861379858950166 ) ) ;
#50300=CARTESIAN_POINT ( 'NONE',  ( -78.29499999999997328, -2.607480562269069768, 8.024999999999991473 ) ) ;
#50304=FACE_OUTER_BOUND ( 'NONE', #49997, .T. ) ;
#50309=CARTESIAN_POINT ( 'NONE',  ( -114.4429263765338050, -1.166476076187852838E-15, -9.524999999999991473 ) ) ;
#50310=CARTESIAN_POINT ( 'NONE',  ( -135.5949999999999989, 2.607480562269073321, 8.024999999999991473 ) ) ;
#50323=DIRECTION ( 'NONE',  ( -1.000000000000000000, -0.000000000000000000, -0.000000000000000000 ) ) ;
#50327=CARTESIAN_POINT ( 'NONE',  ( -130.2549999999999955, -4.716976649647092401, 6.492361379858946790 ) ) ;
#50338=CARTESIAN_POINT ( 'NONE',  ( -52.40499999999997982, -2.607480562269069768, 8.024999999999991473 ) ) ;
#50349=ORIENTED_EDGE ( 'NONE', *, *, #47735, .T. ) ;
#50353=CARTESIAN_POINT ( 'NONE',  ( -164.4549999999999841, 7.632228543268599452, -2.479861379858951942 ) ) ;
#50365=CARTESIAN_POINT ( 'NONE',  ( -72.35499999999998977, -4.716976649647093289, -6.492361379858945902 ) ) ;
#50371=ORIENTED_EDGE ( 'NONE', *, *, #43345, .F. ) ;
#50378=CARTESIAN_POINT ( 'NONE',  ( -109.1949999999999648, 8.437984349512085203, -1.550032578732815448E-15 ) ) ;
#50384=CARTESIAN_POINT ( 'NONE',  ( -19.73190520809190929, 11.89070917026893603, 1.623664015870753596 ) ) ;
#50385=CARTESIAN_POINT ( 'NONE',  ( -153.2929263765337566, 3.094860106618428031, -9.524999999999993250 ) ) ;
#50386=CARTESIAN_POINT ( 'NONE',  ( -169.1949999999999932, 8.437984349512085203, -1.550032578732815448E-15 ) ) ;
#50388=ADVANCED_FACE ( 'NONE', ( #38956 ), #38617, .T. ) ;
#50392=ORIENTED_EDGE ( 'NONE', *, *, #19452, .F. ) ;
#50393=CARTESIAN_POINT ( 'NONE',  ( -69.14292637653379359, 5.598654528085800663, -7.705886871421367523 ) ) ;
#50402=CARTESIAN_POINT ( 'NONE',  ( -173.7549999999999955, 4.716976649647091513, -6.492361379858946790 ) ) ;
#50414=CARTESIAN_POINT ( 'NONE',  ( -83.75499999999998124, 4.716976649647091513, -6.492361379858946790 ) ) ;
#50422=CARTESIAN_POINT ( 'NONE',  ( -174.4429263765337907, -1.166476076187852838E-15, -9.524999999999991473 ) ) ;
#50426=CARTESIAN_POINT ( 'NONE',  ( -140.9070736234666583, -3.094860106609825134, 9.525000000006246026 ) ) ;
#50427=CARTESIAN_POINT ( 'NONE',  ( -56.24499999999999034, -4.716976649647093289, -6.492361379858945902 ) ) ;
#50435=CARTESIAN_POINT ( 'NONE',  ( -56.24499999999999034, -4.716976649647093289, -6.492361379858945902 ) ) ;
#50439=CARTESIAN_POINT ( 'NONE',  ( -105.6549999999999869, -7.632228543268600340, -2.479861379858950166 ) ) ;
#50444=CARTESIAN_POINT ( 'NONE',  ( -149.4570736234661581, -9.058813317711329915, 2.943386871421371787 ) ) ;
#50448=CARTESIAN_POINT ( 'NONE',  ( -83.60707362346616378, -8.102448949553172852, 5.886773742842742685 ) ) ;
#50457=CARTESIAN_POINT ( 'NONE',  ( -134.3050000000000352, 8.437984349512085203, -1.550032578732815448E-15 ) ) ;
#50461=CARTESIAN_POINT ( 'NONE',  ( -132.2949999999999875, -2.607480562269069768, 8.024999999999991473 ) ) ;
#50464=CARTESIAN_POINT ( 'NONE',  ( -131.9949999999999761, -6.826472737025113702, 4.959722759717902107 ) ) ;
#50468=CARTESIAN_POINT ( 'NONE',  ( -145.8570736234661638, -5.598654528085803328, -7.705886871421366635 ) ) ;
#50470=CARTESIAN_POINT ( 'NONE',  ( -177.2929263765337851, 3.094860106618428031, -9.524999999999993250 ) ) ;
#50472=CARTESIAN_POINT ( 'NONE',  ( -50.84499999999997044, -7.632228543268599452, 2.479861379858951054 ) ) ;
#50478=CARTESIAN_POINT ( 'NONE',  ( -96.44292637653380496, -1.166476076187852838E-15, -9.524999999999991473 ) ) ;
#50484=CARTESIAN_POINT ( 'NONE',  ( -81.20707362346617231, 3.094860106618433360, 9.524999999999991473 ) ) ;
#50486=FACE_OUTER_BOUND ( 'NONE', #67811, .T. ) ;
#50503=CARTESIAN_POINT ( 'NONE',  ( -94.79292637653489351, -3.094860106599741201, 9.525000000013569945 ) ) ;
#50508=CARTESIAN_POINT ( 'NONE',  ( -70.55707362346616662, -1.166476076187852838E-15, -9.524999999999991473 ) ) ;
#50509=CARTESIAN_POINT ( 'NONE',  ( -83.99499999999999034, -6.826472737025115478, 4.959722759717900331 ) ) ;
#50514=( BOUNDED_CURVE ( )  B_SPLINE_CURVE ( 2, ( #60132, #23523, #45034, #66443, #18260, #39748, #12974, #949, #22504, #44002, #34434 ),
 .UNSPECIFIED., .F., .T. ) 
 B_SPLINE_CURVE_WITH_KNOTS ( ( 3, 2, 2, 2, 2, 3 ),
 ( 0.9456521739130434590, 0.9478260869565217073, 0.9499999999999999556, 0.9521739130434783149, 0.9543478260869565633, 0.9565217391304348116 ),
 .UNSPECIFIED. ) 
 CURVE ( )  GEOMETRIC_REPRESENTATION_ITEM ( )  RATIONAL_B_SPLINE_CURVE ( ( 1.000000000000000000, 0.9510565162951535312, 1.000000000000000000, 0.9510565162951535312, 1.000000000000000000, 0.9510565162951535312, 1.000000000000000000, 0.9510565162951535312, 1.000000000000000000, 0.9510565162951535312, 1.000000000000000000 ) ) 
 REPRESENTATION_ITEM ( '' )  );
#50533=CARTESIAN_POINT ( 'NONE',  ( -180.5070736234661979, 8.102448949553176405, 5.886773742842740909 ) ) ;
#50536=CARTESIAN_POINT ( 'NONE',  ( -111.5070736234661837, 8.102448949553176405, 5.886773742842740909 ) ) ;
#50537=EDGE_CURVE ( 'NONE', #27751, #21970, #17673, .T. ) ;
#50545=CARTESIAN_POINT ( 'NONE',  ( -164.3049999999999784, 8.437984349512085203, -1.550032578732815448E-15 ) ) ;
#50547=CARTESIAN_POINT ( 'NONE',  ( -183.3519149756361912, 1.436423777000723276E-13, -9.173085024363883733 ) ) ;
#50548=CARTESIAN_POINT ( 'NONE',  ( -164.6949999999999648, -8.437984349512085203, 5.166775262442717831E-16 ) ) ;
#50549=CARTESIAN_POINT ( 'NONE',  ( -152.9950000000000045, -6.826472737025113702, 4.959722759717902107 ) ) ;
#50556=CARTESIAN_POINT ( 'NONE',  ( -77.90500000000000114, 2.607480562269068880, -8.024999999999993250 ) ) ;
#50558=CARTESIAN_POINT ( 'NONE',  ( -166.9429263765337907, 0.000000000000000000, 9.524999999999991473 ) ) ;
#50559=CARTESIAN_POINT ( 'NONE',  ( -67.79499999999998749, 2.607480562269069324, -8.024999999999993250 ) ) ;
#50569=CARTESIAN_POINT ( 'NONE',  ( -120.2929263765346377, 3.094860106604916616, -9.525000000009809398 ) ) ;
#50574=CARTESIAN_POINT ( 'NONE',  ( -156.1429263765338078, 5.598654528085800663, -7.705886871421367523 ) ) ;
#50586=CARTESIAN_POINT ( 'NONE',  ( -110.6949999999999932, -8.437984349512085203, 5.166775262442717831E-16 ) ) ;
#50587=EDGE_LOOP ( 'NONE', ( #54547, #8792, #29198, #2876 ) ) ;
#50588=EDGE_CURVE ( 'NONE', #33393, #1575, #12702, .T. ) ;
#50592=CARTESIAN_POINT ( 'NONE',  ( -10.26016645771925262, -11.89338941245402737, 1.624758447612887347 ) ) ;
#50604=CARTESIAN_POINT ( 'NONE',  ( -157.5570736234661808, -1.166476076187852838E-15, -9.524999999999991473 ) ) ;
#50605=CARTESIAN_POINT ( 'NONE',  ( -131.3050000000000068, 8.437984349512085203, -1.550032578732815448E-15 ) ) ;
#50622=CARTESIAN_POINT ( 'NONE',  ( -184.5550000000000068, 0.000000000000000000, 8.024999999999991473 ) ) ;
#50626=CARTESIAN_POINT ( 'NONE',  ( -51.35707362346617089, 5.598654528085804216, 7.705886871421366635 ) ) ;
#50628=CARTESIAN_POINT ( 'NONE',  ( -177.8070736234661808, 10.01517768586948698, -1.839758294383808966E-15 ) ) ;
#50631=CARTESIAN_POINT ( 'NONE',  ( -145.1070736234661638, 8.102448949553172852, -5.886773742842744461 ) ) ;
#50633=CARTESIAN_POINT ( 'NONE',  ( -98.60499999999997556, 6.826472737025113702, -4.959722759717902107 ) ) ;
#50637=CARTESIAN_POINT ( 'NONE',  ( -96.44499999999999318, 0.000000000000000000, 8.024999999999991473 ) ) ;
#50639=CARTESIAN_POINT ( 'NONE',  ( -81.59499999999997044, 2.607480562269073321, 8.024999999999991473 ) ) ;
#50642=DIRECTION ( 'NONE',  ( 1.000000000000000000, 0.000000000000000000, 0.000000000000000000 ) ) ;
#50644=CARTESIAN_POINT ( 'NONE',  ( -195.0000000000000000, 0.000000000000000000, 0.000000000000000000 ) ) ;
#50649=CARTESIAN_POINT ( 'NONE',  ( -117.7429263765338021, -5.598654528085803328, -7.705886871421366635 ) ) ;
#50650=CARTESIAN_POINT ( 'NONE',  ( -138.1449999999999818, -4.716976649647092401, 6.492361379858946790 ) ) ;
#50662=FACE_OUTER_BOUND ( 'NONE', #10797, .T. ) ;
#50666=CARTESIAN_POINT ( 'NONE',  ( -134.7549999999999955, 4.716976649647091513, -6.492361379858946790 ) ) ;
#50667=ORIENTED_EDGE ( 'NONE', *, *, #26584, .F. ) ;
#50672=CARTESIAN_POINT ( 'NONE',  ( -83.99292637653380211, 8.102448949553172852, -5.886773742842744461 ) ) ;
#50674=VECTOR ( 'NONE', #59311, 1000.000000000000000 ) ;
#50675=CARTESIAN_POINT ( 'NONE',  ( -102.4429263765338050, -1.166476076187852838E-15, -9.524999999999991473 ) ) ;
#50684=CARTESIAN_POINT ( 'NONE',  ( -49.40499999999997982, -2.607480562269069768, 8.024999999999991473 ) ) ;
#50699=CARTESIAN_POINT ( 'NONE',  ( -158.4549999999999841, 7.632228543268599452, -2.479861379858951942 ) ) ;
#50712=CARTESIAN_POINT ( 'NONE',  ( -73.85499999999998977, 4.716976649647094177, 6.492361379858945902 ) ) ;
#50726=CARTESIAN_POINT ( 'NONE',  ( -106.4950000000000045, 6.826472737025113702, -4.959722759717902107 ) ) ;
#50734=CARTESIAN_POINT ( 'NONE',  ( -19.96671590325603418, 11.98602375733942438, -0.6633104301215919651 ) ) ;
#50735=CARTESIAN_POINT ( 'NONE',  ( -140.2429263765338021, 5.598654528085804216, 7.705886871421366635 ) ) ;
#50736=CARTESIAN_POINT ( 'NONE',  ( -164.3950000000000102, -6.826472737025115478, -4.959722759717899443 ) ) ;
#50737=( GEOMETRIC_REPRESENTATION_CONTEXT ( 3 ) GLOBAL_UNCERTAINTY_ASSIGNED_CONTEXT ( ( #13117 ) ) GLOBAL_UNIT_ASSIGNED_CONTEXT ( ( #18254, #7007, #45378 ) ) REPRESENTATION_CONTEXT ( 'NONE', 'WORKASPACE' ) );
#50746=DIRECTION ( 'NONE',  ( -1.000000000000000000, 0.000000000000000000, 0.000000000000000000 ) ) ;
#50752=CARTESIAN_POINT ( 'NONE',  ( -160.2549999999999670, -4.716976649647092401, 6.492361379858946790 ) ) ;
#50762=EDGE_LOOP ( 'NONE', ( #39715, #24940, #7448, #38608 ) ) ;
#50766=CARTESIAN_POINT ( 'NONE',  ( -77.00499999999999545, 6.826472737025115478, 4.959722759717899443 ) ) ;
#50771=EDGE_CURVE ( 'NONE', #16969, #50010, #19086, .T. ) ;
#50775=CARTESIAN_POINT ( 'NONE',  ( -113.7570736234661837, -5.598654528085801552, 7.705886871421367523 ) ) ;
#50777=CARTESIAN_POINT ( 'NONE',  ( -57.29499999999998039, -2.607480562269069768, 8.024999999999991473 ) ) ;
#50784=CARTESIAN_POINT ( 'NONE',  ( -53.24499999999999034, -4.716976649647093289, -6.492361379858945902 ) ) ;
#50789=CARTESIAN_POINT ( 'NONE',  ( -107.4549999999999983, 7.632228543268599452, -2.479861379858951942 ) ) ;
#50794=CARTESIAN_POINT ( 'NONE',  ( -144.6570736234662036, 9.058813317711329915, 2.943386871421369566 ) ) ;
#50799=CARTESIAN_POINT ( 'NONE',  ( -88.55707362346616662, -1.166476076187852838E-15, -9.524999999999991473 ) ) ;
#50806=CARTESIAN_POINT ( 'NONE',  ( -117.0549999999999926, -9.827790563157499189E-16, -8.024999999999991473 ) ) ;
#50808=CARTESIAN_POINT ( 'NONE',  ( -159.2929263765341261, 3.094860106613084305, -9.525000000003878142 ) ) ;
#50810=CARTESIAN_POINT ( 'NONE',  ( -138.5949999999999420, 2.607480562269073321, 8.024999999999991473 ) ) ;
#50811=CARTESIAN_POINT ( 'NONE',  ( -118.3449999999999989, 7.632228543268599452, -2.479861379858951942 ) ) ;
#50816=CARTESIAN_POINT ( 'NONE',  ( -171.7429263765338305, -5.598654528085803328, -7.705886871421366635 ) ) ;
#50818=CARTESIAN_POINT ( 'NONE',  ( -49.19499999999999318, 8.437984349512085203, -1.550032578732815448E-15 ) ) ;
#50825=( BOUNDED_CURVE ( )  B_SPLINE_CURVE ( 2, ( #59673, #6220, #32257, #6537, #43563, #179, #21704, #27299, #27648, #49157, #64625 ),
 .UNSPECIFIED., .F., .F. ) 
 B_SPLINE_CURVE_WITH_KNOTS ( ( 3, 2, 2, 2, 2, 3 ),
 ( 0.1195652173913016314, 0.1217391304347798520, 0.1239130434782580725, 0.1260869565217362653, 0.1282608695652145137, 0.1304347826086927065 ),
 .UNSPECIFIED. ) 
 CURVE ( )  GEOMETRIC_REPRESENTATION_ITEM ( )  RATIONAL_B_SPLINE_CURVE ( ( 1.000000000000061284, 0.9510565162950922469, 1.000000000000000000, 0.9510565162951535312, 1.000000000000000000, 0.9510565162951535312, 1.000000000000000000, 0.9510565162951535312, 1.000000000000000000, 0.9510565162952198115, 0.9999999999999337197 ) ) 
 REPRESENTATION_ITEM ( '' )  );
#50826=CARTESIAN_POINT ( 'NONE',  ( -100.0429263765338135, -9.058813317711329915, -2.943386871421370898 ) ) ;
#50833=CARTESIAN_POINT ( 'NONE',  ( -156.8070736234661524, 10.01517768586948698, -1.839758294383808966E-15 ) ) ;
#50835=EDGE_LOOP ( 'NONE', ( #17414, #8089, #14194, #44933, #7996, #44901, #12622, #69419 ) ) ;
#50848=CARTESIAN_POINT ( 'NONE',  ( -94.94292637653380496, 0.000000000000000000, 9.524999999999991473 ) ) ;
#50855=LINE ( 'NONE', #18827, #54196 ) ;
#50856=CARTESIAN_POINT ( 'NONE',  ( -78.14499999999999602, -4.716976649647092401, 6.492361379858946790 ) ) ;
#50869=DIRECTION ( 'NONE',  ( -1.000000000000000000, -0.000000000000000000, -0.000000000000000000 ) ) ;
#50873=CARTESIAN_POINT ( 'NONE',  ( -168.6570736234661751, 9.058813317711329915, 2.943386871421369566 ) ) ;
#50876=CARTESIAN_POINT ( 'NONE',  ( -117.0570736234661808, 0.000000000000000000, 9.524999999999991473 ) ) ;
#50878=CARTESIAN_POINT ( 'NONE',  ( -183.1589919394749586, 4.545776238418753223, -8.196812015063720480 ) ) ;
#50879=CARTESIAN_POINT ( 'NONE',  ( -84.05707362346618083, 0.000000000000000000, 9.524999999999991473 ) ) ;
#50885=CARTESIAN_POINT ( 'NONE',  ( -149.0049999999999386, 6.826472737025116366, 4.959722759717898555 ) ) ;
#50887=CARTESIAN_POINT ( 'NONE',  ( -164.3950000000000102, -6.826472737025115478, -4.959722759717899443 ) ) ;
#50890=CARTESIAN_POINT ( 'NONE',  ( -160.4949999999999761, 6.826472737025113702, -4.959722759717902107 ) ) ;
#50895=CARTESIAN_POINT ( 'NONE',  ( -69.95499999999998408, -7.632228543268599452, 2.479861379858951054 ) ) ;
#50898=CARTESIAN_POINT ( 'NONE',  ( -73.64499999999998181, 4.716976649647091513, -6.492361379858946790 ) ) ;
#50904=CARTESIAN_POINT ( 'NONE',  ( -195.0000000000000000, 0.000000000000000000, 9.524999999999991473 ) ) ;
#50914=EDGE_CURVE ( 'NONE', #36781, #66538, #16700, .T. ) ;
#50921=DIRECTION ( 'NONE',  ( -1.000000000000000000, -0.000000000000000000, -0.000000000000000000 ) ) ;
#50922=( BOUNDED_CURVE ( )  B_SPLINE_CURVE ( 2, ( #29603, #44787, #39499, #39860, #51415, #61584, #13074, #3160, #23291, #34528, #1780 ),
 .UNSPECIFIED., .F., .F. ) 
 B_SPLINE_CURVE_WITH_KNOTS ( ( 3, 2, 2, 2, 2, 3 ),
 ( 0.9347826086956522174, 0.9369565217391304657, 0.9391304347826087140, 0.9413043478260869623, 0.9434782608695652106, 0.9456521739130434590 ),
 .UNSPECIFIED. ) 
 CURVE ( )  GEOMETRIC_REPRESENTATION_ITEM ( )  RATIONAL_B_SPLINE_CURVE ( ( 1.000000000000000000, 0.9510565162951535312, 1.000000000000000000, 0.9510565162951535312, 1.000000000000000000, 0.9510565162951535312, 1.000000000000000000, 0.9510565162951535312, 1.000000000000000000, 0.9510565162951535312, 1.000000000000000000 ) ) 
 REPRESENTATION_ITEM ( '' )  );
#50927=ORIENTED_EDGE ( 'NONE', *, *, #38372, .T. ) ;
#50937=CARTESIAN_POINT ( 'NONE',  ( -112.9449999999999932, -9.827790563157499189E-16, -8.024999999999991473 ) ) ;
#50941=CARTESIAN_POINT ( 'NONE',  ( -11.03049116848387001, -11.60726128400439805, -3.057421598022181719 ) ) ;
#50943=VERTEX_POINT ( 'NONE', #9959 ) ;
#50948=VECTOR ( 'NONE', #21580, 1000.000000000000000 ) ;
#50955=CARTESIAN_POINT ( 'NONE',  ( -135.3549999999999898, -4.716976649647093289, -6.492361379858945902 ) ) ;
#50967=CARTESIAN_POINT ( 'NONE',  ( -49.40499999999996561, -2.607480562269069768, 8.024999999999991473 ) ) ;
#50972=CARTESIAN_POINT ( 'NONE',  ( -52.10707362346616378, 8.102448949553171076, -5.886773742842744461 ) ) ;
#50980=CARTESIAN_POINT ( 'NONE',  ( -106.1049999999999756, -6.826472737025115478, 4.959722759717900331 ) ) ;
#50984=CARTESIAN_POINT ( 'NONE',  ( -102.5949999999999847, 2.607480562269072433, 8.024999999999991473 ) ) ;
#50986=CARTESIAN_POINT ( 'NONE',  ( -67.04499999999997328, 7.632228543268600340, 2.479861379858949277 ) ) ;
#50997=CARTESIAN_POINT ( 'NONE',  ( -117.8929263765337794, -8.102448949553172852, -5.886773742842741797 ) ) ;
#50998=CARTESIAN_POINT ( 'NONE',  ( -135.8949999999999818, 6.826472737025116366, 4.959722759717898555 ) ) ;
#51005=VERTEX_POINT ( 'NONE', #22232 ) ;
#51009=ADVANCED_FACE ( 'NONE', ( #43728 ), #14635, .T. ) ;
#51015=EDGE_LOOP ( 'NONE', ( #34950, #14995, #37415, #57103 ) ) ;
#51016=CARTESIAN_POINT ( 'NONE',  ( -131.9050000000000011, 2.607480562269069324, -8.024999999999993250 ) ) ;
#51020=CARTESIAN_POINT ( 'NONE',  ( -123.8070736234661808, 10.01517768586948698, -1.839758294383808571E-15 ) ) ;
#51022=CARTESIAN_POINT ( 'NONE',  ( -172.7929263765339840, -3.094860106616026396, 9.525000000001739409 ) ) ;
#51023=CARTESIAN_POINT ( 'NONE',  ( -97.94292637653380496, 0.000000000000000000, 9.524999999999991473 ) ) ;
#51046=AXIS2_PLACEMENT_3D ( 'NONE', #28667, #13895, #50163 ) ;
#51050=CARTESIAN_POINT ( 'NONE',  ( -163.4050000000000011, -2.607480562269069768, 8.024999999999991473 ) ) ;
#51064=CARTESIAN_POINT ( 'NONE',  ( -74.45499999999999829, 7.632228543268599452, -2.479861379858951942 ) ) ;
#51069=CARTESIAN_POINT ( 'NONE',  ( -150.2070736234665560, 3.094860106625255458, 9.524999999995031885 ) ) ;
#51076=EDGE_CURVE ( 'NONE', #51005, #35517, #8201, .T. ) ;
#51080=CARTESIAN_POINT ( 'NONE',  ( -109.9449999999999932, -9.827790563157499189E-16, -8.024999999999991473 ) ) ;
#51081=DIRECTION ( 'NONE',  ( -1.000000000000000000, -0.000000000000000000, -0.000000000000000000 ) ) ;
#51082=CARTESIAN_POINT ( 'NONE',  ( -43.99999999999998579, 0.000000000000000000, 0.000000000000000000 ) ) ;
#51086=CARTESIAN_POINT ( 'NONE',  ( -96.65707362346617515, 9.058813317711329915, 2.943386871421369566 ) ) ;
#51089=CARTESIAN_POINT ( 'NONE',  ( -144.2929263765337566, 3.094860106618428031, -9.524999999999993250 ) ) ;
#51090=CARTESIAN_POINT ( 'NONE',  ( -161.9950000000000045, -6.826472737025115478, 4.959722759717900331 ) ) ;
#51098=VERTEX_POINT ( 'NONE', #43846 ) ;
#51108=CARTESIAN_POINT ( 'NONE',  ( -156.5049999999999955, -6.826472737025113702, -4.959722759717900331 ) ) ;
#51115=CARTESIAN_POINT ( 'NONE',  ( -57.80707362346616662, 10.01517768586948698, -1.839758294383808966E-15 ) ) ;
#51120=CARTESIAN_POINT ( 'NONE',  ( -71.60499999999998977, 6.826472737025113702, -4.959722759717902107 ) ) ;
#51121=VECTOR ( 'NONE', #37189, 1000.000000000000000 ) ;
#51129=ORIENTED_EDGE ( 'NONE', *, *, #48594, .T. ) ;
#51132=CARTESIAN_POINT ( 'NONE',  ( -53.24499999999999034, -4.716976649647093289, -6.492361379858945902 ) ) ;
#51141=CARTESIAN_POINT ( 'NONE',  ( -49.19499999999998607, 8.437984349512086979, -1.550032578732815448E-15 ) ) ;
#51145=CARTESIAN_POINT ( 'NONE',  ( -102.9549999999999841, -7.632228543268599452, 2.479861379858951054 ) ) ;
#51149=CARTESIAN_POINT ( 'NONE',  ( -139.4070736234661751, 3.094860106618428031, -9.524999999999993250 ) ) ;
#51153=CARTESIAN_POINT ( 'NONE',  ( -85.70707362346617231, -3.094860106618431139, -9.524999999999991473 ) ) ;
#51160=EDGE_CURVE ( 'NONE', #41299, #27775, #34284, .T. ) ;
#51162=CARTESIAN_POINT ( 'NONE',  ( -122.0049999999999670, 6.826472737025116366, 4.959722759717898555 ) ) ;
#51164=CARTESIAN_POINT ( 'NONE',  ( -137.5449999999999875, -7.632228543268600340, -2.479861379858950166 ) ) ;
#51166=CARTESIAN_POINT ( 'NONE',  ( -115.0449999999999875, 7.632228543268600340, 2.479861379858949277 ) ) ;
#51173=CARTESIAN_POINT ( 'NONE',  ( -175.9429263765337907, 0.000000000000000000, 9.524999999999991473 ) ) ;
#51179=CARTESIAN_POINT ( 'NONE',  ( -84.44292637653380496, -1.166476076187852838E-15, -9.524999999999991473 ) ) ;
#51182=CARTESIAN_POINT ( 'NONE',  ( -179.5429263765338135, 9.058813317711329915, 2.943386871421369566 ) ) ;
#51184=CARTESIAN_POINT ( 'NONE',  ( -78.95707362346617231, 9.058813317711329915, -2.943386871421373119 ) ) ;
#51209=CARTESIAN_POINT ( 'NONE',  ( -79.94499999999999318, -9.827790563157499189E-16, -8.024999999999991473 ) ) ;
#51213=CARTESIAN_POINT ( 'NONE',  ( -76.49292637653380211, -8.102448949553174629, 5.886773742842742685 ) ) ;
#51223=CARTESIAN_POINT ( 'NONE',  ( -173.1570736234662036, -9.058813317711329915, -2.943386871421370898 ) ) ;
#51226=CARTESIAN_POINT ( 'NONE',  ( -111.8070736234661666, 10.01517768586948698, -1.839758294383808571E-15 ) ) ;
#51236=CARTESIAN_POINT ( 'NONE',  ( -146.4550000000000125, 7.632228543268599452, -2.479861379858951942 ) ) ;
#51239=CARTESIAN_POINT ( 'NONE',  ( -164.5449999999999875, -7.632228543268600340, -2.479861379858950166 ) ) ;
#51242=CARTESIAN_POINT ( 'NONE',  ( -145.0449999999999875, 7.632228543268600340, 2.479861379858949277 ) ) ;
#51243=( BOUNDED_CURVE ( )  B_SPLINE_CURVE ( 2, ( #59066, #10885, #47894, #27026, #21790, #43304, #65021, #45357, #27719, #11918, #66775 ),
 .UNSPECIFIED., .F., .F. ) 
 B_SPLINE_CURVE_WITH_KNOTS ( ( 3, 2, 2, 2, 2, 3 ),
 ( 0.02173913043478211196, 0.02391304347826032212, 0.02608695652173853227, 0.02826086956521674243, 0.03043478260869495605, 0.03260869565217316274 ),
 .UNSPECIFIED. ) 
 CURVE ( )  GEOMETRIC_REPRESENTATION_ITEM ( )  RATIONAL_B_SPLINE_CURVE ( ( 1.000000000000011102, 0.9510565162951423179, 1.000000000000000000, 0.9510565162951535312, 1.000000000000000000, 0.9510565162951535312, 1.000000000000000000, 0.9510565162951535312, 1.000000000000000000, 0.9510565162951704066, 0.9999999999999831246 ) ) 
 REPRESENTATION_ITEM ( '' )  );
#51246=CARTESIAN_POINT ( 'NONE',  ( -67.25499999999998124, -4.716976649647092401, 6.492361379858946790 ) ) ;
#51251=CARTESIAN_POINT ( 'NONE',  ( -59.54499999999998749, -7.632228543268600340, -2.479861379858950166 ) ) ;
#51257=CARTESIAN_POINT ( 'NONE',  ( -159.8070736234661808, 10.01517768586948698, -1.839758294383808966E-15 ) ) ;
#51260=DIRECTION ( 'NONE',  ( -1.000000000000000000, -0.000000000000000000, -0.000000000000000000 ) ) ;
#51273=DIRECTION ( 'NONE',  ( -1.000000000000000000, -0.000000000000000000, -0.000000000000000000 ) ) ;
#51275=VERTEX_POINT ( 'NONE', #67004 ) ;
#51279=VERTEX_POINT ( 'NONE', #3903 ) ;
#51281=CARTESIAN_POINT ( 'NONE',  ( -110.3949999999999818, -6.826472737025115478, -4.959722759717899443 ) ) ;
#51285=CARTESIAN_POINT ( 'NONE',  ( -15.00000000000000000, -10.90871211463571022, -5.000000000000000000 ) ) ;
#51287=ORIENTED_EDGE ( 'NONE', *, *, #52743, .F. ) ;
#51301=CARTESIAN_POINT ( 'NONE',  ( -158.1570736234661751, -9.058813317711329915, -2.943386871421370898 ) ) ;
#51302=CARTESIAN_POINT ( 'NONE',  ( -123.8049999999999926, -8.437984349512085203, 5.166775262442717831E-16 ) ) ;
#51314=CARTESIAN_POINT ( 'NONE',  ( -124.4070736234668857, 3.094860106606395433, -9.525000000008736478 ) ) ;
#51316=CARTESIAN_POINT ( 'NONE',  ( -183.3549999999999898, -4.716976649647093289, -6.492361379858945902 ) ) ;
#51319=CARTESIAN_POINT ( 'NONE',  ( -52.70707362346615099, -3.094860106618431139, -9.524999999999991473 ) ) ;
#51320=ADVANCED_FACE ( 'NONE', ( #49276 ), #38052, .T. ) ;
#51321=CARTESIAN_POINT ( 'NONE',  ( -173.0949999999999989, -2.607480562269071545, -8.024999999999991473 ) ) ;
#51326=CARTESIAN_POINT ( 'NONE',  ( -90.80499999999996419, -8.437984349512085203, 5.166775262442717831E-16 ) ) ;
#51332=CARTESIAN_POINT ( 'NONE',  ( -101.8449999999999847, -7.632228543268599452, 2.479861379858951054 ) ) ;
#51335=CARTESIAN_POINT ( 'NONE',  ( -63.74499999999998323, 4.716976649647094177, 6.492361379858945902 ) ) ;
#51340=( BOUNDED_CURVE ( )  B_SPLINE_CURVE ( 2, ( #64845, #16693, #65189, #31796, #42415, #38158, #32846, #54289, #10370, #53276, #6107 ),
 .UNSPECIFIED., .F., .F. ) 
 B_SPLINE_CURVE_WITH_KNOTS ( ( 3, 2, 2, 2, 2, 3 ),
 ( 0.0004239242079884921540, 0.002173913043478220130, 0.004347826086956429852, 0.006521739130434640007, 0.008695652173912851030, 0.01086956521739105945 ),
 .UNSPECIFIED. ) 
 CURVE ( )  GEOMETRIC_REPRESENTATION_ITEM ( )  RATIONAL_B_SPLINE_CURVE ( ( 0.9846338866369153120, 0.9606007469754098693, 1.000000000000000000, 0.9510565162951535312, 1.000000000000000000, 0.9510565162951535312, 1.000000000000000000, 0.9510565162951535312, 1.000000000000000000, 0.9510565162951590823, 0.9999999999999944489 ) ) 
 REPRESENTATION_ITEM ( '' )  );
#51343=CARTESIAN_POINT ( 'NONE',  ( -110.6929263765338050, 10.01517768586948698, -1.839758294383808571E-15 ) ) ;
#51344=CARTESIAN_POINT ( 'NONE',  ( -127.4950000000000045, 6.826472737025113702, -4.959722759717902107 ) ) ;
#51346=VECTOR ( 'NONE', #55615, 1000.000000000000000 ) ;
#51355=DIRECTION ( 'NONE',  ( -1.000000000000000000, -0.000000000000000000, -0.000000000000000000 ) ) ;
#51356=CARTESIAN_POINT ( 'NONE',  ( -126.2070736234668686, 3.094860106630264784, 9.524999999991395683 ) ) ;
#51358=CARTESIAN_POINT ( 'NONE',  ( -134.1550000000000011, 7.632228543268600340, 2.479861379858949277 ) ) ;
#51361=CARTESIAN_POINT ( 'NONE',  ( -120.0570736234661808, 0.000000000000000000, 9.524999999999991473 ) ) ;
#51362=ORIENTED_EDGE ( 'NONE', *, *, #39279, .F. ) ;
#51385=FACE_OUTER_BOUND ( 'NONE', #16551, .T. ) ;
#51386=CARTESIAN_POINT ( 'NONE',  ( -190.0000000000000000, 0.000000000000000000, 0.000000000000000000 ) ) ;
#51387=CARTESIAN_POINT ( 'NONE',  ( -166.8549999999999898, 4.716976649647094177, 6.492361379858945902 ) ) ;
#51402=CARTESIAN_POINT ( 'NONE',  ( -71.75499999999998124, 4.716976649647091513, -6.492361379858946790 ) ) ;
#51415=CARTESIAN_POINT ( 'NONE',  ( -53.45707362346615810, -9.058813317711329915, 2.943386871421371787 ) ) ;
#51418=CARTESIAN_POINT ( 'NONE',  ( -96.74499999999999034, 4.716976649647094177, 6.492361379858945902 ) ) ;
#51422=CARTESIAN_POINT ( 'NONE',  ( -145.1929263765338192, -10.01517768586948698, 6.132527647946031529E-16 ) ) ;
#51425=CARTESIAN_POINT ( 'NONE',  ( -169.7949999999999875, 2.607480562269068880, -8.024999999999993250 ) ) ;
#51437=CARTESIAN_POINT ( 'NONE',  ( -173.4570736234661865, -9.058813317711329915, 2.943386871421371787 ) ) ;
#51441=CARTESIAN_POINT ( 'NONE',  ( -163.1049999999999898, -6.826472737025113702, 4.959722759717902107 ) ) ;
#51452=CARTESIAN_POINT ( 'NONE',  ( -74.60500000000000398, 6.826472737025113702, -4.959722759717902107 ) ) ;
#51463=CARTESIAN_POINT ( 'NONE',  ( -55.94499999999999318, -9.827790563157499189E-16, -8.024999999999991473 ) ) ;
#51470=VERTEX_POINT ( 'NONE', #14059 ) ;
#51475=CARTESIAN_POINT ( 'NONE',  ( -103.4049999999999869, -2.607480562269069768, 8.024999999999991473 ) ) ;
#51477=CARTESIAN_POINT ( 'NONE',  ( -195.0000000000000000, 0.000000000000000000, 0.000000000000000000 ) ) ;
#51479=CARTESIAN_POINT ( 'NONE',  ( -143.0070736234661695, -8.102448949553172852, -5.886773742842741797 ) ) ;
#51483=CARTESIAN_POINT ( 'NONE',  ( -71.00707362346615525, -8.102448949553172852, -5.886773742842741797 ) ) ;
#51485=CARTESIAN_POINT ( 'NONE',  ( -184.0000000000000000, 1.044011396273115718E-15, 8.524999999999977263 ) ) ;
#51489=CARTESIAN_POINT ( 'NONE',  ( -120.0549999999999926, -9.827790563157499189E-16, -8.024999999999991473 ) ) ;
#51492=CARTESIAN_POINT ( 'NONE',  ( -126.7449999999999903, 4.716976649647094177, 6.492361379858945902 ) ) ;
#51493=CARTESIAN_POINT ( 'NONE',  ( -117.5949999999999847, 2.607480562269072433, 8.024999999999991473 ) ) ;
#51499=CARTESIAN_POINT ( 'NONE',  ( -173.0929263765337964, 3.094860106618433360, 9.524999999999991473 ) ) ;
#51500=CARTESIAN_POINT ( 'NONE',  ( -53.69499999999999318, -8.437984349512085203, 5.166775262442717831E-16 ) ) ;
#51507=CARTESIAN_POINT ( 'NONE',  ( -85.64292637653379359, -5.598654528085801552, 7.705886871421367523 ) ) ;
#51528=CARTESIAN_POINT ( 'NONE',  ( -104.1549999999999869, 7.632228543268600340, 2.479861379858949277 ) ) ;
#51533=CARTESIAN_POINT ( 'NONE',  ( -94.04292637653379927, -9.058813317711329915, -2.943386871421370898 ) ) ;
#51537=CARTESIAN_POINT ( 'NONE',  ( -171.4429263765337907, -1.166476076187852838E-15, -9.524999999999991473 ) ) ;
#51539=CARTESIAN_POINT ( 'NONE',  ( -77.24499999999997613, -4.716976649647093289, -6.492361379858945902 ) ) ;
#51546=ORIENTED_EDGE ( 'NONE', *, *, #28578, .T. ) ;
#51552=ORIENTED_EDGE ( 'NONE', *, *, #23588, .T. ) ;
#51554=ORIENTED_EDGE ( 'NONE', *, *, #39932, .T. ) ;
#51560=CARTESIAN_POINT ( 'NONE',  ( -166.7070736234661865, -3.094860106618431139, -9.524999999999991473 ) ) ;
#51564=CARTESIAN_POINT ( 'NONE',  ( -102.2070736234661865, 3.094860106618433360, 9.524999999999991473 ) ) ;
#51575=CARTESIAN_POINT ( 'NONE',  ( -153.3549999999999898, -4.716976649647093289, -6.492361379858945902 ) ) ;
#51577=CARTESIAN_POINT ( 'NONE',  ( -167.9950000000000045, -6.826472737025115478, 4.959722759717900331 ) ) ;
#51579=CARTESIAN_POINT ( 'NONE',  ( -147.8950000000000102, 6.826472737025115478, 4.959722759717899443 ) ) ;
#51586=CARTESIAN_POINT ( 'NONE',  ( -66.65499999999998693, -7.632228543268600340, -2.479861379858950166 ) ) ;
#51589=CARTESIAN_POINT ( 'NONE',  ( -167.3929263765338078, 8.102448949553176405, 5.886773742842740909 ) ) ;
#51590=CARTESIAN_POINT ( 'NONE',  ( -66.44499999999999318, 0.000000000000000000, 8.024999999999991473 ) ) ;
#51597=VECTOR ( 'NONE', #62025, 1000.000000000000000 ) ;
#51604=CARTESIAN_POINT ( 'NONE',  ( -60.80707362346617373, 10.01517768586948698, -1.839758294383808966E-15 ) ) ;
#51615=CARTESIAN_POINT ( 'NONE',  ( -77.30707362346615241, -10.01517768586948698, 6.132527647946031529E-16 ) ) ;
#51622=CARTESIAN_POINT ( 'NONE',  ( -66.14292637653379359, 5.598654528085800663, -7.705886871421367523 ) ) ;
#51625=CARTESIAN_POINT ( 'NONE',  ( -180.0570736234661808, 0.000000000000000000, 9.524999999999991473 ) ) ;
#51626=CARTESIAN_POINT ( 'NONE',  ( -113.2449999999999903, -4.716976649647093289, -6.492361379858945902 ) ) ;
#51645=CARTESIAN_POINT ( 'NONE',  ( -123.6549999999999869, -7.632228543268600340, -2.479861379858950166 ) ) ;
#51649=DIRECTION ( 'NONE',  ( -1.000000000000000000, -0.000000000000000000, -0.000000000000000000 ) ) ;
#51661=CARTESIAN_POINT ( 'NONE',  ( -124.5570736234661808, -1.166476076187852838E-15, -9.524999999999991473 ) ) ;
#51662=CARTESIAN_POINT ( 'NONE',  ( -178.8549999999999898, 4.716976649647094177, 6.492361379858945902 ) ) ;
#51666=CARTESIAN_POINT ( 'NONE',  ( -54.35707362346617089, 5.598654528085804216, 7.705886871421366635 ) ) ;
#51668=CARTESIAN_POINT ( 'NONE',  ( -172.4950000000000330, 6.826472737025113702, -4.959722759717902107 ) ) ;
#51676=DIRECTION ( 'NONE',  ( -1.000000000000000000, -0.000000000000000000, -0.000000000000000000 ) ) ;
#51677=CARTESIAN_POINT ( 'NONE',  ( -93.50499999999999545, -6.826472737025115478, -4.959722759717899443 ) ) ;
#51681=CARTESIAN_POINT ( 'NONE',  ( -89.39499999999996760, -6.826472737025113702, -4.959722759717900331 ) ) ;
#51683=CARTESIAN_POINT ( 'NONE',  ( -65.54499999999998749, -7.632228543268600340, -2.479861379858950166 ) ) ;
#51693=CARTESIAN_POINT ( 'NONE',  ( -110.0929263765337822, 3.094860106618433360, 9.524999999999991473 ) ) ;
#51694=CARTESIAN_POINT ( 'NONE',  ( -131.0949999999999989, -2.607480562269071545, -8.024999999999991473 ) ) ;
#51711=CARTESIAN_POINT ( 'NONE',  ( -131.1550000000000011, 7.632228543268600340, 2.479861379858949277 ) ) ;
#51713=CARTESIAN_POINT ( 'NONE',  ( -118.7070736234661581, -3.094860106618431139, -9.524999999999991473 ) ) ;
#51718=VERTEX_POINT ( 'NONE', #8356 ) ;
#51721=CARTESIAN_POINT ( 'NONE',  ( -195.0000000000000000, 0.000000000000000000, 9.524999999999991473 ) ) ;
#51743=CARTESIAN_POINT ( 'NONE',  ( -58.04292637653379927, -9.058813317711329915, -2.943386871421370898 ) ) ;
#51747=CARTESIAN_POINT ( 'NONE',  ( -149.6050000000000182, 6.826472737025113702, -4.959722759717902107 ) ) ;
#51762=CARTESIAN_POINT ( 'NONE',  ( -79.40500000000000114, -2.607480562269069768, 8.024999999999991473 ) ) ;
#51771=CARTESIAN_POINT ( 'NONE',  ( -94.94499999999999318, -9.827790563157499189E-16, -8.024999999999991473 ) ) ;
#51779=CARTESIAN_POINT ( 'NONE',  ( -140.3929263765338078, 8.102448949553176405, 5.886773742842740909 ) ) ;
#51781=CARTESIAN_POINT ( 'NONE',  ( -157.4950000000000045, 6.826472737025113702, -4.959722759717902107 ) ) ;
#51800=CARTESIAN_POINT ( 'NONE',  ( -163.8549999999999898, 4.716976649647094177, 6.492361379858945902 ) ) ;
#51807=CYLINDRICAL_SURFACE ( 'NONE', #59564, 9.524999999999991473 ) ;
#51814=CARTESIAN_POINT ( 'NONE',  ( -70.25499999999998124, -4.716976649647092401, 6.492361379858946790 ) ) ;
#51827=CARTESIAN_POINT ( 'NONE',  ( -181.1049999999999898, -6.826472737025115478, 4.959722759717900331 ) ) ;
#51833=CARTESIAN_POINT ( 'NONE',  ( -87.14292637653379359, 5.598654528085800663, -7.705886871421367523 ) ) ;
#51840=CARTESIAN_POINT ( 'NONE',  ( -102.3549999999999898, -4.716976649647093289, -6.492361379858945902 ) ) ;
#51845=CARTESIAN_POINT ( 'NONE',  ( -137.4570736234661865, -9.058813317711329915, 2.943386871421371787 ) ) ;
#51848=CARTESIAN_POINT ( 'NONE',  ( -79.85707362346616378, -5.598654528085803328, -7.705886871421366635 ) ) ;
#51849=CARTESIAN_POINT ( 'NONE',  ( -93.29292637653493614, 3.094860106599470750, -9.525000000013767121 ) ) ;
#51856=CARTESIAN_POINT ( 'NONE',  ( -116.6049999999999756, 6.826472737025113702, -4.959722759717902107 ) ) ;
#51859=CARTESIAN_POINT ( 'NONE',  ( -128.9950000000000045, -6.826472737025115478, 4.959722759717900331 ) ) ;
#51865=DIRECTION ( 'NONE',  ( 0.000000000000000000, 0.000000000000000000, 1.000000000000000000 ) ) ;
#51867=CARTESIAN_POINT ( 'NONE',  ( -172.1929263765337907, -10.01517768586948698, 6.132527647946031529E-16 ) ) ;
#51875=CARTESIAN_POINT ( 'NONE',  ( -82.64292637653379359, -5.598654528085801552, 7.705886871421367523 ) ) ;
#51878=CARTESIAN_POINT ( 'NONE',  ( -180.1429263765338078, 5.598654528085800663, -7.705886871421367523 ) ) ;
#51882=CARTESIAN_POINT ( 'NONE',  ( -156.3570736234661922, 5.598654528085804216, 7.705886871421366635 ) ) ;
#51889=DIRECTION ( 'NONE',  ( -1.000000000000000000, -0.000000000000000000, -0.000000000000000000 ) ) ;
#51897=CARTESIAN_POINT ( 'NONE',  ( -102.2049999999999983, -2.607480562269071545, -8.024999999999991473 ) ) ;
#51905=CARTESIAN_POINT ( 'NONE',  ( -84.14499999999998181, -4.716976649647092401, 6.492361379858946790 ) ) ;
#51919=VERTEX_POINT ( 'NONE', #64220 ) ;
#51922=CARTESIAN_POINT ( 'NONE',  ( -168.9570736234661865, 9.058813317711329915, -2.943386871421373119 ) ) ;
#51925=CARTESIAN_POINT ( 'NONE',  ( -104.4570736234661723, -9.058813317711329915, 2.943386871421371787 ) ) ;
#51929=LINE ( 'NONE', #3683, #38136 ) ;
#51934=CARTESIAN_POINT ( 'NONE',  ( -115.2570736234661695, 5.598654528085800663, -7.705886871421367523 ) ) ;
#51936=CARTESIAN_POINT ( 'NONE',  ( -151.8549999999999898, 4.716976649647094177, 6.492361379858945902 ) ) ;
#51940=CARTESIAN_POINT ( 'NONE',  ( -154.4949999999999477, 6.826472737025113702, -4.959722759717902107 ) ) ;
#51941=CARTESIAN_POINT ( 'NONE',  ( -151.4950000000000045, 6.826472737025113702, -4.959722759717902107 ) ) ;
#51946=CARTESIAN_POINT ( 'NONE',  ( -67.85499999999998977, 4.716976649647094177, 6.492361379858945902 ) ) ;
#51950=CARTESIAN_POINT ( 'NONE',  ( -61.19499999999997897, 8.437984349512086979, -1.550032578732815448E-15 ) ) ;
#51960=CARTESIAN_POINT ( 'NONE',  ( -178.9429263765338192, 0.000000000000000000, 9.524999999999991473 ) ) ;
#51973=EDGE_CURVE ( 'NONE', #57448, #12387, #41499, .T. ) ;
#51987=CARTESIAN_POINT ( 'NONE',  ( -107.0949999999999847, -2.607480562269071545, -8.024999999999991473 ) ) ;
#51999=ORIENTED_EDGE ( 'NONE', *, *, #56059, .F. ) ;
#52003=CARTESIAN_POINT ( 'NONE',  ( -139.9429263765337907, 0.000000000000000000, 9.524999999999991473 ) ) ;
#52007=CARTESIAN_POINT ( 'NONE',  ( -127.1050000000000040, -6.826472737025115478, 4.959722759717900331 ) ) ;
#52013=CARTESIAN_POINT ( 'NONE',  ( -126.1429263765337936, 5.598654528085800663, -7.705886871421367523 ) ) ;
#52023=CARTESIAN_POINT ( 'NONE',  ( -175.4049999999999727, -2.607480562269069768, 8.024999999999991473 ) ) ;
#52027=CARTESIAN_POINT ( 'NONE',  ( -48.95707362346615810, 9.058813317711329915, -2.943386871421373119 ) ) ;
#52029=CARTESIAN_POINT ( 'NONE',  ( -177.8950000000000102, 6.826472737025115478, 4.959722759717899443 ) ) ;
#52033=EDGE_CURVE ( 'NONE', #68810, #31091, #5910, .T. ) ;
#52036=CARTESIAN_POINT ( 'NONE',  ( -91.70499999999998408, 2.607480562269073321, 8.024999999999991473 ) ) ;
#52041=CARTESIAN_POINT ( 'NONE',  ( -92.99499999999999034, -6.826472737025113702, 4.959722759717902107 ) ) ;
#52044=CARTESIAN_POINT ( 'NONE',  ( -66.44499999999999318, 0.000000000000000000, 8.024999999999991473 ) ) ;
#52053=CARTESIAN_POINT ( 'NONE',  ( -109.6429263765338078, -5.598654528085801552, 7.705886871421367523 ) ) ;
#52054=( BOUNDED_CURVE ( )  B_SPLINE_CURVE ( 2, ( #19053, #68667, #29635, #52504, #52161, #14159, #58116, #41970, #25392, #25725, #14485 ),
 .UNSPECIFIED., .F., .F. ) 
 B_SPLINE_CURVE_WITH_KNOTS ( ( 3, 2, 2, 2, 2, 3 ),
 ( 0.5217391304347703818, 0.5239130434782486301, 0.5260869565217267674, 0.5282608695652050157, 0.5304347826086832640, 0.5326086956521615123 ),
 .UNSPECIFIED. ) 
 CURVE ( )  GEOMETRIC_REPRESENTATION_ITEM ( )  RATIONAL_B_SPLINE_CURVE ( ( 1.000000000000274891, 0.9510565162948785289, 1.000000000000000000, 0.9510565162951535312, 1.000000000000000000, 0.9510565162951535312, 1.000000000000000000, 0.9510565162951535312, 1.000000000000000000, 0.9510565162954335294, 0.9999999999997200018 ) ) 
 REPRESENTATION_ITEM ( '' )  );
#52055=CARTESIAN_POINT ( 'NONE',  ( -125.0949999999999847, -2.607480562269071545, -8.024999999999991473 ) ) ;
#52072=CARTESIAN_POINT ( 'NONE',  ( -122.9049999999999727, 2.607480562269069324, -8.024999999999993250 ) ) ;
#52075=CARTESIAN_POINT ( 'NONE',  ( -127.8570736234661780, -5.598654528085803328, -7.705886871421366635 ) ) ;
#52076=VECTOR ( 'NONE', #49052, 1000.000000000000000 ) ;
#52097=CARTESIAN_POINT ( 'NONE',  ( -99.44292637653380496, -1.166476076187852838E-15, -9.524999999999991473 ) ) ;
#52105=CARTESIAN_POINT ( 'NONE',  ( -59.54292637653379927, 9.058813317711329915, 2.943386871421369566 ) ) ;
#52108=CARTESIAN_POINT ( 'NONE',  ( -155.0050000000000239, 6.826472737025116366, 4.959722759717898555 ) ) ;
#52120=CARTESIAN_POINT ( 'NONE',  ( -62.90499999999997982, 2.607480562269068880, -8.024999999999993250 ) ) ;
#52137=CARTESIAN_POINT ( 'NONE',  ( -100.1949999999999790, 8.437984349512085203, -1.550032578732815448E-15 ) ) ;
#52142=CARTESIAN_POINT ( 'NONE',  ( -71.54292637653379927, 9.058813317711329915, 2.943386871421369566 ) ) ;
#52144=CARTESIAN_POINT ( 'NONE',  ( -142.0429263765338135, -9.058813317711329915, -2.943386871421370898 ) ) ;
#52146=CARTESIAN_POINT ( 'NONE',  ( -155.2450000000000045, -4.716976649647093289, -6.492361379858945902 ) ) ;
#52159=CARTESIAN_POINT ( 'NONE',  ( -144.2929263765342967, 3.094860106609957917, -9.525000000006148326 ) ) ;
#52161=CARTESIAN_POINT ( 'NONE',  ( -110.4570736234661723, -9.058813317711329915, 2.943386871421371787 ) ) ;
#52163=ORIENTED_EDGE ( 'NONE', *, *, #34179, .F. ) ;
#52164=CARTESIAN_POINT ( 'NONE',  ( -161.6049999999999898, 6.826472737025113702, -4.959722759717902107 ) ) ;
#52178=CARTESIAN_POINT ( 'NONE',  ( -69.95499999999998408, -7.632228543268599452, 2.479861379858951054 ) ) ;
#52186=DIRECTION ( 'NONE',  ( -1.000000000000000000, -0.000000000000000000, -0.000000000000000000 ) ) ;
#52187=CARTESIAN_POINT ( 'NONE',  ( -178.4050000000000011, -2.607480562269069768, 8.024999999999991473 ) ) ;
#52199=CARTESIAN_POINT ( 'NONE',  ( -92.30499999999999261, 8.437984349512085203, -1.550032578732815448E-15 ) ) ;
#52200=ORIENTED_EDGE ( 'NONE', *, *, #16087, .T. ) ;
#52204=CARTESIAN_POINT ( 'NONE',  ( -142.2570736234661695, 5.598654528085800663, -7.705886871421367523 ) ) ;
#52207=CARTESIAN_POINT ( 'NONE',  ( -74.90707362346616094, -3.094860106618429807, 9.524999999999991473 ) ) ;
#52211=CARTESIAN_POINT ( 'NONE',  ( -15.00000000000000000, -10.90871211463571022, -5.000000000000000000 ) ) ;
#52215=CARTESIAN_POINT ( 'NONE',  ( -118.8549999999999898, 4.716976649647094177, 6.492361379858945902 ) ) ;
#52219=CARTESIAN_POINT ( 'NONE',  ( -130.1950000000000216, 8.437984349512085203, -1.550032578732815448E-15 ) ) ;
#52229=CARTESIAN_POINT ( 'NONE',  ( -172.4929263765338305, -8.102448949553172852, 5.886773742842742685 ) ) ;
#52230=CARTESIAN_POINT ( 'NONE',  ( -181.1949999999999648, 8.437984349512085203, -1.550032578732815448E-15 ) ) ;
#52231=EDGE_CURVE ( 'NONE', #30878, #65754, #18805, .T. ) ;
#52238=CARTESIAN_POINT ( 'NONE',  ( -86.09292637653378222, 3.094860106618433360, 9.524999999999991473 ) ) ;
#52242=CARTESIAN_POINT ( 'NONE',  ( -166.7929263765339840, -3.094860106614799378, 9.525000000002631140 ) ) ;
#52252=CARTESIAN_POINT ( 'NONE',  ( -110.9929263765338163, 8.102448949553172852, -5.886773742842744461 ) ) ;
#52258=CARTESIAN_POINT ( 'NONE',  ( -100.7049999999999699, 2.607480562269072433, 8.024999999999991473 ) ) ;
#52263=CARTESIAN_POINT ( 'NONE',  ( -104.6070736234661780, -8.102448949553174629, 5.886773742842742685 ) ) ;
#52270=CARTESIAN_POINT ( 'NONE',  ( -67.79499999999998749, 2.607480562269068880, -8.024999999999993250 ) ) ;
#52281=EDGE_CURVE ( 'NONE', #35268, #246, #68391, .T. ) ;
#52286=CARTESIAN_POINT ( 'NONE',  ( -167.4570736234661865, -9.058813317711329915, 2.943386871421371787 ) ) ;
#52289=CARTESIAN_POINT ( 'NONE',  ( -107.0070736234661837, -8.102448949553172852, -5.886773742842741797 ) ) ;
#52297=CARTESIAN_POINT ( 'NONE',  ( -82.34292637653379643, -9.058813317711329915, 2.943386871421371787 ) ) ;
#52299=CARTESIAN_POINT ( 'NONE',  ( -147.8050000000000068, -8.437984349512085203, 5.166775262442717831E-16 ) ) ;
#52303=CARTESIAN_POINT ( 'NONE',  ( -156.2949999999999591, -2.607480562269069768, 8.024999999999991473 ) ) ;
#52305=CARTESIAN_POINT ( 'NONE',  ( -151.1949999999999932, 8.437984349512086979, -1.550032578732815448E-15 ) ) ;
#52308=CARTESIAN_POINT ( 'NONE',  ( -64.94292637653380496, 0.000000000000000000, 9.524999999999991473 ) ) ;
#52312=CARTESIAN_POINT ( 'NONE',  ( -60.50499999999998124, -6.826472737025115478, -4.959722759717899443 ) ) ;
#52315=CARTESIAN_POINT ( 'NONE',  ( -60.89499999999998892, 6.826472737025115478, 4.959722759717899443 ) ) ;
#52321=CARTESIAN_POINT ( 'NONE',  ( -153.1429263765338078, 5.598654528085800663, -7.705886871421367523 ) ) ;
#52323=CARTESIAN_POINT ( 'NONE',  ( -177.4429263765338192, -1.166476076187852838E-15, -9.524999999999991473 ) ) ;
#52328=ORIENTED_EDGE ( 'NONE', *, *, #68478, .F. ) ;
#52329=VERTEX_POINT ( 'NONE', #11019 ) ;
#52336=CARTESIAN_POINT ( 'NONE',  ( -77.60707362346613536, -8.102448949553174629, 5.886773742842742685 ) ) ;
#52340=CARTESIAN_POINT ( 'NONE',  ( -195.0000000000000000, 0.000000000000000000, 9.524999999999991473 ) ) ;
#52346=CARTESIAN_POINT ( 'NONE',  ( -101.8449999999999847, -7.632228543268599452, 2.479861379858951054 ) ) ;
#52364=CARTESIAN_POINT ( 'NONE',  ( -124.5549999999999926, 0.000000000000000000, 8.024999999999991473 ) ) ;
#52380=CARTESIAN_POINT ( 'NONE',  ( -153.8929263765338078, -8.102448949553174629, -5.886773742842741797 ) ) ;
#52381=CARTESIAN_POINT ( 'NONE',  ( -174.3549999999999898, -4.716976649647093289, -6.492361379858945902 ) ) ;
#52384=CARTESIAN_POINT ( 'NONE',  ( -46.85707362346616378, -5.598654528085803328, -7.705886871421366635 ) ) ;
#52387=CARTESIAN_POINT ( 'NONE',  ( -174.1449999999999818, -4.716976649647092401, 6.492361379858946790 ) ) ;
#52393=CARTESIAN_POINT ( 'NONE',  ( -10.66860548474816639, 11.73595285652921305, -2.518653182310350402 ) ) ;
#52394=CARTESIAN_POINT ( 'NONE',  ( -89.45499999999999829, 7.632228543268599452, -2.479861379858951942 ) ) ;
#52397=CARTESIAN_POINT ( 'NONE',  ( -91.34499999999998465, 7.632228543268599452, -2.479861379858951942 ) ) ;
#52399=CARTESIAN_POINT ( 'NONE',  ( -69.44499999999999318, 0.000000000000000000, 8.024999999999991473 ) ) ;
#52407=CARTESIAN_POINT ( 'NONE',  ( -100.9429263765338050, 0.000000000000000000, 9.524999999999991473 ) ) ;
#52409=CARTESIAN_POINT ( 'NONE',  ( -126.8949999999999818, 6.826472737025116366, 4.959722759717898555 ) ) ;
#52419=CARTESIAN_POINT ( 'NONE',  ( -175.1070736234661638, 8.102448949553172852, -5.886773742842744461 ) ) ;
#52421=DIRECTION ( 'NONE',  ( 0.000000000000000000, 0.000000000000000000, 1.000000000000000000 ) ) ;
#52424=CARTESIAN_POINT ( 'NONE',  ( -118.1049999999999898, -6.826472737025113702, 4.959722759717902107 ) ) ;
#52425=VERTEX_POINT ( 'NONE', #48712 ) ;
#52428=CARTESIAN_POINT ( 'NONE',  ( -122.6070736234661780, -8.102448949553172852, 5.886773742842742685 ) ) ;
#52454=CARTESIAN_POINT ( 'NONE',  ( -59.09292637653378222, 3.094860106618433360, 9.524999999999991473 ) ) ;
#52456=CARTESIAN_POINT ( 'NONE',  ( -154.7049999999999841, 2.607480562269073321, 8.024999999999991473 ) ) ;
#52462=CARTESIAN_POINT ( 'NONE',  ( -70.79292637653379927, -3.094860106618429807, 9.524999999999991473 ) ) ;
#52465=ORIENTED_EDGE ( 'NONE', *, *, #18041, .T. ) ;
#52469=CARTESIAN_POINT ( 'NONE',  ( -71.00499999999996703, 6.826472737025116366, 4.959722759717898555 ) ) ;
#52470=VERTEX_POINT ( 'NONE', #28205 ) ;
#52480=DIRECTION ( 'NONE',  ( -1.000000000000000000, -0.000000000000000000, -0.000000000000000000 ) ) ;
#52487=CARTESIAN_POINT ( 'NONE',  ( -101.3949999999999676, -6.826472737025115478, -4.959722759717899443 ) ) ;
#52488=LINE ( 'NONE', #58773, #4962 ) ;
#52494=CARTESIAN_POINT ( 'NONE',  ( -134.2429263765338305, 5.598654528085804216, 7.705886871421366635 ) ) ;
#52496=CARTESIAN_POINT ( 'NONE',  ( -152.8449999999999989, -7.632228543268599452, 2.479861379858951054 ) ) ;
#52498=CARTESIAN_POINT ( 'NONE',  ( -132.4429263765338192, -1.166476076187852838E-15, -9.524999999999991473 ) ) ;
#52504=CARTESIAN_POINT ( 'NONE',  ( -110.6070736234661638, -8.102448949553174629, 5.886773742842742685 ) ) ;
#52508=CARTESIAN_POINT ( 'NONE',  ( -149.1549999999999727, 7.632228543268600340, 2.479861379858949277 ) ) ;
#52514=CARTESIAN_POINT ( 'NONE',  ( -58.40707362346616094, 3.094860106618428031, -9.524999999999993250 ) ) ;
#52520=CARTESIAN_POINT ( 'NONE',  ( -68.30499999999999261, 8.437984349512086979, -1.550032578732815448E-15 ) ) ;
#52527=AXIS2_PLACEMENT_3D ( 'NONE', #60437, #12244, #1976 ) ;
#52534=CARTESIAN_POINT ( 'NONE',  ( -181.8549999999999898, 4.716976649647094177, 6.492361379858945902 ) ) ;
#52545=CARTESIAN_POINT ( 'NONE',  ( -95.45499999999998408, 7.632228543268599452, -2.479861379858951942 ) ) ;
#52549=CARTESIAN_POINT ( 'NONE',  ( -133.4070736234661751, 3.094860106618428031, -9.524999999999993250 ) ) ;
#52552=CARTESIAN_POINT ( 'NONE',  ( -77.60707362346613536, -8.102448949553172852, 5.886773742842742685 ) ) ;
#52560=CARTESIAN_POINT ( 'NONE',  ( -107.1549999999999869, 7.632228543268600340, 2.479861379858949277 ) ) ;
#52562=EDGE_CURVE ( 'NONE', #51718, #18409, #30291, .T. ) ;
#52564=CARTESIAN_POINT ( 'NONE',  ( -125.0949999999999847, -2.607480562269071545, -8.024999999999991473 ) ) ;
#52568=CARTESIAN_POINT ( 'NONE',  ( -118.3429263765338106, -9.058813317711329915, 2.943386871421371787 ) ) ;
#52570=CARTESIAN_POINT ( 'NONE',  ( -159.4429263765338192, -1.166476076187852838E-15, -9.524999999999991473 ) ) ;
#52571=SURFACE_STYLE_FILL_AREA ( #9992 ) ;
#52579=CARTESIAN_POINT ( 'NONE',  ( -87.14292637653379359, 5.598654528085800663, -7.705886871421367523 ) ) ;
#52581=CARTESIAN_POINT ( 'NONE',  ( -195.0000000000000000, 0.000000000000000000, 9.524999999999991473 ) ) ;
#52585=CARTESIAN_POINT ( 'NONE',  ( -175.8549999999999898, 4.716976649647094177, 6.492361379858945902 ) ) ;
#52589=EDGE_CURVE ( 'NONE', #24627, #48545, #13110, .T. ) ;
#52599=CARTESIAN_POINT ( 'NONE',  ( -101.0049999999999812, 6.826472737025115478, 4.959722759717899443 ) ) ;
#52610=CARTESIAN_POINT ( 'NONE',  ( -71.09499999999999886, -2.607480562269071545, -8.024999999999991473 ) ) ;
#52626=CARTESIAN_POINT ( 'NONE',  ( -164.0070736234661695, -8.102448949553172852, -5.886773742842741797 ) ) ;
#52628=CARTESIAN_POINT ( 'NONE',  ( -102.8070736234661666, 10.01517768586948698, -1.839758294383808571E-15 ) ) ;
#52630=CARTESIAN_POINT ( 'NONE',  ( -65.00707362346616947, -8.102448949553174629, -5.886773742842741797 ) ) ;
#52635=CARTESIAN_POINT ( 'NONE',  ( -141.6550000000000011, -7.632228543268600340, -2.479861379858950166 ) ) ;
#52638=CARTESIAN_POINT ( 'NONE',  ( -152.0949999999999420, -2.607480562269071545, -8.024999999999991473 ) ) ;
#52640=CARTESIAN_POINT ( 'NONE',  ( -134.9949999999999477, -6.826472737025113702, 4.959722759717902107 ) ) ;
#52645=CARTESIAN_POINT ( 'NONE',  ( -66.35499999999998977, -4.716976649647093289, -6.492361379858945902 ) ) ;
#52651=DIRECTION ( 'NONE',  ( -1.000000000000000000, -0.000000000000000000, -0.000000000000000000 ) ) ;
#52677=CARTESIAN_POINT ( 'NONE',  ( -45.00000000000000000, 1.044011396273118676E-15, -8.525000000000000355 ) ) ;
#52678=CARTESIAN_POINT ( 'NONE',  ( -101.6949999999999790, -8.437984349512085203, 5.166775262442717831E-16 ) ) ;
#52682=CARTESIAN_POINT ( 'NONE',  ( -53.54292637653379217, 9.058813317711329915, 2.943386871421369566 ) ) ;
#52708=CARTESIAN_POINT ( 'NONE',  ( -182.0929263765338249, 3.094860106619032880, 9.524999999999554490 ) ) ;
#52712=CARTESIAN_POINT ( 'NONE',  ( -166.5550000000000068, 0.000000000000000000, 8.024999999999991473 ) ) ;
#52715=CARTESIAN_POINT ( 'NONE',  ( -50.15707362346616094, -9.058813317711329915, -2.943386871421370898 ) ) ;
#52716=CARTESIAN_POINT ( 'NONE',  ( -180.2949999999999591, -2.607480562269069768, 8.024999999999991473 ) ) ;
#52722=CARTESIAN_POINT ( 'NONE',  ( -94.40500000000000114, -2.607480562269069768, 8.024999999999991473 ) ) ;
#52727=CARTESIAN_POINT ( 'NONE',  ( -88.49499999999999034, 6.826472737025113702, -4.959722759717902107 ) ) ;
#52729=CARTESIAN_POINT ( 'NONE',  ( -60.29499999999999460, -2.607480562269069768, 8.024999999999991473 ) ) ;
#52732=CARTESIAN_POINT ( 'NONE',  ( -170.8429263765337964, 9.058813317711329915, -2.943386871421373119 ) ) ;
#52743=EDGE_CURVE ( 'NONE', #13980, #618, #61116, .T. ) ;
#52752=EDGE_CURVE ( 'NONE', #42499, #1545, #15813, .T. ) ;
#52754=CYLINDRICAL_SURFACE ( 'NONE', #7125, 9.524999999999991473 ) ;
#52757=CARTESIAN_POINT ( 'NONE',  ( -117.9549999999999841, -7.632228543268599452, 2.479861379858951054 ) ) ;
#52773=CARTESIAN_POINT ( 'NONE',  ( -136.1070736234661922, 8.102448949553172852, -5.886773742842744461 ) ) ;
#52775=EDGE_CURVE ( 'NONE', #3199, #55926, #20299, .T. ) ;
#52779=LINE ( 'NONE', #20762, #5330 ) ;
#52784=ORIENTED_EDGE ( 'NONE', *, *, #52589, .F. ) ;
#52788=CARTESIAN_POINT ( 'NONE',  ( -58.19292637653381206, -10.01517768586948698, 6.132527647946031529E-16 ) ) ;
#52792=CARTESIAN_POINT ( 'NONE',  ( -157.2549999999999955, -4.716976649647092401, 6.492361379858946790 ) ) ;
#52798=DIRECTION ( 'NONE',  ( 1.000000000000000000, 0.000000000000000000, 0.000000000000000000 ) ) ;
#52799=CARTESIAN_POINT ( 'NONE',  ( -69.89292637653379359, -8.102448949553174629, -5.886773742842741797 ) ) ;
#52803=CARTESIAN_POINT ( 'NONE',  ( -1.000000000000028644, 0.000000000000000000, 0.000000000000000000 ) ) ;
#52805=CARTESIAN_POINT ( 'NONE',  ( -67.25499999999998124, -4.716976649647092401, 6.492361379858946790 ) ) ;
#52810=CARTESIAN_POINT ( 'NONE',  ( -166.5570736234661808, -1.166476076187852838E-15, -9.524999999999991473 ) ) ;
#52819=CARTESIAN_POINT ( 'NONE',  ( -121.7949999999999875, 2.607480562269069324, -8.024999999999993250 ) ) ;
#52821=CARTESIAN_POINT ( 'NONE',  ( -101.0949999999999989, -2.607480562269071545, -8.024999999999991473 ) ) ;
#52824=AXIS2_PLACEMENT_3D ( 'NONE', #450, #33220, #22309 ) ;
#52828=CARTESIAN_POINT ( 'NONE',  ( -138.2929263765338419, 3.094860106618428031, -9.524999999999993250 ) ) ;
#52830=CARTESIAN_POINT ( 'NONE',  ( -195.0000000000000000, 0.000000000000000000, 9.524999999999991473 ) ) ;
#52831=CARTESIAN_POINT ( 'NONE',  ( -161.8449999999999989, -7.632228543268599452, 2.479861379858951054 ) ) ;
#52837=CARTESIAN_POINT ( 'NONE',  ( -133.6429263765338078, -5.598654528085801552, 7.705886871421367523 ) ) ;
#52848=CARTESIAN_POINT ( 'NONE',  ( -152.0049999999999955, 6.826472737025115478, 4.959722759717899443 ) ) ;
#52859=ORIENTED_EDGE ( 'NONE', *, *, #28967, .T. ) ;
#52861=CARTESIAN_POINT ( 'NONE',  ( -60.05499999999998550, -9.827790563157499189E-16, -8.024999999999991473 ) ) ;
#52872=CARTESIAN_POINT ( 'NONE',  ( -195.0000000000000000, 1.166476076187852838E-15, -9.524999999999991473 ) ) ;
#52873=CARTESIAN_POINT ( 'NONE',  ( -183.3549999999999898, -4.716976649647093289, -6.492361379858945902 ) ) ;
#52874=VERTEX_POINT ( 'NONE', #40376 ) ;
#52884=CARTESIAN_POINT ( 'NONE',  ( -98.60499999999997556, 6.826472737025113702, -4.959722759717902107 ) ) ;
#52887=CARTESIAN_POINT ( 'NONE',  ( -130.5570736234661808, -1.166476076187852838E-15, -9.524999999999991473 ) ) ;
#52890=CARTESIAN_POINT ( 'NONE',  ( -76.40707362346614673, 3.094860106618428031, -9.524999999999993250 ) ) ;
#52894=CARTESIAN_POINT ( 'NONE',  ( -17.51869064886620109, -11.19266561951042149, -4.331441116418161208 ) ) ;
#52896=CARTESIAN_POINT ( 'NONE',  ( -113.9049999999999869, 2.607480562269068880, -8.024999999999993250 ) ) ;
#52899=CARTESIAN_POINT ( 'NONE',  ( -121.9449999999999932, -9.827790563157499189E-16, -8.024999999999991473 ) ) ;
#52903=ORIENTED_EDGE ( 'NONE', *, *, #32115, .F. ) ;
#52904=CARTESIAN_POINT ( 'NONE',  ( -163.9429263765338192, 0.000000000000000000, 9.524999999999991473 ) ) ;
#52913=CARTESIAN_POINT ( 'NONE',  ( -72.89292637653380780, -8.102448949553172852, -5.886773742842741797 ) ) ;
#52923=CARTESIAN_POINT ( 'NONE',  ( -175.1050000000000182, -6.826472737025113702, 4.959722759717902107 ) ) ;
#52935=CARTESIAN_POINT ( 'NONE',  ( -91.40499999999998693, -2.607480562269069768, 8.024999999999991473 ) ) ;
#52945=CARTESIAN_POINT ( 'NONE',  ( -75.44499999999997897, 0.000000000000000000, 8.024999999999991473 ) ) ;
#52952=STYLED_ITEM ( 'NONE', ( #47681 ), #6101 ) ;
#52961=CARTESIAN_POINT ( 'NONE',  ( -157.1070736234661354, 8.102448949553171076, -5.886773742842744461 ) ) ;
#52964=CARTESIAN_POINT ( 'NONE',  ( -106.8570736234661780, -5.598654528085803328, -7.705886871421366635 ) ) ;
#52971=CARTESIAN_POINT ( 'NONE',  ( -143.3050000000000068, 8.437984349512085203, -1.550032578732815448E-15 ) ) ;
#52973=CARTESIAN_POINT ( 'NONE',  ( -157.0449999999999875, 7.632228543268600340, 2.479861379858949277 ) ) ;
#52974=CARTESIAN_POINT ( 'NONE',  ( -135.2949999999999875, -2.607480562269069768, 8.024999999999991473 ) ) ;
#52982=CARTESIAN_POINT ( 'NONE',  ( -58.10499999999999687, -6.826472737025115478, 4.959722759717900331 ) ) ;
#52985=EDGE_CURVE ( 'NONE', #12752, #51919, #56687, .T. ) ;
#53013=EDGE_LOOP ( 'NONE', ( #3422, #35965, #22924, #19012 ) ) ;
#53023=CARTESIAN_POINT ( 'NONE',  ( -100.7950000000000017, 2.607480562269068880, -8.024999999999993250 ) ) ;
#53033=DIRECTION ( 'NONE',  ( -1.000000000000000000, -0.000000000000000000, -0.000000000000000000 ) ) ;
#53043=LINE ( 'NONE', #4837, #62064 ) ;
#53051=CARTESIAN_POINT ( 'NONE',  ( -170.0070736234661410, -8.102448949553174629, -5.886773742842741797 ) ) ;
#53055=CARTESIAN_POINT ( 'NONE',  ( -165.9549999999999841, -7.632228543268599452, 2.479861379858951054 ) ) ;
#53057=CARTESIAN_POINT ( 'NONE',  ( -147.9570736234661581, 9.058813317711329915, -2.943386871421373119 ) ) ;
#53059=CARTESIAN_POINT ( 'NONE',  ( -180.5949999999999704, 2.607480562269073321, 8.024999999999991473 ) ) ;
#53061=CARTESIAN_POINT ( 'NONE',  ( -170.3949999999999818, -6.826472737025113702, -4.959722759717900331 ) ) ;
#53066=CARTESIAN_POINT ( 'NONE',  ( -10.25993137369353470, 11.89347840174322002, 1.624321976435927573 ) ) ;
#53067=CARTESIAN_POINT ( 'NONE',  ( -81.80499999999996419, -8.437984349512085203, 5.166775262442717831E-16 ) ) ;
#53069=CARTESIAN_POINT ( 'NONE',  ( -168.6570736234661751, 9.058813317711329915, 2.943386871421369566 ) ) ;
#53072=CARTESIAN_POINT ( 'NONE',  ( -90.89499999999999602, 6.826472737025115478, 4.959722759717899443 ) ) ;
#53076=CARTESIAN_POINT ( 'NONE',  ( -172.4070736234662604, 3.094860106616344808, -9.525000000001510259 ) ) ;
#53092=CARTESIAN_POINT ( 'NONE',  ( -15.00000000000000000, -10.90871211463571200, 5.000000000000000000 ) ) ;
#53093=CARTESIAN_POINT ( 'NONE',  ( -175.4070736234663173, 3.094860106616942108, -9.525000000001076828 ) ) ;
#53101=ORIENTED_EDGE ( 'NONE', *, *, #64031, .T. ) ;
#53102=CARTESIAN_POINT ( 'NONE',  ( -121.1050000000000040, -6.826472737025113702, 4.959722759717902107 ) ) ;
#53105=DIRECTION ( 'NONE',  ( -1.000000000000000000, -0.000000000000000000, -0.000000000000000000 ) ) ;
#53113=ORIENTED_EDGE ( 'NONE', *, *, #12536, .T. ) ;
#53117=CARTESIAN_POINT ( 'NONE',  ( -130.1929263765337907, -10.01517768586948698, 6.132527647946031529E-16 ) ) ;
#53120=DIRECTION ( 'NONE',  ( -1.000000000000000000, -0.000000000000000000, -0.000000000000000000 ) ) ;
#53124=CARTESIAN_POINT ( 'NONE',  ( -98.39292637653380780, 8.102448949553176405, 5.886773742842740909 ) ) ;
#53130=CARTESIAN_POINT ( 'NONE',  ( -53.84292637653378932, 9.058813317711329915, -2.943386871421373119 ) ) ;
#53133=CARTESIAN_POINT ( 'NONE',  ( -150.2049999999999841, -2.607480562269071545, -8.024999999999991473 ) ) ;
#53145=CARTESIAN_POINT ( 'NONE',  ( -66.05499999999999261, -9.827790563157499189E-16, -8.024999999999991473 ) ) ;
#53159=CARTESIAN_POINT ( 'NONE',  ( -119.9949999999999903, -6.826472737025113702, 4.959722759717902107 ) ) ;
#53161=CARTESIAN_POINT ( 'NONE',  ( -87.29500000000000171, -2.607480562269069768, 8.024999999999991473 ) ) ;
#53169=ORIENTED_EDGE ( 'NONE', *, *, #51076, .F. ) ;
#53171=CARTESIAN_POINT ( 'NONE',  ( -136.3429263765337964, -9.058813317711329915, 2.943386871421371787 ) ) ;
#53173=CARTESIAN_POINT ( 'NONE',  ( -151.0449999999999875, 7.632228543268600340, 2.479861379858949277 ) ) ;
#53189=CARTESIAN_POINT ( 'NONE',  ( -154.5550000000000068, 0.000000000000000000, 8.024999999999991473 ) ) ;
#53192=CARTESIAN_POINT ( 'NONE',  ( -195.0000000000000000, 1.166476076187852838E-15, -9.524999999999991473 ) ) ;
#53194=ORIENTED_EDGE ( 'NONE', *, *, #49397, .F. ) ;
#53195=DIRECTION ( 'NONE',  ( -1.000000000000000000, -0.000000000000000000, -0.000000000000000000 ) ) ;
#53205=CARTESIAN_POINT ( 'NONE',  ( -63.95499999999998408, -7.632228543268599452, 2.479861379858951054 ) ) ;
#53217=CARTESIAN_POINT ( 'NONE',  ( -180.5049999999999670, -6.826472737025115478, -4.959722759717899443 ) ) ;
#53219=CARTESIAN_POINT ( 'NONE',  ( -87.35707362346617799, 5.598654528085804216, 7.705886871421366635 ) ) ;
#53228=CARTESIAN_POINT ( 'NONE',  ( -96.65499999999998693, -7.632228543268600340, -2.479861379858950166 ) ) ;
#53233=CARTESIAN_POINT ( 'NONE',  ( -128.3070736234661524, -10.01517768586948698, 6.132527647946031529E-16 ) ) ;
#53236=CARTESIAN_POINT ( 'NONE',  ( -61.85707362346616378, -5.598654528085803328, -7.705886871421366635 ) ) ;
#53248=CARTESIAN_POINT ( 'NONE',  ( -114.2049999999999699, -2.607480562269071545, -8.024999999999991473 ) ) ;
#53250=CARTESIAN_POINT ( 'NONE',  ( -114.7449999999999903, 4.716976649647094177, 6.492361379858945902 ) ) ;
#53259=CARTESIAN_POINT ( 'NONE',  ( -162.1429263765338362, 5.598654528085800663, -7.705886871421367523 ) ) ;
#53260=FACE_OUTER_BOUND ( 'NONE', #45149, .T. ) ;
#53268=CARTESIAN_POINT ( 'NONE',  ( -74.54292637653379927, 9.058813317711329915, 2.943386871421369566 ) ) ;
#53273=CARTESIAN_POINT ( 'NONE',  ( -178.1049999999999613, -6.826472737025113702, 4.959722759717902107 ) ) ;
#53276=CARTESIAN_POINT ( 'NONE',  ( -181.7070736234662149, -3.094860106618727347, -9.524999999999778311 ) ) ;
#53282=CARTESIAN_POINT ( 'NONE',  ( -96.65499999999998693, -7.632228543268600340, -2.479861379858950166 ) ) ;
#53292=CARTESIAN_POINT ( 'NONE',  ( -69.74499999999999034, 4.716976649647094177, 6.492361379858945902 ) ) ;
#53299=CARTESIAN_POINT ( 'NONE',  ( -121.1070736234661922, 8.102448949553172852, -5.886773742842744461 ) ) ;
#53300=CARTESIAN_POINT ( 'NONE',  ( -125.0070736234661979, -8.102448949553174629, -5.886773742842741797 ) ) ;
#53310=EDGE_CURVE ( 'NONE', #19358, #50943, #65368, .T. ) ;
#53316=CARTESIAN_POINT ( 'NONE',  ( -162.2070736234661865, 3.094860106618433360, 9.524999999999991473 ) ) ;
#53318=CARTESIAN_POINT ( 'NONE',  ( -91.40707362346616094, 3.094860106618428031, -9.524999999999993250 ) ) ;
#53328=CARTESIAN_POINT ( 'NONE',  ( -137.7549999999999955, 4.716976649647091513, -6.492361379858946790 ) ) ;
#53331=CARTESIAN_POINT ( 'NONE',  ( -158.8449999999999989, -7.632228543268599452, 2.479861379858951054 ) ) ;
#53332=AXIS2_PLACEMENT_3D ( 'NONE', #24052, #66624, #33565 ) ;
#53333=CARTESIAN_POINT ( 'NONE',  ( -141.4449999999999932, 0.000000000000000000, 8.024999999999991473 ) ) ;
#53335=CARTESIAN_POINT ( 'NONE',  ( -180.0570736234661808, 0.000000000000000000, 9.524999999999991473 ) ) ;
#53339=CARTESIAN_POINT ( 'NONE',  ( -56.15499999999997982, 7.632228543268600340, 2.479861379858949277 ) ) ;
#53348=CARTESIAN_POINT ( 'NONE',  ( -89.15707362346617515, -9.058813317711329915, -2.943386871421370898 ) ) ;
#53371=CARTESIAN_POINT ( 'NONE',  ( -98.69499999999999318, -8.437984349512085203, 5.166775262442717831E-16 ) ) ;
#53388=CYLINDRICAL_SURFACE ( 'NONE', #36720, 9.524999999999991473 ) ;
#53406=CARTESIAN_POINT ( 'NONE',  ( -167.9050000000000011, 2.607480562269068880, -8.024999999999993250 ) ) ;
#53409=CARTESIAN_POINT ( 'NONE',  ( -180.1450000000000102, -4.716976649647092401, 6.492361379858946790 ) ) ;
#53412=CARTESIAN_POINT ( 'NONE',  ( -170.0949999999999989, -2.607480562269071545, -8.024999999999991473 ) ) ;
#53413=ORIENTED_EDGE ( 'NONE', *, *, #32891, .F. ) ;
#53416=CARTESIAN_POINT ( 'NONE',  ( -81.05499999999999261, -9.827790563157499189E-16, -8.024999999999991473 ) ) ;
#53417=DIRECTION ( 'NONE',  ( -1.000000000000000000, -0.000000000000000000, -0.000000000000000000 ) ) ;
#53421=CARTESIAN_POINT ( 'NONE',  ( -84.29499999999998749, -2.607480562269069768, 8.024999999999991473 ) ) ;
#53435=ORIENTED_EDGE ( 'NONE', *, *, #5531, .F. ) ;
#53443=CARTESIAN_POINT ( 'NONE',  ( -121.4049999999999869, -2.607480562269069768, 8.024999999999991473 ) ) ;
#53455=CARTESIAN_POINT ( 'NONE',  ( -117.9570736234661723, 9.058813317711329915, -2.943386871421373119 ) ) ;
#53471=CARTESIAN_POINT ( 'NONE',  ( -147.0549999999999784, -9.827790563157499189E-16, -8.024999999999991473 ) ) ;
#53473=CARTESIAN_POINT ( 'NONE',  ( -175.8570736234661638, -5.598654528085803328, -7.705886871421366635 ) ) ;
#53482=DIRECTION ( 'NONE',  ( -1.000000000000000000, -0.000000000000000000, -0.000000000000000000 ) ) ;
#53484=CARTESIAN_POINT ( 'NONE',  ( -148.9429263765338192, 0.000000000000000000, 9.524999999999991473 ) ) ;
#53485=CARTESIAN_POINT ( 'NONE',  ( -59.75499999999998835, 4.716976649647091513, -6.492361379858946790 ) ) ;
#53497=CARTESIAN_POINT ( 'NONE',  ( -109.9449999999999932, -9.827790563157499189E-16, -8.024999999999991473 ) ) ;
#53499=CARTESIAN_POINT ( 'NONE',  ( -89.09499999999998465, -2.607480562269071545, -8.024999999999991473 ) ) ;
#53503=DIRECTION ( 'NONE',  ( -1.000000000000000000, -0.000000000000000000, -0.000000000000000000 ) ) ;
#53504=( BOUNDED_CURVE ( )  B_SPLINE_CURVE ( 2, ( #8107, #51022, #2783, #41191, #29551, #24601, #62592, #45769, #2412, #57323, #7744 ),
 .UNSPECIFIED., .F., .F. ) 
 B_SPLINE_CURVE_WITH_KNOTS ( ( 3, 2, 2, 2, 2, 3 ),
 ( 0.08695652173912844785, 0.08913043478260665453, 0.09130434782608486122, 0.09347826086956306790, 0.09565217391304127459, 0.09782608695651948127 ),
 .UNSPECIFIED. ) 
 CURVE ( )  GEOMETRIC_REPRESENTATION_ITEM ( )  RATIONAL_B_SPLINE_CURVE ( ( 1.000000000000044631, 0.9510565162951089002, 1.000000000000000000, 0.9510565162951535312, 1.000000000000000000, 0.9510565162951535312, 1.000000000000000000, 0.9510565162951535312, 1.000000000000000000, 0.9510565162952044904, 0.9999999999999490408 ) ) 
 REPRESENTATION_ITEM ( '' )  );
#53505=CARTESIAN_POINT ( 'NONE',  ( -167.1570736234661751, -9.058813317711329915, -2.943386871421370898 ) ) ;
#53508=CARTESIAN_POINT ( 'NONE',  ( -130.9429263765338192, 0.000000000000000000, 9.524999999999991473 ) ) ;
#53509=CARTESIAN_POINT ( 'NONE',  ( -149.6949999999999648, -8.437984349512085203, 5.166775262442717831E-16 ) ) ;
#53512=DIRECTION ( 'NONE',  ( -1.000000000000000000, -0.000000000000000000, -0.000000000000000000 ) ) ;
#53521=CARTESIAN_POINT ( 'NONE',  ( -150.7429263765338021, -5.598654528085803328, -7.705886871421366635 ) ) ;
#53523=CARTESIAN_POINT ( 'NONE',  ( -152.4550000000000125, 7.632228543268599452, -2.479861379858951942 ) ) ;
#53524=ORIENTED_EDGE ( 'NONE', *, *, #48628, .T. ) ;
#53526=ORIENTED_EDGE ( 'NONE', *, *, #25782, .F. ) ;
#53534=CARTESIAN_POINT ( 'NONE',  ( -95.90707362346724096, -3.094860106600548111, 9.525000000012983747 ) ) ;
#53536=CARTESIAN_POINT ( 'NONE',  ( -63.80499999999998550, -8.437984349512086979, 5.166775262442717831E-16 ) ) ;
#53537=CARTESIAN_POINT ( 'NONE',  ( -122.9950000000000045, -6.826472737025115478, 4.959722759717900331 ) ) ;
#53547=DIRECTION ( 'NONE',  ( 0.000000000000000000, 0.000000000000000000, 1.000000000000000000 ) ) ;
#53551=CARTESIAN_POINT ( 'NONE',  ( -170.6050000000000182, 6.826472737025113702, -4.959722759717902107 ) ) ;
#53559=CARTESIAN_POINT ( 'NONE',  ( -129.0570736234661808, 0.000000000000000000, 9.524999999999991473 ) ) ;
#53561=CARTESIAN_POINT ( 'NONE',  ( -98.00500000000000966, 6.826472737025116366, 4.959722759717898555 ) ) ;
#53564=CARTESIAN_POINT ( 'NONE',  ( -130.1070736234661922, 8.102448949553171076, -5.886773742842744461 ) ) ;
#53567=CARTESIAN_POINT ( 'NONE',  ( -68.60707362346614957, -8.102448949553172852, 5.886773742842742685 ) ) ;
#53573=CARTESIAN_POINT ( 'NONE',  ( -110.6049999999999898, 6.826472737025113702, -4.959722759717902107 ) ) ;
#53575=CARTESIAN_POINT ( 'NONE',  ( -113.8449999999999847, -7.632228543268599452, 2.479861379858951054 ) ) ;
#53581=CARTESIAN_POINT ( 'NONE',  ( -158.6929263765338192, 10.01517768586948698, -1.839758294383808571E-15 ) ) ;
#53583=CARTESIAN_POINT ( 'NONE',  ( -171.8949999999999534, 6.826472737025116366, 4.959722759717898555 ) ) ;
#53592=CARTESIAN_POINT ( 'NONE',  ( -79.94292637653380496, 0.000000000000000000, 9.524999999999991473 ) ) ;
#53598=CARTESIAN_POINT ( 'NONE',  ( -183.6549999999999727, -7.632228543268600340, -2.479861379858950166 ) ) ;
#53610=CARTESIAN_POINT ( 'NONE',  ( -94.85499999999998977, 4.716976649647094177, 6.492361379858945902 ) ) ;
#53620=CARTESIAN_POINT ( 'NONE',  ( -73.64499999999998181, 4.716976649647091513, -6.492361379858946790 ) ) ;
#53630=CARTESIAN_POINT ( 'NONE',  ( -121.4049999999999869, -2.607480562269069768, 8.024999999999991473 ) ) ;
#53637=CARTESIAN_POINT ( 'NONE',  ( -159.6570736234661751, 9.058813317711329915, 2.943386871421369566 ) ) ;
#53639=CARTESIAN_POINT ( 'NONE',  ( -93.65707362346617515, 9.058813317711329915, 2.943386871421369566 ) ) ;
#53645=CARTESIAN_POINT ( 'NONE',  ( -139.1049999999999898, -6.826472737025115478, 4.959722759717900331 ) ) ;
#53649=CARTESIAN_POINT ( 'NONE',  ( -142.7949999999999875, 2.607480562269068880, -8.024999999999993250 ) ) ;
#53650=CARTESIAN_POINT ( 'NONE',  ( -140.2450000000000045, -4.716976649647093289, -6.492361379858945902 ) ) ;
#53657=CARTESIAN_POINT ( 'NONE',  ( -53.75499999999999545, 4.716976649647091513, -6.492361379858946790 ) ) ;
#53661=CARTESIAN_POINT ( 'NONE',  ( -155.0070736234661979, -8.102448949553174629, -5.886773742842741797 ) ) ;
#53663=CARTESIAN_POINT ( 'NONE',  ( -104.6929263765337907, 10.01517768586948698, -1.839758294383808571E-15 ) ) ;
#53665=CARTESIAN_POINT ( 'NONE',  ( -152.6929263765337907, 10.01517768586948698, -1.839758294383808966E-15 ) ) ;
#53667=CARTESIAN_POINT ( 'NONE',  ( -90.05707362346616662, 0.000000000000000000, 9.524999999999991473 ) ) ;
#53671=CARTESIAN_POINT ( 'NONE',  ( -76.94292637653380496, 0.000000000000000000, 9.524999999999991473 ) ) ;
#53684=VERTEX_POINT ( 'NONE', #17543 ) ;
#53692=CARTESIAN_POINT ( 'NONE',  ( -97.34499999999998465, 7.632228543268599452, -2.479861379858951942 ) ) ;
#53701=FACE_OUTER_BOUND ( 'NONE', #12398, .T. ) ;
#53705=FACE_OUTER_BOUND ( 'NONE', #35556, .T. ) ;
#53718=CARTESIAN_POINT ( 'NONE',  ( -171.0570736234661808, 0.000000000000000000, 9.524999999999991473 ) ) ;
#53721=CARTESIAN_POINT ( 'NONE',  ( -165.3549999999999898, -4.716976649647093289, -6.492361379858945902 ) ) ;
#53723=CARTESIAN_POINT ( 'NONE',  ( -170.6949999999999932, -8.437984349512085203, 5.166775262442717831E-16 ) ) ;
#53725=CARTESIAN_POINT ( 'NONE',  ( -164.6949999999999932, -8.437984349512086979, 5.166775262442717831E-16 ) ) ;
#53729=CARTESIAN_POINT ( 'NONE',  ( -89.24292637653380211, 5.598654528085804216, 7.705886871421366635 ) ) ;
#53731=CARTESIAN_POINT ( 'NONE',  ( -14.17503136354020477, 10.93867306445503651, -4.934238260594468350 ) ) ;
#53732=CARTESIAN_POINT ( 'NONE',  ( -83.75499999999998124, 4.716976649647091513, -6.492361379858946790 ) ) ;
#53734=CARTESIAN_POINT ( 'NONE',  ( -195.0000000000000000, 0.000000000000000000, 9.524999999999991473 ) ) ;
#53735=AXIS2_PLACEMENT_3D ( 'NONE', #28802, #39755, #1688 ) ;
#53737=CARTESIAN_POINT ( 'NONE',  ( -78.74499999999997613, 4.716976649647094177, 6.492361379858945902 ) ) ;
#53748=AXIS2_PLACEMENT_3D ( 'NONE', #65137, #34519, #7781 ) ;
#53753=DIRECTION ( 'NONE',  ( -1.000000000000000000, -0.000000000000000000, -0.000000000000000000 ) ) ;
#53763=CARTESIAN_POINT ( 'NONE',  ( -69.20707362346617231, 3.094860106618433360, 9.524999999999991473 ) ) ;
#53766=CARTESIAN_POINT ( 'NONE',  ( -108.3549999999999898, -4.716976649647093289, -6.492361379858945902 ) ) ;
#53789=CARTESIAN_POINT ( 'NONE',  ( -52.79292637653378506, -3.094860106618429807, 9.524999999999991473 ) ) ;
#53792=CARTESIAN_POINT ( 'NONE',  ( -140.1550000000000011, 7.632228543268600340, 2.479861379858949277 ) ) ;
#53797=FILL_AREA_STYLE ('',( #33060 ) ) ;
#53801=CARTESIAN_POINT ( 'NONE',  ( -190.0000000000000000, 0.000000000000000000, 0.000000000000000000 ) ) ;
#53804=CARTESIAN_POINT ( 'NONE',  ( -57.65499999999998693, -7.632228543268600340, -2.479861379858950166 ) ) ;
#53821=CARTESIAN_POINT ( 'NONE',  ( -106.6449999999999960, 4.716976649647091513, -6.492361379858946790 ) ) ;
#53823=CARTESIAN_POINT ( 'NONE',  ( -84.44499999999999318, 0.000000000000000000, 8.024999999999991473 ) ) ;
#53832=EDGE_CURVE ( 'NONE', #55926, #32866, #62490, .T. ) ;
#53833=CARTESIAN_POINT ( 'NONE',  ( -133.3429263765337964, -9.058813317711329915, 2.943386871421371787 ) ) ;
#53835=CARTESIAN_POINT ( 'NONE',  ( -150.7449999999999761, 4.716976649647094177, 6.492361379858945902 ) ) ;
#53840=ORIENTED_EDGE ( 'NONE', *, *, #32891, .T. ) ;
#53846=CIRCLE ( 'NONE', #23513, 9.525000000000000355 ) ;
#53852=CARTESIAN_POINT ( 'NONE',  ( -155.4549999999999841, 7.632228543268599452, -2.479861379858951942 ) ) ;
#53855=CARTESIAN_POINT ( 'NONE',  ( -141.2070736234666697, 3.094860106627038032, 9.524999999993740474 ) ) ;
#53856=ORIENTED_EDGE ( 'NONE', *, *, #47139, .T. ) ;
#53864=VERTEX_POINT ( 'NONE', #68139 ) ;
#53866=CARTESIAN_POINT ( 'NONE',  ( -61.70499999999997698, 2.607480562269072433, 8.024999999999991473 ) ) ;
#53867=CARTESIAN_POINT ( 'NONE',  ( -121.9449999999999932, -9.827790563157499189E-16, -8.024999999999991473 ) ) ;
#53877=DIRECTION ( 'NONE',  ( -1.000000000000000000, -0.000000000000000000, -0.000000000000000000 ) ) ;
#53881=CARTESIAN_POINT ( 'NONE',  ( -172.7049999999999841, 2.607480562269073321, 8.024999999999991473 ) ) ;
#53887=ORIENTED_EDGE ( 'NONE', *, *, #47398, .F. ) ;
#53890=CARTESIAN_POINT ( 'NONE',  ( -83.15499999999998693, 7.632228543268600340, 2.479861379858949277 ) ) ;
#53895=( BOUNDED_CURVE ( )  B_SPLINE_CURVE ( 2, ( #30096, #25183, #19553, #57543, #46700, #36104, #19893, #41391, #48896, #15485, #15150 ),
 .UNSPECIFIED., .F., .F. ) 
 B_SPLINE_CURVE_WITH_KNOTS ( ( 3, 2, 2, 2, 2, 3 ),
 ( 0.5543478260869435514, 0.5565217391304217998, 0.5586956521739000481, 0.5608695652173781854, 0.5630434782608564337, 0.5652173913043346820 ),
 .UNSPECIFIED. ) 
 CURVE ( )  GEOMETRIC_REPRESENTATION_ITEM ( )  RATIONAL_B_SPLINE_CURVE ( ( 1.000000000000292433, 0.9510565162948610984, 1.000000000000000000, 0.9510565162951535312, 1.000000000000000000, 0.9510565162951535312, 1.000000000000000000, 0.9510565162951535312, 1.000000000000000000, 0.9510565162954485174, 0.9999999999997050137 ) ) 
 REPRESENTATION_ITEM ( '' )  );
#53896=CARTESIAN_POINT ( 'NONE',  ( -70.10707362346617799, 8.102448949553171076, -5.886773742842744461 ) ) ;
#53901=CARTESIAN_POINT ( 'NONE',  ( -101.9049999999999869, 2.607480562269068880, -8.024999999999993250 ) ) ;
#53903=CARTESIAN_POINT ( 'NONE',  ( -119.8449999999999989, -7.632228543268599452, 2.479861379858951054 ) ) ;
#53912=CARTESIAN_POINT ( 'NONE',  ( -164.8429263765337964, 9.058813317711329915, -2.943386871421373119 ) ) ;
#53913=CARTESIAN_POINT ( 'NONE',  ( -177.1450000000000102, -4.716976649647092401, 6.492361379858946790 ) ) ;
#53915=EDGE_CURVE ( 'NONE', #8408, #64066, #41703, .T. ) ;
#53925=CARTESIAN_POINT ( 'NONE',  ( -73.94292637653379074, 0.000000000000000000, 9.524999999999991473 ) ) ;
#53928=DIRECTION ( 'NONE',  ( -1.000000000000000000, -0.000000000000000000, -0.000000000000000000 ) ) ;
#53931=CARTESIAN_POINT ( 'NONE',  ( -180.3549999999999898, -4.716976649647093289, -6.492361379858945902 ) ) ;
#53932=ORIENTED_EDGE ( 'NONE', *, *, #67944, .F. ) ;
#53941=CARTESIAN_POINT ( 'NONE',  ( -94.25499999999999545, -4.716976649647092401, 6.492361379858946790 ) ) ;
#53951=CARTESIAN_POINT ( 'NONE',  ( -60.59499999999997755, 2.607480562269073321, 8.024999999999991473 ) ) ;
#53955=CARTESIAN_POINT ( 'NONE',  ( -49.34292637653378222, -9.058813317711329915, 2.943386871421371787 ) ) ;
#53956=CARTESIAN_POINT ( 'NONE',  ( -126.0570736234661808, 0.000000000000000000, 9.524999999999991473 ) ) ;
#53964=CARTESIAN_POINT ( 'NONE',  ( -115.2549999999999955, -4.716976649647092401, 6.492361379858946790 ) ) ;
#53970=DIRECTION ( 'NONE',  ( -1.000000000000000000, -0.000000000000000000, -0.000000000000000000 ) ) ;
#53972=CARTESIAN_POINT ( 'NONE',  ( -158.4570736234661581, -9.058813317711329915, 2.943386871421371787 ) ) ;
#53975=CARTESIAN_POINT ( 'NONE',  ( -94.70707362346618652, -3.094860106618431139, -9.524999999999991473 ) ) ;
#53984=B_SPLINE_CURVE_WITH_KNOTS ( 'NONE', 3,
 ( #46204, #30662, #25056, #67989 ),
 .UNSPECIFIED., .F., .F.,
 ( 4, 4 ),
 ( 0.000000000000000000, 1.000000000000000000 ),
 .UNSPECIFIED. ) ;
#53985=CARTESIAN_POINT ( 'NONE',  ( -142.5549999999999784, 0.000000000000000000, 8.024999999999991473 ) ) ;
#53989=CARTESIAN_POINT ( 'NONE',  ( -148.3449999999999989, 7.632228543268599452, -2.479861379858951942 ) ) ;
#53991=CARTESIAN_POINT ( 'NONE',  ( -134.0949999999999704, -2.607480562269071545, -8.024999999999991473 ) ) ;
#54000=CARTESIAN_POINT ( 'NONE',  ( -51.95499999999996987, -7.632228543268599452, 2.479861379858951054 ) ) ;
#54002=CARTESIAN_POINT ( 'NONE',  ( -62.54499999999998749, -7.632228543268600340, -2.479861379858950166 ) ) ;
#54004=CARTESIAN_POINT ( 'NONE',  ( -102.6570736234661751, 9.058813317711329915, 2.943386871421369566 ) ) ;
#54008=CARTESIAN_POINT ( 'NONE',  ( -106.0429263765337993, -9.058813317711329915, -2.943386871421370898 ) ) ;
#54016=ORIENTED_EDGE ( 'NONE', *, *, #43429, .F. ) ;
#54033=LINE ( 'NONE', #5838, #46392 ) ;
#54034=AXIS2_PLACEMENT_3D ( 'NONE', #44803, #67607, #2487 ) ;
#54036=CARTESIAN_POINT ( 'NONE',  ( -89.24499999999999034, -4.716976649647093289, -6.492361379858945902 ) ) ;
#54043=CARTESIAN_POINT ( 'NONE',  ( -175.0429263765338135, -9.058813317711329915, -2.943386871421370898 ) ) ;
#54053=CARTESIAN_POINT ( 'NONE',  ( -195.0000000000000000, 0.000000000000000000, 0.000000000000000000 ) ) ;
#54058=CARTESIAN_POINT ( 'NONE',  ( -69.14292637653379359, 5.598654528085800663, -7.705886871421367523 ) ) ;
#54061=VERTEX_POINT ( 'NONE', #53671 ) ;
#54067=CARTESIAN_POINT ( 'NONE',  ( -173.9049999999999727, 2.607480562269068880, -8.024999999999993250 ) ) ;
#54070=CARTESIAN_POINT ( 'NONE',  ( -147.3570736234661638, 5.598654528085804216, 7.705886871421366635 ) ) ;
#54072=CARTESIAN_POINT ( 'NONE',  ( -172.9449999999999932, -9.827790563157499189E-16, -8.024999999999991473 ) ) ;
#54073=CARTESIAN_POINT ( 'NONE',  ( -168.1449999999999818, -4.716976649647092401, 6.492361379858946790 ) ) ;
#54080=CARTESIAN_POINT ( 'NONE',  ( -82.40500000000000114, -2.607480562269069768, 8.024999999999991473 ) ) ;
#54081=CYLINDRICAL_SURFACE ( 'NONE', #24147, 9.524999999999991473 ) ;
#54084=CARTESIAN_POINT ( 'NONE',  ( -79.49499999999997613, 6.826472737025113702, -4.959722759717902107 ) ) ;
#54108=CARTESIAN_POINT ( 'NONE',  ( -110.4549999999999841, 7.632228543268599452, -2.479861379858951942 ) ) ;
#54122=CARTESIAN_POINT ( 'NONE',  ( -195.0000000000000000, 0.000000000000000000, 0.000000000000000000 ) ) ;
#54123=CARTESIAN_POINT ( 'NONE',  ( -13.68996927307399858, -10.98240371287465322, 4.836514277720893595 ) ) ;
#54124=CARTESIAN_POINT ( 'NONE',  ( -129.7429263765338021, -5.598654528085803328, -7.705886871421366635 ) ) ;
#54128=CARTESIAN_POINT ( 'NONE',  ( -47.60707362346616378, -8.102448949553174629, 5.886773742842742685 ) ) ;
#54129=VECTOR ( 'NONE', #2022, 1000.000000000000000 ) ;
#54133=CARTESIAN_POINT ( 'NONE',  ( -49.64292637653380780, -5.598654528085801552, 7.705886871421367523 ) ) ;
#54136=FACE_OUTER_BOUND ( 'NONE', #50208, .T. ) ;
#54137=CARTESIAN_POINT ( 'NONE',  ( -143.3050000000000068, 8.437984349512085203, -1.550032578732815448E-15 ) ) ;
#54152=CARTESIAN_POINT ( 'NONE',  ( -53.30499999999998550, 8.437984349512085203, -1.550032578732815448E-15 ) ) ;
#54162=ORIENTED_EDGE ( 'NONE', *, *, #14728, .T. ) ;
#54172=CARTESIAN_POINT ( 'NONE',  ( -110.5449999999999875, -7.632228543268600340, -2.479861379858950166 ) ) ;
#54174=CARTESIAN_POINT ( 'NONE',  ( -89.84499999999999886, -7.632228543268599452, 2.479861379858951054 ) ) ;
#54181=CARTESIAN_POINT ( 'NONE',  ( -120.7429263765338021, -5.598654528085803328, -7.705886871421366635 ) ) ;
#54182=CARTESIAN_POINT ( 'NONE',  ( -149.3949999999999818, -6.826472737025115478, -4.959722759717899443 ) ) ;
#54196=VECTOR ( 'NONE', #8641, 1000.000000000000000 ) ;
#54197=CARTESIAN_POINT ( 'NONE',  ( -115.9429263765338050, 0.000000000000000000, 9.524999999999991473 ) ) ;
#54200=CARTESIAN_POINT ( 'NONE',  ( -137.1550000000000011, 7.632228543268600340, 2.479861379858949277 ) ) ;
#54213=CARTESIAN_POINT ( 'NONE',  ( -95.15707362346617515, -9.058813317711329915, -2.943386871421370898 ) ) ;
#54215=CARTESIAN_POINT ( 'NONE',  ( -57.20499999999996987, -2.607480562269071545, -8.024999999999991473 ) ) ;
#54216=CARTESIAN_POINT ( 'NONE',  ( -124.0449999999999875, 7.632228543268600340, 2.479861379858949277 ) ) ;
#54217=CARTESIAN_POINT ( 'NONE',  ( -118.5570736234661808, -1.166476076187852838E-15, -9.524999999999991473 ) ) ;
#54227=CARTESIAN_POINT ( 'NONE',  ( -172.1050000000000182, -6.826472737025115478, 4.959722759717900331 ) ) ;
#54235=VERTEX_POINT ( 'NONE', #6872 ) ;
#54239=CARTESIAN_POINT ( 'NONE',  ( -84.80499999999999261, -8.437984349512085203, 5.166775262442717831E-16 ) ) ;
#54241=VECTOR ( 'NONE', #7363, 1000.000000000000000 ) ;
#54244=CARTESIAN_POINT ( 'NONE',  ( -63.80707362346617373, 10.01517768586948698, -1.839758294383808571E-15 ) ) ;
#54251=CARTESIAN_POINT ( 'NONE',  ( -103.8549999999999898, 4.716976649647094177, 6.492361379858945902 ) ) ;
#54254=CARTESIAN_POINT ( 'NONE',  ( -117.2949999999999875, -2.607480562269069768, 8.024999999999991473 ) ) ;
#54260=CARTESIAN_POINT ( 'NONE',  ( -154.3429263765337964, -9.058813317711329915, 2.943386871421371787 ) ) ;
#54262=CARTESIAN_POINT ( 'NONE',  ( -179.6949999999999932, -8.437984349512085203, 5.166775262442717831E-16 ) ) ;
#54270=CARTESIAN_POINT ( 'NONE',  ( -74.99292637653380211, 8.102448949553171076, -5.886773742842744461 ) ) ;
#54279=CARTESIAN_POINT ( 'NONE',  ( -79.64292637653380780, -5.598654528085801552, 7.705886871421367523 ) ) ;
#54281=CARTESIAN_POINT ( 'NONE',  ( -169.4049999999999443, -2.607480562269069768, 8.024999999999991473 ) ) ;
#54283=CARTESIAN_POINT ( 'NONE',  ( -112.0429263765337993, -9.058813317711329915, -2.943386871421370898 ) ) ;
#54289=CARTESIAN_POINT ( 'NONE',  ( -182.0070736234661979, -8.102448949553174629, -5.886773742842741797 ) ) ;
#54291=ORIENTED_EDGE ( 'NONE', *, *, #9138, .T. ) ;
#54292=DIRECTION ( 'NONE',  ( -1.000000000000000000, -0.000000000000000000, -0.000000000000000000 ) ) ;
#54293=CARTESIAN_POINT ( 'NONE',  ( -92.00499999999998124, 6.826472737025115478, 4.959722759717899443 ) ) ;
#54295=VERTEX_POINT ( 'NONE', #13527 ) ;
#54296=CARTESIAN_POINT ( 'NONE',  ( -92.75707362346618368, -5.598654528085801552, 7.705886871421367523 ) ) ;
#54297=CARTESIAN_POINT ( 'NONE',  ( -169.0429263765338135, -9.058813317711329915, -2.943386871421370898 ) ) ;
#54305=CARTESIAN_POINT ( 'NONE',  ( -66.14499999999998181, -4.716976649647092401, 6.492361379858946790 ) ) ;
#54307=CARTESIAN_POINT ( 'NONE',  ( -49.94292637653380496, 0.000000000000000000, 9.524999999999991473 ) ) ;
#54316=CARTESIAN_POINT ( 'NONE',  ( -110.9049999999999727, 2.607480562269068880, -8.024999999999993250 ) ) ;
#54319=CARTESIAN_POINT ( 'NONE',  ( -73.04292637653379927, -9.058813317711329915, -2.943386871421370898 ) ) ;
#54323=CARTESIAN_POINT ( 'NONE',  ( -152.1570736234661751, -9.058813317711329915, -2.943386871421370898 ) ) ;
#54327=CARTESIAN_POINT ( 'NONE',  ( -97.25707362346618368, 5.598654528085800663, -7.705886871421367523 ) ) ;
#54329=EDGE_CURVE ( 'NONE', #57410, #32866, #49499, .T. ) ;
#54337=CARTESIAN_POINT ( 'NONE',  ( -129.5049999999999670, -6.826472737025115478, -4.959722759717899443 ) ) ;
#54340=CARTESIAN_POINT ( 'NONE',  ( -141.1449999999999818, -4.716976649647092401, 6.492361379858946790 ) ) ;
#54342=CARTESIAN_POINT ( 'NONE',  ( -129.7450000000000045, 4.716976649647094177, 6.492361379858945902 ) ) ;
#54348=CARTESIAN_POINT ( 'NONE',  ( -53.15499999999997982, 7.632228543268600340, 2.479861379858949277 ) ) ;
#54350=CARTESIAN_POINT ( 'NONE',  ( -59.99499999999996902, -6.826472737025115478, 4.959722759717900331 ) ) ;
#54356=CARTESIAN_POINT ( 'NONE',  ( -107.9929263765337879, 8.102448949553171076, -5.886773742842744461 ) ) ;
#54371=VERTEX_POINT ( 'NONE', #36436 ) ;
#54377=CARTESIAN_POINT ( 'NONE',  ( -118.7070736234669539, -3.094860106631741381, -9.524999999990320987 ) ) ;
#54378=EDGE_CURVE ( 'NONE', #40144, #21270, #63032, .T. ) ;
#54382=CARTESIAN_POINT ( 'NONE',  ( -87.74499999999999034, 4.716976649647094177, 6.492361379858945902 ) ) ;
#54386=EDGE_CURVE ( 'NONE', #18337, #65809, #8479, .T. ) ;
#54399=CARTESIAN_POINT ( 'NONE',  ( -195.0000000000000000, 0.000000000000000000, 0.000000000000000000 ) ) ;
#54404=CARTESIAN_POINT ( 'NONE',  ( -183.0000000000000000, 7.623482428031956637, -5.710353812986356026 ) ) ;
#54406=( BOUNDED_CURVE ( )  B_SPLINE_CURVE ( 2, ( #62936, #45442, #45770, #50672, #2413, #23927, #66862, #18666, #40485, #37662, #16183 ),
 .UNSPECIFIED., .F., .F. ) 
 B_SPLINE_CURVE_WITH_KNOTS ( ( 3, 2, 2, 2, 2, 3 ),
 ( 0.7282608695652174058, 0.7304347826086956541, 0.7326086956521739024, 0.7347826086956521507, 0.7369565217391303991, 0.7391304347826086474 ),
 .UNSPECIFIED. ) 
 CURVE ( )  GEOMETRIC_REPRESENTATION_ITEM ( )  RATIONAL_B_SPLINE_CURVE ( ( 1.000000000000000000, 0.9510565162951535312, 1.000000000000000000, 0.9510565162951535312, 1.000000000000000000, 0.9510565162951535312, 1.000000000000000000, 0.9510565162951535312, 1.000000000000000000, 0.9510565162951535312, 1.000000000000000000 ) ) 
 REPRESENTATION_ITEM ( '' )  );
#54415=CARTESIAN_POINT ( 'NONE',  ( -163.5550000000000068, 0.000000000000000000, 8.024999999999991473 ) ) ;
#54417=CARTESIAN_POINT ( 'NONE',  ( -147.6570736234662036, 9.058813317711329915, 2.943386871421369566 ) ) ;
#54418=CARTESIAN_POINT ( 'NONE',  ( -175.4949999999999761, 6.826472737025113702, -4.959722759717902107 ) ) ;
#54419=CARTESIAN_POINT ( 'NONE',  ( -171.4449999999999932, 0.000000000000000000, 8.024999999999991473 ) ) ;
#54425=CARTESIAN_POINT ( 'NONE',  ( -84.35499999999998977, -4.716976649647093289, -6.492361379858945902 ) ) ;
#54429=CARTESIAN_POINT ( 'NONE',  ( -79.34499999999998465, 7.632228543268599452, -2.479861379858951942 ) ) ;
#54431=CARTESIAN_POINT ( 'NONE',  ( -134.4570736234661865, -9.058813317711329915, 2.943386871421371787 ) ) ;
#54458=CARTESIAN_POINT ( 'NONE',  ( -110.1549999999999869, 7.632228543268600340, 2.479861379858949277 ) ) ;
#54468=EDGE_CURVE ( 'NONE', #36987, #33115, #46884, .T. ) ;
#54472=DIRECTION ( 'NONE',  ( -1.000000000000000000, -0.000000000000000000, -0.000000000000000000 ) ) ;
#54483=CARTESIAN_POINT ( 'NONE',  ( -50.84292637653378932, 9.058813317711329915, -2.943386871421373119 ) ) ;
#54487=CARTESIAN_POINT ( 'NONE',  ( -159.0570736234661808, 0.000000000000000000, 9.524999999999991473 ) ) ;
#54489=CARTESIAN_POINT ( 'NONE',  ( -147.3549999999999898, -4.716976649647093289, -6.492361379858945902 ) ) ;
#54499=CARTESIAN_POINT ( 'NONE',  ( -108.5929263765347770, -3.094860106634296670, -9.524999999988466470 ) ) ;
#54500=CARTESIAN_POINT ( 'NONE',  ( -60.50499999999998124, -6.826472737025115478, -4.959722759717899443 ) ) ;
#54518=CARTESIAN_POINT ( 'NONE',  ( -105.7449999999999903, 4.716976649647094177, 6.492361379858945902 ) ) ;
#54520=CARTESIAN_POINT ( 'NONE',  ( -91.64499999999999602, 4.716976649647091513, -6.492361379858946790 ) ) ;
#54529=ORIENTED_EDGE ( 'NONE', *, *, #41495, .F. ) ;
#54530=CARTESIAN_POINT ( 'NONE',  ( -123.5929263765337822, -3.094860106618431139, -9.524999999999991473 ) ) ;
#54531=CARTESIAN_POINT ( 'NONE',  ( -144.1449999999999818, -4.716976649647092401, 6.492361379858946790 ) ) ;
#54543=CARTESIAN_POINT ( 'NONE',  ( -50.60707362346616378, -8.102448949553174629, 5.886773742842742685 ) ) ;
#54544=CARTESIAN_POINT ( 'NONE',  ( -151.6429263765338078, -5.598654528085801552, 7.705886871421367523 ) ) ;
#54546=CARTESIAN_POINT ( 'NONE',  ( -140.3049999999999500, 8.437984349512086979, -1.550032578732815448E-15 ) ) ;
#54547=ORIENTED_EDGE ( 'NONE', *, *, #40551, .F. ) ;
#54562=CARTESIAN_POINT ( 'NONE',  ( -50.75499999999999545, 4.716976649647091513, -6.492361379858946790 ) ) ;
#54564=CARTESIAN_POINT ( 'NONE',  ( -115.6449999999999818, 4.716976649647091513, -6.492361379858946790 ) ) ;
#54574=EDGE_CURVE ( 'NONE', #16179, #34526, #65706, .T. ) ;
#54578=CARTESIAN_POINT ( 'NONE',  ( -167.9050000000000011, 2.607480562269068880, -8.024999999999993250 ) ) ;
#54588=TOROIDAL_SURFACE ( 'NONE', #2831, 9.525000000000000355, 1.000000000000000888 ) ;
#54590=CARTESIAN_POINT ( 'NONE',  ( -86.60500000000000398, 6.826472737025113702, -4.959722759717902107 ) ) ;
#54596=CARTESIAN_POINT ( 'NONE',  ( -69.50707362346615525, 8.102448949553176405, 5.886773742842740909 ) ) ;
#54603=CARTESIAN_POINT ( 'NONE',  ( -100.4050000000000011, -2.607480562269069768, 8.024999999999991473 ) ) ;
#54605=CARTESIAN_POINT ( 'NONE',  ( -113.0949999999999989, -2.607480562269071545, -8.024999999999991473 ) ) ;
#54608=CARTESIAN_POINT ( 'NONE',  ( -154.1070736234661922, 8.102448949553172852, -5.886773742842744461 ) ) ;
#54609=CARTESIAN_POINT ( 'NONE',  ( -149.6929263765338192, 10.01517768586948698, -1.839758294383808571E-15 ) ) ;
#54610=CARTESIAN_POINT ( 'NONE',  ( -175.3449999999999989, 7.632228543268599452, -2.479861379858951942 ) ) ;
#54617=CARTESIAN_POINT ( 'NONE',  ( -66.44292637653380496, -1.166476076187852838E-15, -9.524999999999991473 ) ) ;
#54621=CARTESIAN_POINT ( 'NONE',  ( -142.1929263765337339, -10.01517768586948698, 6.132527647946031529E-16 ) ) ;
#54623=EDGE_CURVE ( 'NONE', #48074, #51470, #17479, .T. ) ;
#54626=ORIENTED_EDGE ( 'NONE', *, *, #34052, .F. ) ;
#54627=CARTESIAN_POINT ( 'NONE',  ( -172.2549999999999955, -4.716976649647092401, 6.492361379858946790 ) ) ;
#54629=VECTOR ( 'NONE', #27376, 1000.000000000000000 ) ;
#54641=CARTESIAN_POINT ( 'NONE',  ( -80.45499999999998408, 7.632228543268599452, -2.479861379858951942 ) ) ;
#54652=CARTESIAN_POINT ( 'NONE',  ( -59.84499999999998465, -7.632228543268599452, 2.479861379858951054 ) ) ;
#54656=ORIENTED_EDGE ( 'NONE', *, *, #66817, .T. ) ;
#54663=CARTESIAN_POINT ( 'NONE',  ( -113.3049999999999784, 8.437984349512085203, -1.550032578732815448E-15 ) ) ;
#54670=CARTESIAN_POINT ( 'NONE',  ( -155.1570736234661751, -9.058813317711329915, -2.943386871421370898 ) ) ;
#54673=CARTESIAN_POINT ( 'NONE',  ( -96.50707362346616947, 8.102448949553176405, 5.886773742842740909 ) ) ;
#54678=CARTESIAN_POINT ( 'NONE',  ( -135.3549999999999898, -4.716976649647093289, -6.492361379858945902 ) ) ;
#54682=CARTESIAN_POINT ( 'NONE',  ( -143.6949999999999932, -8.437984349512085203, 5.166775262442717831E-16 ) ) ;
#54684=CARTESIAN_POINT ( 'NONE',  ( -127.0449999999999875, 7.632228543268600340, 2.479861379858949277 ) ) ;
#54687=CARTESIAN_POINT ( 'NONE',  ( -49.25499999999999545, -4.716976649647092401, 6.492361379858946790 ) ) ;
#54688=( BOUNDED_CURVE ( )  B_SPLINE_CURVE ( 2, ( #58263, #60256, #54279, #17382, #12058, #65885, #54955, #44810, #11374, #36849, #20982 ),
 .UNSPECIFIED., .F., .F. ) 
 B_SPLINE_CURVE_WITH_KNOTS ( ( 3, 2, 2, 2, 2, 3 ),
 ( 0.7608695652173913526, 0.7630434782608696009, 0.7652173913043478493, 0.7673913043478260976, 0.7695652173913043459, 0.7717391304347825942 ),
 .UNSPECIFIED. ) 
 CURVE ( )  GEOMETRIC_REPRESENTATION_ITEM ( )  RATIONAL_B_SPLINE_CURVE ( ( 1.000000000000000000, 0.9510565162951535312, 1.000000000000000000, 0.9510565162951535312, 1.000000000000000000, 0.9510565162951535312, 1.000000000000000000, 0.9510565162951535312, 1.000000000000000000, 0.9510565162951535312, 1.000000000000000000 ) ) 
 REPRESENTATION_ITEM ( '' )  );
#54689=CARTESIAN_POINT ( 'NONE',  ( -58.64499999999998892, 4.716976649647091513, -6.492361379858946790 ) ) ;
#54695=CARTESIAN_POINT ( 'NONE',  ( -91.04292637653379927, -9.058813317711329915, -2.943386871421370898 ) ) ;
#54702=EDGE_CURVE ( 'NONE', #47647, #60379, #35096, .T. ) ;
#54712=CARTESIAN_POINT ( 'NONE',  ( -117.0570736234661808, 0.000000000000000000, 9.524999999999991473 ) ) ;
#54719=CARTESIAN_POINT ( 'NONE',  ( -89.39499999999996760, -6.826472737025115478, -4.959722759717899443 ) ) ;
#54732=FACE_OUTER_BOUND ( 'NONE', #8882, .T. ) ;
#54735=CARTESIAN_POINT ( 'NONE',  ( -176.0070736234661695, -8.102448949553172852, -5.886773742842741797 ) ) ;
#54739=CARTESIAN_POINT ( 'NONE',  ( -115.9429263765338050, 0.000000000000000000, 9.524999999999991473 ) ) ;
#54743=CARTESIAN_POINT ( 'NONE',  ( -149.3070736234662093, -10.01517768586948698, 6.132527647946031529E-16 ) ) ;
#54744=ORIENTED_EDGE ( 'NONE', *, *, #2994, .T. ) ;
#54745=CARTESIAN_POINT ( 'NONE',  ( -155.4549999999999841, 7.632228543268599452, -2.479861379858951942 ) ) ;
#54747=CARTESIAN_POINT ( 'NONE',  ( -183.8867045463858574, -8.535045582951720888, -1.368092718024570109 ) ) ;
#54748=CARTESIAN_POINT ( 'NONE',  ( -171.2949999999999875, -2.607480562269069768, 8.024999999999991473 ) ) ;
#54749=CARTESIAN_POINT ( 'NONE',  ( -160.7949999999999591, 2.607480562269069324, -8.024999999999993250 ) ) ;
#54753=AXIS2_PLACEMENT_3D ( 'NONE', #46349, #18855, #14293 ) ;
#54755=CARTESIAN_POINT ( 'NONE',  ( -73.85499999999998977, 4.716976649647094177, 6.492361379858945902 ) ) ;
#54759=CARTESIAN_POINT ( 'NONE',  ( -68.84499999999998465, -7.632228543268599452, 2.479861379858951054 ) ) ;
#54776=DIRECTION ( 'NONE',  ( -1.000000000000000000, -0.000000000000000000, -0.000000000000000000 ) ) ;
#54786=CARTESIAN_POINT ( 'NONE',  ( -69.80707362346613820, 10.01517768586948698, -1.839758294383808966E-15 ) ) ;
#54788=CARTESIAN_POINT ( 'NONE',  ( -108.6549999999999869, -7.632228543268600340, -2.479861379858950166 ) ) ;
#54792=ORIENTED_EDGE ( 'NONE', *, *, #16734, .T. ) ;
#54809=CARTESIAN_POINT ( 'NONE',  ( -104.6929263765337907, 10.01517768586948698, -1.839758294383808966E-15 ) ) ;
#54811=ORIENTED_EDGE ( 'NONE', *, *, #51076, .T. ) ;
#54814=CARTESIAN_POINT ( 'NONE',  ( -49.34292637653378222, -9.058813317711329915, 2.943386871421371787 ) ) ;
#54818=CARTESIAN_POINT ( 'NONE',  ( -146.7549999999999955, 4.716976649647091513, -6.492361379858946790 ) ) ;
#54822=CARTESIAN_POINT ( 'NONE',  ( -106.7929263765347656, -3.094860106602296046, 9.525000000011715429 ) ) ;
#54829=CARTESIAN_POINT ( 'NONE',  ( -109.7929263765347656, -3.094860106602833394, 9.525000000011322854 ) ) ;
#54830=CARTESIAN_POINT ( 'NONE',  ( -54.05499999999999261, -9.827790563157499189E-16, -8.024999999999991473 ) ) ;
#54831=ORIENTED_EDGE ( 'NONE', *, *, #17429, .T. ) ;
#54836=DIRECTION ( 'NONE',  ( -1.000000000000000000, -0.000000000000000000, -0.000000000000000000 ) ) ;
#54837=CARTESIAN_POINT ( 'NONE',  ( -96.59292637653489066, -3.094860106636716512, -9.524999999986706101 ) ) ;
#54839=CARTESIAN_POINT ( 'NONE',  ( -145.2570736234661695, 5.598654528085800663, -7.705886871421367523 ) ) ;
#54845=CARTESIAN_POINT ( 'NONE',  ( -109.7949999999999875, 2.607480562269069324, -8.024999999999993250 ) ) ;
#54847=CARTESIAN_POINT ( 'NONE',  ( -73.79499999999997328, 2.607480562269068880, -8.024999999999993250 ) ) ;
#54858=CARTESIAN_POINT ( 'NONE',  ( -121.6429263765338078, -5.598654528085801552, 7.705886871421367523 ) ) ;
#54859=CARTESIAN_POINT ( 'NONE',  ( -136.6449999999999818, 4.716976649647091513, -6.492361379858946790 ) ) ;
#54864=CARTESIAN_POINT ( 'NONE',  ( -66.50707362346616947, 8.102448949553176405, 5.886773742842740909 ) ) ;
#54876=CARTESIAN_POINT ( 'NONE',  ( -141.9549999999999841, -7.632228543268599452, 2.479861379858951054 ) ) ;
#54882=CARTESIAN_POINT ( 'NONE',  ( -195.0000000000000000, 1.166476076187852838E-15, -9.524999999999991473 ) ) ;
#54887=CARTESIAN_POINT ( 'NONE',  ( -51.65499999999997982, -7.632228543268600340, -2.479861379858950166 ) ) ;
#54900=LINE ( 'NONE', #28523, #45265 ) ;
#54901=CARTESIAN_POINT ( 'NONE',  ( -170.7549999999999955, 4.716976649647091513, -6.492361379858946790 ) ) ;
#54907=CARTESIAN_POINT ( 'NONE',  ( -183.9999999999999716, -7.591759853317446627, 2.884858859289065602 ) ) ;
#54913=CARTESIAN_POINT ( 'NONE',  ( -87.80500000000000682, -8.437984349512085203, 5.166775262442717831E-16 ) ) ;
#54918=CARTESIAN_POINT ( 'NONE',  ( -52.40707362346616804, 3.094860106618428031, -9.524999999999993250 ) ) ;
#54929=CARTESIAN_POINT ( 'NONE',  ( -104.9949999999999761, -6.826472737025115478, 4.959722759717900331 ) ) ;
#54932=CARTESIAN_POINT ( 'NONE',  ( -15.32933058623710565, 10.90871211463570845, -4.999999999999999112 ) ) ;
#54935=CARTESIAN_POINT ( 'NONE',  ( -148.6429263765338078, -5.598654528085801552, 7.705886871421367523 ) ) ;
#54936=CARTESIAN_POINT ( 'NONE',  ( -175.4949999999999761, 6.826472737025113702, -4.959722759717902107 ) ) ;
#54940=ADVANCED_FACE ( 'NONE', ( #32413 ), #694, .T. ) ;
#54945=ORIENTED_EDGE ( 'NONE', *, *, #32640, .F. ) ;
#54946=CARTESIAN_POINT ( 'NONE',  ( -65.54292637653379927, 9.058813317711329915, 2.943386871421369566 ) ) ;
#54955=CARTESIAN_POINT ( 'NONE',  ( -79.04292637653379927, -9.058813317711329915, -2.943386871421370898 ) ) ;
#54957=CARTESIAN_POINT ( 'NONE',  ( -167.6050000000000182, 6.826472737025113702, -4.959722759717902107 ) ) ;
#54966=ORIENTED_EDGE ( 'NONE', *, *, #10624, .T. ) ;
#54968=CARTESIAN_POINT ( 'NONE',  ( -81.05499999999999261, -9.827790563157499189E-16, -8.024999999999991473 ) ) ;
#54972=CARTESIAN_POINT ( 'NONE',  ( -126.4429263765338192, -1.166476076187852838E-15, -9.524999999999991473 ) ) ;
#54980=CARTESIAN_POINT ( 'NONE',  ( -61.49499999999998323, 6.826472737025113702, -4.959722759717902107 ) ) ;
#54993=CARTESIAN_POINT ( 'NONE',  ( -110.6049999999999898, 6.826472737025113702, -4.959722759717902107 ) ) ;
#54999=CARTESIAN_POINT ( 'NONE',  ( -154.5570736234661808, -1.166476076187852838E-15, -9.524999999999991473 ) ) ;
#55003=CARTESIAN_POINT ( 'NONE',  ( -83.15707362346617515, -9.058813317711329915, -2.943386871421370898 ) ) ;
#55013=CARTESIAN_POINT ( 'NONE',  ( -128.0049999999999670, 6.826472737025116366, 4.959722759717898555 ) ) ;
#55018=CARTESIAN_POINT ( 'NONE',  ( -141.8950000000000102, 6.826472737025116366, 4.959722759717898555 ) ) ;
#55020=CARTESIAN_POINT ( 'NONE',  ( -124.3449999999999847, 7.632228543268599452, -2.479861379858951942 ) ) ;
#55029=CARTESIAN_POINT ( 'NONE',  ( -181.1929263765337907, -10.01517768586948698, 6.132527647946031529E-16 ) ) ;
#55031=CARTESIAN_POINT ( 'NONE',  ( -56.09499999999997044, -2.607480562269071545, -8.024999999999991473 ) ) ;
#55034=CARTESIAN_POINT ( 'NONE',  ( -102.2070736234672097, 3.094860106635239028, 9.524999999987784349 ) ) ;
#55040=CARTESIAN_POINT ( 'NONE',  ( -91.64292637653380780, -5.598654528085801552, 7.705886871421367523 ) ) ;
#55046=DIRECTION ( 'NONE',  ( -1.000000000000000000, -0.000000000000000000, -0.000000000000000000 ) ) ;
#55048=ORIENTED_EDGE ( 'NONE', *, *, #23920, .F. ) ;
#55067=CARTESIAN_POINT ( 'NONE',  ( -88.64499999999998181, 4.716976649647091513, -6.492361379858946790 ) ) ;
#55073=VERTEX_POINT ( 'NONE', #27811 ) ;
#55078=ADVANCED_FACE ( 'NONE', ( #38458 ), #44433, .F. ) ;
#55083=CARTESIAN_POINT ( 'NONE',  ( -180.6570736234661751, 9.058813317711329915, 2.943386871421369566 ) ) ;
#55092=( BOUNDED_CURVE ( )  B_SPLINE_CURVE ( 2, ( #64631, #42879, #55722, #28622, #40606, #29682, #62021, #7528, #67664, #66264, #61332 ),
 .UNSPECIFIED., .F., .F. ) 
 B_SPLINE_CURVE_WITH_KNOTS ( ( 3, 2, 2, 2, 2, 3 ),
 ( 0.8913043478260869179, 0.8934782608695651662, 0.8956521739130435256, 0.8978260869565217739, 0.9000000000000000222, 0.9021739130434782705 ),
 .UNSPECIFIED. ) 
 CURVE ( )  GEOMETRIC_REPRESENTATION_ITEM ( )  RATIONAL_B_SPLINE_CURVE ( ( 1.000000000000000000, 0.9510565162951535312, 1.000000000000000000, 0.9510565162951535312, 1.000000000000000000, 0.9510565162951535312, 1.000000000000000000, 0.9510565162951535312, 1.000000000000000000, 0.9510565162951535312, 1.000000000000000000 ) ) 
 REPRESENTATION_ITEM ( '' )  );
#55095=CARTESIAN_POINT ( 'NONE',  ( -148.7070736234666697, -3.094860106625556995, -9.524999999994815170 ) ) ;
#55099=CARTESIAN_POINT ( 'NONE',  ( -162.6550000000000011, -7.632228543268600340, -2.479861379858950166 ) ) ;
#55100=DIRECTION ( 'NONE',  ( 0.000000000000000000, 0.000000000000000000, 1.000000000000000000 ) ) ;
#55101=CARTESIAN_POINT ( 'NONE',  ( -183.5232763065959602, -3.916627572773804022, -8.111163545727393398 ) ) ;
#55103=CARTESIAN_POINT ( 'NONE',  ( -177.7449999999999761, 4.716976649647094177, 6.492361379858945902 ) ) ;
#55104=CARTESIAN_POINT ( 'NONE',  ( -157.0449999999999875, 7.632228543268600340, 2.479861379858949277 ) ) ;
#55109=CARTESIAN_POINT ( 'NONE',  ( -68.75499999999998124, 4.716976649647091513, -6.492361379858946790 ) ) ;
#55113=CARTESIAN_POINT ( 'NONE',  ( -72.74499999999999034, 4.716976649647094177, 6.492361379858945902 ) ) ;
#55115=FACE_OUTER_BOUND ( 'NONE', #45519, .T. ) ;
#55117=CARTESIAN_POINT ( 'NONE',  ( -176.5429263765338135, 9.058813317711329915, 2.943386871421369566 ) ) ;
#55123=CARTESIAN_POINT ( 'NONE',  ( -50.99292637653379501, 8.102448949553172852, -5.886773742842744461 ) ) ;
#55132=VECTOR ( 'NONE', #51676, 1000.000000000000000 ) ;
#55138=CARTESIAN_POINT ( 'NONE',  ( -116.7549999999999812, 4.716976649647091513, -6.492361379858946790 ) ) ;
#55143=CARTESIAN_POINT ( 'NONE',  ( -56.24292637653380211, 5.598654528085804216, 7.705886871421366635 ) ) ;
#55165=VERTEX_POINT ( 'NONE', #41541 ) ;
#55167=CARTESIAN_POINT ( 'NONE',  ( -131.0049999999999670, 6.826472737025116366, 4.959722759717898555 ) ) ;
#55181=ORIENTED_EDGE ( 'NONE', *, *, #54378, .F. ) ;
#55189=CYLINDRICAL_SURFACE ( 'NONE', #21683, 9.524999999999991473 ) ;
#55203=CARTESIAN_POINT ( 'NONE',  ( -103.9449999999999932, -9.827790563157499189E-16, -8.024999999999991473 ) ) ;
#55205=CARTESIAN_POINT ( 'NONE',  ( -75.59499999999998465, 2.607480562269073321, 8.024999999999991473 ) ) ;
#55214=ORIENTED_EDGE ( 'NONE', *, *, #7547, .F. ) ;
#55215=CARTESIAN_POINT ( 'NONE',  ( -119.8429263765338106, 9.058813317711329915, -2.943386871421373119 ) ) ;
#55217=CARTESIAN_POINT ( 'NONE',  ( -133.1950000000000216, 8.437984349512085203, -1.550032578732815448E-15 ) ) ;
#55230=DIRECTION ( 'NONE',  ( -1.000000000000000000, -0.000000000000000000, -0.000000000000000000 ) ) ;
#55233=CARTESIAN_POINT ( 'NONE',  ( -143.3049999999999784, 8.437984349512086979, -1.550032578732815448E-15 ) ) ;
#55239=VECTOR ( 'NONE', #27774, 1000.000000000000000 ) ;
#55249=CARTESIAN_POINT ( 'NONE',  ( -54.35499999999998977, -4.716976649647093289, -6.492361379858945902 ) ) ;
#55253=CARTESIAN_POINT ( 'NONE',  ( -195.0000000000000000, 1.166476076187852838E-15, -9.524999999999991473 ) ) ;
#55259=VERTEX_POINT ( 'NONE', #8489 ) ;
#55264=CARTESIAN_POINT ( 'NONE',  ( -159.5049999999999955, -6.826472737025115478, -4.959722759717899443 ) ) ;
#55281=CARTESIAN_POINT ( 'NONE',  ( -87.50499999999995282, -6.826472737025115478, -4.959722759717899443 ) ) ;
#55296=CARTESIAN_POINT ( 'NONE',  ( -108.8949999999999960, 6.826472737025116366, 4.959722759717898555 ) ) ;
#55298=DIRECTION ( 'NONE',  ( 0.000000000000000000, 0.000000000000000000, 1.000000000000000000 ) ) ;
#55300=CARTESIAN_POINT ( 'NONE',  ( -18.05533399021871332, 11.32548081226861569, 3.971246689443173050 ) ) ;
#55302=CARTESIAN_POINT ( 'NONE',  ( -157.0429263765338135, -9.058813317711329915, -2.943386871421370898 ) ) ;
#55303=CARTESIAN_POINT ( 'NONE',  ( -171.4449999999999932, 0.000000000000000000, 8.024999999999991473 ) ) ;
#55310=CARTESIAN_POINT ( 'NONE',  ( -66.59292637653381064, -3.094860106618431139, -9.524999999999991473 ) ) ;
#55321=CARTESIAN_POINT ( 'NONE',  ( -173.3049999999999500, 8.437984349512086979, -1.550032578732815448E-15 ) ) ;
#55327=FACE_BOUND ( 'NONE', #14392, .T. ) ;
#55333=CARTESIAN_POINT ( 'NONE',  ( -87.65499999999998693, -7.632228543268600340, -2.479861379858950166 ) ) ;
#55341=CARTESIAN_POINT ( 'NONE',  ( -113.2429263765338163, 5.598654528085804216, 7.705886871421366635 ) ) ;
#55347=CARTESIAN_POINT ( 'NONE',  ( -140.4570736234661865, -9.058813317711329915, 2.943386871421371787 ) ) ;
#55348=CARTESIAN_POINT ( 'NONE',  ( -57.89499999999996760, 6.826472737025116366, 4.959722759717898555 ) ) ;
#55358=CARTESIAN_POINT ( 'NONE',  ( -57.14499999999997470, -4.716976649647092401, 6.492361379858946790 ) ) ;
#55361=CARTESIAN_POINT ( 'NONE',  ( -114.5050000000000097, -6.826472737025115478, -4.959722759717899443 ) ) ;
#55369=CARTESIAN_POINT ( 'NONE',  ( -150.8070736234661808, 10.01517768586948698, -1.839758294383808571E-15 ) ) ;
#55374=CARTESIAN_POINT ( 'NONE',  ( -84.05707362346618083, 0.000000000000000000, 9.524999999999991473 ) ) ;
#55382=CARTESIAN_POINT ( 'NONE',  ( -133.4049999999999443, -2.607480562269069768, 8.024999999999991473 ) ) ;
#55386=CARTESIAN_POINT ( 'NONE',  ( -54.89292637653381490, -8.102448949553174629, -5.886773742842741797 ) ) ;
#55387=CARTESIAN_POINT ( 'NONE',  ( -139.0450000000000159, 7.632228543268600340, 2.479861379858949277 ) ) ;
#55388=CARTESIAN_POINT ( 'NONE',  ( -126.4450000000000074, 0.000000000000000000, 8.024999999999991473 ) ) ;
#55394=CARTESIAN_POINT ( 'NONE',  ( -181.4929263765337737, -8.102448949553172852, 5.886773742842742685 ) ) ;
#55395=CARTESIAN_POINT ( 'NONE',  ( -48.14499999999999602, -4.716976649647092401, 6.492361379858946790 ) ) ;
#55397=CARTESIAN_POINT ( 'NONE',  ( -102.0570736234661808, 0.000000000000000000, 9.524999999999991473 ) ) ;
#55400=CARTESIAN_POINT ( 'NONE',  ( -94.49292637653381632, -8.102448949553172852, 5.886773742842742685 ) ) ;
#55404=CARTESIAN_POINT ( 'NONE',  ( -163.0429263765338135, -9.058813317711329915, -2.943386871421370898 ) ) ;
#55411=CARTESIAN_POINT ( 'NONE',  ( -45.00000000000000000, 0.000000000000000000, 0.000000000000000000 ) ) ;
#55418=CARTESIAN_POINT ( 'NONE',  ( -195.0000000000000000, 1.166476076187852838E-15, -9.524999999999991473 ) ) ;
#55430=CARTESIAN_POINT ( 'NONE',  ( -94.19499999999999318, 8.437984349512085203, -1.550032578732815448E-15 ) ) ;
#55432=( BOUNDED_CURVE ( )  B_SPLINE_CURVE ( 2, ( #38383, #54829, #65415, #39401, #33730, #60799, #60459, #59785, #61167, #54499, #28433 ),
 .UNSPECIFIED., .F., .F. ) 
 B_SPLINE_CURVE_WITH_KNOTS ( ( 3, 2, 2, 2, 2, 3 ),
 ( 0.5434782608695523098, 0.5456521739130305582, 0.5478260869565086955, 0.5499999999999870548, 0.5521739130434651921, 0.5543478260869434404 ),
 .UNSPECIFIED. ) 
 CURVE ( )  GEOMETRIC_REPRESENTATION_ITEM ( )  RATIONAL_B_SPLINE_CURVE ( ( 1.000000000000289990, 0.9510565162948635409, 1.000000000000000000, 0.9510565162951535312, 1.000000000000000000, 0.9510565162951535312, 1.000000000000000000, 0.9510565162951535312, 1.000000000000000000, 0.9510565162954485174, 0.9999999999997050137 ) ) 
 REPRESENTATION_ITEM ( '' )  );
#55446=FACE_OUTER_BOUND ( 'NONE', #61926, .T. ) ;
#55450=CARTESIAN_POINT ( 'NONE',  ( -181.1070736234661638, 8.102448949553171076, -5.886773742842744461 ) ) ;
#55453=CARTESIAN_POINT ( 'NONE',  ( -109.8570736234661780, -5.598654528085803328, -7.705886871421366635 ) ) ;
#55463=CARTESIAN_POINT ( 'NONE',  ( -159.3549999999999898, -4.716976649647093289, -6.492361379858945902 ) ) ;
#55464=CARTESIAN_POINT ( 'NONE',  ( -183.9715320224743778, -8.560729921636262674, 0.5282838339113725690 ) ) ;
#55465=CARTESIAN_POINT ( 'NONE',  ( -163.3449999999999989, 7.632228543268599452, -2.479861379858951942 ) ) ;
#55467=CARTESIAN_POINT ( 'NONE',  ( -153.2949999999999875, -2.607480562269069768, 8.024999999999991473 ) ) ;
#55474=CARTESIAN_POINT ( 'NONE',  ( -72.35499999999998977, -4.716976649647093289, -6.492361379858945902 ) ) ;
#55478=CARTESIAN_POINT ( 'NONE',  ( -73.79499999999997328, 2.607480562269069324, -8.024999999999993250 ) ) ;
#55482=CARTESIAN_POINT ( 'NONE',  ( -177.2929263765339556, 3.094860106616924345, -9.525000000001085709 ) ) ;
#55492=ORIENTED_EDGE ( 'NONE', *, *, #66654, .T. ) ;
#55494=CARTESIAN_POINT ( 'NONE',  ( -195.0000000000000000, 9.184850993605130195E-16, -7.499999999999984901 ) ) ;
#55495=CARTESIAN_POINT ( 'NONE',  ( -133.4070736234668004, 3.094860106608142925, -9.525000000007466383 ) ) ;
#55501=CARTESIAN_POINT ( 'NONE',  ( -107.4549999999999983, 7.632228543268599452, -2.479861379858951942 ) ) ;
#55506=VERTEX_POINT ( 'NONE', #2709 ) ;
#55533=DIRECTION ( 'NONE',  ( 0.000000000000000000, 0.000000000000000000, 1.000000000000000000 ) ) ;
#55534=CARTESIAN_POINT ( 'NONE',  ( -133.2549999999999955, -4.716976649647092401, 6.492361379858946790 ) ) ;
#55540=CARTESIAN_POINT ( 'NONE',  ( -156.7429263765338021, -5.598654528085803328, -7.705886871421366635 ) ) ;
#55542=ORIENTED_EDGE ( 'NONE', *, *, #39131, .T. ) ;
#55555=CARTESIAN_POINT ( 'NONE',  ( -178.5570736234661808, -1.166476076187852838E-15, -9.524999999999991473 ) ) ;
#55556=ORIENTED_EDGE ( 'NONE', *, *, #50537, .F. ) ;
#55564=CARTESIAN_POINT ( 'NONE',  ( -99.44499999999999318, 0.000000000000000000, 8.024999999999991473 ) ) ;
#55566=CARTESIAN_POINT ( 'NONE',  ( -73.64499999999998181, 4.716976649647091513, -6.492361379858946790 ) ) ;
#55574=VERTEX_POINT ( 'NONE', #56914 ) ;
#55575=CARTESIAN_POINT ( 'NONE',  ( -127.0429263765337993, -9.058813317711329915, -2.943386871421370898 ) ) ;
#55577=CARTESIAN_POINT ( 'NONE',  ( -140.5450000000000159, -7.632228543268600340, -2.479861379858950166 ) ) ;
#55581=ORIENTED_EDGE ( 'NONE', *, *, #6677, .F. ) ;
#55588=CARTESIAN_POINT ( 'NONE',  ( -166.9429263765337907, 0.000000000000000000, 9.524999999999991473 ) ) ;
#55592=CARTESIAN_POINT ( 'NONE',  ( -138.6550000000000011, -7.632228543268600340, -2.479861379858950166 ) ) ;
#55607=ORIENTED_EDGE ( 'NONE', *, *, #34052, .T. ) ;
#55611=CARTESIAN_POINT ( 'NONE',  ( -55.70499999999997698, 2.607480562269072433, 8.024999999999991473 ) ) ;
#55615=DIRECTION ( 'NONE',  ( -1.000000000000000000, -0.000000000000000000, -0.000000000000000000 ) ) ;
#55628=CARTESIAN_POINT ( 'NONE',  ( -166.5550000000000068, 0.000000000000000000, 8.024999999999991473 ) ) ;
#55640=CARTESIAN_POINT ( 'NONE',  ( -73.10499999999996135, -6.826472737025115478, 4.959722759717900331 ) ) ;
#55652=CARTESIAN_POINT ( 'NONE',  ( -106.3449999999999989, 7.632228543268599452, -2.479861379858951942 ) ) ;
#55656=CARTESIAN_POINT ( 'NONE',  ( -97.25707362346618368, 5.598654528085800663, -7.705886871421367523 ) ) ;
#55658=CARTESIAN_POINT ( 'NONE',  ( -157.7929263765337566, -3.094860106618429807, 9.524999999999991473 ) ) ;
#55660=CARTESIAN_POINT ( 'NONE',  ( -167.6949999999999363, -8.437984349512085203, 5.166775262442717831E-16 ) ) ;
#55661=CARTESIAN_POINT ( 'NONE',  ( -156.0570736234661808, 0.000000000000000000, 9.524999999999991473 ) ) ;
#55667=CARTESIAN_POINT ( 'NONE',  ( -68.09292637653379643, 3.094860106618433360, 9.524999999999991473 ) ) ;
#55676=CARTESIAN_POINT ( 'NONE',  ( -170.3049999999999784, 8.437984349512086979, -1.550032578732815448E-15 ) ) ;
#55680=EDGE_CURVE ( 'NONE', #31059, #26061, #1351, .T. ) ;
#55689=ADVANCED_FACE ( 'NONE', ( #53701 ), #5488, .T. ) ;
#55690=CARTESIAN_POINT ( 'NONE',  ( -84.50499999999998124, -6.826472737025113702, -4.959722759717900331 ) ) ;
#55693=CARTESIAN_POINT ( 'NONE',  ( -114.4429263765338050, -1.166476076187852838E-15, -9.524999999999991473 ) ) ;
#55696=CARTESIAN_POINT ( 'NONE',  ( -73.10707362346616378, 8.102448949553172852, -5.886773742842744461 ) ) ;
#55701=VECTOR ( 'NONE', #53105, 1000.000000000000000 ) ;
#55704=CARTESIAN_POINT ( 'NONE',  ( -53.69499999999999318, -8.437984349512085203, 5.166775262442717831E-16 ) ) ;
#55711=CARTESIAN_POINT ( 'NONE',  ( -52.64499999999999602, 4.716976649647091513, -6.492361379858946790 ) ) ;
#55716=CARTESIAN_POINT ( 'NONE',  ( -106.5549999999999784, 0.000000000000000000, 8.024999999999991473 ) ) ;
#55721=CARTESIAN_POINT ( 'NONE',  ( -149.6070736234661638, -8.102448949553172852, 5.886773742842742685 ) ) ;
#55722=CARTESIAN_POINT ( 'NONE',  ( -59.75707362346617657, -5.598654528085801552, 7.705886871421367523 ) ) ;
#55725=CARTESIAN_POINT ( 'NONE',  ( -82.40707362346617515, 3.094860106618428031, -9.524999999999993250 ) ) ;
#55731=CARTESIAN_POINT ( 'NONE',  ( -15.00000000000000000, -12.00000000000000000, -5.000000000000000000 ) ) ;
#55733=CARTESIAN_POINT ( 'NONE',  ( -132.6550000000000011, -7.632228543268600340, -2.479861379858950166 ) ) ;
#55737=CARTESIAN_POINT ( 'NONE',  ( -137.9950000000000045, -6.826472737025115478, 4.959722759717900331 ) ) ;
#55738=CARTESIAN_POINT ( 'NONE',  ( -125.3949999999999818, -6.826472737025113702, -4.959722759717900331 ) ) ;
#55744=CARTESIAN_POINT ( 'NONE',  ( -120.7429263765338021, -5.598654528085803328, -7.705886871421366635 ) ) ;
#55745=CARTESIAN_POINT ( 'NONE',  ( -179.8429263765338249, 9.058813317711329915, -2.943386871421373119 ) ) ;
#55747=CARTESIAN_POINT ( 'NONE',  ( -51.59499999999997755, 2.607480562269073321, 8.024999999999991473 ) ) ;
#55757=CARTESIAN_POINT ( 'NONE',  ( -92.54292637653379927, 9.058813317711329915, 2.943386871421369566 ) ) ;
#55768=CARTESIAN_POINT ( 'NONE',  ( -63.89292637653380780, -8.102448949553174629, -5.886773742842741797 ) ) ;
#55780=CARTESIAN_POINT ( 'NONE',  ( -85.79499999999997328, 2.607480562269068880, -8.024999999999993250 ) ) ;
#55789=CARTESIAN_POINT ( 'NONE',  ( -138.2929263765344103, 3.094860106608815276, -9.525000000006976109 ) ) ;
#55794=CARTESIAN_POINT ( 'NONE',  ( -181.5570736234661808, -1.166476076187852838E-15, -9.524999999999991473 ) ) ;
#55795=DIRECTION ( 'NONE',  ( -1.000000000000000000, -0.000000000000000000, -0.000000000000000000 ) ) ;
#55797=CARTESIAN_POINT ( 'NONE',  ( -116.6070736234661638, -8.102448949553172852, 5.886773742842742685 ) ) ;
#55800=CARTESIAN_POINT ( 'NONE',  ( -85.10707362346616378, 8.102448949553172852, -5.886773742842744461 ) ) ;
#55808=CARTESIAN_POINT ( 'NONE',  ( -163.7049999999999841, 2.607480562269073321, 8.024999999999991473 ) ) ;
#55810=CARTESIAN_POINT ( 'NONE',  ( -183.5631645208122791, -4.726186399133334604, -7.620781825058602799 ) ) ;
#55811=CARTESIAN_POINT ( 'NONE',  ( -168.2950000000000159, -2.607480562269069768, 8.024999999999991473 ) ) ;
#55812=CARTESIAN_POINT ( 'NONE',  ( -154.1949999999999648, 8.437984349512086979, -1.550032578732815448E-15 ) ) ;
#55817=CARTESIAN_POINT ( 'NONE',  ( -75.65499999999998693, -7.632228543268600340, -2.479861379858950166 ) ) ;
#55819=CARTESIAN_POINT ( 'NONE',  ( -167.9929263765338305, 8.102448949553172852, -5.886773742842744461 ) ) ;
#55821=CARTESIAN_POINT ( 'NONE',  ( -70.79499999999998749, 2.607480562269069324, -8.024999999999993250 ) ) ;
#55830=ADVANCED_FACE ( 'NONE', ( #59671 ), #39739, .T. ) ;
#55833=FACE_OUTER_BOUND ( 'NONE', #8129, .T. ) ;
#55840=CARTESIAN_POINT ( 'NONE',  ( -156.2929263765341545, 3.094860106612411954, -9.525000000004366640 ) ) ;
#55857=CARTESIAN_POINT ( 'NONE',  ( -121.3449999999999989, 7.632228543268599452, -2.479861379858951942 ) ) ;
#55862=CARTESIAN_POINT ( 'NONE',  ( -10.16352198286304009, -11.93264351171969118, -1.310612615857368546 ) ) ;
#55877=CARTESIAN_POINT ( 'NONE',  ( -136.8550000000000182, 4.716976649647094177, 6.492361379858945902 ) ) ;
#55899=CARTESIAN_POINT ( 'NONE',  ( -177.6570736234662036, 9.058813317711329915, 2.943386871421369566 ) ) ;
#55900=VERTEX_POINT ( 'NONE', #46321 ) ;
#55905=CARTESIAN_POINT ( 'NONE',  ( -98.90500000000000114, 2.607480562269068880, -8.024999999999993250 ) ) ;
#55909=CARTESIAN_POINT ( 'NONE',  ( -96.74499999999999034, 4.716976649647094177, 6.492361379858945902 ) ) ;
#55910=ADVANCED_FACE ( 'NONE', ( #45633 ), #67050, .T. ) ;
#55912=CARTESIAN_POINT ( 'NONE',  ( -82.19499999999999318, 8.437984349512085203, -1.550032578732815448E-15 ) ) ;
#55919=CARTESIAN_POINT ( 'NONE',  ( -113.6929263765337907, 10.01517768586948698, -1.839758294383808571E-15 ) ) ;
#55920=CARTESIAN_POINT ( 'NONE',  ( -134.3949999999999250, -6.826472737025115478, -4.959722759717899443 ) ) ;
#55924=CARTESIAN_POINT ( 'NONE',  ( -173.3929263765337510, 8.102448949553176405, 5.886773742842740909 ) ) ;
#55926=VERTEX_POINT ( 'NONE', #25168 ) ;
#55927=DIRECTION ( 'NONE',  ( -1.000000000000000000, -0.000000000000000000, -0.000000000000000000 ) ) ;
#55930=CARTESIAN_POINT ( 'NONE',  ( -98.60707362346616378, -8.102448949553174629, 5.886773742842742685 ) ) ;
#55933=CARTESIAN_POINT ( 'NONE',  ( -127.4070736234668715, 3.094860106606866168, -9.525000000008395418 ) ) ;
#55935=CARTESIAN_POINT ( 'NONE',  ( -129.5049999999999955, -6.826472737025113702, -4.959722759717900331 ) ) ;
#55948=DIRECTION ( 'NONE',  ( -1.000000000000000000, -0.000000000000000000, -0.000000000000000000 ) ) ;
#55959=LINE ( 'NONE', #13747, #25793 ) ;
#55962=CARTESIAN_POINT ( 'NONE',  ( -161.7549999999999955, 4.716976649647091513, -6.492361379858946790 ) ) ;
#55971=ORIENTED_EDGE ( 'NONE', *, *, #33436, .T. ) ;
#55973=CYLINDRICAL_SURFACE ( 'NONE', #49312, 9.524999999999991473 ) ;
#55974=CARTESIAN_POINT ( 'NONE',  ( -80.15499999999998693, 7.632228543268600340, 2.479861379858949277 ) ) ;
#55975=EDGE_LOOP ( 'NONE', ( #10852, #36081, #40995, #28744 ) ) ;
#55977=CARTESIAN_POINT ( 'NONE',  ( -64.25707362346616947, 5.598654528085800663, -7.705886871421367523 ) ) ;
#55982=EDGE_LOOP ( 'NONE', ( #36871, #40535, #19059, #15841 ) ) ;
#55990=CARTESIAN_POINT ( 'NONE',  ( -111.1449999999999960, -4.716976649647092401, 6.492361379858946790 ) ) ;
#55993=CARTESIAN_POINT ( 'NONE',  ( -19.86963632605004548, 11.94623282526795371, 1.146258047298002181 ) ) ;
#55994=CARTESIAN_POINT ( 'NONE',  ( -140.9929263765338305, 8.102448949553171076, -5.886773742842744461 ) ) ;
#55995=CARTESIAN_POINT ( 'NONE',  ( -162.5949999999999704, 2.607480562269073321, 8.024999999999991473 ) ) ;
#56010=CARTESIAN_POINT ( 'NONE',  ( -161.3050000000000068, 8.437984349512086979, -1.550032578732815448E-15 ) ) ;
#56014=FACE_OUTER_BOUND ( 'NONE', #15147, .T. ) ;
#56020=CARTESIAN_POINT ( 'NONE',  ( -82.10499999999996135, -6.826472737025113702, 4.959722759717902107 ) ) ;
#56028=ORIENTED_EDGE ( 'NONE', *, *, #19924, .T. ) ;
#56031=CARTESIAN_POINT ( 'NONE',  ( -52.64499999999999602, 4.716976649647091513, -6.492361379858946790 ) ) ;
#56040=CARTESIAN_POINT ( 'NONE',  ( -53.54499999999998039, -7.632228543268600340, -2.479861379858950166 ) ) ;
#56045=CARTESIAN_POINT ( 'NONE',  ( -109.4049999999999727, -2.607480562269069768, 8.024999999999991473 ) ) ;
#56051=CARTESIAN_POINT ( 'NONE',  ( -138.3570736234661638, 5.598654528085804216, 7.705886871421366635 ) ) ;
#56054=CARTESIAN_POINT ( 'NONE',  ( -80.30707362346616662, -10.01517768586948698, 6.132527647946031529E-16 ) ) ;
#56056=CARTESIAN_POINT ( 'NONE',  ( -95.39292637653380780, 8.102448949553176405, 5.886773742842740909 ) ) ;
#56059=EDGE_CURVE ( 'NONE', #10174, #42918, #22997, .T. ) ;
#56063=CARTESIAN_POINT ( 'NONE',  ( -120.5049999999999812, -6.826472737025115478, -4.959722759717899443 ) ) ;
#56065=DIRECTION ( 'NONE',  ( 0.000000000000000000, 0.000000000000000000, 1.000000000000000000 ) ) ;
#56066=CARTESIAN_POINT ( 'NONE',  ( -159.4429263765338192, -1.166476076187852838E-15, -9.524999999999991473 ) ) ;
#56068=CARTESIAN_POINT ( 'NONE',  ( -140.0949999999999989, -2.607480562269071545, -8.024999999999991473 ) ) ;
#56072=CARTESIAN_POINT ( 'NONE',  ( -119.6949999999999932, -8.437984349512086979, 5.166775262442717831E-16 ) ) ;
#56082=CARTESIAN_POINT ( 'NONE',  ( -172.6429263765338078, -5.598654528085801552, 7.705886871421367523 ) ) ;
#56089=CARTESIAN_POINT ( 'NONE',  ( -94.64292637653380780, -5.598654528085801552, 7.705886871421367523 ) ) ;
#56093=CARTESIAN_POINT ( 'NONE',  ( -179.2429263765338021, 5.598654528085804216, 7.705886871421366635 ) ) ;
#56095=CARTESIAN_POINT ( 'NONE',  ( -79.55707362346616662, -1.166476076187852838E-15, -9.524999999999991473 ) ) ;
#56112=CARTESIAN_POINT ( 'NONE',  ( -79.04499999999998749, 7.632228543268600340, 2.479861379858949277 ) ) ;
#56124=ORIENTED_EDGE ( 'NONE', *, *, #19140, .T. ) ;
#56125=CARTESIAN_POINT ( 'NONE',  ( -138.1429263765338078, 5.598654528085800663, -7.705886871421367523 ) ) ;
#56128=CARTESIAN_POINT ( 'NONE',  ( -178.2570736234661695, 5.598654528085800663, -7.705886871421367523 ) ) ;
#56132=CARTESIAN_POINT ( 'NONE',  ( -112.8570736234661638, -5.598654528085803328, -7.705886871421366635 ) ) ;
#56133=CARTESIAN_POINT ( 'NONE',  ( -183.1444352087858363, 4.866151391066206422, -8.027994637291957503 ) ) ;
#56141=CARTESIAN_POINT ( 'NONE',  ( -146.3049999999999784, 8.437984349512085203, -1.550032578732815448E-15 ) ) ;
#56143=CARTESIAN_POINT ( 'NONE',  ( -164.9949999999999761, -6.826472737025115478, 4.959722759717900331 ) ) ;
#56145=CARTESIAN_POINT ( 'NONE',  ( -158.5449999999999875, -7.632228543268600340, -2.479861379858950166 ) ) ;
#56148=( BOUNDED_CURVE ( )  B_SPLINE_CURVE ( 2, ( #28605, #60610, #447, #60964, #44843, #39211, #27563, #39561, #64863, #50102, #21978 ),
 .UNSPECIFIED., .F., .F. ) 
 B_SPLINE_CURVE_WITH_KNOTS ( ( 3, 2, 2, 2, 2, 3 ),
 ( 0.3152173913043405107, 0.3173913043478187035, 0.3195652173912968963, 0.3217391304347750891, 0.3239130434782533374, 0.3260869565217315302 ),
 .UNSPECIFIED. ) 
 CURVE ( )  GEOMETRIC_REPRESENTATION_ITEM ( )  RATIONAL_B_SPLINE_CURVE ( ( 1.000000000000164979, 0.9510565162949885520, 1.000000000000000000, 0.9510565162951535312, 1.000000000000000000, 0.9510565162951535312, 1.000000000000000000, 0.9510565162951535312, 1.000000000000000000, 0.9510565162953247276, 0.9999999999998288036 ) ) 
 REPRESENTATION_ITEM ( '' )  );
#56154=CARTESIAN_POINT ( 'NONE',  ( -74.15499999999998693, 7.632228543268600340, 2.479861379858949277 ) ) ;
#56156=CARTESIAN_POINT ( 'NONE',  ( -67.64499999999998181, 4.716976649647091513, -6.492361379858946790 ) ) ;
#56161=CARTESIAN_POINT ( 'NONE',  ( -160.4070736234664594, 3.094860106613722905, -9.525000000003412737 ) ) ;
#56168=VERTEX_POINT ( 'NONE', #57016 ) ;
#56171=CARTESIAN_POINT ( 'NONE',  ( -61.25707362346617657, 5.598654528085800663, -7.705886871421367523 ) ) ;
#56172=CARTESIAN_POINT ( 'NONE',  ( -155.6929263765338192, 10.01517768586948698, -1.839758294383808966E-15 ) ) ;
#56188=CARTESIAN_POINT ( 'NONE',  ( -107.2449999999999903, -4.716976649647093289, -6.492361379858945902 ) ) ;
#56192=CARTESIAN_POINT ( 'NONE',  ( -11.69070681507827736, -11.39755657220772633, 3.762028377819578218 ) ) ;
#56209=CARTESIAN_POINT ( 'NONE',  ( -137.3049999999999784, 8.437984349512085203, -1.550032578732815448E-15 ) ) ;
#56210=DIRECTION ( 'NONE',  ( -1.000000000000000000, -0.000000000000000000, -0.000000000000000000 ) ) ;
#56223=CARTESIAN_POINT ( 'NONE',  ( -93.05707362346616662, 0.000000000000000000, 9.524999999999991473 ) ) ;
#56230=CARTESIAN_POINT ( 'NONE',  ( -57.50707362346615525, 8.102448949553176405, 5.886773742842740909 ) ) ;
#56232=DIRECTION ( 'NONE',  ( 0.000000000000000000, 0.000000000000000000, 1.000000000000000000 ) ) ;
#56235=EDGE_LOOP ( 'NONE', ( #37510, #43864, #24863, #23272 ) ) ;
#56239=CARTESIAN_POINT ( 'NONE',  ( -97.40499999999997272, -2.607480562269069768, 8.024999999999991473 ) ) ;
#56243=CARTESIAN_POINT ( 'NONE',  ( -96.14499999999999602, -4.716976649647092401, 6.492361379858946790 ) ) ;
#56245=CARTESIAN_POINT ( 'NONE',  ( -78.14499999999999602, -4.716976649647092401, 6.492361379858946790 ) ) ;
#56247=CARTESIAN_POINT ( 'NONE',  ( -56.75707362346615525, -5.598654528085801552, 7.705886871421367523 ) ) ;
#56255=CARTESIAN_POINT ( 'NONE',  ( -117.2929263765337993, 3.094860106618428031, -9.524999999999993250 ) ) ;
#56257=CARTESIAN_POINT ( 'NONE',  ( -134.6950000000000216, -8.437984349512085203, 5.166775262442717831E-16 ) ) ;
#56266=CARTESIAN_POINT ( 'NONE',  ( -62.24292637653379501, 5.598654528085804216, 7.705886871421366635 ) ) ;
#56274=CARTESIAN_POINT ( 'NONE',  ( -129.3549999999999898, -4.716976649647093289, -6.492361379858945902 ) ) ;
#56276=CARTESIAN_POINT ( 'NONE',  ( -122.1570736234661751, -9.058813317711329915, -2.943386871421370898 ) ) ;
#56303=CARTESIAN_POINT ( 'NONE',  ( -165.3549999999999898, -4.716976649647093289, -6.492361379858945902 ) ) ;
#56316=CARTESIAN_POINT ( 'NONE',  ( -77.30499999999996419, 8.437984349512085203, -1.550032578732815448E-15 ) ) ;
#56329=CARTESIAN_POINT ( 'NONE',  ( -103.7949999999999733, 2.607480562269068880, -8.024999999999993250 ) ) ;
#56338=CARTESIAN_POINT ( 'NONE',  ( -141.5929263765337680, -3.094860106618431139, -9.524999999999991473 ) ) ;
#56340=CARTESIAN_POINT ( 'NONE',  ( -169.3449999999999989, 7.632228543268599452, -2.479861379858951942 ) ) ;
#56355=CARTESIAN_POINT ( 'NONE',  ( -157.5550000000000068, 0.000000000000000000, 8.024999999999991473 ) ) ;
#56357=CARTESIAN_POINT ( 'NONE',  ( -195.0000000000000000, 1.166476076187852838E-15, -9.524999999999991473 ) ) ;
#56359=EDGE_CURVE ( 'NONE', #28296, #30333, #51340, .T. ) ;
#56371=CARTESIAN_POINT ( 'NONE',  ( -72.35499999999998977, -4.716976649647093289, -6.492361379858945902 ) ) ;
#56379=AXIS2_PLACEMENT_3D ( 'NONE', #53801, #27049, #6309 ) ;
#56384=CARTESIAN_POINT ( 'NONE',  ( -54.74499999999999034, 4.716976649647094177, 6.492361379858945902 ) ) ;
#56392=CARTESIAN_POINT ( 'NONE',  ( -49.94499999999998607, -9.827790563157499189E-16, -8.024999999999991473 ) ) ;
#56398=CARTESIAN_POINT ( 'NONE',  ( -107.3049999999999784, 8.437984349512085203, -1.550032578732815448E-15 ) ) ;
#56402=CARTESIAN_POINT ( 'NONE',  ( -140.3070736234661524, -10.01517768586948698, 6.132527647946031529E-16 ) ) ;
#56406=CARTESIAN_POINT ( 'NONE',  ( -86.90707362346616094, -3.094860106618429807, 9.524999999999991473 ) ) ;
#56415=CARTESIAN_POINT ( 'NONE',  ( -126.0550000000000068, -9.827790563157499189E-16, -8.024999999999991473 ) ) ;
#56419=CARTESIAN_POINT ( 'NONE',  ( -131.0949999999999989, -2.607480562269071545, -8.024999999999991473 ) ) ;
#56420=CARTESIAN_POINT ( 'NONE',  ( -115.6449999999999818, 4.716976649647091513, -6.492361379858946790 ) ) ;
#56428=CARTESIAN_POINT ( 'NONE',  ( -168.4429263765337907, -1.166476076187852838E-15, -9.524999999999991473 ) ) ;
#56430=CARTESIAN_POINT ( 'NONE',  ( -51.29499999999997328, -2.607480562269069768, 8.024999999999991473 ) ) ;
#56438=CARTESIAN_POINT ( 'NONE',  ( -85.19292637653381917, -10.01517768586948698, 6.132527647946031529E-16 ) ) ;
#56443=CARTESIAN_POINT ( 'NONE',  ( -79.40707362346617515, 3.094860106618428031, -9.524999999999993250 ) ) ;
#56465=CARTESIAN_POINT ( 'NONE',  ( -71.75707362346616947, -5.598654528085801552, 7.705886871421367523 ) ) ;
#56466=CARTESIAN_POINT ( 'NONE',  ( -78.29499999999997328, -2.607480562269069768, 8.024999999999991473 ) ) ;
#56475=CARTESIAN_POINT ( 'NONE',  ( -75.59292637653379643, -3.094860106618431139, -9.524999999999991473 ) ) ;
#56485=CARTESIAN_POINT ( 'NONE',  ( -164.9070736234662036, -3.094860106618429807, 9.524999999999991473 ) ) ;
#56488=CARTESIAN_POINT ( 'NONE',  ( -117.6570736234661894, 9.058813317711329915, 2.943386871421369566 ) ) ;
#56490=CARTESIAN_POINT ( 'NONE',  ( -69.05707362346618083, 0.000000000000000000, 9.524999999999991473 ) ) ;
#56496=CARTESIAN_POINT ( 'NONE',  ( -152.6050000000000182, 6.826472737025113702, -4.959722759717902107 ) ) ;
#56498=CARTESIAN_POINT ( 'NONE',  ( -147.4429263765338192, -1.166476076187852838E-15, -9.524999999999991473 ) ) ;
#56499=CARTESIAN_POINT ( 'NONE',  ( -165.4450000000000216, 0.000000000000000000, 8.024999999999991473 ) ) ;
#56501=CARTESIAN_POINT ( 'NONE',  ( -146.8449999999999989, -7.632228543268599452, 2.479861379858951054 ) ) ;
#56504=CARTESIAN_POINT ( 'NONE',  ( -123.4429263765338192, -1.166476076187852838E-15, -9.524999999999991473 ) ) ;
#56505=CARTESIAN_POINT ( 'NONE',  ( -61.10499999999997556, -6.826472737025115478, 4.959722759717900331 ) ) ;
#56508=CARTESIAN_POINT ( 'NONE',  ( -59.39499999999998892, -6.826472737025113702, -4.959722759717900331 ) ) ;
#56521=EDGE_CURVE ( 'NONE', #65809, #58402, #37429, .T. ) ;
#56524=ORIENTED_EDGE ( 'NONE', *, *, #57023, .T. ) ;
#56537=CARTESIAN_POINT ( 'NONE',  ( -145.6429263765338078, -5.598654528085801552, 7.705886871421367523 ) ) ;
#56538=VERTEX_POINT ( 'NONE', #25739 ) ;
#56540=VECTOR ( 'NONE', #28704, 1000.000000000000000 ) ;
#56543=CARTESIAN_POINT ( 'NONE',  ( -111.1449999999999960, -4.716976649647092401, 6.492361379858946790 ) ) ;
#56544=ORIENTED_EDGE ( 'NONE', *, *, #11771, .F. ) ;
#56547=CARTESIAN_POINT ( 'NONE',  ( -14.33487782743413064, -10.92424365012867504, -4.966485406155142890 ) ) ;
#56554=DIRECTION ( 'NONE',  ( -1.000000000000000000, -0.000000000000000000, -0.000000000000000000 ) ) ;
#56558=ORIENTED_EDGE ( 'NONE', *, *, #17028, .F. ) ;
#56564=CARTESIAN_POINT ( 'NONE',  ( -158.0070736234661695, -8.102448949553174629, -5.886773742842741797 ) ) ;
#56565=CARTESIAN_POINT ( 'NONE',  ( -135.5049999999999670, -6.826472737025115478, -4.959722759717899443 ) ) ;
#56584=VERTEX_POINT ( 'NONE', #62672 ) ;
#56586=CARTESIAN_POINT ( 'NONE',  ( -180.0550000000000068, -9.827790563157499189E-16, -8.024999999999991473 ) ) ;
#56589=CARTESIAN_POINT ( 'NONE',  ( -51.65707362346616804, 9.058813317711329915, 2.943386871421369566 ) ) ;
#56591=CARTESIAN_POINT ( 'NONE',  ( -174.2949999999999875, -2.607480562269069768, 8.024999999999991473 ) ) ;
#56596=CARTESIAN_POINT ( 'NONE',  ( -160.5570736234661808, -1.166476076187852838E-15, -9.524999999999991473 ) ) ;
#56599=CARTESIAN_POINT ( 'NONE',  ( -96.50499999999998124, -6.826472737025115478, -4.959722759717899443 ) ) ;
#56604=CARTESIAN_POINT ( 'NONE',  ( -101.5449999999999875, -7.632228543268600340, -2.479861379858950166 ) ) ;
#56606=CARTESIAN_POINT ( 'NONE',  ( -63.89499999999998181, 6.826472737025116366, 4.959722759717898555 ) ) ;
#56615=CARTESIAN_POINT ( 'NONE',  ( -112.9429263765338050, 0.000000000000000000, 9.524999999999991473 ) ) ;
#56616=CARTESIAN_POINT ( 'NONE',  ( -126.7449999999999903, 4.716976649647094177, 6.492361379858945902 ) ) ;
#56629=EDGE_CURVE ( 'NONE', #50943, #19358, #6162, .T. ) ;
#56634=CARTESIAN_POINT ( 'NONE',  ( -126.9570736234661723, 9.058813317711329915, -2.943386871421373119 ) ) ;
#56636=CARTESIAN_POINT ( 'NONE',  ( -131.6049999999999898, 6.826472737025113702, -4.959722759717902107 ) ) ;
#56640=CARTESIAN_POINT ( 'NONE',  ( -120.6570736234661751, 9.058813317711329915, 2.943386871421369566 ) ) ;
#56669=CARTESIAN_POINT ( 'NONE',  ( -165.6550000000000011, -7.632228543268600340, -2.479861379858950166 ) ) ;
#56670=VERTEX_POINT ( 'NONE', #37403 ) ;
#56673=DIRECTION ( 'NONE',  ( 0.000000000000000000, 0.000000000000000000, -1.000000000000000000 ) ) ;
#56681=CARTESIAN_POINT ( 'NONE',  ( -71.90499999999995850, 2.607480562269068880, -8.024999999999993250 ) ) ;
#56685=CARTESIAN_POINT ( 'NONE',  ( -63.50707362346615525, 8.102448949553176405, 5.886773742842740909 ) ) ;
#56687=( BOUNDED_CURVE ( )  B_SPLINE_CURVE ( 2, ( #38587, #811, #1876, #22355, #6862, #17112, #59981, #38923, #33263, #6496, #60325 ),
 .UNSPECIFIED., .F., .F. ) 
 B_SPLINE_CURVE_WITH_KNOTS ( ( 3, 2, 2, 2, 2, 3 ),
 ( 0.7717391304347825942, 0.7739130434782608425, 0.7760869565217390909, 0.7782608695652173392, 0.7804347826086956985, 0.7826086956521739468 ),
 .UNSPECIFIED. ) 
 CURVE ( )  GEOMETRIC_REPRESENTATION_ITEM ( )  RATIONAL_B_SPLINE_CURVE ( ( 1.000000000000000000, 0.9510565162951535312, 1.000000000000000000, 0.9510565162951535312, 1.000000000000000000, 0.9510565162951535312, 1.000000000000000000, 0.9510565162951535312, 1.000000000000000000, 0.9510565162951535312, 1.000000000000000000 ) ) 
 REPRESENTATION_ITEM ( '' )  );
#56698=CARTESIAN_POINT ( 'NONE',  ( -95.54499999999998749, -7.632228543268600340, -2.479861379858950166 ) ) ;
#56705=CARTESIAN_POINT ( 'NONE',  ( -144.4429263765337907, -1.166476076187852838E-15, -9.524999999999991473 ) ) ;
#56707=CARTESIAN_POINT ( 'NONE',  ( -163.1949999999999648, 8.437984349512085203, -1.550032578732815448E-15 ) ) ;
#56727=CARTESIAN_POINT ( 'NONE',  ( -157.2549999999999955, -4.716976649647092401, 6.492361379858946790 ) ) ;
#56731=ORIENTED_EDGE ( 'NONE', *, *, #28963, .T. ) ;
#56741=CARTESIAN_POINT ( 'NONE',  ( -76.10499999999997556, -6.826472737025113702, 4.959722759717902107 ) ) ;
#56744=CARTESIAN_POINT ( 'NONE',  ( -80.00707362346618368, -8.102448949553174629, -5.886773742842741797 ) ) ;
#56745=ORIENTED_EDGE ( 'NONE', *, *, #34309, .F. ) ;
#56754=CARTESIAN_POINT ( 'NONE',  ( -48.44499999999998607, 0.000000000000000000, 8.024999999999991473 ) ) ;
#56762=CARTESIAN_POINT ( 'NONE',  ( -57.29499999999998039, -2.607480562269069768, 8.024999999999991473 ) ) ;
#56765=CARTESIAN_POINT ( 'NONE',  ( -101.0049999999999812, 6.826472737025116366, 4.959722759717898555 ) ) ;
#56766=ORIENTED_EDGE ( 'NONE', *, *, #28165, .T. ) ;
#56769=CARTESIAN_POINT ( 'NONE',  ( -136.2570736234661695, 5.598654528085800663, -7.705886871421367523 ) ) ;
#56773=CARTESIAN_POINT ( 'NONE',  ( -78.95707362346617231, 9.058813317711329915, -2.943386871421373119 ) ) ;
#56775=CARTESIAN_POINT ( 'NONE',  ( -18.75822517221693175, -11.53590615615684634, 3.313539367360412324 ) ) ;
#56779=CARTESIAN_POINT ( 'NONE',  ( -117.6550000000000011, -7.632228543268600340, -2.479861379858950166 ) ) ;
#56782=CARTESIAN_POINT ( 'NONE',  ( -134.9950000000000045, -6.826472737025115478, 4.959722759717900331 ) ) ;
#56784=CARTESIAN_POINT ( 'NONE',  ( -120.5949999999999704, 2.607480562269072433, 8.024999999999991473 ) ) ;
#56788=LINE ( 'NONE', #24075, #39284 ) ;
#56791=CARTESIAN_POINT ( 'NONE',  ( -121.4929263765337879, -8.102448949553174629, 5.886773742842742685 ) ) ;
#56792=CARTESIAN_POINT ( 'NONE',  ( -176.2429263765338021, 5.598654528085804216, 7.705886871421366635 ) ) ;
#56793=CARTESIAN_POINT ( 'NONE',  ( -50.69499999999998607, -8.437984349512085203, 5.166775262442717831E-16 ) ) ;
#56800=CARTESIAN_POINT ( 'NONE',  ( -83.99292637653380211, 8.102448949553171076, -5.886773742842744461 ) ) ;
#56816=FACE_OUTER_BOUND ( 'NONE', #38393, .T. ) ;
#56822=CARTESIAN_POINT ( 'NONE',  ( -106.7049999999999983, 2.607480562269072433, 8.024999999999991473 ) ) ;
#56834=CARTESIAN_POINT ( 'NONE',  ( -77.54499999999998749, -7.632228543268600340, -2.479861379858950166 ) ) ;
#56843=ORIENTED_EDGE ( 'NONE', *, *, #54386, .T. ) ;
#56847=CARTESIAN_POINT ( 'NONE',  ( -173.0070736234661979, -8.102448949553172852, -5.886773742842741797 ) ) ;
#56850=CARTESIAN_POINT ( 'NONE',  ( -105.3570736234661780, 5.598654528085804216, 7.705886871421366635 ) ) ;
#56851=CARTESIAN_POINT ( 'NONE',  ( -82.94292637653380496, 0.000000000000000000, 9.524999999999991473 ) ) ;
#56859=CARTESIAN_POINT ( 'NONE',  ( -153.8049999999999784, -8.437984349512085203, 5.166775262442717831E-16 ) ) ;
#56860=CARTESIAN_POINT ( 'NONE',  ( -148.1929263765338192, -10.01517768586948698, 6.132527647946031529E-16 ) ) ;
#56861=EDGE_CURVE ( 'NONE', #13067, #36987, #12676, .T. ) ;
#56862=CARTESIAN_POINT ( 'NONE',  ( -163.1949999999999648, 8.437984349512085203, -1.550032578732815448E-15 ) ) ;
#56864=CARTESIAN_POINT ( 'NONE',  ( -146.6949999999999932, -8.437984349512086979, 5.166775262442717831E-16 ) ) ;
#56867=CYLINDRICAL_SURFACE ( 'NONE', #54753, 9.524999999999991473 ) ;
#56869=CARTESIAN_POINT ( 'NONE',  ( -62.00499999999999545, 6.826472737025116366, 4.959722759717898555 ) ) ;
#56873=EDGE_CURVE ( 'NONE', #64020, #55574, #6365, .T. ) ;
#56874=CARTESIAN_POINT ( 'NONE',  ( -58.64499999999998892, 4.716976649647091513, -6.492361379858946790 ) ) ;
#56877=CIRCLE ( 'NONE', #33275, 1.000000000000000888 ) ;
#56886=ORIENTED_EDGE ( 'NONE', *, *, #35192, .T. ) ;
#56893=ORIENTED_EDGE ( 'NONE', *, *, #63526, .T. ) ;
#56905=CARTESIAN_POINT ( 'NONE',  ( -108.4449999999999790, 0.000000000000000000, 8.024999999999991473 ) ) ;
#56906=VERTEX_POINT ( 'NONE', #3469 ) ;
#56914=CARTESIAN_POINT ( 'NONE',  ( -126.0570736234661808, 0.000000000000000000, 9.524999999999991473 ) ) ;
#56917=CYLINDRICAL_SURFACE ( 'NONE', #58246, 9.524999999999991473 ) ;
#56919=CARTESIAN_POINT ( 'NONE',  ( -158.6070736234661922, -8.102448949553174629, 5.886773742842742685 ) ) ;
#56920=CARTESIAN_POINT ( 'NONE',  ( -124.2549999999999955, -4.716976649647092401, 6.492361379858946790 ) ) ;
#56921=CARTESIAN_POINT ( 'NONE',  ( -183.9999999999998863, -2.671725603995652953, 7.577260112568927397 ) ) ;
#56936=CARTESIAN_POINT ( 'NONE',  ( -176.6049999999999898, 6.826472737025113702, -4.959722759717902107 ) ) ;
#56939=CARTESIAN_POINT ( 'NONE',  ( -55.25707362346615525, 5.598654528085800663, -7.705886871421367523 ) ) ;
#56940=CARTESIAN_POINT ( 'NONE',  ( -172.7950000000000159, 2.607480562269069324, -8.024999999999993250 ) ) ;
#56945=CARTESIAN_POINT ( 'NONE',  ( -92.15499999999998693, 7.632228543268600340, 2.479861379858949277 ) ) ;
#56949=CARTESIAN_POINT ( 'NONE',  ( -89.54499999999998749, -7.632228543268600340, -2.479861379858950166 ) ) ;
#56953=CARTESIAN_POINT ( 'NONE',  ( -66.29500000000000171, -2.607480562269069768, 8.024999999999991473 ) ) ;
#56963=CARTESIAN_POINT ( 'NONE',  ( -110.5429263765337993, 9.058813317711329915, 2.943386871421369566 ) ) ;
#56964=( BOUNDED_CURVE ( )  B_SPLINE_CURVE ( 2, ( #17464, #64221, #1180, #27611, #5455, #21663, #26906, #16763, #22714, #6179, #49129 ),
 .UNSPECIFIED., .F., .F. ) 
 B_SPLINE_CURVE_WITH_KNOTS ( ( 3, 2, 2, 2, 2, 3 ),
 ( 0.5978260869565077407, 0.5999999999999858780, 0.6021739130434641263, 0.6043478260869422636, 0.6065217391304206229, 0.6086956521738987602 ),
 .UNSPECIFIED. ) 
 CURVE ( )  GEOMETRIC_REPRESENTATION_ITEM ( )  RATIONAL_B_SPLINE_CURVE ( ( 1.000000000000314859, 0.9510565162948385609, 1.000000000000000000, 0.9510565162951535312, 1.000000000000000000, 0.9510565162951535312, 1.000000000000000000, 0.9510565162951535312, 1.000000000000000000, 0.9510565162954759399, 0.9999999999996775912 ) ) 
 REPRESENTATION_ITEM ( '' )  );
#56965=CARTESIAN_POINT ( 'NONE',  ( -125.9949999999999903, -6.826472737025115478, 4.959722759717900331 ) ) ;
#56971=CARTESIAN_POINT ( 'NONE',  ( -62.54292637653379927, 9.058813317711329915, 2.943386871421369566 ) ) ;
#56977=CARTESIAN_POINT ( 'NONE',  ( -128.4549999999999841, 7.632228543268599452, -2.479861379858951942 ) ) ;
#56980=CARTESIAN_POINT ( 'NONE',  ( -127.2570736234661695, 5.598654528085800663, -7.705886871421367523 ) ) ;
#56989=ORIENTED_EDGE ( 'NONE', *, *, #30460, .T. ) ;
#56992=CARTESIAN_POINT ( 'NONE',  ( -48.35499999999998266, -4.716976649647093289, -6.492361379858945902 ) ) ;
#57007=CARTESIAN_POINT ( 'NONE',  ( -156.0550000000000068, -9.827790563157499189E-16, -8.024999999999991473 ) ) ;
#57016=CARTESIAN_POINT ( 'NONE',  ( -130.5570736234661808, -1.166476076187852838E-15, -9.524999999999991473 ) ) ;
#57018=CARTESIAN_POINT ( 'NONE',  ( -46.64499999999998892, 4.716976649647091513, -6.492361379858946790 ) ) ;
#57020=CARTESIAN_POINT ( 'NONE',  ( -79.10499999999998977, -6.826472737025115478, 4.959722759717900331 ) ) ;
#57023=EDGE_CURVE ( 'NONE', #6192, #59896, #20028, .T. ) ;
#57024=CARTESIAN_POINT ( 'NONE',  ( -124.0429263765337993, -9.058813317711329915, -2.943386871421370898 ) ) ;
#57034=CARTESIAN_POINT ( 'NONE',  ( -100.0450000000000017, 7.632228543268600340, 2.479861379858949277 ) ) ;
#57042=CARTESIAN_POINT ( 'NONE',  ( -142.6429263765338078, -5.598654528085801552, 7.705886871421367523 ) ) ;
#57044=CARTESIAN_POINT ( 'NONE',  ( -152.6949999999999932, -8.437984349512085203, 5.166775262442717831E-16 ) ) ;
#57058=CARTESIAN_POINT ( 'NONE',  ( -164.1550000000000011, 7.632228543268600340, 2.479861379858949277 ) ) ;
#57070=CARTESIAN_POINT ( 'NONE',  ( -73.40500000000000114, -2.607480562269069768, 8.024999999999991473 ) ) ;
#57080=CARTESIAN_POINT ( 'NONE',  ( -57.14499999999997470, -4.716976649647092401, 6.492361379858946790 ) ) ;
#57083=( BOUNDED_CURVE ( )  B_SPLINE_CURVE ( 2, ( #36867, #4440, #58280, #48120, #31888, #9423, #37219, #41800, #4092, #63221, #10108 ),
 .UNSPECIFIED., .F., .F. ) 
 B_SPLINE_CURVE_WITH_KNOTS ( ( 3, 2, 2, 2, 2, 3 ),
 ( 0.7173913043478260532, 0.7195652173913043015, 0.7217391304347826608, 0.7239130434782609091, 0.7260869565217391575, 0.7282608695652174058 ),
 .UNSPECIFIED. ) 
 CURVE ( )  GEOMETRIC_REPRESENTATION_ITEM ( )  RATIONAL_B_SPLINE_CURVE ( ( 1.000000000000000000, 0.9510565162951535312, 1.000000000000000000, 0.9510565162951535312, 1.000000000000000000, 0.9510565162951535312, 1.000000000000000000, 0.9510565162951535312, 1.000000000000000000, 0.9510565162951535312, 1.000000000000000000 ) ) 
 REPRESENTATION_ITEM ( '' )  );
#57092=CARTESIAN_POINT ( 'NONE',  ( -109.1050000000000040, -6.826472737025115478, 4.959722759717900331 ) ) ;
#57097=CARTESIAN_POINT ( 'NONE',  ( -141.2070736234661581, 3.094860106618433360, 9.524999999999991473 ) ) ;
#57100=CARTESIAN_POINT ( 'NONE',  ( -77.45707362346617231, -9.058813317711329915, 2.943386871421371787 ) ) ;
#57103=ORIENTED_EDGE ( 'NONE', *, *, #33153, .F. ) ;
#57105=CARTESIAN_POINT ( 'NONE',  ( -19.99962819189825680, -11.99984508003516304, 0.3398326153005359340 ) ) ;
#57107=CARTESIAN_POINT ( 'NONE',  ( -125.7550000000000097, 4.716976649647091513, -6.492361379858946790 ) ) ;
#57108=CARTESIAN_POINT ( 'NONE',  ( -181.9429263765338192, 0.000000000000000000, 9.524999999999991473 ) ) ;
#57110=CARTESIAN_POINT ( 'NONE',  ( -121.4949999999999761, 6.826472737025113702, -4.959722759717902107 ) ) ;
#57112=CARTESIAN_POINT ( 'NONE',  ( -115.1949999999999932, 8.437984349512086979, -1.550032578732815448E-15 ) ) ;
#57119=CARTESIAN_POINT ( 'NONE',  ( -168.8929263765337794, -8.102448949553172852, -5.886773742842741797 ) ) ;
#57120=CARTESIAN_POINT ( 'NONE',  ( -181.6450000000000102, 4.716976649647091513, -6.492361379858946790 ) ) ;
#57125=VERTEX_POINT ( 'NONE', #12233 ) ;
#57126=CARTESIAN_POINT ( 'NONE',  ( -83.09292637653381064, 3.094860106618433360, 9.524999999999991473 ) ) ;
#57133=CARTESIAN_POINT ( 'NONE',  ( -195.0000000000000000, 1.166476076187852838E-15, -9.524999999999991473 ) ) ;
#57137=CARTESIAN_POINT ( 'NONE',  ( -103.7929263765348225, -3.094860106601490024, 9.525000000012299850 ) ) ;
#57143=CARTESIAN_POINT ( 'NONE',  ( -104.4549999999999983, 7.632228543268599452, -2.479861379858951942 ) ) ;
#57153=CARTESIAN_POINT ( 'NONE',  ( -84.59499999999998465, 2.607480562269073321, 8.024999999999991473 ) ) ;
#57172=CARTESIAN_POINT ( 'NONE',  ( -170.7570736234661695, -5.598654528085801552, 7.705886871421367523 ) ) ;
#57176=CARTESIAN_POINT ( 'NONE',  ( -104.9070736234661751, -3.094860106618429807, 9.524999999999991473 ) ) ;
#57188=CARTESIAN_POINT ( 'NONE',  ( -151.1049999999999613, -6.826472737025115478, 4.959722759717900331 ) ) ;
#57190=CARTESIAN_POINT ( 'NONE',  ( -152.2450000000000045, -4.716976649647093289, -6.492361379858945902 ) ) ;
#57192=CARTESIAN_POINT ( 'NONE',  ( -143.5449999999999875, -7.632228543268600340, -2.479861379858950166 ) ) ;
#57198=CARTESIAN_POINT ( 'NONE',  ( -60.65499999999998693, -7.632228543268600340, -2.479861379858950166 ) ) ;
#57200=CARTESIAN_POINT ( 'NONE',  ( -61.94499999999998607, -9.827790563157499189E-16, -8.024999999999991473 ) ) ;
#57212=CARTESIAN_POINT ( 'NONE',  ( -177.7429263765338021, -5.598654528085803328, -7.705886871421366635 ) ) ;
#57233=LINE ( 'NONE', #13626, #4020 ) ;
#57238=CARTESIAN_POINT ( 'NONE',  ( -108.7449999999999903, 4.716976649647094177, 6.492361379858945902 ) ) ;
#57245=VERTEX_POINT ( 'NONE', #44999 ) ;
#57256=CARTESIAN_POINT ( 'NONE',  ( -141.1429263765338078, 5.598654528085800663, -7.705886871421367523 ) ) ;
#57258=CARTESIAN_POINT ( 'NONE',  ( -123.5049999999999955, -6.826472737025115478, -4.959722759717899443 ) ) ;
#57275=CARTESIAN_POINT ( 'NONE',  ( -183.2050000000000125, -2.607480562269071545, -8.024999999999991473 ) ) ;
#57278=CARTESIAN_POINT ( 'NONE',  ( -53.30707362346616662, -10.01517768586948698, 6.132527647946031529E-16 ) ) ;
#57280=CARTESIAN_POINT ( 'NONE',  ( -179.6949999999999932, -8.437984349512086979, 5.166775262442717831E-16 ) ) ;
#57285=CARTESIAN_POINT ( 'NONE',  ( -88.85499999999998977, 4.716976649647094177, 6.492361379858945902 ) ) ;
#57290=CARTESIAN_POINT ( 'NONE',  ( -86.99499999999997613, -6.826472737025113702, 4.959722759717902107 ) ) ;
#57292=CARTESIAN_POINT ( 'NONE',  ( -70.49499999999996191, 6.826472737025113702, -4.959722759717902107 ) ) ;
#57301=CARTESIAN_POINT ( 'NONE',  ( -48.44292637653380496, -1.166476076187852838E-15, -9.524999999999991473 ) ) ;
#57303=CARTESIAN_POINT ( 'NONE',  ( -101.6929263765337907, 10.01517768586948698, -1.839758294383808571E-15 ) ) ;
#57304=CARTESIAN_POINT ( 'NONE',  ( -126.1450000000000102, -4.716976649647092401, 6.492361379858946790 ) ) ;
#57312=CARTESIAN_POINT ( 'NONE',  ( -62.69292637653379785, 10.01517768586948698, -1.839758294383808966E-15 ) ) ;
#57318=CARTESIAN_POINT ( 'NONE',  ( -131.7549999999999955, 4.716976649647091513, -6.492361379858946790 ) ) ;
#57321=CARTESIAN_POINT ( 'NONE',  ( -121.8570736234661780, -5.598654528085803328, -7.705886871421366635 ) ) ;
#57323=CARTESIAN_POINT ( 'NONE',  ( -171.5929263765339670, -3.094860106621170281, -9.524999999998001954 ) ) ;
#57350=CARTESIAN_POINT ( 'NONE',  ( -60.29292637653380638, 3.094860106618428031, -9.524999999999993250 ) ) ;
#57351=AXIS2_PLACEMENT_3D ( 'NONE', #49181, #33335, #6247 ) ;
#57354=CARTESIAN_POINT ( 'NONE',  ( -148.1049999999999898, -6.826472737025115478, 4.959722759717900331 ) ) ;
#57361=EDGE_CURVE ( 'NONE', #63234, #68810, #15413, .T. ) ;
#57368=CARTESIAN_POINT ( 'NONE',  ( -96.05707362346618083, 0.000000000000000000, 9.524999999999991473 ) ) ;
#57371=CARTESIAN_POINT ( 'NONE',  ( -66.95499999999998408, -7.632228543268599452, 2.479861379858951054 ) ) ;
#57386=CARTESIAN_POINT ( 'NONE',  ( -96.59499999999998465, 2.607480562269073321, 8.024999999999991473 ) ) ;
#57392=CARTESIAN_POINT ( 'NONE',  ( -72.29292637653379927, 3.094860106618428031, -9.524999999999993250 ) ) ;
#57393=ORIENTED_EDGE ( 'NONE', *, *, #57361, .T. ) ;
#57394=CARTESIAN_POINT ( 'NONE',  ( -146.3929263765337794, 8.102448949553176405, 5.886773742842740909 ) ) ;
#57396=CARTESIAN_POINT ( 'NONE',  ( -158.5449999999999875, -7.632228543268600340, -2.479861379858950166 ) ) ;
#57399=CARTESIAN_POINT ( 'NONE',  ( -195.0000000000000000, 0.000000000000000000, 0.000000000000000000 ) ) ;
#57400=CARTESIAN_POINT ( 'NONE',  ( -132.8929263765337794, -8.102448949553174629, -5.886773742842741797 ) ) ;
#57410=VERTEX_POINT ( 'NONE', #62160 ) ;
#57411=CARTESIAN_POINT ( 'NONE',  ( -155.9049999999999727, 2.607480562269069324, -8.024999999999993250 ) ) ;
#57425=CARTESIAN_POINT ( 'NONE',  ( -78.65499999999998693, -7.632228543268600340, -2.479861379858950166 ) ) ;
#57441=CARTESIAN_POINT ( 'NONE',  ( -181.7050000000000125, 2.607480562269073321, 8.024999999999991473 ) ) ;
#57445=CARTESIAN_POINT ( 'NONE',  ( -176.1570736234662036, -9.058813317711329915, -2.943386871421370898 ) ) ;
#57448=VERTEX_POINT ( 'NONE', #59215 ) ;
#57452=CARTESIAN_POINT ( 'NONE',  ( -98.90500000000000114, 2.607480562269068880, -8.024999999999993250 ) ) ;
#57454=AXIS2_PLACEMENT_3D ( 'NONE', #23104, #14525, #61059 ) ;
#57455=CARTESIAN_POINT ( 'NONE',  ( -136.4070736234661751, 3.094860106618428031, -9.524999999999993250 ) ) ;
#57458=CARTESIAN_POINT ( 'NONE',  ( -74.15707362346617515, -9.058813317711329915, -2.943386871421370898 ) ) ;
#57460=ORIENTED_EDGE ( 'NONE', *, *, #10027, .T. ) ;
#57462=CARTESIAN_POINT ( 'NONE',  ( -18.30189000360816465, -11.39540925085623968, 3.768464141822855495 ) ) ;
#57463=CONICAL_SURFACE ( 'NONE', #34964, 8.524999999999977263, 0.7853981633974552734 ) ;
#57465=CARTESIAN_POINT ( 'NONE',  ( -121.1050000000000040, -6.826472737025115478, 4.959722759717900331 ) ) ;
#57467=CARTESIAN_POINT ( 'NONE',  ( -127.1949999999999932, 8.437984349512085203, -1.550032578732815448E-15 ) ) ;
#57475=CARTESIAN_POINT ( 'NONE',  ( -167.6929263765338476, 10.01517768586948698, -1.839758294383808571E-15 ) ) ;
#57477=CARTESIAN_POINT ( 'NONE',  ( -181.4950000000000045, 6.826472737025113702, -4.959722759717902107 ) ) ;
#57484=CARTESIAN_POINT ( 'NONE',  ( -82.04292637653379927, -9.058813317711329915, -2.943386871421370898 ) ) ;
#57486=CARTESIAN_POINT ( 'NONE',  ( -166.6429263765338078, -5.598654528085801552, 7.705886871421367523 ) ) ;
#57499=CARTESIAN_POINT ( 'NONE',  ( -103.0429263765337993, -9.058813317711329915, -2.943386871421370898 ) ) ;
#57504=( BOUNDED_CURVE ( )  B_SPLINE_CURVE ( 2, ( #54739, #17163, #38981, #539, #21715, #16481, #862, #43908, #5502, #11850, #10481 ),
 .UNSPECIFIED., .F., .F. ) 
 B_SPLINE_CURVE_WITH_KNOTS ( ( 3, 2, 2, 2, 2, 3 ),
 ( 0.4999999999999881206, 0.5021739130434663689, 0.5043478260869445062, 0.5065217391304227545, 0.5086956521739008918, 0.5108695652173792512 ),
 .UNSPECIFIED. ) 
 CURVE ( )  GEOMETRIC_REPRESENTATION_ITEM ( )  RATIONAL_B_SPLINE_CURVE ( ( 1.000000000000267342, 0.9510565162948860785, 1.000000000000000000, 0.9510565162951535312, 1.000000000000000000, 0.9510565162951535312, 1.000000000000000000, 0.9510565162951535312, 1.000000000000000000, 0.9510565162954259799, 0.9999999999997275513 ) ) 
 REPRESENTATION_ITEM ( '' )  );
#57507=CARTESIAN_POINT ( 'NONE',  ( -104.0049999999999670, 6.826472737025115478, 4.959722759717899443 ) ) ;
#57517=CARTESIAN_POINT ( 'NONE',  ( -68.39499999999999602, -6.826472737025115478, -4.959722759717899443 ) ) ;
#57525=CARTESIAN_POINT ( 'NONE',  ( -195.0000000000000000, 0.000000000000000000, 0.000000000000000000 ) ) ;
#57535=CARTESIAN_POINT ( 'NONE',  ( -167.6070736234661638, -8.102448949553172852, 5.886773742842742685 ) ) ;
#57538=CARTESIAN_POINT ( 'NONE',  ( -100.5570736234661808, -1.166476076187852838E-15, -9.524999999999991473 ) ) ;
#57543=CARTESIAN_POINT ( 'NONE',  ( -106.1070736234661638, 8.102448949553172852, -5.886773742842744461 ) ) ;
#57544=DIRECTION ( 'NONE',  ( -1.000000000000000000, -0.000000000000000000, -0.000000000000000000 ) ) ;
#57546=CARTESIAN_POINT ( 'NONE',  ( -148.5550000000000068, 0.000000000000000000, 8.024999999999991473 ) ) ;
#57550=CARTESIAN_POINT ( 'NONE',  ( -153.1450000000000102, -4.716976649647092401, 6.492361379858946790 ) ) ;
#57551=CARTESIAN_POINT ( 'NONE',  ( -144.8949999999999818, 6.826472737025115478, 4.959722759717899443 ) ) ;
#57554=CARTESIAN_POINT ( 'NONE',  ( -181.2570736234661979, 5.598654528085800663, -7.705886871421367523 ) ) ;
#57558=CARTESIAN_POINT ( 'NONE',  ( -59.45499999999997698, 7.632228543268599452, -2.479861379858951942 ) ) ;
#57560=CARTESIAN_POINT ( 'NONE',  ( -153.5070736234661979, 8.102448949553176405, 5.886773742842740909 ) ) ;
#57561=CARTESIAN_POINT ( 'NONE',  ( -64.04499999999998749, 7.632228543268600340, 2.479861379858949277 ) ) ;
#57570=CARTESIAN_POINT ( 'NONE',  ( -178.6429263765338078, -5.598654528085801552, 7.705886871421367523 ) ) ;
#57585=CARTESIAN_POINT ( 'NONE',  ( -76.55707362346616662, -1.166476076187852838E-15, -9.524999999999991473 ) ) ;
#57599=CARTESIAN_POINT ( 'NONE',  ( -111.7449999999999903, 4.716976649647094177, 6.492361379858945902 ) ) ;
#57618=CARTESIAN_POINT ( 'NONE',  ( -122.0049999999999670, 6.826472737025116366, 4.959722759717898555 ) ) ;
#57634=CARTESIAN_POINT ( 'NONE',  ( -177.0549999999999784, -9.827790563157499189E-16, -8.024999999999991473 ) ) ;
#57637=CARTESIAN_POINT ( 'NONE',  ( -49.10707362346617089, 8.102448949553171076, -5.886773742842744461 ) ) ;
#57638=CARTESIAN_POINT ( 'NONE',  ( -174.7449999999999761, 4.716976649647094177, 6.492361379858945902 ) ) ;
#57643=CARTESIAN_POINT ( 'NONE',  ( -88.25499999999998124, -4.716976649647092401, 6.492361379858946790 ) ) ;
#57649=CARTESIAN_POINT ( 'NONE',  ( -86.24499999999999034, -4.716976649647093289, -6.492361379858945902 ) ) ;
#57651=CARTESIAN_POINT ( 'NONE',  ( -64.34499999999998465, 7.632228543268599452, -2.479861379858951942 ) ) ;
#57659=VERTEX_POINT ( 'NONE', #50422 ) ;
#57661=CARTESIAN_POINT ( 'NONE',  ( -108.7429263765338021, -5.598654528085803328, -7.705886871421366635 ) ) ;
#57662=CARTESIAN_POINT ( 'NONE',  ( -129.2949999999999875, -2.607480562269069768, 8.024999999999991473 ) ) ;
#57665=FACE_OUTER_BOUND ( 'NONE', #50587, .T. ) ;
#57679=CARTESIAN_POINT ( 'NONE',  ( -126.2049999999999841, -2.607480562269071545, -8.024999999999991473 ) ) ;
#57680=VERTEX_POINT ( 'NONE', #24029 ) ;
#57682=CARTESIAN_POINT ( 'NONE',  ( -120.8070736234661666, 10.01517768586948698, -1.839758294383808571E-15 ) ) ;
#57697=VERTEX_POINT ( 'NONE', #18417 ) ;
#57703=EDGE_CURVE ( 'NONE', #62431, #13981, #44605, .T. ) ;
#57707=CARTESIAN_POINT ( 'NONE',  ( -62.54292637653379927, 9.058813317711329915, 2.943386871421369566 ) ) ;
#57710=CARTESIAN_POINT ( 'NONE',  ( -149.1549999999999727, 7.632228543268600340, 2.479861379858949277 ) ) ;
#57714=( BOUNDED_CURVE ( )  B_SPLINE_CURVE ( 2, ( #60915, #3167, #55656, #13421, #46177, #34889, #51086, #24657, #66193, #18717, #45501 ),
 .UNSPECIFIED., .F., .F. ) 
 B_SPLINE_CURVE_WITH_KNOTS ( ( 3, 2, 2, 2, 2, 3 ),
 ( 0.6195652173912897798, 0.6217391304347680281, 0.6239130434782461654, 0.6260869565217245247, 0.6282608695652026620, 0.6304347826086809103 ),
 .UNSPECIFIED. ) 
 CURVE ( )  GEOMETRIC_REPRESENTATION_ITEM ( )  RATIONAL_B_SPLINE_CURVE ( ( 1.000000000000327516, 0.9510565162948261264, 1.000000000000000000, 0.9510565162951535312, 1.000000000000000000, 0.9510565162951535312, 1.000000000000000000, 0.9510565162951535312, 1.000000000000000000, 0.9510565162954859320, 0.9999999999996675992 ) ) 
 REPRESENTATION_ITEM ( '' )  );
#57719=ORIENTED_EDGE ( 'NONE', *, *, #46446, .T. ) ;
#57724=CARTESIAN_POINT ( 'NONE',  ( -69.20499999999998408, -2.607480562269071545, -8.024999999999991473 ) ) ;
#57731=CARTESIAN_POINT ( 'NONE',  ( -90.50707362346618368, 8.102448949553176405, 5.886773742842740909 ) ) ;
#57740=CARTESIAN_POINT ( 'NONE',  ( -93.59499999999997044, 2.607480562269073321, 8.024999999999991473 ) ) ;
#57747=CARTESIAN_POINT ( 'NONE',  ( -136.0429263765338135, -9.058813317711329915, -2.943386871421370898 ) ) ;
#57751=CARTESIAN_POINT ( 'NONE',  ( -154.3449999999999704, 7.632228543268599452, -2.479861379858951942 ) ) ;
#57756=CARTESIAN_POINT ( 'NONE',  ( -63.05707362346617373, 0.000000000000000000, 9.524999999999991473 ) ) ;
#57771=CARTESIAN_POINT ( 'NONE',  ( -153.5049999999999670, -6.826472737025113702, -4.959722759717900331 ) ) ;
#57782=CARTESIAN_POINT ( 'NONE',  ( -57.74292637653380211, -5.598654528085803328, -7.705886871421366635 ) ) ;
#57784=CARTESIAN_POINT ( 'NONE',  ( -74.00499999999996703, 6.826472737025115478, 4.959722759717899443 ) ) ;
#57790=ORIENTED_EDGE ( 'NONE', *, *, #39279, .T. ) ;
#57792=VECTOR ( 'NONE', #39573, 1000.000000000000000 ) ;
#57795=CARTESIAN_POINT ( 'NONE',  ( -182.7549999999999955, 4.716976649647091513, -6.492361379858946790 ) ) ;
#57800=VECTOR ( 'NONE', #63275, 1000.000000000000000 ) ;
#57806=AXIS2_PLACEMENT_3D ( 'NONE', #16940, #55230, #27784 ) ;
#57808=CARTESIAN_POINT ( 'NONE',  ( -96.80499999999999261, -8.437984349512085203, 5.166775262442717831E-16 ) ) ;
#57812=CARTESIAN_POINT ( 'NONE',  ( -130.2570736234661695, 5.598654528085800663, -7.705886871421367523 ) ) ;
#57814=CARTESIAN_POINT ( 'NONE',  ( -75.80707362346616662, 10.01517768586948698, -1.839758294383808571E-15 ) ) ;
#57819=CARTESIAN_POINT ( 'NONE',  ( -15.65737470746391580, -10.92375055806530071, 4.967564989580693258 ) ) ;
#57823=CARTESIAN_POINT ( 'NONE',  ( -107.3049999999999784, 8.437984349512085203, -1.550032578732815448E-15 ) ) ;
#57825=CARTESIAN_POINT ( 'NONE',  ( -123.2949999999999875, -2.607480562269069768, 8.024999999999991473 ) ) ;
#57829=CARTESIAN_POINT ( 'NONE',  ( -111.8070736234661666, 10.01517768586948698, -1.839758294383808966E-15 ) ) ;
#57833=ORIENTED_EDGE ( 'NONE', *, *, #25803, .T. ) ;
#57834=CARTESIAN_POINT ( 'NONE',  ( -167.9070736234663457, -3.094860106615454853, 9.525000000002153300 ) ) ;
#57835=CARTESIAN_POINT ( 'NONE',  ( -166.9429263765337907, 0.000000000000000000, 9.524999999999991473 ) ) ;
#57849=CARTESIAN_POINT ( 'NONE',  ( -89.39292637653377938, 8.102448949553176405, 5.886773742842740909 ) ) ;
#57851=CARTESIAN_POINT ( 'NONE',  ( -166.3429263765337964, -9.058813317711329915, 2.943386871421371787 ) ) ;
#57857=CARTESIAN_POINT ( 'NONE',  ( -178.5549999999999784, 0.000000000000000000, 8.024999999999991473 ) ) ;
#57863=CARTESIAN_POINT ( 'NONE',  ( -102.5929263765348338, -3.094860106635640928, -9.524999999987485921 ) ) ;
#57869=CARTESIAN_POINT ( 'NONE',  ( -101.9070736234671841, -3.094860106601623695, 9.525000000012200374 ) ) ;
#57870=CARTESIAN_POINT ( 'NONE',  ( -99.05499999999999261, -9.827790563157499189E-16, -8.024999999999991473 ) ) ;
#57880=CARTESIAN_POINT ( 'NONE',  ( -75.59499999999998465, 2.607480562269073321, 8.024999999999991473 ) ) ;
#57883=CARTESIAN_POINT ( 'NONE',  ( -120.8070736234661666, 10.01517768586948698, -1.839758294383808966E-15 ) ) ;
#57886=CARTESIAN_POINT ( 'NONE',  ( -195.0000000000000000, 7.499999999999984901, 0.000000000000000000 ) ) ;
#57896=CARTESIAN_POINT ( 'NONE',  ( -170.0070736234661410, -8.102448949553172852, -5.886773742842741797 ) ) ;
#57898=VECTOR ( 'NONE', #44747, 1000.000000000000000 ) ;
#57899=CARTESIAN_POINT ( 'NONE',  ( -106.1070736234661638, 8.102448949553171076, -5.886773742842744461 ) ) ;
#57905=CYLINDRICAL_SURFACE ( 'NONE', #63812, 9.524999999999991473 ) ;
#57906=CARTESIAN_POINT ( 'NONE',  ( -115.5570736234661808, -1.166476076187852838E-15, -9.524999999999991473 ) ) ;
#57908=CARTESIAN_POINT ( 'NONE',  ( -138.8050000000000068, -8.437984349512085203, 5.166775262442717831E-16 ) ) ;
#57911=CARTESIAN_POINT ( 'NONE',  ( -150.8950000000000102, 6.826472737025116366, 4.959722759717898555 ) ) ;
#57913=CARTESIAN_POINT ( 'NONE',  ( -148.9449999999999932, -9.827790563157499189E-16, -8.024999999999991473 ) ) ;
#57922=CARTESIAN_POINT ( 'NONE',  ( -62.15499999999998693, 7.632228543268600340, 2.479861379858949277 ) ) ;
#57925=CARTESIAN_POINT ( 'NONE',  ( -65.54499999999998749, -7.632228543268600340, -2.479861379858950166 ) ) ;
#57934=ADVANCED_FACE ( 'NONE', ( #65116 ), #21890, .F. ) ;
#57935=CARTESIAN_POINT ( 'NONE',  ( -82.40707362346617515, 3.094860106618428031, -9.524999999999993250 ) ) ;
#57936=CARTESIAN_POINT ( 'NONE',  ( -177.8929263765338078, -8.102448949553174629, -5.886773742842741797 ) ) ;
#57959=CARTESIAN_POINT ( 'NONE',  ( -102.4449999999999932, 0.000000000000000000, 8.024999999999991473 ) ) ;
#57962=CARTESIAN_POINT ( 'NONE',  ( -52.94292637653380496, 0.000000000000000000, 9.524999999999991473 ) ) ;
#57963=ORIENTED_EDGE ( 'NONE', *, *, #35763, .F. ) ;
#57971=ORIENTED_EDGE ( 'NONE', *, *, #42385, .T. ) ;
#57974=CARTESIAN_POINT ( 'NONE',  ( -140.2429263765338021, 5.598654528085804216, 7.705886871421366635 ) ) ;
#57981=CARTESIAN_POINT ( 'NONE',  ( -183.0000000000000284, -1.154738647139537111, 9.454745033939424559 ) ) ;
#57988=CARTESIAN_POINT ( 'NONE',  ( -182.5429263765337851, 9.058813317711329915, 2.943386871421369566 ) ) ;
#57993=CARTESIAN_POINT ( 'NONE',  ( -154.9429263765338192, 0.000000000000000000, 9.524999999999991473 ) ) ;
#57994=CARTESIAN_POINT ( 'NONE',  ( -176.7549999999999955, 4.716976649647091513, -6.492361379858946790 ) ) ;
#57996=LINE ( 'NONE', #62886, #32999 ) ;
#57998=CARTESIAN_POINT ( 'NONE',  ( -179.5450000000000159, -7.632228543268600340, -2.479861379858950166 ) ) ;
#57999=VECTOR ( 'NONE', #58487, 1000.000000000000000 ) ;
#58000=CARTESIAN_POINT ( 'NONE',  ( -173.8449999999999989, -7.632228543268599452, 2.479861379858951054 ) ) ;
#58007=CARTESIAN_POINT ( 'NONE',  ( -95.90500000000000114, 2.607480562269068880, -8.024999999999993250 ) ) ;
#58012=CARTESIAN_POINT ( 'NONE',  ( -93.29499999999998749, -2.607480562269069768, 8.024999999999991473 ) ) ;
#58014=CARTESIAN_POINT ( 'NONE',  ( -68.09499999999998465, -2.607480562269071545, -8.024999999999991473 ) ) ;
#58031=( BOUNDED_CURVE ( )  B_SPLINE_CURVE ( 2, ( #53559, #69395, #5344, #15268, #25771, #10990, #14907, #42367, #63751, #10313, #26114 ),
 .UNSPECIFIED., .F., .F. ) 
 B_SPLINE_CURVE_WITH_KNOTS ( ( 3, 2, 2, 2, 2, 3 ),
 ( 0.3913043478260777031, 0.3934782608695558959, 0.3956521739130340887, 0.3978260869565122815, 0.3999999999999905298, 0.4021739130434687226 ),
 .UNSPECIFIED. ) 
 CURVE ( )  GEOMETRIC_REPRESENTATION_ITEM ( )  RATIONAL_B_SPLINE_CURVE ( ( 1.000000000000208722, 0.9510565162949448093, 1.000000000000000000, 0.9510565162951535312, 1.000000000000000000, 0.9510565162951535312, 1.000000000000000000, 0.9510565162951535312, 1.000000000000000000, 0.9510565162953684704, 0.9999999999997850608 ) ) 
 REPRESENTATION_ITEM ( '' )  );
#58038=CARTESIAN_POINT ( 'NONE',  ( -126.0550000000000068, -9.827790563157499189E-16, -8.024999999999991473 ) ) ;
#58043=ORIENTED_EDGE ( 'NONE', *, *, #15888, .T. ) ;
#58045=ORIENTED_EDGE ( 'NONE', *, *, #2746, .F. ) ;
#58057=CARTESIAN_POINT ( 'NONE',  ( -46.85707362346616378, -5.598654528085803328, -7.705886871421366635 ) ) ;
#58064=CARTESIAN_POINT ( 'NONE',  ( -55.04292637653379927, -9.058813317711329915, -2.943386871421370898 ) ) ;
#58066=CARTESIAN_POINT ( 'NONE',  ( -152.3050000000000068, 8.437984349512085203, -1.550032578732815448E-15 ) ) ;
#58071=CARTESIAN_POINT ( 'NONE',  ( -45.99999999999998579, 0.000000000000000000, 0.000000000000000000 ) ) ;
#58081=CARTESIAN_POINT ( 'NONE',  ( -70.85499999999998977, 4.716976649647094177, 6.492361379858945902 ) ) ;
#58082=ORIENTED_EDGE ( 'NONE', *, *, #26984, .F. ) ;
#58087=DIRECTION ( 'NONE',  ( 0.000000000000000000, 0.000000000000000000, 1.000000000000000000 ) ) ;
#58096=CARTESIAN_POINT ( 'NONE',  ( -101.5449999999999875, -7.632228543268600340, -2.479861379858950166 ) ) ;
#58101=ORIENTED_EDGE ( 'NONE', *, *, #2917, .T. ) ;
#58102=CARTESIAN_POINT ( 'NONE',  ( -134.3929263765338078, 8.102448949553176405, 5.886773742842740909 ) ) ;
#58105=CARTESIAN_POINT ( 'NONE',  ( -160.0449999999999875, 7.632228543268600340, 2.479861379858949277 ) ) ;
#58116=CARTESIAN_POINT ( 'NONE',  ( -110.1570736234661751, -9.058813317711329915, -2.943386871421370898 ) ) ;
#58119=CARTESIAN_POINT ( 'NONE',  ( -153.8049999999999784, -8.437984349512086979, 5.166775262442717831E-16 ) ) ;
#58124=ORIENTED_EDGE ( 'NONE', *, *, #35594, .F. ) ;
#58127=ORIENTED_EDGE ( 'NONE', *, *, #28963, .F. ) ;
#58130=CARTESIAN_POINT ( 'NONE',  ( -62.75499999999998835, 4.716976649647091513, -6.492361379858946790 ) ) ;
#58135=FACE_OUTER_BOUND ( 'NONE', #20729, .T. ) ;
#58141=CARTESIAN_POINT ( 'NONE',  ( -195.0000000000000000, 0.000000000000000000, 9.524999999999991473 ) ) ;
#58142=CARTESIAN_POINT ( 'NONE',  ( -176.9050000000000011, 2.607480562269068880, -8.024999999999993250 ) ) ;
#58148=ORIENTED_EDGE ( 'NONE', *, *, #29859, .F. ) ;
#58155=CARTESIAN_POINT ( 'NONE',  ( -95.90500000000000114, 2.607480562269068880, -8.024999999999993250 ) ) ;
#58156=ORIENTED_EDGE ( 'NONE', *, *, #16908, .F. ) ;
#58158=CARTESIAN_POINT ( 'NONE',  ( -128.4570736234661865, -9.058813317711329915, 2.943386871421371787 ) ) ;
#58160=CARTESIAN_POINT ( 'NONE',  ( -70.85707362346617799, -5.598654528085803328, -7.705886871421366635 ) ) ;
#58167=CARTESIAN_POINT ( 'NONE',  ( -112.5549999999999926, 0.000000000000000000, 8.024999999999991473 ) ) ;
#58170=CARTESIAN_POINT ( 'NONE',  ( -122.0949999999999847, -2.607480562269071545, -8.024999999999991473 ) ) ;
#58175=CARTESIAN_POINT ( 'NONE',  ( -162.5929263765337964, -3.094860106618431139, -9.524999999999991473 ) ) ;
#58176=SURFACE_SIDE_STYLE ('',( #52571 ) ) ;
#58183=CARTESIAN_POINT ( 'NONE',  ( -76.79292637653379927, -3.094860106618429807, 9.524999999999991473 ) ) ;
#58187=CARTESIAN_POINT ( 'NONE',  ( -177.5049999999999670, -6.826472737025113702, -4.959722759717900331 ) ) ;
#58191=CARTESIAN_POINT ( 'NONE',  ( -105.4429263765338050, -1.166476076187852838E-15, -9.524999999999991473 ) ) ;
#58193=CARTESIAN_POINT ( 'NONE',  ( -110.6929263765338050, 10.01517768586948698, -1.839758294383808966E-15 ) ) ;
#58199=CARTESIAN_POINT ( 'NONE',  ( -93.35499999999998977, -4.716976649647093289, -6.492361379858945902 ) ) ;
#58209=CARTESIAN_POINT ( 'NONE',  ( -129.0570736234661808, 0.000000000000000000, 9.524999999999991473 ) ) ;
#58210=CARTESIAN_POINT ( 'NONE',  ( -74.39499999999999602, -6.826472737025115478, -4.959722759717899443 ) ) ;
#58214=CARTESIAN_POINT ( 'NONE',  ( -125.1570736234661751, -9.058813317711329915, -2.943386871421370898 ) ) ;
#58228=CARTESIAN_POINT ( 'NONE',  ( -159.2070736234661297, 3.094860106618433360, 9.524999999999991473 ) ) ;
#58231=CARTESIAN_POINT ( 'NONE',  ( -102.9570736234661723, 9.058813317711329915, -2.943386871421373119 ) ) ;
#58235=CARTESIAN_POINT ( 'NONE',  ( -106.9429263765337907, 0.000000000000000000, 9.524999999999991473 ) ) ;
#58240=CARTESIAN_POINT ( 'NONE',  ( -141.0549999999999784, -9.827790563157499189E-16, -8.024999999999991473 ) ) ;
#58242=CARTESIAN_POINT ( 'NONE',  ( -150.5949999999999989, 2.607480562269073321, 8.024999999999991473 ) ) ;
#58244=CARTESIAN_POINT ( 'NONE',  ( -140.9949999999999761, -6.826472737025113702, 4.959722759717902107 ) ) ;
#58245=ORIENTED_EDGE ( 'NONE', *, *, #36998, .T. ) ;
#58246=AXIS2_PLACEMENT_3D ( 'NONE', #68180, #19624, #20315 ) ;
#58247=CARTESIAN_POINT ( 'NONE',  ( -180.3570736234661638, 5.598654528085804216, 7.705886871421366635 ) ) ;
#58249=CARTESIAN_POINT ( 'NONE',  ( -52.55499999999999261, 0.000000000000000000, 8.024999999999991473 ) ) ;
#58252=CARTESIAN_POINT ( 'NONE',  ( -52.79292637653378506, -3.094860106618429807, 9.524999999999991473 ) ) ;
#58259=CARTESIAN_POINT ( 'NONE',  ( -82.55707362346618083, -1.166476076187852838E-15, -9.524999999999991473 ) ) ;
#58263=CARTESIAN_POINT ( 'NONE',  ( -79.94292637653380496, 0.000000000000000000, 9.524999999999991473 ) ) ;
#58272=CARTESIAN_POINT ( 'NONE',  ( -76.85707362346616378, -5.598654528085803328, -7.705886871421366635 ) ) ;
#58280=CARTESIAN_POINT ( 'NONE',  ( -85.64292637653379359, -5.598654528085801552, 7.705886871421367523 ) ) ;
#58283=AXIS2_PLACEMENT_3D ( 'NONE', #59023, #1603, #38299 ) ;
#58285=CARTESIAN_POINT ( 'NONE',  ( -103.4949999999999761, 6.826472737025113702, -4.959722759717902107 ) ) ;
#58290=ORIENTED_EDGE ( 'NONE', *, *, #60241, .T. ) ;
#58301=FACE_OUTER_BOUND ( 'NONE', #9264, .T. ) ;
#58310=LINE ( 'NONE', #47464, #18048 ) ;
#58319=CARTESIAN_POINT ( 'NONE',  ( -169.5549999999999784, 0.000000000000000000, 8.024999999999991473 ) ) ;
#58321=CARTESIAN_POINT ( 'NONE',  ( -181.6450000000000102, 4.716976649647091513, -6.492361379858946790 ) ) ;
#58322=CARTESIAN_POINT ( 'NONE',  ( -166.1949999999999932, 8.437984349512086979, -1.550032578732815448E-15 ) ) ;
#58326=CARTESIAN_POINT ( 'NONE',  ( -14.83546612668997433, 10.90871211463571022, -5.000000000000001776 ) ) ;
#58327=CARTESIAN_POINT ( 'NONE',  ( -83.00499999999995282, 6.826472737025116366, 4.959722759717898555 ) ) ;
#58329=CARTESIAN_POINT ( 'NONE',  ( -168.0570736234661808, 0.000000000000000000, 9.524999999999991473 ) ) ;
#58332=CARTESIAN_POINT ( 'NONE',  ( -94.94499999999999318, -9.827790563157499189E-16, -8.024999999999991473 ) ) ;
#58337=AXIS2_PLACEMENT_3D ( 'NONE', #5731, #10358, #58885 ) ;
#58345=CARTESIAN_POINT ( 'NONE',  ( -195.0000000000000000, 1.166476076187852838E-15, -9.524999999999991473 ) ) ;
#58356=CARTESIAN_POINT ( 'NONE',  ( -124.5549999999999926, 0.000000000000000000, 8.024999999999991473 ) ) ;
#58359=CARTESIAN_POINT ( 'NONE',  ( -137.7570736234661695, -5.598654528085801552, 7.705886871421367523 ) ) ;
#58374=CARTESIAN_POINT ( 'NONE',  ( -136.4070736234667720, 3.094860106608949835, -9.525000000006881962 ) ) ;
#58387=CARTESIAN_POINT ( 'NONE',  ( -55.94292637653380496, 0.000000000000000000, 9.524999999999991473 ) ) ;
#58391=CARTESIAN_POINT ( 'NONE',  ( -153.5049999999999670, -6.826472737025115478, -4.959722759717899443 ) ) ;
#58402=VERTEX_POINT ( 'NONE', #65393 ) ;
#58403=FACE_OUTER_BOUND ( 'NONE', #50762, .T. ) ;
#58405=CARTESIAN_POINT ( 'NONE',  ( -70.70499999999996987, 2.607480562269073321, 8.024999999999991473 ) ) ;
#58420=CARTESIAN_POINT ( 'NONE',  ( -121.6449999999999960, 4.716976649647091513, -6.492361379858946790 ) ) ;
#58422=CARTESIAN_POINT ( 'NONE',  ( -84.59499999999998465, 2.607480562269073321, 8.024999999999991473 ) ) ;
#58426=( BOUNDED_CURVE ( )  B_SPLINE_CURVE ( 2, ( #53956, #10721, #47356, #21248, #26538, #59223, #58214, #53300, #14984, #63494, #31460 ),
 .UNSPECIFIED., .F., .F. ) 
 B_SPLINE_CURVE_WITH_KNOTS ( ( 3, 2, 2, 2, 2, 3 ),
 ( 0.4130434782608597977, 0.4152173913043379905, 0.4173913043478162388, 0.4195652173912944871, 0.4217391304347727354, 0.4239130434782509282 ),
 .UNSPECIFIED. ) 
 CURVE ( )  GEOMETRIC_REPRESENTATION_ITEM ( )  RATIONAL_B_SPLINE_CURVE ( ( 1.000000000000220046, 0.9510565162949335960, 1.000000000000000000, 0.9510565162951535312, 1.000000000000000000, 0.9510565162951535312, 1.000000000000000000, 0.9510565162951535312, 1.000000000000000000, 0.9510565162953772411, 0.9999999999997762901 ) ) 
 REPRESENTATION_ITEM ( '' )  );
#58431=CARTESIAN_POINT ( 'NONE',  ( -136.6429263765338078, -5.598654528085801552, 7.705886871421367523 ) ) ;
#58433=CARTESIAN_POINT ( 'NONE',  ( -157.9449999999999932, -9.827790563157499189E-16, -8.024999999999991473 ) ) ;
#58443=VECTOR ( 'NONE', #51260, 1000.000000000000000 ) ;
#58447=CARTESIAN_POINT ( 'NONE',  ( -59.39292637653377938, 8.102448949553176405, 5.886773742842740909 ) ) ;
#58449=VERTEX_POINT ( 'NONE', #13289 ) ;
#58450=CARTESIAN_POINT ( 'NONE',  ( -154.7049999999999841, 2.607480562269072433, 8.024999999999991473 ) ) ;
#58465=CARTESIAN_POINT ( 'NONE',  ( -64.40499999999998693, -2.607480562269069768, 8.024999999999991473 ) ) ;
#58478=CARTESIAN_POINT ( 'NONE',  ( -183.0550000000000068, -9.827790563157499189E-16, -8.024999999999991473 ) ) ;
#58487=DIRECTION ( 'NONE',  ( -1.000000000000000000, -0.000000000000000000, -0.000000000000000000 ) ) ;
#58490=CARTESIAN_POINT ( 'NONE',  ( -98.30499999999997840, 8.437984349512085203, -1.550032578732815448E-15 ) ) ;
#58493=CARTESIAN_POINT ( 'NONE',  ( -134.3070736234661240, -10.01517768586948698, 6.132527647946031529E-16 ) ) ;
#58497=CARTESIAN_POINT ( 'NONE',  ( -62.00707362346618368, -8.102448949553172852, -5.886773742842741797 ) ) ;
#58504=DIRECTION ( 'NONE',  ( -1.000000000000000000, -0.000000000000000000, -0.000000000000000000 ) ) ;
#58505=CARTESIAN_POINT ( 'NONE',  ( -113.7549999999999955, 4.716976649647091513, -6.492361379858946790 ) ) ;
#58507=CARTESIAN_POINT ( 'NONE',  ( -127.7949999999999875, 2.607480562269068880, -8.024999999999993250 ) ) ;
#58511=CARTESIAN_POINT ( 'NONE',  ( -160.6429263765338362, -5.598654528085801552, 7.705886871421367523 ) ) ;
#58512=SHAPE_REPRESENTATION_RELATIONSHIP ( 'NONE' , 'NONE' ,  #14155, #6101 ) ;
#58515=DIRECTION ( 'NONE',  ( -1.000000000000000000, -0.000000000000000000, -0.000000000000000000 ) ) ;
#58521=CARTESIAN_POINT ( 'NONE',  ( -71.84292637653381064, 9.058813317711329915, -2.943386871421373119 ) ) ;
#58529=CARTESIAN_POINT ( 'NONE',  ( -181.1049999999999898, -6.826472737025113702, 4.959722759717902107 ) ) ;
#58542=CARTESIAN_POINT ( 'NONE',  ( -89.30499999999997840, 8.437984349512086979, -1.550032578732815448E-15 ) ) ;
#58552=CARTESIAN_POINT ( 'NONE',  ( -72.14499999999998181, -4.716976649647092401, 6.492361379858946790 ) ) ;
#58561=COLOUR_RGB ( '', 0.40784314, 0.44705882, 0.49803922) ;
#58570=CARTESIAN_POINT ( 'NONE',  ( -160.1070736234661922, 8.102448949553171076, -5.886773742842744461 ) ) ;
#58574=CARTESIAN_POINT ( 'NONE',  ( -93.50707362346618368, 8.102448949553176405, 5.886773742842740909 ) ) ;
#58582=CARTESIAN_POINT ( 'NONE',  ( -144.3549999999999898, -4.716976649647093289, -6.492361379858945902 ) ) ;
#58586=CARTESIAN_POINT ( 'NONE',  ( -155.3950000000000102, -6.826472737025115478, -4.959722759717899443 ) ) ;
#58587=CARTESIAN_POINT ( 'NONE',  ( -140.0949999999999989, -2.607480562269071545, -8.024999999999991473 ) ) ;
#58595=CARTESIAN_POINT ( 'NONE',  ( -57.95499999999997698, -7.632228543268599452, 2.479861379858951054 ) ) ;
#58604=CARTESIAN_POINT ( 'NONE',  ( -88.70707362346615810, -3.094860106618431139, -9.524999999999991473 ) ) ;
#58636=CARTESIAN_POINT ( 'NONE',  ( -100.4949999999999761, 6.826472737025113702, -4.959722759717902107 ) ) ;
#58639=CARTESIAN_POINT ( 'NONE',  ( -140.1570736234661751, -9.058813317711329915, -2.943386871421370898 ) ) ;
#58660=CARTESIAN_POINT ( 'NONE',  ( -173.6049999999999898, 6.826472737025113702, -4.959722759717902107 ) ) ;
#58663=CARTESIAN_POINT ( 'NONE',  ( -181.3449999999999989, 7.632228543268599452, -2.479861379858951942 ) ) ;
#58665=CARTESIAN_POINT ( 'NONE',  ( -171.8949999999999534, 6.826472737025115478, 4.959722759717899443 ) ) ;
#58670=CARTESIAN_POINT ( 'NONE',  ( -84.65500000000000114, -7.632228543268600340, -2.479861379858950166 ) ) ;
#58674=CARTESIAN_POINT ( 'NONE',  ( -79.94499999999999318, -9.827790563157499189E-16, -8.024999999999991473 ) ) ;
#58679=CARTESIAN_POINT ( 'NONE',  ( -171.2070736234663570, 3.094860106620802132, 9.524999999998270184 ) ) ;
#58710=VERTEX_POINT ( 'NONE', #22749 ) ;
#58711=CARTESIAN_POINT ( 'NONE',  ( -120.3549999999999898, -4.716976649647093289, -6.492361379858945902 ) ) ;
#58714=CARTESIAN_POINT ( 'NONE',  ( -137.9070736234667436, -3.094860106609220285, 9.525000000006683010 ) ) ;
#58727=CARTESIAN_POINT ( 'NONE',  ( -135.9570736234661865, 9.058813317711329915, -2.943386871421373119 ) ) ;
#58728=CARTESIAN_POINT ( 'NONE',  ( -130.0429263765338135, -9.058813317711329915, -2.943386871421370898 ) ) ;
#58731=LINE ( 'NONE', #44670, #39079 ) ;
#58740=EDGE_LOOP ( 'NONE', ( #65134, #16220, #55971, #47880 ) ) ;
#58741=CARTESIAN_POINT ( 'NONE',  ( -57.59292637653379643, -3.094860106618431139, -9.524999999999991473 ) ) ;
#58744=CARTESIAN_POINT ( 'NONE',  ( -147.6549999999999727, -7.632228543268600340, -2.479861379858950166 ) ) ;
#58757=CARTESIAN_POINT ( 'NONE',  ( -65.30499999999999261, 8.437984349512085203, -1.550032578732815448E-15 ) ) ;
#58762=CARTESIAN_POINT ( 'NONE',  ( -127.9429263765338192, 0.000000000000000000, 9.524999999999991473 ) ) ;
#58770=CARTESIAN_POINT ( 'NONE',  ( -110.0949999999999704, -2.607480562269071545, -8.024999999999991473 ) ) ;
#58772=CARTESIAN_POINT ( 'NONE',  ( -85.94499999999999318, -9.827790563157499189E-16, -8.024999999999991473 ) ) ;
#58773=CARTESIAN_POINT ( 'NONE',  ( -195.0000000000000000, 0.000000000000000000, 9.524999999999991473 ) ) ;
#58779=DIRECTION ( 'NONE',  ( 0.000000000000000000, -0.000000000000000000, 1.000000000000000000 ) ) ;
#58781=CARTESIAN_POINT ( 'NONE',  ( -135.8929263765338362, -8.102448949553172852, -5.886773742842741797 ) ) ;
#58783=CARTESIAN_POINT ( 'NONE',  ( -145.4949999999999477, 6.826472737025113702, -4.959722759717902107 ) ) ;
#58786=CARTESIAN_POINT ( 'NONE',  ( -67.25707362346616947, 5.598654528085800663, -7.705886871421367523 ) ) ;
#58799=CARTESIAN_POINT ( 'NONE',  ( -148.7049999999999841, 2.607480562269072433, 8.024999999999991473 ) ) ;
#58803=CARTESIAN_POINT ( 'NONE',  ( -142.2570736234661695, 5.598654528085800663, -7.705886871421367523 ) ) ;
#58813=CARTESIAN_POINT ( 'NONE',  ( -66.80499999999999261, -8.437984349512086979, 5.166775262442717831E-16 ) ) ;
#58814=CARTESIAN_POINT ( 'NONE',  ( -116.6949999999999790, -8.437984349512085203, 5.166775262442717831E-16 ) ) ;
#58826=CARTESIAN_POINT ( 'NONE',  ( -183.6549999999999727, -7.632228543268600340, -2.479861379858950166 ) ) ;
#58836=CARTESIAN_POINT ( 'NONE',  ( -96.50499999999998124, -6.826472737025115478, -4.959722759717899443 ) ) ;
#58841=CARTESIAN_POINT ( 'NONE',  ( -132.0570736234661808, 0.000000000000000000, 9.524999999999991473 ) ) ;
#58843=( BOUNDED_CURVE ( )  B_SPLINE_CURVE ( 2, ( #66221, #39888, #18045, #65540, #60262, #6785, #54283, #60584, #61293, #28919, #12401 ),
 .UNSPECIFIED., .F., .F. ) 
 B_SPLINE_CURVE_WITH_KNOTS ( ( 3, 2, 2, 2, 2, 3 ),
 ( 0.5217391304347702707, 0.5239130434782484080, 0.5260869565217266564, 0.5282608695652047937, 0.5304347826086831530, 0.5326086956521612903 ),
 .UNSPECIFIED. ) 
 CURVE ( )  GEOMETRIC_REPRESENTATION_ITEM ( )  RATIONAL_B_SPLINE_CURVE ( ( 1.000000000000277556, 0.9510565162948760864, 1.000000000000000000, 0.9510565162951535312, 1.000000000000000000, 0.9510565162951535312, 1.000000000000000000, 0.9510565162951535312, 1.000000000000000000, 0.9510565162954385254, 0.9999999999997150057 ) ) 
 REPRESENTATION_ITEM ( '' )  );
#58846=CARTESIAN_POINT ( 'NONE',  ( -66.35707362346616378, 5.598654528085804216, 7.705886871421366635 ) ) ;
#58848=CARTESIAN_POINT ( 'NONE',  ( -79.94292637653380496, 0.000000000000000000, 9.524999999999991473 ) ) ;
#58858=CARTESIAN_POINT ( 'NONE',  ( -113.6049999999999898, 6.826472737025113702, -4.959722759717902107 ) ) ;
#58861=CARTESIAN_POINT ( 'NONE',  ( -115.7949999999999875, 2.607480562269068880, -8.024999999999993250 ) ) ;
#58865=CARTESIAN_POINT ( 'NONE',  ( -153.3570736234661922, 5.598654528085804216, 7.705886871421366635 ) ) ;
#58869=CARTESIAN_POINT ( 'NONE',  ( -158.2429263765338021, 5.598654528085804216, 7.705886871421366635 ) ) ;
#58870=CARTESIAN_POINT ( 'NONE',  ( -173.5450000000000159, -7.632228543268600340, -2.479861379858950166 ) ) ;
#58879=CARTESIAN_POINT ( 'NONE',  ( -79.64292637653380780, -5.598654528085801552, 7.705886871421367523 ) ) ;
#58885=DIRECTION ( 'NONE',  ( 0.000000000000000000, 0.000000000000000000, 1.000000000000000000 ) ) ;
#58886=CARTESIAN_POINT ( 'NONE',  ( -180.6550000000000011, -7.632228543268600340, -2.479861379858950166 ) ) ;
#58898=CARTESIAN_POINT ( 'NONE',  ( -89.00499999999998124, 6.826472737025115478, 4.959722759717899443 ) ) ;
#58908=CARTESIAN_POINT ( 'NONE',  ( -69.14499999999998181, -4.716976649647092401, 6.492361379858946790 ) ) ;
#58921=CARTESIAN_POINT ( 'NONE',  ( -122.4549999999999983, 7.632228543268599452, -2.479861379858951942 ) ) ;
#58928=CARTESIAN_POINT ( 'NONE',  ( -163.5570736234661524, -1.166476076187852838E-15, -9.524999999999991473 ) ) ;
#58930=CARTESIAN_POINT ( 'NONE',  ( -92.75707362346618368, -5.598654528085801552, 7.705886871421367523 ) ) ;
#58939=CARTESIAN_POINT ( 'NONE',  ( -140.6050000000000182, 6.826472737025113702, -4.959722759717902107 ) ) ;
#58943=CARTESIAN_POINT ( 'NONE',  ( -147.4449999999999932, 0.000000000000000000, 8.024999999999991473 ) ) ;
#58944=CARTESIAN_POINT ( 'NONE',  ( -135.1449999999999818, -4.716976649647092401, 6.492361379858946790 ) ) ;
#58948=CARTESIAN_POINT ( 'NONE',  ( -76.55707362346616662, -1.166476076187852838E-15, -9.524999999999991473 ) ) ;
#58949=CARTESIAN_POINT ( 'NONE',  ( -52.25499999999999545, -4.716976649647092401, 6.492361379858946790 ) ) ;
#58952=CARTESIAN_POINT ( 'NONE',  ( -138.4429263765337907, -1.166476076187852838E-15, -9.524999999999991473 ) ) ;
#58953=CARTESIAN_POINT ( 'NONE',  ( -51.44292637653380496, -1.166476076187852838E-15, -9.524999999999991473 ) ) ;
#58955=CARTESIAN_POINT ( 'NONE',  ( -106.7929263765337851, -3.094860106618429807, 9.524999999999991473 ) ) ;
#58973=AXIS2_PLACEMENT_3D ( 'NONE', #44255, #55795, #66343 ) ;
#58983=CARTESIAN_POINT ( 'NONE',  ( -98.99499999999997613, -6.826472737025115478, 4.959722759717900331 ) ) ;
#59012=VERTEX_POINT ( 'NONE', #33223 ) ;
#59015=CARTESIAN_POINT ( 'NONE',  ( -171.6550000000000011, -7.632228543268600340, -2.479861379858950166 ) ) ;
#59017=CARTESIAN_POINT ( 'NONE',  ( -148.4070736234666015, 3.094860106611302619, -9.525000000005171330 ) ) ;
#59018=CARTESIAN_POINT ( 'NONE',  ( -173.8449999999999989, -7.632228543268599452, 2.479861379858951054 ) ) ;
#59021=CARTESIAN_POINT ( 'NONE',  ( -165.5949999999999420, 2.607480562269072433, 8.024999999999991473 ) ) ;
#59023=CARTESIAN_POINT ( 'NONE',  ( -195.0000000000000000, 0.000000000000000000, 0.000000000000000000 ) ) ;
#59026=CARTESIAN_POINT ( 'NONE',  ( -84.50499999999999545, -6.826472737025115478, -4.959722759717899443 ) ) ;
#59028=LINE ( 'NONE', #53734, #62915 ) ;
#59031=CARTESIAN_POINT ( 'NONE',  ( -83.24499999999999034, -4.716976649647093289, -6.492361379858945902 ) ) ;
#59038=VERTEX_POINT ( 'NONE', #18356 ) ;
#59047=CARTESIAN_POINT ( 'NONE',  ( -174.2070736234663570, 3.094860106620215046, 9.524999999998700062 ) ) ;
#59050=ORIENTED_EDGE ( 'NONE', *, *, #50219, .F. ) ;
#59051=CARTESIAN_POINT ( 'NONE',  ( -115.8549999999999898, 4.716976649647094177, 6.492361379858945902 ) ) ;
#59066=CARTESIAN_POINT ( 'NONE',  ( -181.9429263765338192, 0.000000000000000000, 9.524999999999991473 ) ) ;
#59074=VERTEX_POINT ( 'NONE', #5763 ) ;
#59079=CARTESIAN_POINT ( 'NONE',  ( -53.24292637653380211, 5.598654528085804216, 7.705886871421366635 ) ) ;
#59080=AXIS2_PLACEMENT_3D ( 'NONE', #31047, #41298, #69056 ) ;
#59083=CARTESIAN_POINT ( 'NONE',  ( -143.4550000000000125, 7.632228543268599452, -2.479861379858951942 ) ) ;
#59084=CARTESIAN_POINT ( 'NONE',  ( -176.0070736234661695, -8.102448949553174629, -5.886773742842741797 ) ) ;
#59092=CARTESIAN_POINT ( 'NONE',  ( -56.90499999999998693, 2.607480562269068880, -8.024999999999993250 ) ) ;
#59101=CARTESIAN_POINT ( 'NONE',  ( -129.4429263765338192, -1.166476076187852838E-15, -9.524999999999991473 ) ) ;
#59106=CARTESIAN_POINT ( 'NONE',  ( -111.8949999999999960, 6.826472737025115478, 4.959722759717899443 ) ) ;
#59108=CARTESIAN_POINT ( 'NONE',  ( -84.89499999999996760, 6.826472737025116366, 4.959722759717898555 ) ) ;
#59110=CARTESIAN_POINT ( 'NONE',  ( -195.0000000000000000, 0.000000000000000000, 0.000000000000000000 ) ) ;
#59114=CARTESIAN_POINT ( 'NONE',  ( -137.5429263765338135, 9.058813317711329915, 2.943386871421369566 ) ) ;
#59115=CARTESIAN_POINT ( 'NONE',  ( -150.8950000000000102, 6.826472737025116366, 4.959722759717898555 ) ) ;
#59117=CARTESIAN_POINT ( 'NONE',  ( -67.55707362346618083, -1.166476076187852838E-15, -9.524999999999991473 ) ) ;
#59124=CARTESIAN_POINT ( 'NONE',  ( -151.3429263765337964, -9.058813317711329915, 2.943386871421371787 ) ) ;
#59126=CARTESIAN_POINT ( 'NONE',  ( -146.6049999999999898, 6.826472737025113702, -4.959722759717902107 ) ) ;
#59129=CARTESIAN_POINT ( 'NONE',  ( -142.1070736234661638, 8.102448949553172852, -5.886773742842744461 ) ) ;
#59138=CARTESIAN_POINT ( 'NONE',  ( -65.45499999999998408, 7.632228543268599452, -2.479861379858951942 ) ) ;
#59139=CARTESIAN_POINT ( 'NONE',  ( -124.1950000000000074, 8.437984349512085203, -1.550032578732815448E-15 ) ) ;
#59147=EDGE_CURVE ( 'NONE', #38125, #56906, #46449, .T. ) ;
#59152=CARTESIAN_POINT ( 'NONE',  ( -168.3550000000000182, -4.716976649647093289, -6.492361379858945902 ) ) ;
#59160=CARTESIAN_POINT ( 'NONE',  ( -190.0000000000000000, 0.000000000000000000, 0.000000000000000000 ) ) ;
#59161=CARTESIAN_POINT ( 'NONE',  ( -84.35499999999998977, -4.716976649647093289, -6.492361379858945902 ) ) ;
#59167=CARTESIAN_POINT ( 'NONE',  ( -62.45707362346617231, -9.058813317711329915, 2.943386871421371787 ) ) ;
#59175=CARTESIAN_POINT ( 'NONE',  ( -111.5049999999999955, -6.826472737025115478, -4.959722759717899443 ) ) ;
#59177=CARTESIAN_POINT ( 'NONE',  ( -117.7449999999999903, 4.716976649647094177, 6.492361379858945902 ) ) ;
#59180=CARTESIAN_POINT ( 'NONE',  ( -166.3429263765337964, -9.058813317711329915, 2.943386871421371787 ) ) ;
#59181=CARTESIAN_POINT ( 'NONE',  ( -178.6450000000000102, 4.716976649647091513, -6.492361379858946790 ) ) ;
#59189=CARTESIAN_POINT ( 'NONE',  ( -77.09292637653378222, 3.094860106618433360, 9.524999999999991473 ) ) ;
#59194=( BOUNDED_CURVE ( )  B_SPLINE_CURVE ( 2, ( #15231, #62335, #61977, #35261, #51437, #67616, #4247, #46907, #35617, #19419, #40916 ),
 .UNSPECIFIED., .F., .F. ) 
 B_SPLINE_CURVE_WITH_KNOTS ( ( 3, 2, 2, 2, 2, 3 ),
 ( 0.06521739130434635323, 0.06739130434782455992, 0.06956521739130278048, 0.07173913043478098717, 0.07391304347825920773, 0.07608695652173741442 ),
 .UNSPECIFIED. ) 
 CURVE ( )  GEOMETRIC_REPRESENTATION_ITEM ( )  RATIONAL_B_SPLINE_CURVE ( ( 1.000000000000033085, 0.9510565162951203355, 1.000000000000000000, 0.9510565162951535312, 1.000000000000000000, 0.9510565162951535312, 1.000000000000000000, 0.9510565162951535312, 1.000000000000000000, 0.9510565162951922780, 0.9999999999999612532 ) ) 
 REPRESENTATION_ITEM ( '' )  );
#59198=CARTESIAN_POINT ( 'NONE',  ( -177.6550000000000011, -7.632228543268600340, -2.479861379858950166 ) ) ;
#59208=CARTESIAN_POINT ( 'NONE',  ( -94.55499999999999261, 0.000000000000000000, 8.024999999999991473 ) ) ;
#59215=CARTESIAN_POINT ( 'NONE',  ( -90.05707362346616662, 0.000000000000000000, 9.524999999999991473 ) ) ;
#59219=CARTESIAN_POINT ( 'NONE',  ( -65.24499999999999034, -4.716976649647093289, -6.492361379858945902 ) ) ;
#59223=CARTESIAN_POINT ( 'NONE',  ( -125.3070736234661808, -10.01517768586948698, 6.132527647946031529E-16 ) ) ;
#59229=CARTESIAN_POINT ( 'NONE',  ( -123.2049999999999699, -2.607480562269071545, -8.024999999999991473 ) ) ;
#59232=CARTESIAN_POINT ( 'NONE',  ( -73.34292637653381064, -9.058813317711329915, 2.943386871421371787 ) ) ;
#59235=CARTESIAN_POINT ( 'NONE',  ( -160.6429263765338362, -5.598654528085801552, 7.705886871421367523 ) ) ;
#59238=CARTESIAN_POINT ( 'NONE',  ( -161.4570736234661865, -9.058813317711329915, 2.943386871421371787 ) ) ;
#59241=CARTESIAN_POINT ( 'NONE',  ( -96.95707362346617231, 9.058813317711329915, -2.943386871421373119 ) ) ;
#59249=CARTESIAN_POINT ( 'NONE',  ( -135.8049999999999500, -8.437984349512085203, 5.166775262442717831E-16 ) ) ;
#59253=CARTESIAN_POINT ( 'NONE',  ( -144.2950000000000159, -2.607480562269069768, 8.024999999999991473 ) ) ;
#59254=CARTESIAN_POINT ( 'NONE',  ( -141.5949999999999989, 2.607480562269072433, 8.024999999999991473 ) ) ;
#59255=ORIENTED_EDGE ( 'NONE', *, *, #50771, .F. ) ;
#59259=CARTESIAN_POINT ( 'NONE',  ( -56.00499999999996703, 6.826472737025116366, 4.959722759717898555 ) ) ;
#59261=CARTESIAN_POINT ( 'NONE',  ( -54.29499999999998749, -2.607480562269069768, 8.024999999999991473 ) ) ;
#59266=CARTESIAN_POINT ( 'NONE',  ( -105.2929263765337993, 3.094860106618428031, -9.524999999999993250 ) ) ;
#59268=FACE_OUTER_BOUND ( 'NONE', #39842, .T. ) ;
#59286=CARTESIAN_POINT ( 'NONE',  ( -116.9070736234669994, -3.094860106604782946, 9.525000000009905321 ) ) ;
#59295=CARTESIAN_POINT ( 'NONE',  ( -93.20707362346729496, 3.094860106636853292, 9.524999999986610177 ) ) ;
#59297=CARTESIAN_POINT ( 'NONE',  ( -95.69499999999997897, -8.437984349512085203, 5.166775262442717831E-16 ) ) ;
#59303=CARTESIAN_POINT ( 'NONE',  ( -175.7929263765338987, -3.094860106616613926, 9.525000000001307754 ) ) ;
#59311=DIRECTION ( 'NONE',  ( -1.000000000000000000, -0.000000000000000000, -0.000000000000000000 ) ) ;
#59317=( BOUNDED_CURVE ( )  B_SPLINE_CURVE ( 2, ( #33044, #43632, #39042, #33383, #22136, #54809, #37676, #60441, #59395, #1304, #28414 ),
 .UNSPECIFIED., .F., .F. ) 
 B_SPLINE_CURVE_WITH_KNOTS ( ( 3, 2, 2, 2, 2, 3 ),
 ( 0.5760869565217253685, 0.5782608695652036168, 0.5804347826086817541, 0.5826086956521600024, 0.5847826086956381397, 0.5869565217391164991 ),
 .UNSPECIFIED. ) 
 CURVE ( )  GEOMETRIC_REPRESENTATION_ITEM ( )  RATIONAL_B_SPLINE_CURVE ( ( 1.000000000000309974, 0.9510565162948435569, 1.000000000000000000, 0.9510565162951535312, 1.000000000000000000, 0.9510565162951535312, 1.000000000000000000, 0.9510565162951535312, 1.000000000000000000, 0.9510565162954685015, 0.9999999999996850297 ) ) 
 REPRESENTATION_ITEM ( '' )  );
#59325=CARTESIAN_POINT ( 'NONE',  ( -150.0570736234661808, 0.000000000000000000, 9.524999999999991473 ) ) ;
#59329=CARTESIAN_POINT ( 'NONE',  ( -166.2549999999999955, -4.716976649647092401, 6.492361379858946790 ) ) ;
#59330=DIRECTION ( 'NONE',  ( -1.000000000000000000, -0.000000000000000000, -0.000000000000000000 ) ) ;
#59331=CARTESIAN_POINT ( 'NONE',  ( -148.5570736234661808, -1.166476076187852838E-15, -9.524999999999991473 ) ) ;
#59332=CARTESIAN_POINT ( 'NONE',  ( -173.6949999999999648, -8.437984349512085203, 5.166775262442717831E-16 ) ) ;
#59334=CARTESIAN_POINT ( 'NONE',  ( -167.5449999999999875, -7.632228543268600340, -2.479861379858950166 ) ) ;
#59336=ORIENTED_EDGE ( 'NONE', *, *, #37482, .F. ) ;
#59340=CARTESIAN_POINT ( 'NONE',  ( -80.90499999999995850, 2.607480562269068880, -8.024999999999993250 ) ) ;
#59345=CARTESIAN_POINT ( 'NONE',  ( -82.49499999999997613, 6.826472737025113702, -4.959722759717902107 ) ) ;
#59365=CARTESIAN_POINT ( 'NONE',  ( -151.5570736234661808, -1.166476076187852838E-15, -9.524999999999991473 ) ) ;
#59370=CARTESIAN_POINT ( 'NONE',  ( -114.8049999999999926, -8.437984349512086979, 5.166775262442717831E-16 ) ) ;
#59383=ORIENTED_EDGE ( 'NONE', *, *, #54468, .F. ) ;
#59395=CARTESIAN_POINT ( 'NONE',  ( -104.2429263765338021, 5.598654528085804216, 7.705886871421366635 ) ) ;
#59400=CARTESIAN_POINT ( 'NONE',  ( -51.29292637653378506, 3.094860106618428031, -9.524999999999993250 ) ) ;
#59401=CYLINDRICAL_SURFACE ( 'NONE', #60163, 9.524999999999991473 ) ;
#59402=CARTESIAN_POINT ( 'NONE',  ( -141.5049999999999955, -6.826472737025115478, -4.959722759717899443 ) ) ;
#59415=CARTESIAN_POINT ( 'NONE',  ( -59.45499999999997698, 7.632228543268599452, -2.479861379858951942 ) ) ;
#59431=CARTESIAN_POINT ( 'NONE',  ( -112.1949999999999932, 8.437984349512086979, -1.550032578732815448E-15 ) ) ;
#59433=CARTESIAN_POINT ( 'NONE',  ( -83.84499999999998465, -7.632228543268599452, 2.479861379858951054 ) ) ;
#59443=CARTESIAN_POINT ( 'NONE',  ( -122.3929263765337936, 8.102448949553176405, 5.886773742842740909 ) ) ;
#59444=CARTESIAN_POINT ( 'NONE',  ( -144.7449999999999761, 4.716976649647094177, 6.492361379858945902 ) ) ;
#59459=CARTESIAN_POINT ( 'NONE',  ( -116.5429263765338135, 9.058813317711329915, 2.943386871421369566 ) ) ;
#59463=CARTESIAN_POINT ( 'NONE',  ( -142.4050000000000011, -2.607480562269069768, 8.024999999999991473 ) ) ;
#59478=EDGE_LOOP ( 'NONE', ( #8939, #8002, #36529, #61217 ) ) ;
#59482=CARTESIAN_POINT ( 'NONE',  ( -61.25499999999998835, -4.716976649647092401, 6.492361379858946790 ) ) ;
#59483=CARTESIAN_POINT ( 'NONE',  ( -121.6449999999999960, 4.716976649647091513, -6.492361379858946790 ) ) ;
#59497=CARTESIAN_POINT ( 'NONE',  ( -175.2549999999999955, -4.716976649647092401, 6.492361379858946790 ) ) ;
#59503=CYLINDRICAL_SURFACE ( 'NONE', #20665, 9.524999999999991473 ) ;
#59508=CARTESIAN_POINT ( 'NONE',  ( -89.15499999999998693, 7.632228543268600340, 2.479861379858949277 ) ) ;
#59516=CARTESIAN_POINT ( 'NONE',  ( -65.00707362346616947, -8.102448949553172852, -5.886773742842741797 ) ) ;
#59523=CARTESIAN_POINT ( 'NONE',  ( -102.9549999999999841, -7.632228543268599452, 2.479861379858951054 ) ) ;
#59525=CARTESIAN_POINT ( 'NONE',  ( -121.1949999999999790, 8.437984349512085203, -1.550032578732815448E-15 ) ) ;
#59533=CARTESIAN_POINT ( 'NONE',  ( -156.2929263765338135, 3.094860106618428031, -9.524999999999993250 ) ) ;
#59534=CARTESIAN_POINT ( 'NONE',  ( -178.7949999999999875, 2.607480562269068880, -8.024999999999993250 ) ) ;
#59544=CARTESIAN_POINT ( 'NONE',  ( -79.49292637653380211, -8.102448949553172852, 5.886773742842742685 ) ) ;
#59551=EDGE_CURVE ( 'NONE', #25953, #66309, #58310, .T. ) ;
#59553=CARTESIAN_POINT ( 'NONE',  ( -167.1550000000000011, 7.632228543268600340, 2.479861379858949277 ) ) ;
#59564=AXIS2_PLACEMENT_3D ( 'NONE', #3556, #62346, #29647 ) ;
#59567=CARTESIAN_POINT ( 'NONE',  ( -88.70499999999998408, 2.607480562269072433, 8.024999999999991473 ) ) ;
#59571=CARTESIAN_POINT ( 'NONE',  ( -92.90707362346728360, -3.094860106600009875, 9.525000000013374546 ) ) ;
#59578=CARTESIAN_POINT ( 'NONE',  ( -63.89499999999998181, 6.826472737025116366, 4.959722759717898555 ) ) ;
#59580=ORIENTED_EDGE ( 'NONE', *, *, #23485, .F. ) ;
#59589=CARTESIAN_POINT ( 'NONE',  ( -112.5549999999999926, 0.000000000000000000, 8.024999999999991473 ) ) ;
#59595=CYLINDRICAL_SURFACE ( 'NONE', #7536, 7.499999999999985789 ) ;
#59596=CARTESIAN_POINT ( 'NONE',  ( -153.5070736234661979, 8.102448949553176405, 5.886773742842740909 ) ) ;
#59599=CARTESIAN_POINT ( 'NONE',  ( -91.85707362346617799, -5.598654528085803328, -7.705886871421366635 ) ) ;
#59609=CARTESIAN_POINT ( 'NONE',  ( -129.9549999999999841, -7.632228543268599452, 2.479861379858951054 ) ) ;
#59610=CARTESIAN_POINT ( 'NONE',  ( -86.60707362346619220, -8.102448949553174629, 5.886773742842742685 ) ) ;
#59611=CARTESIAN_POINT ( 'NONE',  ( -142.6449999999999818, 4.716976649647091513, -6.492361379858946790 ) ) ;
#59612=CARTESIAN_POINT ( 'NONE',  ( -134.6950000000000500, -8.437984349512086979, 5.166775262442717831E-16 ) ) ;
#59613=VECTOR ( 'NONE', #33342, 1000.000000000000000 ) ;
#59619=CARTESIAN_POINT ( 'NONE',  ( -56.90499999999998693, 2.607480562269068880, -8.024999999999993250 ) ) ;
#59620=( BOUNDED_CURVE ( )  B_SPLINE_CURVE ( 2, ( #60645, #12461, #35333, #28275, #7889, #23048, #18464, #28978, #50468, #23375, #39947 ),
 .UNSPECIFIED., .F., .F. ) 
 B_SPLINE_CURVE_WITH_KNOTS ( ( 3, 2, 2, 2, 2, 3 ),
 ( 0.2608695652173851909, 0.2630434782608633837, 0.2652173913043416320, 0.2673913043478198803, 0.2695652173912980731, 0.2717391304347762659 ),
 .UNSPECIFIED. ) 
 CURVE ( )  GEOMETRIC_REPRESENTATION_ITEM ( )  RATIONAL_B_SPLINE_CURVE ( ( 1.000000000000137446, 0.9510565162950160856, 1.000000000000000000, 0.9510565162951535312, 1.000000000000000000, 0.9510565162951535312, 1.000000000000000000, 0.9510565162951535312, 1.000000000000000000, 0.9510565162952959728, 0.9999999999998575584 ) ) 
 REPRESENTATION_ITEM ( '' )  );
#59622=CARTESIAN_POINT ( 'NONE',  ( -60.74499999999997613, 4.716976649647094177, 6.492361379858945902 ) ) ;
#59623=EDGE_CURVE ( 'NONE', #1575, #64348, #60752, .T. ) ;
#59624=CARTESIAN_POINT ( 'NONE',  ( -139.6429263765338078, -5.598654528085801552, 7.705886871421367523 ) ) ;
#59629=CARTESIAN_POINT ( 'NONE',  ( -101.9929263765338021, 8.102448949553171076, -5.886773742842744461 ) ) ;
#59650=MECHANICAL_DESIGN_GEOMETRIC_PRESENTATION_REPRESENTATION('',(#52952),#31586);
#59659=CARTESIAN_POINT ( 'NONE',  ( -88.79499999999998749, 2.607480562269068880, -8.024999999999993250 ) ) ;
#59671=FACE_OUTER_BOUND ( 'NONE', #2117, .T. ) ;
#59673=CARTESIAN_POINT ( 'NONE',  ( -166.5570736234661808, -1.166476076187852838E-15, -9.524999999999991473 ) ) ;
#59674=CARTESIAN_POINT ( 'NONE',  ( -195.0000000000000000, 0.000000000000000000, 0.000000000000000000 ) ) ;
#59684=CARTESIAN_POINT ( 'NONE',  ( -161.2429263765338021, 5.598654528085804216, 7.705886871421366635 ) ) ;
#59686=CARTESIAN_POINT ( 'NONE',  ( -149.1570736234661751, -9.058813317711329915, -2.943386871421370898 ) ) ;
#59688=VERTEX_POINT ( 'NONE', #32632 ) ;
#59690=CARTESIAN_POINT ( 'NONE',  ( -168.6550000000000011, -7.632228543268600340, -2.479861379858950166 ) ) ;
#59694=CARTESIAN_POINT ( 'NONE',  ( -177.1450000000000102, -4.716976649647092401, 6.492361379858946790 ) ) ;
#59695=CARTESIAN_POINT ( 'NONE',  ( -169.6449999999999818, 4.716976649647091513, -6.492361379858946790 ) ) ;
#59704=CARTESIAN_POINT ( 'NONE',  ( -83.90500000000000114, 2.607480562269068880, -8.024999999999993250 ) ) ;
#59709=CARTESIAN_POINT ( 'NONE',  ( -78.14499999999999602, -4.716976649647092401, 6.492361379858946790 ) ) ;
#59734=EDGE_CURVE ( 'NONE', #57680, #47261, #44293, .T. ) ;
#59739=CARTESIAN_POINT ( 'NONE',  ( -113.1549999999999869, 7.632228543268600340, 2.479861379858949277 ) ) ;
#59740=EDGE_LOOP ( 'NONE', ( #33639, #28501, #30268, #31045 ) ) ;
#59746=EDGE_LOOP ( 'NONE', ( #37021, #44167 ) ) ;
#59754=CARTESIAN_POINT ( 'NONE',  ( -117.6570736234661894, 9.058813317711329915, 2.943386871421369566 ) ) ;
#59760=CYLINDRICAL_SURFACE ( 'NONE', #60225, 9.524999999999991473 ) ;
#59761=VECTOR ( 'NONE', #15257, 1000.000000000000000 ) ;
#59767=CARTESIAN_POINT ( 'NONE',  ( -48.89292637653380780, -8.102448949553172852, -5.886773742842741797 ) ) ;
#59772=CARTESIAN_POINT ( 'NONE',  ( -139.1049999999999898, -6.826472737025115478, 4.959722759717900331 ) ) ;
#59784=CARTESIAN_POINT ( 'NONE',  ( -195.0000000000000000, 0.000000000000000000, 0.000000000000000000 ) ) ;
#59785=CARTESIAN_POINT ( 'NONE',  ( -108.8929263765338078, -8.102448949553174629, -5.886773742842741797 ) ) ;
#59786=CARTESIAN_POINT ( 'NONE',  ( -57.35499999999998977, -4.716976649647093289, -6.492361379858945902 ) ) ;
#59801=EDGE_CURVE ( 'NONE', #62258, #58402, #28374, .T. ) ;
#59803=CARTESIAN_POINT ( 'NONE',  ( -108.7449999999999903, 4.716976649647094177, 6.492361379858945902 ) ) ;
#59805=CARTESIAN_POINT ( 'NONE',  ( -88.19499999999996476, 8.437984349512085203, -1.550032578732815448E-15 ) ) ;
#59812=CARTESIAN_POINT ( 'NONE',  ( -126.4429263765338192, -1.166476076187852838E-15, -9.524999999999991473 ) ) ;
#59814=CARTESIAN_POINT ( 'NONE',  ( -146.2449999999999761, -4.716976649647093289, -6.492361379858945902 ) ) ;
#59827=CARTESIAN_POINT ( 'NONE',  ( -151.4929263765338021, -8.102448949553174629, 5.886773742842742685 ) ) ;
#59829=CARTESIAN_POINT ( 'NONE',  ( -141.6550000000000011, -7.632228543268600340, -2.479861379858950166 ) ) ;
#59847=CARTESIAN_POINT ( 'NONE',  ( -57.50499999999997414, -6.826472737025113702, -4.959722759717900331 ) ) ;
#59848=CARTESIAN_POINT ( 'NONE',  ( -117.2949999999999875, -2.607480562269069768, 8.024999999999991473 ) ) ;
#59861=CARTESIAN_POINT ( 'NONE',  ( -172.4050000000000296, -2.607480562269069768, 8.024999999999991473 ) ) ;
#59862=ORIENTED_EDGE ( 'NONE', *, *, #66654, .F. ) ;
#59869=CARTESIAN_POINT ( 'NONE',  ( -89.30499999999999261, 8.437984349512085203, -1.550032578732815448E-15 ) ) ;
#59874=CARTESIAN_POINT ( 'NONE',  ( -63.20707362346617231, 3.094860106618433360, 9.524999999999991473 ) ) ;
#59875=ORIENTED_EDGE ( 'NONE', *, *, #17189, .T. ) ;
#59879=CARTESIAN_POINT ( 'NONE',  ( -106.8549999999999898, 4.716976649647094177, 6.492361379858945902 ) ) ;
#59883=CARTESIAN_POINT ( 'NONE',  ( -119.0949999999999847, -2.607480562269071545, -8.024999999999991473 ) ) ;
#59889=CARTESIAN_POINT ( 'NONE',  ( -155.8429263765337964, 9.058813317711329915, -2.943386871421373119 ) ) ;
#59892=CARTESIAN_POINT ( 'NONE',  ( -177.2950000000000159, -2.607480562269069768, 8.024999999999991473 ) ) ;
#59896=VERTEX_POINT ( 'NONE', #47320 ) ;
#59899=CARTESIAN_POINT ( 'NONE',  ( -65.09292637653379643, 3.094860106618433360, 9.524999999999991473 ) ) ;
#59908=CARTESIAN_POINT ( 'NONE',  ( -165.3549999999999898, -4.716976649647093289, -6.492361379858945902 ) ) ;
#59920=CARTESIAN_POINT ( 'NONE',  ( -80.00499999999999545, 6.826472737025115478, 4.959722759717899443 ) ) ;
#59925=ORIENTED_EDGE ( 'NONE', *, *, #29632, .F. ) ;
#59929=CARTESIAN_POINT ( 'NONE',  ( -60.14499999999998892, -4.716976649647092401, 6.492361379858946790 ) ) ;
#59940=CARTESIAN_POINT ( 'NONE',  ( -113.4549999999999841, 7.632228543268599452, -2.479861379858951942 ) ) ;
#59948=CARTESIAN_POINT ( 'NONE',  ( -147.0570736234661808, 0.000000000000000000, 9.524999999999991473 ) ) ;
#59953=CARTESIAN_POINT ( 'NONE',  ( -90.95707362346617231, 9.058813317711329915, -2.943386871421373119 ) ) ;
#59963=CARTESIAN_POINT ( 'NONE',  ( -129.0549999999999784, -9.827790563157499189E-16, -8.024999999999991473 ) ) ;
#59964=EDGE_CURVE ( 'NONE', #4472, #57125, #20891, .T. ) ;
#59966=CARTESIAN_POINT ( 'NONE',  ( -54.44292637653380496, -1.166476076187852838E-15, -9.524999999999991473 ) ) ;
#59967=CARTESIAN_POINT ( 'NONE',  ( -148.4950000000000045, 6.826472737025113702, -4.959722759717902107 ) ) ;
#59970=CARTESIAN_POINT ( 'NONE',  ( -127.6450000000000102, 4.716976649647091513, -6.492361379858946790 ) ) ;
#59976=CARTESIAN_POINT ( 'NONE',  ( -184.6429263765338078, -5.598654528085801552, 7.705886871421367523 ) ) ;
#59977=CARTESIAN_POINT ( 'NONE',  ( 0.000000000000000000, 0.000000000000000000, 0.000000000000000000 ) ) ;
#59978=CARTESIAN_POINT ( 'NONE',  ( -54.59499999999997044, 2.607480562269073321, 8.024999999999991473 ) ) ;
#59979=CARTESIAN_POINT ( 'NONE',  ( -43.99999999999998579, 0.000000000000000000, 11.99999999999999467 ) ) ;
#59981=CARTESIAN_POINT ( 'NONE',  ( -75.65707362346617515, 9.058813317711329915, 2.943386871421369566 ) ) ;
#59982=CARTESIAN_POINT ( 'NONE',  ( -93.74292637653380211, -5.598654528085803328, -7.705886871421366635 ) ) ;
#59986=CARTESIAN_POINT ( 'NONE',  ( -163.2570736234661695, 5.598654528085800663, -7.705886871421367523 ) ) ;
#60012=CARTESIAN_POINT ( 'NONE',  ( -90.89499999999999602, 6.826472737025116366, 4.959722759717898555 ) ) ;
#60019=CARTESIAN_POINT ( 'NONE',  ( -175.3429263765338249, -9.058813317711329915, 2.943386871421371787 ) ) ;
#60032=CARTESIAN_POINT ( 'NONE',  ( -182.7570736234661979, -5.598654528085801552, 7.705886871421367523 ) ) ;
#60040=CARTESIAN_POINT ( 'NONE',  ( -161.0929263765340806, 3.094860106623507967, 9.524999999996303757 ) ) ;
#60045=CARTESIAN_POINT ( 'NONE',  ( -156.9549999999999841, -7.632228543268599452, 2.479861379858951054 ) ) ;
#60048=CARTESIAN_POINT ( 'NONE',  ( -177.4449999999999932, 0.000000000000000000, 8.024999999999991473 ) ) ;
#60050=CARTESIAN_POINT ( 'NONE',  ( -157.9449999999999932, -9.827790563157499189E-16, -8.024999999999991473 ) ) ;
#60055=CARTESIAN_POINT ( 'NONE',  ( -195.0000000000000000, 0.000000000000000000, 9.524999999999991473 ) ) ;
#60056=CARTESIAN_POINT ( 'NONE',  ( -75.20499999999995566, -2.607480562269071545, -8.024999999999991473 ) ) ;
#60059=CARTESIAN_POINT ( 'NONE',  ( -81.89499999999998181, 6.826472737025115478, 4.959722759717899443 ) ) ;
#60061=CARTESIAN_POINT ( 'NONE',  ( -134.3070736234661524, -10.01517768586948698, 6.132527647946031529E-16 ) ) ;
#60067=DIRECTION ( 'NONE',  ( -1.000000000000000000, -0.000000000000000000, -0.000000000000000000 ) ) ;
#60075=CYLINDRICAL_SURFACE ( 'NONE', #29620, 9.524999999999991473 ) ;
#60086=CARTESIAN_POINT ( 'NONE',  ( -110.7549999999999955, 4.716976649647091513, -6.492361379858946790 ) ) ;
#60090=ORIENTED_EDGE ( 'NONE', *, *, #34394, .F. ) ;
#60092=ORIENTED_EDGE ( 'NONE', *, *, #20545, .T. ) ;
#60099=CARTESIAN_POINT ( 'NONE',  ( -117.0570736234661808, 0.000000000000000000, 9.524999999999991473 ) ) ;
#60120=CARTESIAN_POINT ( 'NONE',  ( -138.3550000000000182, -4.716976649647093289, -6.492361379858945902 ) ) ;
#60126=CARTESIAN_POINT ( 'NONE',  ( -105.5929263765348054, -3.094860106635102692, -9.524999999987880273 ) ) ;
#60127=CARTESIAN_POINT ( 'NONE',  ( -157.4929263765337737, -8.102448949553174629, 5.886773742842742685 ) ) ;
#60132=CARTESIAN_POINT ( 'NONE',  ( -52.55707362346618083, -1.166476076187852838E-15, -9.524999999999991473 ) ) ;
#60133=CARTESIAN_POINT ( 'NONE',  ( -55.10499999999998266, -6.826472737025115478, 4.959722759717900331 ) ) ;
#60138=CARTESIAN_POINT ( 'NONE',  ( -195.0000000000000000, 0.000000000000000000, 0.000000000000000000 ) ) ;
#60142=CARTESIAN_POINT ( 'NONE',  ( -97.94292637653380496, 0.000000000000000000, 9.524999999999991473 ) ) ;
#60147=ADVANCED_FACE ( 'NONE', ( #19043 ), #7810, .T. ) ;
#60150=CARTESIAN_POINT ( 'NONE',  ( -113.5449999999999875, -7.632228543268600340, -2.479861379858950166 ) ) ;
#60152=CARTESIAN_POINT ( 'NONE',  ( -74.69499999999997897, -8.437984349512085203, 5.166775262442717831E-16 ) ) ;
#60160=ORIENTED_EDGE ( 'NONE', *, *, #59551, .T. ) ;
#60161=CARTESIAN_POINT ( 'NONE',  ( -121.9429263765338050, 0.000000000000000000, 9.524999999999991473 ) ) ;
#60162=CARTESIAN_POINT ( 'NONE',  ( -151.7949999999999591, 2.607480562269068880, -8.024999999999993250 ) ) ;
#60163=AXIS2_PLACEMENT_3D ( 'NONE', #1312, #6627, #55533 ) ;
#60164=CARTESIAN_POINT ( 'NONE',  ( -47.54499999999997328, -7.632228543268600340, -2.479861379858950166 ) ) ;
#60172=CARTESIAN_POINT ( 'NONE',  ( -130.8570736234661922, -5.598654528085803328, -7.705886871421366635 ) ) ;
#60176=CARTESIAN_POINT ( 'NONE',  ( -145.8549999999999898, 4.716976649647094177, 6.492361379858945902 ) ) ;
#60193=CARTESIAN_POINT ( 'NONE',  ( -51.80499999999997840, -8.437984349512086979, 5.166775262442717831E-16 ) ) ;
#60208=DIRECTION ( 'NONE',  ( -1.000000000000000000, -0.000000000000000000, -0.000000000000000000 ) ) ;
#60209=CARTESIAN_POINT ( 'NONE',  ( -168.2050000000000125, -2.607480562269071545, -8.024999999999991473 ) ) ;
#60217=CARTESIAN_POINT ( 'NONE',  ( -77.69292637653380496, 10.01517768586948698, -1.839758294383808966E-15 ) ) ;
#60218=ORIENTED_EDGE ( 'NONE', *, *, #44010, .F. ) ;
#60222=CARTESIAN_POINT ( 'NONE',  ( -81.35499999999998977, -4.716976649647093289, -6.492361379858945902 ) ) ;
#60225=AXIS2_PLACEMENT_3D ( 'NONE', #49221, #43977, #22479 ) ;
#60229=CARTESIAN_POINT ( 'NONE',  ( -55.55707362346618083, -1.166476076187852838E-15, -9.524999999999991473 ) ) ;
#60238=CARTESIAN_POINT ( 'NONE',  ( -110.5449999999999875, -7.632228543268600340, -2.479861379858950166 ) ) ;
#60241=EDGE_CURVE ( 'NONE', #37066, #44394, #67995, .T. ) ;
#60244=CARTESIAN_POINT ( 'NONE',  ( -16.31125505495063166, 10.98243589408808951, -4.836450918052216608 ) ) ;
#60245=CARTESIAN_POINT ( 'NONE',  ( -153.8929263765338362, -8.102448949553172852, -5.886773742842741797 ) ) ;
#60247=CARTESIAN_POINT ( 'NONE',  ( -178.1949999999999648, 8.437984349512085203, -1.550032578732815448E-15 ) ) ;
#60251=ORIENTED_EDGE ( 'NONE', *, *, #49300, .T. ) ;
#60252=CARTESIAN_POINT ( 'NONE',  ( -67.49292637653380211, -8.102448949553172852, 5.886773742842742685 ) ) ;
#60256=CARTESIAN_POINT ( 'NONE',  ( -79.79292637653379927, -3.094860106618429807, 9.524999999999991473 ) ) ;
#60259=CARTESIAN_POINT ( 'NONE',  ( -173.6049999999999898, 6.826472737025113702, -4.959722759717902107 ) ) ;
#60262=CARTESIAN_POINT ( 'NONE',  ( -112.3429263765337964, -9.058813317711329915, 2.943386871421371787 ) ) ;
#60272=CARTESIAN_POINT ( 'NONE',  ( -86.75499999999998124, 4.716976649647091513, -6.492361379858946790 ) ) ;
#60281=CARTESIAN_POINT ( 'NONE',  ( -141.0570736234661808, 0.000000000000000000, 9.524999999999991473 ) ) ;
#60282=CARTESIAN_POINT ( 'NONE',  ( -66.29500000000000171, -2.607480562269069768, 8.024999999999991473 ) ) ;
#60286=CARTESIAN_POINT ( 'NONE',  ( -49.19292637653380496, -10.01517768586948698, 6.132527647946031529E-16 ) ) ;
#60294=CARTESIAN_POINT ( 'NONE',  ( -110.7549999999999955, 4.716976649647091513, -6.492361379858946790 ) ) ;
#60299=CARTESIAN_POINT ( 'NONE',  ( -148.4070736234661751, 3.094860106618428031, -9.524999999999993250 ) ) ;
#60301=CARTESIAN_POINT ( 'NONE',  ( -83.00707362346614104, -8.102448949553172852, -5.886773742842741797 ) ) ;
#60307=CARTESIAN_POINT ( 'NONE',  ( -127.8549999999999898, 4.716976649647094177, 6.492361379858945902 ) ) ;
#60312=CARTESIAN_POINT ( 'NONE',  ( -142.0449999999999875, 7.632228543268600340, 2.479861379858949277 ) ) ;
#60314=CARTESIAN_POINT ( 'NONE',  ( -130.7949999999999875, 2.607480562269069324, -8.024999999999993250 ) ) ;
#60316=FACE_OUTER_BOUND ( 'NONE', #22989, .T. ) ;
#60319=CARTESIAN_POINT ( 'NONE',  ( -181.7929263765337566, -3.094860106618429807, 9.524999999999991473 ) ) ;
#60320=CARTESIAN_POINT ( 'NONE',  ( -54.14499999999999602, -4.716976649647092401, 6.492361379858946790 ) ) ;
#60325=CARTESIAN_POINT ( 'NONE',  ( -75.05707362346616662, 0.000000000000000000, 9.524999999999991473 ) ) ;
#60326=CARTESIAN_POINT ( 'NONE',  ( -92.39292637653379359, 8.102448949553176405, 5.886773742842740909 ) ) ;
#60329=CARTESIAN_POINT ( 'NONE',  ( -195.0000000000000000, 0.000000000000000000, 0.000000000000000000 ) ) ;
#60349=CARTESIAN_POINT ( 'NONE',  ( -93.80707362346615241, 10.01517768586948698, -1.839758294383808966E-15 ) ) ;
#60350=EDGE_CURVE ( 'NONE', #50251, #58449, #69680, .T. ) ;
#60353=CARTESIAN_POINT ( 'NONE',  ( -92.54499999999998749, -7.632228543268600340, -2.479861379858950166 ) ) ;
#60357=EDGE_CURVE ( 'NONE', #42918, #23561, #5999, .T. ) ;
#60372=CARTESIAN_POINT ( 'NONE',  ( -179.0070736234661410, -8.102448949553172852, -5.886773742842741797 ) ) ;
#60374=CARTESIAN_POINT ( 'NONE',  ( -84.35707362346617799, 5.598654528085804216, 7.705886871421366635 ) ) ;
#60376=CARTESIAN_POINT ( 'NONE',  ( -48.20707362346615099, 3.094860106618433360, 9.524999999999991473 ) ) ;
#60379=VERTEX_POINT ( 'NONE', #48967 ) ;
#60380=CARTESIAN_POINT ( 'NONE',  ( -158.9050000000000011, 2.607480562269068880, -8.024999999999993250 ) ) ;
#60382=CARTESIAN_POINT ( 'NONE',  ( -183.8192599248787076, -8.214053869287363696, -2.901243250066394719 ) ) ;
#60383=CARTESIAN_POINT ( 'NONE',  ( -171.4449999999999932, 0.000000000000000000, 8.024999999999991473 ) ) ;
#60384=CARTESIAN_POINT ( 'NONE',  ( -156.2949999999999591, -2.607480562269069768, 8.024999999999991473 ) ) ;
#60386=CYLINDRICAL_SURFACE ( 'NONE', #58283, 9.524999999999991473 ) ;
#60390=CARTESIAN_POINT ( 'NONE',  ( -76.70499999999999829, 2.607480562269073321, 8.024999999999991473 ) ) ;
#60394=CARTESIAN_POINT ( 'NONE',  ( -71.54499999999998749, -7.632228543268600340, -2.479861379858950166 ) ) ;
#60417=CARTESIAN_POINT ( 'NONE',  ( -114.5049999999999955, -6.826472737025113702, -4.959722759717900331 ) ) ;
#60422=CARTESIAN_POINT ( 'NONE',  ( -56.84292637653378932, 9.058813317711329915, -2.943386871421373119 ) ) ;
#60425=EDGE_CURVE ( 'NONE', #57659, #49213, #18051, .T. ) ;
#60432=CARTESIAN_POINT ( 'NONE',  ( -152.0070736234661695, -8.102448949553174629, -5.886773742842741797 ) ) ;
#60435=VERTEX_POINT ( 'NONE', #34122 ) ;
#60437=CARTESIAN_POINT ( 'NONE',  ( -195.0000000000000000, 0.000000000000000000, 0.000000000000000000 ) ) ;
#60441=CARTESIAN_POINT ( 'NONE',  ( -104.3929263765338078, 8.102448949553176405, 5.886773742842740909 ) ) ;
#60445=CARTESIAN_POINT ( 'NONE',  ( -48.29292637653378506, 3.094860106618428031, -9.524999999999993250 ) ) ;
#60448=CARTESIAN_POINT ( 'NONE',  ( -130.7049999999999841, 2.607480562269073321, 8.024999999999991473 ) ) ;
#60459=CARTESIAN_POINT ( 'NONE',  ( -109.0429263765337993, -9.058813317711329915, -2.943386871421370898 ) ) ;
#60460=CARTESIAN_POINT ( 'NONE',  ( -57.05499999999999261, -9.827790563157499189E-16, -8.024999999999991473 ) ) ;
#60463=CARTESIAN_POINT ( 'NONE',  ( -183.2949999999999591, -2.607480562269069768, 8.024999999999991473 ) ) ;
#60474=CARTESIAN_POINT ( 'NONE',  ( -97.94499999999999318, -9.827790563157499189E-16, -8.024999999999991473 ) ) ;
#60476=CARTESIAN_POINT ( 'NONE',  ( -76.94499999999997897, -9.827790563157499189E-16, -8.024999999999991473 ) ) ;
#60480=FACE_OUTER_BOUND ( 'NONE', #24258, .T. ) ;
#60482=CARTESIAN_POINT ( 'NONE',  ( -122.9929263765338163, 8.102448949553171076, -5.886773742842744461 ) ) ;
#60483=CARTESIAN_POINT ( 'NONE',  ( -140.6949999999999363, -8.437984349512085203, 5.166775262442717831E-16 ) ) ;
#60489=CARTESIAN_POINT ( 'NONE',  ( -174.4429263765337907, -1.166476076187852838E-15, -9.524999999999991473 ) ) ;
#60495=CARTESIAN_POINT ( 'NONE',  ( -99.05707362346618083, 0.000000000000000000, 9.524999999999991473 ) ) ;
#60499=CARTESIAN_POINT ( 'NONE',  ( -145.4050000000000011, -2.607480562269069768, 8.024999999999991473 ) ) ;
#60511=CARTESIAN_POINT ( 'NONE',  ( -54.65499999999997982, -7.632228543268600340, -2.479861379858950166 ) ) ;
#60518=CYLINDRICAL_SURFACE ( 'NONE', #652, 9.524999999999991473 ) ;
#60529=CARTESIAN_POINT ( 'NONE',  ( -160.7049999999999841, 2.607480562269073321, 8.024999999999991473 ) ) ;
#60530=ORIENTED_EDGE ( 'NONE', *, *, #66817, .F. ) ;
#60542=CARTESIAN_POINT ( 'NONE',  ( -87.95499999999999829, -7.632228543268599452, 2.479861379858951054 ) ) ;
#60553=CARTESIAN_POINT ( 'NONE',  ( -102.1449999999999818, -4.716976649647092401, 6.492361379858946790 ) ) ;
#60556=CARTESIAN_POINT ( 'NONE',  ( -16.30670699309780503, 10.98201309903883072, 4.837397118674712893 ) ) ;
#60559=CARTESIAN_POINT ( 'NONE',  ( -155.5429263765338135, 9.058813317711329915, 2.943386871421369566 ) ) ;
#60561=CARTESIAN_POINT ( 'NONE',  ( -163.4949999999999761, 6.826472737025113702, -4.959722759717902107 ) ) ;
#60569=CARTESIAN_POINT ( 'NONE',  ( -65.84292637653379643, 9.058813317711329915, -2.943386871421373119 ) ) ;
#60582=CARTESIAN_POINT ( 'NONE',  ( -170.4549999999999841, 7.632228543268599452, -2.479861379858951942 ) ) ;
#60584=CARTESIAN_POINT ( 'NONE',  ( -111.8929263765338078, -8.102448949553174629, -5.886773742842741797 ) ) ;
#60591=CARTESIAN_POINT ( 'NONE',  ( -82.85499999999998977, 4.716976649647094177, 6.492361379858945902 ) ) ;
#60595=CARTESIAN_POINT ( 'NONE',  ( -195.0000000000000000, 0.000000000000000000, 0.000000000000000000 ) ) ;
#60597=CARTESIAN_POINT ( 'NONE',  ( -126.5929263765345496, -3.094860106630666241, -9.524999999991102584 ) ) ;
#60600=CARTESIAN_POINT ( 'NONE',  ( -112.8570736234661638, -5.598654528085803328, -7.705886871421366635 ) ) ;
#60607=CARTESIAN_POINT ( 'NONE',  ( -59.09499999999997044, -2.607480562269071545, -8.024999999999991473 ) ) ;
#60608=ORIENTED_EDGE ( 'NONE', *, *, #56629, .T. ) ;
#60610=CARTESIAN_POINT ( 'NONE',  ( -139.4070736234667152, 3.094860106609554684, -9.525000000006441425 ) ) ;
#60614=CARTESIAN_POINT ( 'NONE',  ( -54.74499999999999034, 4.716976649647094177, 6.492361379858945902 ) ) ;
#60618=CARTESIAN_POINT ( 'NONE',  ( -109.5549999999999926, 0.000000000000000000, 8.024999999999991473 ) ) ;
#60624=LINE ( 'NONE', #6825, #57792 ) ;
#60627=CARTESIAN_POINT ( 'NONE',  ( -149.1570736234661751, -9.058813317711329915, -2.943386871421370898 ) ) ;
#60630=CARTESIAN_POINT ( 'NONE',  ( -84.80707362346616662, 10.01517768586948698, -1.839758294383808571E-15 ) ) ;
#60638=CARTESIAN_POINT ( 'NONE',  ( -131.9050000000000011, 2.607480562269068880, -8.024999999999993250 ) ) ;
#60639=CARTESIAN_POINT ( 'NONE',  ( -164.9929263765338021, 8.102448949553172852, -5.886773742842744461 ) ) ;
#60640=CARTESIAN_POINT ( 'NONE',  ( -132.8950000000000102, 6.826472737025116366, 4.959722759717898555 ) ) ;
#60642=CARTESIAN_POINT ( 'NONE',  ( -132.1449999999999818, -4.716976649647092401, 6.492361379858946790 ) ) ;
#60645=CARTESIAN_POINT ( 'NONE',  ( -147.0570736234661808, 0.000000000000000000, 9.524999999999991473 ) ) ;
#60650=CARTESIAN_POINT ( 'NONE',  ( -49.10499999999998977, -6.826472737025115478, 4.959722759717900331 ) ) ;
#60651=CARTESIAN_POINT ( 'NONE',  ( -61.34499999999998465, 7.632228543268599452, -2.479861379858951942 ) ) ;
#60658=CARTESIAN_POINT ( 'NONE',  ( -97.64292637653380780, -5.598654528085801552, 7.705886871421367523 ) ) ;
#60662=CYLINDRICAL_SURFACE ( 'NONE', #42835, 9.524999999999991473 ) ;
#60663=CIRCLE ( 'NONE', #31496, 9.524999999999991473 ) ;
#60672=CARTESIAN_POINT ( 'NONE',  ( -1.000000000000028644, 1.469576158976823553E-15, -11.99999999999999645 ) ) ;
#60686=CARTESIAN_POINT ( 'NONE',  ( -119.0070736234661695, -8.102448949553174629, -5.886773742842741797 ) ) ;
#60690=CARTESIAN_POINT ( 'NONE',  ( -89.54499999999998749, -7.632228543268600340, -2.479861379858950166 ) ) ;
#60708=CARTESIAN_POINT ( 'NONE',  ( -181.7070736234661865, -3.094860106618431139, -9.524999999999991473 ) ) ;
#60712=CARTESIAN_POINT ( 'NONE',  ( -112.5570736234661808, -1.166476076187852838E-15, -9.524999999999991473 ) ) ;
#60720=CARTESIAN_POINT ( 'NONE',  ( -157.2549999999999955, -4.716976649647092401, 6.492361379858946790 ) ) ;
#60723=CARTESIAN_POINT ( 'NONE',  ( -163.9449999999999932, -9.827790563157499189E-16, -8.024999999999991473 ) ) ;
#60724=CARTESIAN_POINT ( 'NONE',  ( -153.5949999999999704, 2.607480562269072433, 8.024999999999991473 ) ) ;
#60728=CARTESIAN_POINT ( 'NONE',  ( -77.30499999999996419, 8.437984349512085203, -1.550032578732815448E-15 ) ) ;
#60733=CARTESIAN_POINT ( 'NONE',  ( -71.99499999999999034, -6.826472737025113702, 4.959722759717902107 ) ) ;
#60739=B_SPLINE_CURVE_WITH_KNOTS ( 'NONE', 3,
 ( #29766, #40013, #61405, #13221, #67060, #56133, #50878, #2636, #24135, #13570, #13932, #35743 ),
 .UNSPECIFIED., .F., .F.,
 ( 4, 2, 2, 2, 2, 4 ),
 ( 2.969228936714856331E-16, 0.002162875435572643792, 0.003244313153358819105, 0.004325750871144991815, 0.006488626306717332030, 0.008651501742289673114 ),
 .UNSPECIFIED. ) ;
#60752=( BOUNDED_CURVE ( )  B_SPLINE_CURVE ( 2, ( #57301, #20719, #47138 ),
 .UNSPECIFIED., .F., .F. ) 
 B_SPLINE_CURVE_WITH_KNOTS ( ( 3, 3 ),
 ( 0.9891304347826086474, 0.9913043478260870067 ),
 .UNSPECIFIED. ) 
 CURVE ( )  GEOMETRIC_REPRESENTATION_ITEM ( )  RATIONAL_B_SPLINE_CURVE ( ( 1.000000000000000000, 0.9510565162951535312, 1.000000000000000000 ) ) 
 REPRESENTATION_ITEM ( '' )  );
#60759=CARTESIAN_POINT ( 'NONE',  ( -105.3549999999999898, -4.716976649647093289, -6.492361379858945902 ) ) ;
#60788=CARTESIAN_POINT ( 'NONE',  ( -133.8549999999999898, 4.716976649647094177, 6.492361379858945902 ) ) ;
#60799=CARTESIAN_POINT ( 'NONE',  ( -109.1929263765337907, -10.01517768586948698, 6.132527647946031529E-16 ) ) ;
#60807=CARTESIAN_POINT ( 'NONE',  ( -182.5449999999999875, -7.632228543268600340, -2.479861379858950166 ) ) ;
#60822=CARTESIAN_POINT ( 'NONE',  ( -101.9949999999999903, -6.826472737025113702, 4.959722759717902107 ) ) ;
#60824=CARTESIAN_POINT ( 'NONE',  ( -80.39499999999998181, -6.826472737025115478, -4.959722759717899443 ) ) ;
#60836=CARTESIAN_POINT ( 'NONE',  ( -128.0929263765337964, 3.094860106618433360, 9.524999999999991473 ) ) ;
#60838=CARTESIAN_POINT ( 'NONE',  ( -136.9449999999999932, -9.827790563157499189E-16, -8.024999999999991473 ) ) ;
#60850=CARTESIAN_POINT ( 'NONE',  ( -130.5570736234661808, -1.166476076187852838E-15, -9.524999999999991473 ) ) ;
#60855=CARTESIAN_POINT ( 'NONE',  ( -139.7049999999999841, 2.607480562269072433, 8.024999999999991473 ) ) ;
#60870=CARTESIAN_POINT ( 'NONE',  ( -59.30499999999999972, 8.437984349512086979, -1.550032578732815448E-15 ) ) ;
#60882=CARTESIAN_POINT ( 'NONE',  ( -121.5570736234661808, -1.166476076187852838E-15, -9.524999999999991473 ) ) ;
#60884=CARTESIAN_POINT ( 'NONE',  ( -157.7049999999999557, 2.607480562269073321, 8.024999999999991473 ) ) ;
#60890=CARTESIAN_POINT ( 'NONE',  ( -184.0000000000000000, -7.358988424933670558, 3.200923985616050071 ) ) ;
#60896=DIRECTION ( 'NONE',  ( 0.000000000000000000, 0.000000000000000000, 1.000000000000000000 ) ) ;
#60897=CARTESIAN_POINT ( 'NONE',  ( -73.70499999999998408, 2.607480562269073321, 8.024999999999991473 ) ) ;
#60912=CARTESIAN_POINT ( 'NONE',  ( -105.7449999999999903, 4.716976649647094177, 6.492361379858945902 ) ) ;
#60915=CARTESIAN_POINT ( 'NONE',  ( -97.55707362346618083, -1.166476076187852838E-15, -9.524999999999991473 ) ) ;
#60916=CARTESIAN_POINT ( 'NONE',  ( -18.76341613659756646, 11.53760461768462697, 3.307647553967739018 ) ) ;
#60918=CARTESIAN_POINT ( 'NONE',  ( -151.3429263765337964, -9.058813317711329915, 2.943386871421371787 ) ) ;
#60920=CARTESIAN_POINT ( 'NONE',  ( -166.6449999999999818, 4.716976649647091513, -6.492361379858946790 ) ) ;
#60926=DIRECTION ( 'NONE',  ( 0.000000000000000000, 0.000000000000000000, 1.000000000000000000 ) ) ;
#60928=CARTESIAN_POINT ( 'NONE',  ( -69.59292637653381064, -3.094860106618431139, -9.524999999999991473 ) ) ;
#60933=CARTESIAN_POINT ( 'NONE',  ( -169.1049999999999898, -6.826472737025113702, 4.959722759717902107 ) ) ;
#60945=CARTESIAN_POINT ( 'NONE',  ( -81.50499999999999545, -6.826472737025113702, -4.959722759717900331 ) ) ;
#60952=CARTESIAN_POINT ( 'NONE',  ( -127.3429263765337964, -9.058813317711329915, 2.943386871421371787 ) ) ;
#60960=CARTESIAN_POINT ( 'NONE',  ( -50.99499999999999034, -6.826472737025115478, 4.959722759717900331 ) ) ;
#60962=DIRECTION ( 'NONE',  ( -1.000000000000000000, -0.000000000000000000, -0.000000000000000000 ) ) ;
#60964=CARTESIAN_POINT ( 'NONE',  ( -139.1070736234661638, 8.102448949553172852, -5.886773742842744461 ) ) ;
#60968=CARTESIAN_POINT ( 'NONE',  ( -54.59499999999997044, 2.607480562269072433, 8.024999999999991473 ) ) ;
#60973=CARTESIAN_POINT ( 'NONE',  ( -116.9050000000000011, 2.607480562269068880, -8.024999999999993250 ) ) ;
#60980=CARTESIAN_POINT ( 'NONE',  ( -152.0070736234661695, -8.102448949553172852, -5.886773742842741797 ) ) ;
#60983=CARTESIAN_POINT ( 'NONE',  ( -89.00707362346618368, -8.102448949553172852, -5.886773742842741797 ) ) ;
#60992=CARTESIAN_POINT ( 'NONE',  ( -135.5049999999999670, -6.826472737025115478, -4.959722759717899443 ) ) ;
#60994=CARTESIAN_POINT ( 'NONE',  ( -147.1429263765338078, 5.598654528085800663, -7.705886871421367523 ) ) ;
#60997=CARTESIAN_POINT ( 'NONE',  ( -140.2450000000000045, -4.716976649647093289, -6.492361379858945902 ) ) ;
#60999=CARTESIAN_POINT ( 'NONE',  ( -129.4449999999999648, 0.000000000000000000, 8.024999999999991473 ) ) ;
#61005=CARTESIAN_POINT ( 'NONE',  ( -120.8929263765338078, -8.102448949553174629, -5.886773742842741797 ) ) ;
#61007=CARTESIAN_POINT ( 'NONE',  ( -184.0429263765338135, -9.058813317711329915, -2.943386871421370898 ) ) ;
#61009=CARTESIAN_POINT ( 'NONE',  ( -47.54499999999997328, -7.632228543268600340, -2.479861379858950166 ) ) ;
#61016=CARTESIAN_POINT ( 'NONE',  ( -98.84292637653379643, 9.058813317711329915, -2.943386871421373119 ) ) ;
#61041=CARTESIAN_POINT ( 'NONE',  ( -83.69499999999997897, -8.437984349512085203, 5.166775262442717831E-16 ) ) ;
#61059=DIRECTION ( 'NONE',  ( 0.000000000000000000, 0.000000000000000000, 1.000000000000000000 ) ) ;
#61065=CARTESIAN_POINT ( 'NONE',  ( -175.7070736234662149, -3.094860106618431139, -9.524999999999991473 ) ) ;
#61067=CARTESIAN_POINT ( 'NONE',  ( -118.1070736234661780, 8.102448949553171076, -5.886773742842744461 ) ) ;
#61080=CARTESIAN_POINT ( 'NONE',  ( -155.3050000000000068, 8.437984349512085203, -1.550032578732815448E-15 ) ) ;
#61083=CARTESIAN_POINT ( 'NONE',  ( -161.2450000000000045, -4.716976649647093289, -6.492361379858945902 ) ) ;
#61084=VECTOR ( 'NONE', #30086, 1000.000000000000000 ) ;
#61085=CARTESIAN_POINT ( 'NONE',  ( -161.8449999999999989, -7.632228543268599452, 2.479861379858951054 ) ) ;
#61086=( BOUNDED_SURFACE ( )  B_SPLINE_SURFACE ( 1, 2, ( 
 ( #68743, #5045, #21210, #26493, #62732, #63449, #42046, #35687, #3990, #20535, #8947, #14566, #57120, #57477, #30725, #52230, #48346, #12041, #22613, #43758, #5369, #21928, #6764, #27163, #38832, #54262, #44117, #33506, #16334, #37811, #17008, #59534, #59181, #11009, #17367, #60247, #6082, #38496, #27848, #65162, #32447, #59892, #53913, #28192, #11353, #5717, #64825, #38, #48698, #65518, #6417, #15984, #49700, #54936, #54610, #21571, #1436, #10678, #42734, #37467, #33177, #401, #27515, #43441, #64491, #64133, #58870, #32130, #16670, #11709, #38135, #32822, #49352, #1072, #49041, #731, #22263, #53583, #26808, #43085, #55303, #23992, #2842, #44800, #29964, #33841, #39872, #23639, #66196, #29254, #18387, #51425, #8174, #22966, #56340, #50386, #24332, #39511, #44466, #28898, #45144, #66563, #17700, #18024, #13084, #55660, #18719, #23301, #13791, #45506, #61276, #65870, #60920, #13425, #19038, #40549, #45826, #12737, #34538, #67250, #8529, #29617, #1790, #66921, #2482, #35247, #34208, #50736, #39168, #50058, #7474, #2112, #61962, #60561, #28553, #56707, #12379, #40193, #7127, #55995, #7805, #61598, #34894, #51090, #52831, #63704, #46545, #67971, #47233, #20086, #19753, #41250, #47599, #69005, #14848, #68654, #58105, #4234, #62646, #20453, #14473, #37025, #41588, #35949, #25378, #30280, #57396, #4608, #36685, #46182, #58433, #20812, #15219, #51781, #15548, #40904, #26065, #67603, #63364, #9220, #36326, #30639, #25036, #3172, #24662, #62323, #46897, #25710, #52146, #3902, #41957, #9915, #68301, #63008, #57751, #19406, #9580, #42318, #35605, #31332, #10259, #30998, #31694, #14144, #52496, #57044, #8860, #3530, #48619, #11971, #38415, #60162, #16929, #10935, #33093, #69674, #53173, #59115, #53835, #27084, #47945, #5290, #43361, #16254, #48961, #53509, #44034, #54182, #4964, #314, #17290, #984, #64403, #43683, #26736, #32370, #32730, #38755, #32047, #26412, #38051, #5995, #69344, #64047, #6340, #42641, #21136, #15895, #59814, #37376, #22187, #48259, #21486, #58783, #64753, #11627, #42998, #16594, #59444, #65442, #37730, #5631, #54531, #659, #10601, #21847, #11276, #27434, #65073, #27771, #49275, #22532, #49979, #67169, #34463, #12296, #23554, #40460, #28471, #6680, #7040, #61879, #18646, #1713, #66479, #60483, #55577, #23230, #18301, #44724, #18957, #2029, #39094, #29162, #23910, #7399, #33428, #40126, #61516, #12654, #39784, #13343, #50650, #39436, #45752, #28828, #2390, #66116, #45422, #45066, #60838, #17945, #54859, #28114, #66843, #34119, #49621, #50998, #34802, #50310, #1358, #61200, #24252, #65791, #13007, #56257, #17626, #55920, #22891, #7726, #29528, #8083, #2763, #44388, #33768, #55217, #8778, #63281, #30913, #62914, #36607, #3810, #46818, #8447, #41504, #3087, #24943, #46455, #25624, #51694, #25295, #47143, #67879, #67513, #41863, #24579, #29881, #35161, #36235, #19672, #46093, #57662, #15129, #41168, #68568, #35857, #68221, #20360, #62570, #19313, #13701, #40816, #62233, #51344, #9490, #14387, #14058, #52409, #56616, #14760, #35519, #4154, #57304, #56965, #30201, #3441, #9134, #19999, #30552, #52055, #37762, #61131, #21516, #347, #39713, #59139, #54216, #64078, #5323, #32402, #5666, #18228, #69374, #53537, #12941, #27800, #48995, #10629, #27114, #34404, #53867, #45001, #59483, #49306, #55857, #43034, #64438, #22217, #64782, #16286, #10964, #22564, #66410, #11310, #43712, #33127, #685, #48648, #65107, #21881, #7658, #16620, #43392, #38086, #26766, #32766, #1016, #11657, #21165, #47975, #42676, #59848, #48292, #15931, #37411, #58814, #32080, #38448, #6032, #27469, #16961, #32688, #54564, #6371, #18582, #3024, #30141, #61801, #45693, #67810, #24875, #24186, #24516, #67109, #23845, #62162, #25233, #61458, #51626, #9071, #50937, #36169, #40069, #46033, #29816, #2694, #35460, #67446, #57599, #14330, #29091, #62514, #56543, #30490, #18894, #50586, #35093, #51281, #19243, #45350, #40393, #40750, #13632, #66768, #2322, #35795, #13995, #13276, #57238, #62853, #56905, #46752, #8715, #8016, #34730, #3381, #46386, #14695, #56188, #51987, #29466, #8382, #19607, #41106, #3740, #68165, #19946, #41443, #63224, #21003, #64248, #47439, #42498, #15742, #21693, #31184, #15411, #10796, #5154, #68505, #31542, #20297, #9426, #58285, #47802, #63893, #160, #25913, #43209, #10460, #57959, #69202, #16458, #4444, #52346, #52678, #37923, #16104, #68861, #37224, #36541, #53023, #20663, #58636, #42174, #64614, #31892, #15069, #26602, #69528, #4815, #30850, #37586, #58983, #10114, #53371, #32244, #48123, #36870, #4096, #26268, #21331, #63565, #42854, #53692, #5479, #26929, #25565, #47078, #48465, #41805, #9775, #7255, #23089, #11822, #59297, #65641, #50174, #22044, #38951, #6893, #43548, #27970, #48822, #1208, #55430, #49824, #44581, #33294, #64934, #1566, #49145, #44919, #39287, #65980, #18150, #60353, #12156, #5842, #28320, #16788, #17140, #38612, #28681, #43885, #33626, #1898, #60012, #38260, #23408, #517, #32574, #17809, #65292, #11125, #66326, #60690, #54719, #54036, #17484, #27281, #59659, #55067, #12502, #11478, #49477, #32949, #22739, #54382, #33969, #6205, #6525, #27634, #841, #22381, #44237, #19523, #30070, #68091, #19165, #62079, #55780, #8642, #2236, #67037, #18828, #35721, #24115, #40668, #57153, #40310, #66687, #51905, #50509, #7586, #61041, #3303, #13547, #23763, #24791, #3661, #35015, #8987, #29744, #18503, #12864, #24441, #13913, #25157, #45268, #62444, #29015, #39630, #39988, #45619, #14258, #46671, #61386, #34653, #13201, #51209, #46306, #7934, #2951, #45945, #34329, #56112, #61719, #41026, #35379, #29376, #56466, #50856, #2614, #8303, #67372, #56834, #30402, #51539, #67728, #20932, #68420, #10032, #26849, #14980, #62770, #63140, #48386, #5083, #57880, #52945, #47008, #42092, #36458, #4732, #9701, #5408, #58210, #25493, #15662, #10387, #63490, #53620, #26534, #48052, #68781, #26183, #69458, #37144, #25842, #32170, #15340, #58552, #31109, #31810, #31456, #47351, #4357, #19870, #52610, #20575, #63819, #36796, #47725, #69125, #64168, #16026, #42428, #53292, #21245, #42776, #37503, #58908, #10716, #41367, #14608, #36074, #57517, #20215, #9343, #30769, #52270, #4027, #41715, #17737, #12080, #48740, #12420, #37847, #23009, #64533, #60282, #54305, #11745, #16711, #21974, #76, #21608, #59219, #43798, #1118, #32865, #38176, #38873, #65558, #64858, #65206, #59578, #16375, #33214, #65909, #32491, #22655, #49741, #43478, #7172, #11045, #17057, #763, #11395, #6455, #38538, #28599, #54980, #43122, #33551, #27559, #1479, #6126, #53951, #49079, #22299, #59929, #5752, #54652, #27890, #49393, #17407, #442, #60607, #44161, #27202, #6806, #33882, #39208, #28232, #44505, #55348, #29298, #29665, #14188, #50777, #57080, #45185, #40589, #46227, #67647, #3219, #50427, #24034, #51463, #35645, #39908, #62366, #23684, #2527, #40946, #61314, #56384, #66244, #7511, #34576, #7846, #19446, #1827, #55704, #8902, #30000, #51132, #12779, #45541, #50098, #56031, #23337, #61639, #24707, #44839, #18069, #2879, #28935, #40235, #39554, #66607, #60960, #18423, #34248, #35295, #13125, #13467, #2152, #66961, #18757, #34937, #8218, #24369, #45863, #67297, #19084, #62004, #13833, #56754, #8568, #15589, #9622, #15258, #37065, #47639, #36378, #42693, #25760, #69046, #20127, #42358 ),
 ( #62687, #63742, #41636, #15945, #10303, #20855, #58826, #9954, #52873, #46589, #58478, #14515, #57795, #31040, #26458, #14897, #31374, #47986, #52534, #57441, #64092, #41291, #68012, #51827, #31732, #4279, #35992, #53217, #37426, #47276, #69386, #20497, #9267, #3575, #36726, #4652, #30326, #30683, #5004, #19800, #25081, #52187, #68698, #21176, #3949, #25422, #46937, #68345, #42006, #63054, #63413, #58142, #26105, #22936, #32417, #16634, #12017, #6386, #6832, #32782, #21534, #10642, #59497, #49004, #65123, #1411, #27129, #699, #43403, #27815, #10980, #44436, #11670, #39139, #6046, #65837, #28154, #21895, #1033, #53881, #11322, #59861, #17670, #54227, #32093, #5679, #22577, #6728, #49666, #33476, #48664, #27482, #54901, #53551, #365, #5337, #64794, #22228, #26779, #38100, #16972, #48306, #37772, #43724, #38461, #43046, #64453, #16300, #59152, #60209, #33142, #54578, #49319, #44081, #65483, #17335, #38796, #40512, #51387, #34174, #55628, #34852, #7768, #7447, #28870, #35210, #56669, #2444, #56303, #45795, #61563, #8137, #1760, #28524, #50353, #23954, #2080, #46142, #29215, #66165, #29579, #51050, #34510, #24626, #67215, #19003, #39833, #45468, #61925, #2809, #66528, #3133, #55962, #24297, #23609, #13750, #66887, #18351, #45113, #60529, #33811, #8494, #61246, #12342, #29927, #67565, #13055, #55264, #18691, #19362, #23271, #40168, #7093, #44767, #50699, #50023, #13391, #17990, #39480, #60884, #12699, #3492, #52792, #30601, #26373, #20774, #31293, #69306, #20410, #63327, #57007, #9877, #24993, #68268, #20047, #36288, #4565, #52108, #26020, #52456, #41547, #25342, #40866, #14110, #47553, #46863, #62286, #58391, #68967, #62963, #35567, #47194, #31653, #46502, #41914, #58066, #67932, #9542, #30244, #4201, #36979, #42283, #63668, #14807, #19722, #15512, #3860, #47908, #10215, #53133, #8819, #15181, #36647, #51747, #4920, #41215, #57710, #30958, #62614, #25673, #14430, #35905, #68613, #57354, #9185, #32002, #58744, #42600, #54489, #64714, #53471, #6300, #54818, #16555, #17250, #11237, #69630, #64007, #5950, #22143, #6628, #5254, #43987, #10561, #21102, #37335, #27040, #65402, #28070, #21441, #16210, #26701, #32684, #27731, #59083, #54137, #27395, #33389, #42959, #48575, #22492, #16892, #48221, #43320, #64361, #15854, #271, #59402, #48926, #11935, #37685, #49581, #43641, #10899, #624, #32340, #53792, #5594, #21805, #38016, #49234, #65031, #38370, #59772, #11578, #33053, #939, #38714, #60120, #39734, #7001, #66792, #61474, #45023, #35117, #56209, #8037, #50267, #55877, #29488, #18608, #7359, #13654, #28421, #40085, #13297, #66430, #56565, #50955, #2715, #1989, #7678, #24207, #34752, #28786, #8399, #18248, #45714, #60788, #67126, #12964, #23509, #55534, #1314, #44343, #18914, #61155, #22846, #40412, #61822, #34422, #65744, #29113, #29834, #33719, #50605, #17586, #55167, #2343, #60448, #23865, #39052, #12254, #49933, #45372, #1671, #23190, #12610, #44681, #66077, #17904, #39389, #34077, #4114, #67467, #20318, #14012, #9091, #30507, #48397, #35815, #30869, #88, #52007, #8733, #64545, #62185, #19263, #3042, #16035, #25252, #35475, #37515, #16386, #46773, #21618, #41461, #30163, #24536, #36191, #52364, #37861, #56920, #5415, #40772, #51302, #51645, #57258, #26858, #59229, #3401, #46407, #24894, #62868, #58921, #19627, #14714, #57618, #11057, #67831, #3761, #53630, #47097, #41126, #68183, #62531, #46050, #19961, #9438, #25580, #43134, #14346, #68520, #41824, #63239, #10729, #32179, #27570, #5765, #6139, #39570, #17750, #65220, #28243, #43487, #453, #49088, #65569, #776, #18082, #1132, #60973, #27900, #66254, #50111, #43810, #23021, #22315, #11758, #12092, #32501, #33225, #53964, #17069, #44517, #28612, #1839, #55361, #32878, #6466, #33896, #27213, #38548, #44853, #59940, #54663, #23350, #49409, #38884, #48754, #59589, #22668, #44171, #21985, #64870, #38186, #16724, #12434, #33561, #11408, #17418, #54316, #60294, #54993, #6818, #7187, #49754, #1493, #65921, #39219, #60618, #56045, #7859, #57092, #8914, #24380, #8579, #67658, #2891, #13478, #34953, #29311, #46606, #29676, #50789, #56398, #39923, #45555, #14197, #46239, #55716, #68024, #30337, #24719, #61326, #25091, #50439, #35655, #7523, #3232, #66975, #45877, #2539, #34590, #12793, #34259, #2166, #8231, #13843, #18770, #24049, #51475, #30011, #40247, #51145, #61651, #28949, #67308, #51840, #45199, #35307, #62377, #19095, #19812, #23698, #40600, #62015, #56765, #19458, #40961, #41300, #3587, #66620, #18438, #13137, #42706, #9632, #13, #68712, #63426, #36738, #57452, #14909, #52884, #25772, #58490, #63067, #53561, #63752, #36390, #42018, #42369, #26788, #15271, #21547, #57808, #53228, #58836, #10651, #15958, #31052, #58155, #64104, #48318, #52545, #5346, #4290, #9968, #62701, #47285, #69060, #9274, #20140, #20509, #31386, #32106, #14528, #68357, #36004, #37439, #15604, #25435, #4665, #30692, #26117, #52199, #47652, #3961, #46947, #20866, #37078, #10315, #31741, #5016, #26470, #41647, #47997, #69396, #21185, #28168, #33156, #43735, #65138, #38115, #7105, #59869, #59508, #16983, #375, #6058, #44444, #6741, #16309, #28534, #60542, #54913, #21904, #55281, #10992, #65851, #37786, #33484, #27496, #54590, #11330, #64802, #43058, #64462, #32428, #38474, #44095, #49015, #32795, #12028, #38809, #54239, #11682, #710, #59161, #6396, #39151, #5690, #65493, #22945, #16645, #50035, #53890, #27827, #49328, #22239, #1048, #22593, #1770, #49684, #27144, #1419, #17347, #17684, #60222, #48675, #12356, #33821, #43416, #18000, #45124, #13404, #55974, #19016, #23619, #14122, #24311, #51762, #18703, #57020, #40882, #34520, #13766, #46156, #30262, #66541, #18362, #7457, #34868, #8506, #61257, #56316, #29591, #35581, #39847, #29231, #24639, #40525, #12711, #45478, #34187, #23283, #2458, #61575, #8154, #8834, #13066, #44779, #45808, #2093, #51064, #66177, #7783, #39490, #50712, #60897, #29938, #23966, #61938, #55640, #28879, #66899, #2818, #40177, #50365, #67227, #35225, #56681, #51402, #3149, #67581, #19380, #62300, #52469, #58081, #58405, #20786, #9554, #15867, #68626, #42294, #62980, #15524, #15193, #30972, #57724, #3505, #46518, #63680, #4213, #25008, #21114, #36993, #25684, #67947, #9892, #64019, #35923, #52805, #10229, #57371, #41930, #62627, #36658, #69319, #31667, #53145, #47207, #9198, #4935, #14823, #58757, #26387, #47919, #32015, #4578, #26034, #19732, #42613, #30616, #20428, #63339, #37348, #31307, #47571, #10574, #68981, #52120, #41226, #14445, #3875, #25355, #46876, #68279, #20062, #41563, #36303, #27408, #49596, #43654, #32348, #5265, #38384, #54500, #17599, #64376, #6640, #42972, #53485, #69645, #59415, #16224, #21458, #26714, #17264, #48935, #37697, #38728, #39065, #634, #1327, #65046, #53804, #48233, #59786, #6311, #60460, #59092, #28082, #10912, #5605, #27052, #11248, #22860, #12263, #48588, #287, #21817, #16903, #60133, #43330, #11595, #33066, #65759, #64723, #32696, #54830, #49246, #16567, #5966, #38028, #54152, #22156, #27742, #950, #44355, #22505, #44003, #65416, #11946, #33401, #40784, #28798, #7014, #7369, #62202, #18928, #66444, #29502, #44695, #1683, #50280, #66809, #2002, #19276, #2358, #39402, #50967, #24219, #7693, #67481, #40428, #61841, #12975, #18620, #13669, #2728, #39750, #46064 ) ),
 .UNSPECIFIED., .F., .F., .T. ) 
 B_SPLINE_SURFACE_WITH_KNOTS ( ( 2, 2 ),
 ( 3, 2, 2, 2, 2, 2, 2, 2, 2, 2, 2, 2, 2, 2, 2, 2, 2, 2, 2, 2, 2, 2, 2, 2, 2, 2, 2, 2, 2, 2, 2, 2, 2, 2, 2, 2, 2, 2, 2, 2, 2, 2, 2, 2, 2, 2, 2, 2, 2, 2, 2, 2, 2, 2, 2, 2, 2, 2, 2, 2, 2, 2, 2, 2, 2, 2, 2, 2, 2, 2, 2, 2, 2, 2, 2, 2, 2, 2, 2, 2, 2, 2, 2, 2, 2, 2, 2, 2, 2, 2, 2, 2, 2, 2, 2, 2, 2, 2, 2, 2, 2, 2, 2, 2, 2, 2, 2, 2, 2, 2, 2, 2, 2, 2, 2, 2, 2, 2, 2, 2, 2, 2, 2, 2, 2, 2, 2, 2, 2, 2, 2, 2, 2, 2, 2, 2, 2, 2, 2, 2, 2, 2, 2, 2, 2, 2, 2, 2, 2, 2, 2, 2, 2, 2, 2, 2, 2, 2, 2, 2, 2, 2, 2, 2, 2, 2, 2, 2, 2, 2, 2, 2, 2, 2, 2, 2, 2, 2, 2, 2, 2, 2, 2, 2, 2, 2, 2, 2, 2, 2, 2, 2, 2, 2, 2, 2, 2, 2, 2, 2, 2, 2, 2, 2, 2, 2, 2, 2, 2, 2, 2, 2, 2, 2, 2, 2, 2, 2, 2, 2, 2, 2, 2, 2, 2, 2, 2, 2, 2, 2, 2, 2, 2, 2, 2, 2, 2, 2, 2, 2, 2, 2, 2, 2, 2, 2, 2, 2, 2, 2, 2, 2, 2, 2, 2, 2, 2, 2, 2, 2, 2, 2, 2, 2, 2, 2, 2, 2, 2, 2, 2, 2, 2, 2, 2, 2, 2, 2, 2, 2, 2, 2, 2, 2, 2, 2, 2, 2, 2, 2, 2, 2, 2, 2, 2, 2, 2, 2, 2, 2, 2, 2, 2, 2, 2, 2, 2, 2, 2, 2, 2, 2, 2, 2, 2, 2, 2, 2, 2, 2, 2, 2, 2, 2, 2, 2, 2, 2, 2, 2, 2, 2, 2, 2, 2, 2, 2, 2, 2, 2, 2, 2, 2, 2, 2, 2, 2, 2, 2, 2, 2, 2, 2, 2, 2, 2, 2, 2, 2, 2, 2, 2, 2, 2, 2, 2, 2, 2, 2, 2, 2, 2, 2, 2, 2, 2, 2, 2, 2, 2, 2, 2, 2, 2, 2, 2, 2, 2, 2, 2, 2, 2, 2, 2, 2, 2, 2, 2, 2, 2, 2, 2, 2, 2, 2, 2, 2, 2, 2, 2, 2, 2, 2, 2, 2, 2, 2, 2, 2, 2, 2, 2, 2, 2, 2, 2, 2, 2, 2, 2, 2, 2, 2, 2, 2, 2, 2, 2, 2, 2, 2, 2, 2, 2, 2, 2, 2, 2, 2, 2, 2, 2, 2, 2, 2, 2, 3 ),
 ( 0.000000000000000000, 1.000000000000000000 ),
 ( 0.000000000000000000, 0.002173913043478260896, 0.004347826086956521792, 0.006521739130434782254, 0.008695652173913043584, 0.01086956521739130405, 0.01304347826086956451, 0.01521739130434782671, 0.01739130434782608717, 0.01956521739130434936, 0.02173913043478260809, 0.02391304347826087029, 0.02608695652173912902, 0.02826086956521739121, 0.03043478260869565341, 0.03260869565217391214, 0.03478260869565217434, 0.03695652173913043653, 0.03913043478260869873, 0.04130434782608695399, 0.04347826086956521618, 0.04565217391304347838, 0.04782608695652174058, 0.05000000000000000278, 0.05217391304347825803, 0.05434782608695652023, 0.05652173913043478243, 0.05869565217391304462, 0.06086956521739130682, 0.06304347826086956208, 0.06521739130434782428, 0.06739130434782608647, 0.06956521739130434867, 0.07173913043478261087, 0.07391304347826087306, 0.07608695652173913526, 0.07826086956521739746, 0.08043478260869564578, 0.08260869565217390798, 0.08478260869565217017, 0.08695652173913043237, 0.08913043478260869457, 0.09130434782608695676, 0.09347826086956521896, 0.09565217391304348116, 0.09782608695652174335, 0.1000000000000000056, 0.1021739130434782677, 0.1043478260869565161, 0.1065217391304347783, 0.1086956521739130405, 0.1108695652173913027, 0.1130434782608695649, 0.1152173913043478271, 0.1173913043478260892, 0.1195652173913043514, 0.1217391304347826136, 0.1239130434782608758, 0.1260869565217391242, 0.1282608695652174002, 0.1304347826086956486, 0.1326086956521739246, 0.1347826086956521729, 0.1369565217391304213, 0.1391304347826086973, 0.1413043478260869457, 0.1434782608695652217, 0.1456521739130434701, 0.1478260869565217461, 0.1499999999999999944, 0.1521739130434782705, 0.1543478260869565188, 0.1565217391304347949, 0.1586956521739130432, 0.1608695652173912916, 0.1630434782608695676, 0.1652173913043478160, 0.1673913043478260920, 0.1695652173913043403, 0.1717391304347826164, 0.1739130434782608647, 0.1760869565217391408, 0.1782608695652173891, 0.1804347826086956652, 0.1826086956521739135, 0.1847826086956521618, 0.1869565217391304379, 0.1891304347826086862, 0.1913043478260869623, 0.1934782608695652106, 0.1956521739130434867, 0.1978260869565217350, 0.2000000000000000111, 0.2021739130434782594, 0.2043478260869565355, 0.2065217391304347838, 0.2086956521739130321, 0.2108695652173913082, 0.2130434782608695565, 0.2152173913043478326, 0.2173913043478260809, 0.2195652173913043570, 0.2217391304347826053, 0.2239130434782608814, 0.2260869565217391297, 0.2282608695652173780, 0.2304347826086956541, 0.2326086956521739024, 0.2347826086956521785, 0.2369565217391304268, 0.2391304347826087029, 0.2413043478260869512, 0.2434782608695652273, 0.2456521739130434756, 0.2478260869565217517, 0.2500000000000000000, 0.2521739130434782483, 0.2543478260869564966, 0.2565217391304348005, 0.2586956521739130488, 0.2608695652173912971, 0.2630434782608695454, 0.2652173913043478493, 0.2673913043478260976, 0.2695652173913043459, 0.2717391304347825942, 0.2739130434782608425, 0.2760869565217391464, 0.2782608695652173947, 0.2804347826086956430, 0.2826086956521738913, 0.2847826086956521952, 0.2869565217391304435, 0.2891304347826086918, 0.2913043478260869401, 0.2934782608695652439, 0.2956521739130434923, 0.2978260869565217406, 0.2999999999999999889, 0.3021739130434782372, 0.3043478260869565410, 0.3065217391304347894, 0.3086956521739130377, 0.3108695652173912860, 0.3130434782608695898, 0.3152173913043478382, 0.3173913043478260865, 0.3195652173913043348, 0.3217391304347825831, 0.3239130434782608869, 0.3260869565217391353, 0.3282608695652173836, 0.3304347826086956319, 0.3326086956521739357, 0.3347826086956521840, 0.3369565217391304324, 0.3391304347826086807, 0.3413043478260869290, 0.3434782608695652328, 0.3456521739130434812, 0.3478260869565217295, 0.3499999999999999778, 0.3521739130434782816, 0.3543478260869565299, 0.3565217391304347783, 0.3586956521739130266, 0.3608695652173913304, 0.3630434782608695787, 0.3652173913043478271, 0.3673913043478260754, 0.3695652173913043237, 0.3717391304347826275, 0.3739130434782608758, 0.3760869565217391242, 0.3782608695652173725, 0.3804347826086956763, 0.3826086956521739246, 0.3847826086956521729, 0.3869565217391304213, 0.3891304347826086696, 0.3913043478260869734, 0.3934782608695652217, 0.3956521739130434701, 0.3978260869565217184, 0.4000000000000000222, 0.4021739130434782705, 0.4043478260869565188, 0.4065217391304347672, 0.4086956521739130710, 0.4108695652173913193, 0.4130434782608695676, 0.4152173913043478160, 0.4173913043478260643, 0.4195652173913043681, 0.4217391304347826164, 0.4239130434782608647, 0.4260869565217391131, 0.4282608695652174169, 0.4304347826086956652, 0.4326086956521739135, 0.4347826086956521618, 0.4369565217391304102, 0.4391304347826087140, 0.4413043478260869623, 0.4434782608695652106, 0.4456521739130434590, 0.4478260869565217628, 0.4500000000000000111, 0.4521739130434782594, 0.4543478260869565077, 0.4565217391304347561, 0.4586956521739130599, 0.4608695652173913082, 0.4630434782608695565, 0.4652173913043478048, 0.4673913043478261087, 0.4695652173913043570, 0.4717391304347826053, 0.4739130434782608536, 0.4760869565217391575, 0.4782608695652174058, 0.4804347826086956541, 0.4826086956521739024, 0.4847826086956521507, 0.4869565217391304546, 0.4891304347826087029, 0.4913043478260869512, 0.4934782608695651995, 0.4956521739130435034, 0.4978260869565217517, 0.5000000000000000000, 0.5021739130434782483, 0.5043478260869564966, 0.5065217391304347450, 0.5086956521739129933, 0.5108695652173913526, 0.5130434782608696009, 0.5152173913043478493, 0.5173913043478260976, 0.5195652173913043459, 0.5217391304347825942, 0.5239130434782608425, 0.5260869565217390909, 0.5282608695652173392, 0.5304347826086956985, 0.5326086956521739468, 0.5347826086956521952, 0.5369565217391304435, 0.5391304347826086918, 0.5413043478260869401, 0.5434782608695651884, 0.5456521739130434367, 0.5478260869565216851, 0.5500000000000000444, 0.5521739130434782927, 0.5543478260869565410, 0.5565217391304347894, 0.5586956521739130377, 0.5608695652173912860, 0.5630434782608695343, 0.5652173913043477826, 0.5673913043478261420, 0.5695652173913043903, 0.5717391304347826386, 0.5739130434782608869, 0.5760869565217391353, 0.5782608695652173836, 0.5804347826086956319, 0.5826086956521738802, 0.5847826086956521285, 0.5869565217391304879, 0.5891304347826087362, 0.5913043478260869845, 0.5934782608695652328, 0.5956521739130434812, 0.5978260869565217295, 0.5999999999999999778, 0.6021739130434782261, 0.6043478260869564744, 0.6065217391304348338, 0.6086956521739130821, 0.6108695652173913304, 0.6130434782608695787, 0.6152173913043478271, 0.6173913043478260754, 0.6195652173913043237, 0.6217391304347825720, 0.6239130434782608203, 0.6260869565217391797, 0.6282608695652174280, 0.6304347826086956763, 0.6326086956521739246, 0.6347826086956521729, 0.6369565217391304213, 0.6391304347826086696, 0.6413043478260869179, 0.6434782608695651662, 0.6456521739130435256, 0.6478260869565217739, 0.6500000000000000222, 0.6521739130434782705, 0.6543478260869565188, 0.6565217391304347672, 0.6586956521739130155, 0.6608695652173912638, 0.6630434782608695121, 0.6652173913043478715, 0.6673913043478261198, 0.6695652173913043681, 0.6717391304347826164, 0.6739130434782608647, 0.6760869565217391131, 0.6782608695652173614, 0.6804347826086956097, 0.6826086956521738580, 0.6847826086956522174, 0.6869565217391304657, 0.6891304347826087140, 0.6913043478260869623, 0.6934782608695652106, 0.6956521739130434590, 0.6978260869565217073, 0.6999999999999999556, 0.7021739130434783149, 0.7043478260869565633, 0.7065217391304348116, 0.7086956521739130599, 0.7108695652173913082, 0.7130434782608695565, 0.7152173913043478048, 0.7173913043478260532, 0.7195652173913043015, 0.7217391304347826608, 0.7239130434782609091, 0.7260869565217391575, 0.7282608695652174058, 0.7304347826086956541, 0.7326086956521739024, 0.7347826086956521507, 0.7369565217391303991, 0.7391304347826086474, 0.7413043478260870067, 0.7434782608695652550, 0.7456521739130435034, 0.7478260869565217517, 0.7500000000000000000, 0.7521739130434782483, 0.7543478260869564966, 0.7565217391304347450, 0.7586956521739129933, 0.7608695652173913526, 0.7630434782608696009, 0.7652173913043478493, 0.7673913043478260976, 0.7695652173913043459, 0.7717391304347825942, 0.7739130434782608425, 0.7760869565217390909, 0.7782608695652173392, 0.7804347826086956985, 0.7826086956521739468, 0.7847826086956521952, 0.7869565217391304435, 0.7891304347826086918, 0.7913043478260869401, 0.7934782608695651884, 0.7956521739130434367, 0.7978260869565216851, 0.8000000000000000444, 0.8021739130434782927, 0.8043478260869565410, 0.8065217391304347894, 0.8086956521739130377, 0.8108695652173912860, 0.8130434782608695343, 0.8152173913043477826, 0.8173913043478261420, 0.8195652173913043903, 0.8217391304347826386, 0.8239130434782608869, 0.8260869565217391353, 0.8282608695652173836, 0.8304347826086956319, 0.8326086956521738802, 0.8347826086956521285, 0.8369565217391304879, 0.8391304347826087362, 0.8413043478260869845, 0.8434782608695652328, 0.8456521739130434812, 0.8478260869565217295, 0.8499999999999999778, 0.8521739130434782261, 0.8543478260869564744, 0.8565217391304348338, 0.8586956521739130821, 0.8608695652173913304, 0.8630434782608695787, 0.8652173913043478271, 0.8673913043478260754, 0.8695652173913043237, 0.8717391304347825720, 0.8739130434782608203, 0.8760869565217391797, 0.8782608695652174280, 0.8804347826086956763, 0.8826086956521739246, 0.8847826086956521729, 0.8869565217391304213, 0.8891304347826086696, 0.8913043478260869179, 0.8934782608695651662, 0.8956521739130435256, 0.8978260869565217739, 0.9000000000000000222, 0.9021739130434782705, 0.9043478260869565188, 0.9065217391304347672, 0.9086956521739130155, 0.9108695652173912638, 0.9130434782608695121, 0.9152173913043478715, 0.9173913043478261198, 0.9195652173913043681, 0.9217391304347826164, 0.9239130434782608647, 0.9260869565217391131, 0.9282608695652173614, 0.9304347826086956097, 0.9326086956521738580, 0.9347826086956522174, 0.9369565217391304657, 0.9391304347826087140, 0.9413043478260869623, 0.9434782608695652106, 0.9456521739130434590, 0.9478260869565217073, 0.9499999999999999556, 0.9521739130434783149, 0.9543478260869565633, 0.9565217391304348116, 0.9586956521739130599, 0.9608695652173913082, 0.9630434782608695565, 0.9652173913043478048, 0.9673913043478260532, 0.9695652173913043015, 0.9717391304347826608, 0.9739130434782609091, 0.9760869565217391575, 0.9782608695652174058, 0.9804347826086956541, 0.9826086956521739024, 0.9847826086956521507, 0.9869565217391303991, 0.9891304347826086474, 0.9913043478260870067 ),
 .UNSPECIFIED. ) 
 GEOMETRIC_REPRESENTATION_ITEM ( )  RATIONAL_B_SPLINE_SURFACE ( (
 ( 1.000000000000000000, 0.9510565162951535312, 1.000000000000000000, 0.9510565162951535312, 1.000000000000000000, 0.9510565162951535312, 1.000000000000000000, 0.9510565162951535312, 1.000000000000000000, 0.9510565162951535312, 1.000000000000000000, 0.9510565162951535312, 1.000000000000000000, 0.9510565162951535312, 1.000000000000000000, 0.9510565162951535312, 1.000000000000000000, 0.9510565162951535312, 1.000000000000000000, 0.9510565162951535312, 1.000000000000000000, 0.9510565162951535312, 1.000000000000000000, 0.9510565162951535312, 1.000000000000000000, 0.9510565162951535312, 1.000000000000000000, 0.9510565162951535312, 1.000000000000000000, 0.9510565162951535312, 1.000000000000000000, 0.9510565162951535312, 1.000000000000000000, 0.9510565162951535312, 1.000000000000000000, 0.9510565162951535312, 1.000000000000000000, 0.9510565162951535312, 1.000000000000000000, 0.9510565162951535312, 1.000000000000000000, 0.9510565162951535312, 1.000000000000000000, 0.9510565162951535312, 1.000000000000000000, 0.9510565162951535312, 1.000000000000000000, 0.9510565162951535312, 1.000000000000000000, 0.9510565162951535312, 1.000000000000000000, 0.9510565162951535312, 1.000000000000000000, 0.9510565162951535312, 1.000000000000000000, 0.9510565162951535312, 1.000000000000000000, 0.9510565162951535312, 1.000000000000000000, 0.9510565162951535312, 1.000000000000000000, 0.9510565162951535312, 1.000000000000000000, 0.9510565162951535312, 1.000000000000000000, 0.9510565162951535312, 1.000000000000000000, 0.9510565162951535312, 1.000000000000000000, 0.9510565162951535312, 1.000000000000000000, 0.9510565162951535312, 1.000000000000000000, 0.9510565162951535312, 1.000000000000000000, 0.9510565162951535312, 1.000000000000000000, 0.9510565162951535312, 1.000000000000000000, 0.9510565162951535312, 1.000000000000000000, 0.9510565162951535312, 1.000000000000000000, 0.9510565162951535312, 1.000000000000000000, 0.9510565162951535312, 1.000000000000000000, 0.9510565162951535312, 1.000000000000000000, 0.9510565162951535312, 1.000000000000000000, 0.9510565162951535312, 1.000000000000000000, 0.9510565162951535312, 1.000000000000000000, 0.9510565162951535312, 1.000000000000000000, 0.9510565162951535312, 1.000000000000000000, 0.9510565162951535312, 1.000000000000000000, 0.9510565162951535312, 1.000000000000000000, 0.9510565162951535312, 1.000000000000000000, 0.9510565162951535312, 1.000000000000000000, 0.9510565162951535312, 1.000000000000000000, 0.9510565162951535312, 1.000000000000000000, 0.9510565162951535312, 1.000000000000000000, 0.9510565162951535312, 1.000000000000000000, 0.9510565162951535312, 1.000000000000000000, 0.9510565162951535312, 1.000000000000000000, 0.9510565162951535312, 1.000000000000000000, 0.9510565162951535312, 1.000000000000000000, 0.9510565162951535312, 1.000000000000000000, 0.9510565162951535312, 1.000000000000000000, 0.9510565162951535312, 1.000000000000000000, 0.9510565162951535312, 1.000000000000000000, 0.9510565162951535312, 1.000000000000000000, 0.9510565162951535312, 1.000000000000000000, 0.9510565162951535312, 1.000000000000000000, 0.9510565162951535312, 1.000000000000000000, 0.9510565162951535312, 1.000000000000000000, 0.9510565162951535312, 1.000000000000000000, 0.9510565162951535312, 1.000000000000000000, 0.9510565162951535312, 1.000000000000000000, 0.9510565162951535312, 1.000000000000000000, 0.9510565162951535312, 1.000000000000000000, 0.9510565162951535312, 1.000000000000000000, 0.9510565162951535312, 1.000000000000000000, 0.9510565162951535312, 1.000000000000000000, 0.9510565162951535312, 1.000000000000000000, 0.9510565162951535312, 1.000000000000000000, 0.9510565162951535312, 1.000000000000000000, 0.9510565162951535312, 1.000000000000000000, 0.9510565162951535312, 1.000000000000000000, 0.9510565162951535312, 1.000000000000000000, 0.9510565162951535312, 1.000000000000000000, 0.9510565162951535312, 1.000000000000000000, 0.9510565162951535312, 1.000000000000000000, 0.9510565162951535312, 1.000000000000000000, 0.9510565162951535312, 1.000000000000000000, 0.9510565162951535312, 1.000000000000000000, 0.9510565162951535312, 1.000000000000000000, 0.9510565162951535312, 1.000000000000000000, 0.9510565162951535312, 1.000000000000000000, 0.9510565162951535312, 1.000000000000000000, 0.9510565162951535312, 1.000000000000000000, 0.9510565162951535312, 1.000000000000000000, 0.9510565162951535312, 1.000000000000000000, 0.9510565162951535312, 1.000000000000000000, 0.9510565162951535312, 1.000000000000000000, 0.9510565162951535312, 1.000000000000000000, 0.9510565162951535312, 1.000000000000000000, 0.9510565162951535312, 1.000000000000000000, 0.9510565162951535312, 1.000000000000000000, 0.9510565162951535312, 1.000000000000000000, 0.9510565162951535312, 1.000000000000000000, 0.9510565162951535312, 1.000000000000000000, 0.9510565162951535312, 1.000000000000000000, 0.9510565162951535312, 1.000000000000000000, 0.9510565162951535312, 1.000000000000000000, 0.9510565162951535312, 1.000000000000000000, 0.9510565162951535312, 1.000000000000000000, 0.9510565162951535312, 1.000000000000000000, 0.9510565162951535312, 1.000000000000000000, 0.9510565162951535312, 1.000000000000000000, 0.9510565162951535312, 1.000000000000000000, 0.9510565162951535312, 1.000000000000000000, 0.9510565162951535312, 1.000000000000000000, 0.9510565162951535312, 1.000000000000000000, 0.9510565162951535312, 1.000000000000000000, 0.9510565162951535312, 1.000000000000000000, 0.9510565162951535312, 1.000000000000000000, 0.9510565162951535312, 1.000000000000000000, 0.9510565162951535312, 1.000000000000000000, 0.9510565162951535312, 1.000000000000000000, 0.9510565162951535312, 1.000000000000000000, 0.9510565162951535312, 1.000000000000000000, 0.9510565162951535312, 1.000000000000000000, 0.9510565162951535312, 1.000000000000000000, 0.9510565162951535312, 1.000000000000000000, 0.9510565162951535312, 1.000000000000000000, 0.9510565162951535312, 1.000000000000000000, 0.9510565162951535312, 1.000000000000000000, 0.9510565162951535312, 1.000000000000000000, 0.9510565162951535312, 1.000000000000000000, 0.9510565162951535312, 1.000000000000000000, 0.9510565162951535312, 1.000000000000000000, 0.9510565162951535312, 1.000000000000000000, 0.9510565162951535312, 1.000000000000000000, 0.9510565162951535312, 1.000000000000000000, 0.9510565162951535312, 1.000000000000000000, 0.9510565162951535312, 1.000000000000000000, 0.9510565162951535312, 1.000000000000000000, 0.9510565162951535312, 1.000000000000000000, 0.9510565162951535312, 1.000000000000000000, 0.9510565162951535312, 1.000000000000000000, 0.9510565162951535312, 1.000000000000000000, 0.9510565162951535312, 1.000000000000000000, 0.9510565162951535312, 1.000000000000000000, 0.9510565162951535312, 1.000000000000000000, 0.9510565162951535312, 1.000000000000000000, 0.9510565162951535312, 1.000000000000000000, 0.9510565162951535312, 1.000000000000000000, 0.9510565162951535312, 1.000000000000000000, 0.9510565162951535312, 1.000000000000000000, 0.9510565162951535312, 1.000000000000000000, 0.9510565162951535312, 1.000000000000000000, 0.9510565162951535312, 1.000000000000000000, 0.9510565162951535312, 1.000000000000000000, 0.9510565162951535312, 1.000000000000000000, 0.9510565162951535312, 1.000000000000000000, 0.9510565162951535312, 1.000000000000000000, 0.9510565162951535312, 1.000000000000000000, 0.9510565162951535312, 1.000000000000000000, 0.9510565162951535312, 1.000000000000000000, 0.9510565162951535312, 1.000000000000000000, 0.9510565162951535312, 1.000000000000000000, 0.9510565162951535312, 1.000000000000000000, 0.9510565162951535312, 1.000000000000000000, 0.9510565162951535312, 1.000000000000000000, 0.9510565162951535312, 1.000000000000000000, 0.9510565162951535312, 1.000000000000000000, 0.9510565162951535312, 1.000000000000000000, 0.9510565162951535312, 1.000000000000000000, 0.9510565162951535312, 1.000000000000000000, 0.9510565162951535312, 1.000000000000000000, 0.9510565162951535312, 1.000000000000000000, 0.9510565162951535312, 1.000000000000000000, 0.9510565162951535312, 1.000000000000000000, 0.9510565162951535312, 1.000000000000000000, 0.9510565162951535312, 1.000000000000000000, 0.9510565162951535312, 1.000000000000000000, 0.9510565162951535312, 1.000000000000000000, 0.9510565162951535312, 1.000000000000000000, 0.9510565162951535312, 1.000000000000000000, 0.9510565162951535312, 1.000000000000000000, 0.9510565162951535312, 1.000000000000000000, 0.9510565162951535312, 1.000000000000000000, 0.9510565162951535312, 1.000000000000000000, 0.9510565162951535312, 1.000000000000000000, 0.9510565162951535312, 1.000000000000000000, 0.9510565162951535312, 1.000000000000000000, 0.9510565162951535312, 1.000000000000000000, 0.9510565162951535312, 1.000000000000000000, 0.9510565162951535312, 1.000000000000000000, 0.9510565162951535312, 1.000000000000000000, 0.9510565162951535312, 1.000000000000000000, 0.9510565162951535312, 1.000000000000000000, 0.9510565162951535312, 1.000000000000000000, 0.9510565162951535312, 1.000000000000000000, 0.9510565162951535312, 1.000000000000000000, 0.9510565162951535312, 1.000000000000000000, 0.9510565162951535312, 1.000000000000000000, 0.9510565162951535312, 1.000000000000000000, 0.9510565162951535312, 1.000000000000000000, 0.9510565162951535312, 1.000000000000000000, 0.9510565162951535312, 1.000000000000000000, 0.9510565162951535312, 1.000000000000000000, 0.9510565162951535312, 1.000000000000000000, 0.9510565162951535312, 1.000000000000000000, 0.9510565162951535312, 1.000000000000000000, 0.9510565162951535312, 1.000000000000000000, 0.9510565162951535312, 1.000000000000000000, 0.9510565162951535312, 1.000000000000000000, 0.9510565162951535312, 1.000000000000000000, 0.9510565162951535312, 1.000000000000000000, 0.9510565162951535312, 1.000000000000000000, 0.9510565162951535312, 1.000000000000000000, 0.9510565162951535312, 1.000000000000000000, 0.9510565162951535312, 1.000000000000000000, 0.9510565162951535312, 1.000000000000000000, 0.9510565162951535312, 1.000000000000000000, 0.9510565162951535312, 1.000000000000000000, 0.9510565162951535312, 1.000000000000000000, 0.9510565162951535312, 1.000000000000000000, 0.9510565162951535312, 1.000000000000000000, 0.9510565162951535312, 1.000000000000000000, 0.9510565162951535312, 1.000000000000000000, 0.9510565162951535312, 1.000000000000000000, 0.9510565162951535312, 1.000000000000000000, 0.9510565162951535312, 1.000000000000000000, 0.9510565162951535312, 1.000000000000000000, 0.9510565162951535312, 1.000000000000000000, 0.9510565162951535312, 1.000000000000000000, 0.9510565162951535312, 1.000000000000000000, 0.9510565162951535312, 1.000000000000000000, 0.9510565162951535312, 1.000000000000000000, 0.9510565162951535312, 1.000000000000000000, 0.9510565162951535312, 1.000000000000000000, 0.9510565162951535312, 1.000000000000000000, 0.9510565162951535312, 1.000000000000000000, 0.9510565162951535312, 1.000000000000000000, 0.9510565162951535312, 1.000000000000000000, 0.9510565162951535312, 1.000000000000000000, 0.9510565162951535312, 1.000000000000000000, 0.9510565162951535312, 1.000000000000000000, 0.9510565162951535312, 1.000000000000000000, 0.9510565162951535312, 1.000000000000000000, 0.9510565162951535312, 1.000000000000000000, 0.9510565162951535312, 1.000000000000000000, 0.9510565162951535312, 1.000000000000000000, 0.9510565162951535312, 1.000000000000000000, 0.9510565162951535312, 1.000000000000000000, 0.9510565162951535312, 1.000000000000000000, 0.9510565162951535312, 1.000000000000000000, 0.9510565162951535312, 1.000000000000000000, 0.9510565162951535312, 1.000000000000000000, 0.9510565162951535312, 1.000000000000000000, 0.9510565162951535312, 1.000000000000000000, 0.9510565162951535312, 1.000000000000000000, 0.9510565162951535312, 1.000000000000000000, 0.9510565162951535312, 1.000000000000000000, 0.9510565162951535312, 1.000000000000000000, 0.9510565162951535312, 1.000000000000000000, 0.9510565162951535312, 1.000000000000000000, 0.9510565162951535312, 1.000000000000000000, 0.9510565162951535312, 1.000000000000000000, 0.9510565162951535312, 1.000000000000000000, 0.9510565162951535312, 1.000000000000000000, 0.9510565162951535312, 1.000000000000000000, 0.9510565162951535312, 1.000000000000000000, 0.9510565162951535312, 1.000000000000000000, 0.9510565162951535312, 1.000000000000000000, 0.9510565162951535312, 1.000000000000000000, 0.9510565162951535312, 1.000000000000000000, 0.9510565162951535312, 1.000000000000000000, 0.9510565162951535312, 1.000000000000000000, 0.9510565162951535312, 1.000000000000000000, 0.9510565162951535312, 1.000000000000000000, 0.9510565162951535312, 1.000000000000000000, 0.9510565162951535312, 1.000000000000000000, 0.9510565162951535312, 1.000000000000000000, 0.9510565162951535312, 1.000000000000000000, 0.9510565162951535312, 1.000000000000000000, 0.9510565162951535312, 1.000000000000000000, 0.9510565162951535312, 1.000000000000000000, 0.9510565162951535312, 1.000000000000000000, 0.9510565162951535312, 1.000000000000000000, 0.9510565162951535312, 1.000000000000000000, 0.9510565162951535312, 1.000000000000000000, 0.9510565162951535312, 1.000000000000000000, 0.9510565162951535312, 1.000000000000000000, 0.9510565162951535312, 1.000000000000000000, 0.9510565162951535312, 1.000000000000000000, 0.9510565162951535312, 1.000000000000000000, 0.9510565162951535312, 1.000000000000000000, 0.9510565162951535312, 1.000000000000000000, 0.9510565162951535312, 1.000000000000000000, 0.9510565162951535312, 1.000000000000000000, 0.9510565162951535312, 1.000000000000000000, 0.9510565162951535312, 1.000000000000000000, 0.9510565162951535312, 1.000000000000000000, 0.9510565162951535312, 1.000000000000000000, 0.9510565162951535312, 1.000000000000000000, 0.9510565162951535312, 1.000000000000000000, 0.9510565162951535312, 1.000000000000000000, 0.9510565162951535312, 1.000000000000000000, 0.9510565162951535312, 1.000000000000000000, 0.9510565162951535312, 1.000000000000000000, 0.9510565162951535312, 1.000000000000000000, 0.9510565162951535312, 1.000000000000000000, 0.9510565162951535312, 1.000000000000000000, 0.9510565162951535312, 1.000000000000000000, 0.9510565162951535312, 1.000000000000000000, 0.9510565162951535312, 1.000000000000000000, 0.9510565162951535312, 1.000000000000000000, 0.9510565162951535312, 1.000000000000000000, 0.9510565162951535312, 1.000000000000000000, 0.9510565162951535312, 1.000000000000000000, 0.9510565162951535312, 1.000000000000000000, 0.9510565162951535312, 1.000000000000000000, 0.9510565162951535312, 1.000000000000000000, 0.9510565162951535312, 1.000000000000000000, 0.9510565162951535312, 1.000000000000000000, 0.9510565162951535312, 1.000000000000000000, 0.9510565162951535312, 1.000000000000000000, 0.9510565162951535312, 1.000000000000000000, 0.9510565162951535312, 1.000000000000000000, 0.9510565162951535312, 1.000000000000000000, 0.9510565162951535312, 1.000000000000000000, 0.9510565162951535312, 1.000000000000000000, 0.9510565162951535312, 1.000000000000000000, 0.9510565162951535312, 1.000000000000000000, 0.9510565162951535312, 1.000000000000000000, 0.9510565162951535312, 1.000000000000000000, 0.9510565162951535312, 1.000000000000000000, 0.9510565162951535312, 1.000000000000000000, 0.9510565162951535312, 1.000000000000000000, 0.9510565162951535312, 1.000000000000000000, 0.9510565162951535312, 1.000000000000000000, 0.9510565162951535312, 1.000000000000000000, 0.9510565162951535312, 1.000000000000000000, 0.9510565162951535312, 1.000000000000000000, 0.9510565162951535312, 1.000000000000000000, 0.9510565162951535312, 1.000000000000000000, 0.9510565162951535312, 1.000000000000000000, 0.9510565162951535312, 1.000000000000000000, 0.9510565162951535312, 1.000000000000000000, 0.9510565162951535312, 1.000000000000000000, 0.9510565162951535312, 1.000000000000000000, 0.9510565162951535312, 1.000000000000000000, 0.9510565162951535312, 1.000000000000000000, 0.9510565162951535312, 1.000000000000000000, 0.9510565162951535312, 1.000000000000000000, 0.9510565162951535312, 1.000000000000000000, 0.9510565162951535312, 1.000000000000000000, 0.9510565162951535312, 1.000000000000000000, 0.9510565162951535312, 1.000000000000000000, 0.9510565162951535312, 1.000000000000000000, 0.9510565162951535312, 1.000000000000000000, 0.9510565162951535312, 1.000000000000000000, 0.9510565162951535312, 1.000000000000000000, 0.9510565162951535312, 1.000000000000000000, 0.9510565162951535312, 1.000000000000000000, 0.9510565162951535312, 1.000000000000000000, 0.9510565162951535312, 1.000000000000000000, 0.9510565162951535312, 1.000000000000000000, 0.9510565162951535312, 1.000000000000000000, 0.9510565162951535312, 1.000000000000000000, 0.9510565162951535312, 1.000000000000000000, 0.9510565162951535312, 1.000000000000000000, 0.9510565162951535312, 1.000000000000000000, 0.9510565162951535312, 1.000000000000000000, 0.9510565162951535312, 1.000000000000000000, 0.9510565162951535312, 1.000000000000000000, 0.9510565162951535312, 1.000000000000000000, 0.9510565162951535312, 1.000000000000000000, 0.9510565162951535312, 1.000000000000000000, 0.9510565162951535312, 1.000000000000000000, 0.9510565162951535312, 1.000000000000000000, 0.9510565162951535312, 1.000000000000000000, 0.9510565162951535312, 1.000000000000000000, 0.9510565162951535312, 1.000000000000000000, 0.9510565162951535312, 1.000000000000000000, 0.9510565162951535312, 1.000000000000000000, 0.9510565162951535312, 1.000000000000000000, 0.9510565162951535312, 1.000000000000000000, 0.9510565162951535312, 1.000000000000000000, 0.9510565162951535312, 1.000000000000000000, 0.9510565162951535312, 1.000000000000000000, 0.9510565162951535312, 1.000000000000000000, 0.9510565162951535312, 1.000000000000000000, 0.9510565162951535312, 1.000000000000000000, 0.9510565162951535312, 1.000000000000000000, 0.9510565162951535312, 1.000000000000000000, 0.9510565162951535312, 1.000000000000000000, 0.9510565162951535312, 1.000000000000000000, 0.9510565162951535312, 1.000000000000000000, 0.9510565162951535312, 1.000000000000000000, 0.9510565162951535312, 1.000000000000000000, 0.9510565162951535312, 1.000000000000000000, 0.9510565162951535312, 1.000000000000000000, 0.9510565162951535312, 1.000000000000000000, 0.9510565162951535312, 1.000000000000000000, 0.9510565162951535312, 1.000000000000000000, 0.9510565162951535312, 1.000000000000000000, 0.9510565162951535312, 1.000000000000000000, 0.9510565162951535312, 1.000000000000000000, 0.9510565162951535312, 1.000000000000000000, 0.9510565162951535312, 1.000000000000000000, 0.9510565162951535312, 1.000000000000000000, 0.9510565162951535312, 1.000000000000000000, 0.9510565162951535312, 1.000000000000000000, 0.9510565162951535312, 1.000000000000000000, 0.9510565162951535312, 1.000000000000000000, 0.9510565162951535312, 1.000000000000000000, 0.9510565162951535312, 1.000000000000000000, 0.9510565162951535312, 1.000000000000000000, 0.9510565162951535312, 1.000000000000000000, 0.9510565162951535312, 1.000000000000000000, 0.9510565162951535312, 1.000000000000000000, 0.9510565162951535312, 1.000000000000000000, 0.9510565162951535312, 1.000000000000000000, 0.9510565162951535312, 1.000000000000000000, 0.9510565162951535312, 1.000000000000000000, 0.9510565162951535312, 1.000000000000000000, 0.9510565162951535312, 1.000000000000000000, 0.9510565162951535312, 1.000000000000000000, 0.9510565162951535312, 1.000000000000000000, 0.9510565162951535312, 1.000000000000000000, 0.9510565162951535312, 1.000000000000000000, 0.9510565162951535312, 1.000000000000000000, 0.9510565162951535312, 1.000000000000000000, 0.9510565162951535312, 1.000000000000000000, 0.9510565162951535312, 1.000000000000000000, 0.9510565162951535312, 1.000000000000000000, 0.9510565162951535312, 1.000000000000000000, 0.9510565162951535312, 1.000000000000000000, 0.9510565162951535312, 1.000000000000000000, 0.9510565162951535312, 1.000000000000000000, 0.9510565162951535312, 1.000000000000000000, 0.9510565162951535312, 1.000000000000000000, 0.9510565162951535312, 1.000000000000000000, 0.9510565162951535312, 1.000000000000000000, 0.9510565162951535312, 1.000000000000000000, 0.9510565162951535312, 1.000000000000000000, 0.9510565162951535312, 1.000000000000000000, 0.9510565162951535312, 1.000000000000000000, 0.9510565162951535312, 1.000000000000000000, 0.9510565162951535312, 1.000000000000000000, 0.9510565162951535312, 1.000000000000000000, 0.9510565162951535312, 1.000000000000000000, 0.9510565162951535312, 1.000000000000000000, 0.9510565162951535312, 1.000000000000000000, 0.9510565162951535312, 1.000000000000000000, 0.9510565162951535312, 1.000000000000000000, 0.9510565162951535312, 1.000000000000000000),
 ( 1.000000000000000000, 0.9510565162951535312, 1.000000000000000000, 0.9510565162951535312, 1.000000000000000000, 0.9510565162951535312, 1.000000000000000000, 0.9510565162951535312, 1.000000000000000000, 0.9510565162951535312, 1.000000000000000000, 0.9510565162951535312, 1.000000000000000000, 0.9510565162951535312, 1.000000000000000000, 0.9510565162951535312, 1.000000000000000000, 0.9510565162951535312, 1.000000000000000000, 0.9510565162951535312, 1.000000000000000000, 0.9510565162951535312, 1.000000000000000000, 0.9510565162951535312, 1.000000000000000000, 0.9510565162951535312, 1.000000000000000000, 0.9510565162951535312, 1.000000000000000000, 0.9510565162951535312, 1.000000000000000000, 0.9510565162951535312, 1.000000000000000000, 0.9510565162951535312, 1.000000000000000000, 0.9510565162951535312, 1.000000000000000000, 0.9510565162951535312, 1.000000000000000000, 0.9510565162951535312, 1.000000000000000000, 0.9510565162951535312, 1.000000000000000000, 0.9510565162951535312, 1.000000000000000000, 0.9510565162951535312, 1.000000000000000000, 0.9510565162951535312, 1.000000000000000000, 0.9510565162951535312, 1.000000000000000000, 0.9510565162951535312, 1.000000000000000000, 0.9510565162951535312, 1.000000000000000000, 0.9510565162951535312, 1.000000000000000000, 0.9510565162951535312, 1.000000000000000000, 0.9510565162951535312, 1.000000000000000000, 0.9510565162951535312, 1.000000000000000000, 0.9510565162951535312, 1.000000000000000000, 0.9510565162951535312, 1.000000000000000000, 0.9510565162951535312, 1.000000000000000000, 0.9510565162951535312, 1.000000000000000000, 0.9510565162951535312, 1.000000000000000000, 0.9510565162951535312, 1.000000000000000000, 0.9510565162951535312, 1.000000000000000000, 0.9510565162951535312, 1.000000000000000000, 0.9510565162951535312, 1.000000000000000000, 0.9510565162951535312, 1.000000000000000000, 0.9510565162951535312, 1.000000000000000000, 0.9510565162951535312, 1.000000000000000000, 0.9510565162951535312, 1.000000000000000000, 0.9510565162951535312, 1.000000000000000000, 0.9510565162951535312, 1.000000000000000000, 0.9510565162951535312, 1.000000000000000000, 0.9510565162951535312, 1.000000000000000000, 0.9510565162951535312, 1.000000000000000000, 0.9510565162951535312, 1.000000000000000000, 0.9510565162951535312, 1.000000000000000000, 0.9510565162951535312, 1.000000000000000000, 0.9510565162951535312, 1.000000000000000000, 0.9510565162951535312, 1.000000000000000000, 0.9510565162951535312, 1.000000000000000000, 0.9510565162951535312, 1.000000000000000000, 0.9510565162951535312, 1.000000000000000000, 0.9510565162951535312, 1.000000000000000000, 0.9510565162951535312, 1.000000000000000000, 0.9510565162951535312, 1.000000000000000000, 0.9510565162951535312, 1.000000000000000000, 0.9510565162951535312, 1.000000000000000000, 0.9510565162951535312, 1.000000000000000000, 0.9510565162951535312, 1.000000000000000000, 0.9510565162951535312, 1.000000000000000000, 0.9510565162951535312, 1.000000000000000000, 0.9510565162951535312, 1.000000000000000000, 0.9510565162951535312, 1.000000000000000000, 0.9510565162951535312, 1.000000000000000000, 0.9510565162951535312, 1.000000000000000000, 0.9510565162951535312, 1.000000000000000000, 0.9510565162951535312, 1.000000000000000000, 0.9510565162951535312, 1.000000000000000000, 0.9510565162951535312, 1.000000000000000000, 0.9510565162951535312, 1.000000000000000000, 0.9510565162951535312, 1.000000000000000000, 0.9510565162951535312, 1.000000000000000000, 0.9510565162951535312, 1.000000000000000000, 0.9510565162951535312, 1.000000000000000000, 0.9510565162951535312, 1.000000000000000000, 0.9510565162951535312, 1.000000000000000000, 0.9510565162951535312, 1.000000000000000000, 0.9510565162951535312, 1.000000000000000000, 0.9510565162951535312, 1.000000000000000000, 0.9510565162951535312, 1.000000000000000000, 0.9510565162951535312, 1.000000000000000000, 0.9510565162951535312, 1.000000000000000000, 0.9510565162951535312, 1.000000000000000000, 0.9510565162951535312, 1.000000000000000000, 0.9510565162951535312, 1.000000000000000000, 0.9510565162951535312, 1.000000000000000000, 0.9510565162951535312, 1.000000000000000000, 0.9510565162951535312, 1.000000000000000000, 0.9510565162951535312, 1.000000000000000000, 0.9510565162951535312, 1.000000000000000000, 0.9510565162951535312, 1.000000000000000000, 0.9510565162951535312, 1.000000000000000000, 0.9510565162951535312, 1.000000000000000000, 0.9510565162951535312, 1.000000000000000000, 0.9510565162951535312, 1.000000000000000000, 0.9510565162951535312, 1.000000000000000000, 0.9510565162951535312, 1.000000000000000000, 0.9510565162951535312, 1.000000000000000000, 0.9510565162951535312, 1.000000000000000000, 0.9510565162951535312, 1.000000000000000000, 0.9510565162951535312, 1.000000000000000000, 0.9510565162951535312, 1.000000000000000000, 0.9510565162951535312, 1.000000000000000000, 0.9510565162951535312, 1.000000000000000000, 0.9510565162951535312, 1.000000000000000000, 0.9510565162951535312, 1.000000000000000000, 0.9510565162951535312, 1.000000000000000000, 0.9510565162951535312, 1.000000000000000000, 0.9510565162951535312, 1.000000000000000000, 0.9510565162951535312, 1.000000000000000000, 0.9510565162951535312, 1.000000000000000000, 0.9510565162951535312, 1.000000000000000000, 0.9510565162951535312, 1.000000000000000000, 0.9510565162951535312, 1.000000000000000000, 0.9510565162951535312, 1.000000000000000000, 0.9510565162951535312, 1.000000000000000000, 0.9510565162951535312, 1.000000000000000000, 0.9510565162951535312, 1.000000000000000000, 0.9510565162951535312, 1.000000000000000000, 0.9510565162951535312, 1.000000000000000000, 0.9510565162951535312, 1.000000000000000000, 0.9510565162951535312, 1.000000000000000000, 0.9510565162951535312, 1.000000000000000000, 0.9510565162951535312, 1.000000000000000000, 0.9510565162951535312, 1.000000000000000000, 0.9510565162951535312, 1.000000000000000000, 0.9510565162951535312, 1.000000000000000000, 0.9510565162951535312, 1.000000000000000000, 0.9510565162951535312, 1.000000000000000000, 0.9510565162951535312, 1.000000000000000000, 0.9510565162951535312, 1.000000000000000000, 0.9510565162951535312, 1.000000000000000000, 0.9510565162951535312, 1.000000000000000000, 0.9510565162951535312, 1.000000000000000000, 0.9510565162951535312, 1.000000000000000000, 0.9510565162951535312, 1.000000000000000000, 0.9510565162951535312, 1.000000000000000000, 0.9510565162951535312, 1.000000000000000000, 0.9510565162951535312, 1.000000000000000000, 0.9510565162951535312, 1.000000000000000000, 0.9510565162951535312, 1.000000000000000000, 0.9510565162951535312, 1.000000000000000000, 0.9510565162951535312, 1.000000000000000000, 0.9510565162951535312, 1.000000000000000000, 0.9510565162951535312, 1.000000000000000000, 0.9510565162951535312, 1.000000000000000000, 0.9510565162951535312, 1.000000000000000000, 0.9510565162951535312, 1.000000000000000000, 0.9510565162951535312, 1.000000000000000000, 0.9510565162951535312, 1.000000000000000000, 0.9510565162951535312, 1.000000000000000000, 0.9510565162951535312, 1.000000000000000000, 0.9510565162951535312, 1.000000000000000000, 0.9510565162951535312, 1.000000000000000000, 0.9510565162951535312, 1.000000000000000000, 0.9510565162951535312, 1.000000000000000000, 0.9510565162951535312, 1.000000000000000000, 0.9510565162951535312, 1.000000000000000000, 0.9510565162951535312, 1.000000000000000000, 0.9510565162951535312, 1.000000000000000000, 0.9510565162951535312, 1.000000000000000000, 0.9510565162951535312, 1.000000000000000000, 0.9510565162951535312, 1.000000000000000000, 0.9510565162951535312, 1.000000000000000000, 0.9510565162951535312, 1.000000000000000000, 0.9510565162951535312, 1.000000000000000000, 0.9510565162951535312, 1.000000000000000000, 0.9510565162951535312, 1.000000000000000000, 0.9510565162951535312, 1.000000000000000000, 0.9510565162951535312, 1.000000000000000000, 0.9510565162951535312, 1.000000000000000000, 0.9510565162951535312, 1.000000000000000000, 0.9510565162951535312, 1.000000000000000000, 0.9510565162951535312, 1.000000000000000000, 0.9510565162951535312, 1.000000000000000000, 0.9510565162951535312, 1.000000000000000000, 0.9510565162951535312, 1.000000000000000000, 0.9510565162951535312, 1.000000000000000000, 0.9510565162951535312, 1.000000000000000000, 0.9510565162951535312, 1.000000000000000000, 0.9510565162951535312, 1.000000000000000000, 0.9510565162951535312, 1.000000000000000000, 0.9510565162951535312, 1.000000000000000000, 0.9510565162951535312, 1.000000000000000000, 0.9510565162951535312, 1.000000000000000000, 0.9510565162951535312, 1.000000000000000000, 0.9510565162951535312, 1.000000000000000000, 0.9510565162951535312, 1.000000000000000000, 0.9510565162951535312, 1.000000000000000000, 0.9510565162951535312, 1.000000000000000000, 0.9510565162951535312, 1.000000000000000000, 0.9510565162951535312, 1.000000000000000000, 0.9510565162951535312, 1.000000000000000000, 0.9510565162951535312, 1.000000000000000000, 0.9510565162951535312, 1.000000000000000000, 0.9510565162951535312, 1.000000000000000000, 0.9510565162951535312, 1.000000000000000000, 0.9510565162951535312, 1.000000000000000000, 0.9510565162951535312, 1.000000000000000000, 0.9510565162951535312, 1.000000000000000000, 0.9510565162951535312, 1.000000000000000000, 0.9510565162951535312, 1.000000000000000000, 0.9510565162951535312, 1.000000000000000000, 0.9510565162951535312, 1.000000000000000000, 0.9510565162951535312, 1.000000000000000000, 0.9510565162951535312, 1.000000000000000000, 0.9510565162951535312, 1.000000000000000000, 0.9510565162951535312, 1.000000000000000000, 0.9510565162951535312, 1.000000000000000000, 0.9510565162951535312, 1.000000000000000000, 0.9510565162951535312, 1.000000000000000000, 0.9510565162951535312, 1.000000000000000000, 0.9510565162951535312, 1.000000000000000000, 0.9510565162951535312, 1.000000000000000000, 0.9510565162951535312, 1.000000000000000000, 0.9510565162951535312, 1.000000000000000000, 0.9510565162951535312, 1.000000000000000000, 0.9510565162951535312, 1.000000000000000000, 0.9510565162951535312, 1.000000000000000000, 0.9510565162951535312, 1.000000000000000000, 0.9510565162951535312, 1.000000000000000000, 0.9510565162951535312, 1.000000000000000000, 0.9510565162951535312, 1.000000000000000000, 0.9510565162951535312, 1.000000000000000000, 0.9510565162951535312, 1.000000000000000000, 0.9510565162951535312, 1.000000000000000000, 0.9510565162951535312, 1.000000000000000000, 0.9510565162951535312, 1.000000000000000000, 0.9510565162951535312, 1.000000000000000000, 0.9510565162951535312, 1.000000000000000000, 0.9510565162951535312, 1.000000000000000000, 0.9510565162951535312, 1.000000000000000000, 0.9510565162951535312, 1.000000000000000000, 0.9510565162951535312, 1.000000000000000000, 0.9510565162951535312, 1.000000000000000000, 0.9510565162951535312, 1.000000000000000000, 0.9510565162951535312, 1.000000000000000000, 0.9510565162951535312, 1.000000000000000000, 0.9510565162951535312, 1.000000000000000000, 0.9510565162951535312, 1.000000000000000000, 0.9510565162951535312, 1.000000000000000000, 0.9510565162951535312, 1.000000000000000000, 0.9510565162951535312, 1.000000000000000000, 0.9510565162951535312, 1.000000000000000000, 0.9510565162951535312, 1.000000000000000000, 0.9510565162951535312, 1.000000000000000000, 0.9510565162951535312, 1.000000000000000000, 0.9510565162951535312, 1.000000000000000000, 0.9510565162951535312, 1.000000000000000000, 0.9510565162951535312, 1.000000000000000000, 0.9510565162951535312, 1.000000000000000000, 0.9510565162951535312, 1.000000000000000000, 0.9510565162951535312, 1.000000000000000000, 0.9510565162951535312, 1.000000000000000000, 0.9510565162951535312, 1.000000000000000000, 0.9510565162951535312, 1.000000000000000000, 0.9510565162951535312, 1.000000000000000000, 0.9510565162951535312, 1.000000000000000000, 0.9510565162951535312, 1.000000000000000000, 0.9510565162951535312, 1.000000000000000000, 0.9510565162951535312, 1.000000000000000000, 0.9510565162951535312, 1.000000000000000000, 0.9510565162951535312, 1.000000000000000000, 0.9510565162951535312, 1.000000000000000000, 0.9510565162951535312, 1.000000000000000000, 0.9510565162951535312, 1.000000000000000000, 0.9510565162951535312, 1.000000000000000000, 0.9510565162951535312, 1.000000000000000000, 0.9510565162951535312, 1.000000000000000000, 0.9510565162951535312, 1.000000000000000000, 0.9510565162951535312, 1.000000000000000000, 0.9510565162951535312, 1.000000000000000000, 0.9510565162951535312, 1.000000000000000000, 0.9510565162951535312, 1.000000000000000000, 0.9510565162951535312, 1.000000000000000000, 0.9510565162951535312, 1.000000000000000000, 0.9510565162951535312, 1.000000000000000000, 0.9510565162951535312, 1.000000000000000000, 0.9510565162951535312, 1.000000000000000000, 0.9510565162951535312, 1.000000000000000000, 0.9510565162951535312, 1.000000000000000000, 0.9510565162951535312, 1.000000000000000000, 0.9510565162951535312, 1.000000000000000000, 0.9510565162951535312, 1.000000000000000000, 0.9510565162951535312, 1.000000000000000000, 0.9510565162951535312, 1.000000000000000000, 0.9510565162951535312, 1.000000000000000000, 0.9510565162951535312, 1.000000000000000000, 0.9510565162951535312, 1.000000000000000000, 0.9510565162951535312, 1.000000000000000000, 0.9510565162951535312, 1.000000000000000000, 0.9510565162951535312, 1.000000000000000000, 0.9510565162951535312, 1.000000000000000000, 0.9510565162951535312, 1.000000000000000000, 0.9510565162951535312, 1.000000000000000000, 0.9510565162951535312, 1.000000000000000000, 0.9510565162951535312, 1.000000000000000000, 0.9510565162951535312, 1.000000000000000000, 0.9510565162951535312, 1.000000000000000000, 0.9510565162951535312, 1.000000000000000000, 0.9510565162951535312, 1.000000000000000000, 0.9510565162951535312, 1.000000000000000000, 0.9510565162951535312, 1.000000000000000000, 0.9510565162951535312, 1.000000000000000000, 0.9510565162951535312, 1.000000000000000000, 0.9510565162951535312, 1.000000000000000000, 0.9510565162951535312, 1.000000000000000000, 0.9510565162951535312, 1.000000000000000000, 0.9510565162951535312, 1.000000000000000000, 0.9510565162951535312, 1.000000000000000000, 0.9510565162951535312, 1.000000000000000000, 0.9510565162951535312, 1.000000000000000000, 0.9510565162951535312, 1.000000000000000000, 0.9510565162951535312, 1.000000000000000000, 0.9510565162951535312, 1.000000000000000000, 0.9510565162951535312, 1.000000000000000000, 0.9510565162951535312, 1.000000000000000000, 0.9510565162951535312, 1.000000000000000000, 0.9510565162951535312, 1.000000000000000000, 0.9510565162951535312, 1.000000000000000000, 0.9510565162951535312, 1.000000000000000000, 0.9510565162951535312, 1.000000000000000000, 0.9510565162951535312, 1.000000000000000000, 0.9510565162951535312, 1.000000000000000000, 0.9510565162951535312, 1.000000000000000000, 0.9510565162951535312, 1.000000000000000000, 0.9510565162951535312, 1.000000000000000000, 0.9510565162951535312, 1.000000000000000000, 0.9510565162951535312, 1.000000000000000000, 0.9510565162951535312, 1.000000000000000000, 0.9510565162951535312, 1.000000000000000000, 0.9510565162951535312, 1.000000000000000000, 0.9510565162951535312, 1.000000000000000000, 0.9510565162951535312, 1.000000000000000000, 0.9510565162951535312, 1.000000000000000000, 0.9510565162951535312, 1.000000000000000000, 0.9510565162951535312, 1.000000000000000000, 0.9510565162951535312, 1.000000000000000000, 0.9510565162951535312, 1.000000000000000000, 0.9510565162951535312, 1.000000000000000000, 0.9510565162951535312, 1.000000000000000000, 0.9510565162951535312, 1.000000000000000000, 0.9510565162951535312, 1.000000000000000000, 0.9510565162951535312, 1.000000000000000000, 0.9510565162951535312, 1.000000000000000000, 0.9510565162951535312, 1.000000000000000000, 0.9510565162951535312, 1.000000000000000000, 0.9510565162951535312, 1.000000000000000000, 0.9510565162951535312, 1.000000000000000000, 0.9510565162951535312, 1.000000000000000000, 0.9510565162951535312, 1.000000000000000000, 0.9510565162951535312, 1.000000000000000000, 0.9510565162951535312, 1.000000000000000000, 0.9510565162951535312, 1.000000000000000000, 0.9510565162951535312, 1.000000000000000000, 0.9510565162951535312, 1.000000000000000000, 0.9510565162951535312, 1.000000000000000000, 0.9510565162951535312, 1.000000000000000000, 0.9510565162951535312, 1.000000000000000000, 0.9510565162951535312, 1.000000000000000000, 0.9510565162951535312, 1.000000000000000000, 0.9510565162951535312, 1.000000000000000000, 0.9510565162951535312, 1.000000000000000000, 0.9510565162951535312, 1.000000000000000000, 0.9510565162951535312, 1.000000000000000000, 0.9510565162951535312, 1.000000000000000000, 0.9510565162951535312, 1.000000000000000000, 0.9510565162951535312, 1.000000000000000000, 0.9510565162951535312, 1.000000000000000000, 0.9510565162951535312, 1.000000000000000000, 0.9510565162951535312, 1.000000000000000000, 0.9510565162951535312, 1.000000000000000000, 0.9510565162951535312, 1.000000000000000000, 0.9510565162951535312, 1.000000000000000000, 0.9510565162951535312, 1.000000000000000000, 0.9510565162951535312, 1.000000000000000000, 0.9510565162951535312, 1.000000000000000000, 0.9510565162951535312, 1.000000000000000000, 0.9510565162951535312, 1.000000000000000000, 0.9510565162951535312, 1.000000000000000000, 0.9510565162951535312, 1.000000000000000000, 0.9510565162951535312, 1.000000000000000000, 0.9510565162951535312, 1.000000000000000000, 0.9510565162951535312, 1.000000000000000000, 0.9510565162951535312, 1.000000000000000000, 0.9510565162951535312, 1.000000000000000000, 0.9510565162951535312, 1.000000000000000000, 0.9510565162951535312, 1.000000000000000000, 0.9510565162951535312, 1.000000000000000000, 0.9510565162951535312, 1.000000000000000000, 0.9510565162951535312, 1.000000000000000000, 0.9510565162951535312, 1.000000000000000000, 0.9510565162951535312, 1.000000000000000000, 0.9510565162951535312, 1.000000000000000000, 0.9510565162951535312, 1.000000000000000000, 0.9510565162951535312, 1.000000000000000000, 0.9510565162951535312, 1.000000000000000000, 0.9510565162951535312, 1.000000000000000000, 0.9510565162951535312, 1.000000000000000000, 0.9510565162951535312, 1.000000000000000000, 0.9510565162951535312, 1.000000000000000000, 0.9510565162951535312, 1.000000000000000000, 0.9510565162951535312, 1.000000000000000000, 0.9510565162951535312, 1.000000000000000000, 0.9510565162951535312, 1.000000000000000000, 0.9510565162951535312, 1.000000000000000000, 0.9510565162951535312, 1.000000000000000000, 0.9510565162951535312, 1.000000000000000000, 0.9510565162951535312, 1.000000000000000000, 0.9510565162951535312, 1.000000000000000000, 0.9510565162951535312, 1.000000000000000000, 0.9510565162951535312, 1.000000000000000000, 0.9510565162951535312, 1.000000000000000000, 0.9510565162951535312, 1.000000000000000000, 0.9510565162951535312, 1.000000000000000000, 0.9510565162951535312, 1.000000000000000000, 0.9510565162951535312, 1.000000000000000000, 0.9510565162951535312, 1.000000000000000000, 0.9510565162951535312, 1.000000000000000000, 0.9510565162951535312, 1.000000000000000000, 0.9510565162951535312, 1.000000000000000000, 0.9510565162951535312, 1.000000000000000000, 0.9510565162951535312, 1.000000000000000000, 0.9510565162951535312, 1.000000000000000000, 0.9510565162951535312, 1.000000000000000000, 0.9510565162951535312, 1.000000000000000000, 0.9510565162951535312, 1.000000000000000000, 0.9510565162951535312, 1.000000000000000000, 0.9510565162951535312, 1.000000000000000000, 0.9510565162951535312, 1.000000000000000000, 0.9510565162951535312, 1.000000000000000000, 0.9510565162951535312, 1.000000000000000000, 0.9510565162951535312, 1.000000000000000000, 0.9510565162951535312, 1.000000000000000000, 0.9510565162951535312, 1.000000000000000000, 0.9510565162951535312, 1.000000000000000000, 0.9510565162951535312, 1.000000000000000000, 0.9510565162951535312, 1.000000000000000000, 0.9510565162951535312, 1.000000000000000000, 0.9510565162951535312, 1.000000000000000000, 0.9510565162951535312, 1.000000000000000000, 0.9510565162951535312, 1.000000000000000000, 0.9510565162951535312, 1.000000000000000000, 0.9510565162951535312, 1.000000000000000000, 0.9510565162951535312, 1.000000000000000000, 0.9510565162951535312, 1.000000000000000000, 0.9510565162951535312, 1.000000000000000000, 0.9510565162951535312, 1.000000000000000000, 0.9510565162951535312, 1.000000000000000000, 0.9510565162951535312, 1.000000000000000000, 0.9510565162951535312, 1.000000000000000000) ) ) 
 REPRESENTATION_ITEM ( '' )  SURFACE ( )  );
#61089=CARTESIAN_POINT ( 'NONE',  ( -67.34292637653379643, -9.058813317711329915, 2.943386871421371787 ) ) ;
#61093=CARTESIAN_POINT ( 'NONE',  ( -71.75499999999998124, 4.716976649647091513, -6.492361379858946790 ) ) ;
#61098=CARTESIAN_POINT ( 'NONE',  ( -68.09499999999998465, -2.607480562269071545, -8.024999999999991473 ) ) ;
#61116=LINE ( 'NONE', #49896, #30449 ) ;
#61124=ORIENTED_EDGE ( 'NONE', *, *, #30172, .F. ) ;
#61131=CARTESIAN_POINT ( 'NONE',  ( -124.7949999999999733, 2.607480562269068880, -8.024999999999993250 ) ) ;
#61138=CARTESIAN_POINT ( 'NONE',  ( -10.00006165262988134, -11.99997431140458382, 0.3302327102163540307 ) ) ;
#61154=CARTESIAN_POINT ( 'NONE',  ( -157.7070736234665276, -3.094860106623708251, -9.524999999996159872 ) ) ;
#61155=CARTESIAN_POINT ( 'NONE',  ( -132.6550000000000011, -7.632228543268600340, -2.479861379858950166 ) ) ;
#61157=ORIENTED_EDGE ( 'NONE', *, *, #49981, .F. ) ;
#61162=VERTEX_POINT ( 'NONE', #60672 ) ;
#61167=CARTESIAN_POINT ( 'NONE',  ( -108.7429263765338021, -5.598654528085803328, -7.705886871421366635 ) ) ;
#61171=CARTESIAN_POINT ( 'NONE',  ( -91.79292637653496456, -3.094860106599068406, 9.525000000014060220 ) ) ;
#61180=CARTESIAN_POINT ( 'NONE',  ( -106.5549999999999784, 0.000000000000000000, 8.024999999999991473 ) ) ;
#61186=CARTESIAN_POINT ( 'NONE',  ( -97.34499999999998465, 7.632228543268599452, -2.479861379858951942 ) ) ;
#61188=CARTESIAN_POINT ( 'NONE',  ( -78.74499999999997613, 4.716976649647094177, 6.492361379858945902 ) ) ;
#61195=CARTESIAN_POINT ( 'NONE',  ( -195.0000000000000000, 0.000000000000000000, 0.000000000000000000 ) ) ;
#61197=CARTESIAN_POINT ( 'NONE',  ( -118.4929263765338021, -8.102448949553172852, 5.886773742842742685 ) ) ;
#61200=CARTESIAN_POINT ( 'NONE',  ( -135.2950000000000159, -2.607480562269069768, 8.024999999999991473 ) ) ;
#61210=CARTESIAN_POINT ( 'NONE',  ( -131.6070736234661922, -8.102448949553174629, 5.886773742842742685 ) ) ;
#61214=CARTESIAN_POINT ( 'NONE',  ( -129.0549999999999784, -9.827790563157499189E-16, -8.024999999999991473 ) ) ;
#61217=ORIENTED_EDGE ( 'NONE', *, *, #30657, .F. ) ;
#61244=CARTESIAN_POINT ( 'NONE',  ( -122.1570736234661751, -9.058813317711329915, -2.943386871421370898 ) ) ;
#61246=CARTESIAN_POINT ( 'NONE',  ( -160.2549999999999670, -4.716976649647092401, 6.492361379858946790 ) ) ;
#61257=CARTESIAN_POINT ( 'NONE',  ( -77.45499999999998408, 7.632228543268599452, -2.479861379858951942 ) ) ;
#61258=ORIENTED_EDGE ( 'NONE', *, *, #68364, .T. ) ;
#61259=CARTESIAN_POINT ( 'NONE',  ( -64.55707362346618083, -1.166476076187852838E-15, -9.524999999999991473 ) ) ;
#61268=CARTESIAN_POINT ( 'NONE',  ( -109.4949999999999761, 6.826472737025113702, -4.959722759717902107 ) ) ;
#61274=CARTESIAN_POINT ( 'NONE',  ( -141.8929263765337794, -8.102448949553172852, -5.886773742842741797 ) ) ;
#61276=CARTESIAN_POINT ( 'NONE',  ( -166.9450000000000216, -9.827790563157499189E-16, -8.024999999999991473 ) ) ;
#61291=CARTESIAN_POINT ( 'NONE',  ( -160.8549999999999898, 4.716976649647094177, 6.492361379858945902 ) ) ;
#61293=CARTESIAN_POINT ( 'NONE',  ( -111.7429263765338163, -5.598654528085803328, -7.705886871421366635 ) ) ;
#61298=EDGE_CURVE ( 'NONE', #51919, #23561, #62617, .T. ) ;
#61303=CARTESIAN_POINT ( 'NONE',  ( -85.85499999999998977, 4.716976649647094177, 6.492361379858945902 ) ) ;
#61311=AXIS2_PLACEMENT_3D ( 'NONE', #27011, #36623, #27362 ) ;
#61314=CARTESIAN_POINT ( 'NONE',  ( -54.89499999999997470, 6.826472737025116366, 4.959722759717898555 ) ) ;
#61322=CARTESIAN_POINT ( 'NONE',  ( -50.99499999999998323, -6.826472737025113702, 4.959722759717902107 ) ) ;
#61326=CARTESIAN_POINT ( 'NONE',  ( -105.9549999999999983, -7.632228543268599452, 2.479861379858951054 ) ) ;
#61331=CARTESIAN_POINT ( 'NONE',  ( -145.2570736234661695, 5.598654528085800663, -7.705886871421367523 ) ) ;
#61332=CARTESIAN_POINT ( 'NONE',  ( -58.55707362346616662, -1.166476076187852838E-15, -9.524999999999991473 ) ) ;
#61335=CARTESIAN_POINT ( 'NONE',  ( -84.50707362346616947, 8.102448949553176405, 5.886773742842740909 ) ) ;
#61336=CARTESIAN_POINT ( 'NONE',  ( -96.29292637653490772, 3.094860106600143101, -9.525000000013280399 ) ) ;
#61339=CARTESIAN_POINT ( 'NONE',  ( -124.7049999999999841, 2.607480562269073321, 8.024999999999991473 ) ) ;
#61343=CARTESIAN_POINT ( 'NONE',  ( -137.6949999999999932, -8.437984349512085203, 5.166775262442717831E-16 ) ) ;
#61344=CARTESIAN_POINT ( 'NONE',  ( -128.2450000000000045, -4.716976649647093289, -6.492361379858945902 ) ) ;
#61352=CARTESIAN_POINT ( 'NONE',  ( -178.0429263765338135, -9.058813317711329915, -2.943386871421370898 ) ) ;
#61354=CARTESIAN_POINT ( 'NONE',  ( -52.64499999999999602, 4.716976649647091513, -6.492361379858946790 ) ) ;
#61361=CARTESIAN_POINT ( 'NONE',  ( -97.34292637653379643, -9.058813317711329915, 2.943386871421371787 ) ) ;
#61370=VERTEX_POINT ( 'NONE', #58191 ) ;
#61384=CARTESIAN_POINT ( 'NONE',  ( -178.9429263765338192, 0.000000000000000000, 9.524999999999991473 ) ) ;
#61386=CARTESIAN_POINT ( 'NONE',  ( -80.39499999999998181, -6.826472737025115478, -4.959722759717899443 ) ) ;
#61398=CARTESIAN_POINT ( 'NONE',  ( -137.6929263765337623, 10.01517768586948698, -1.839758294383808966E-15 ) ) ;
#61401=CARTESIAN_POINT ( 'NONE',  ( -180.9570736234661865, 9.058813317711329915, -2.943386871421373119 ) ) ;
#61404=CARTESIAN_POINT ( 'NONE',  ( -116.4570736234661723, -9.058813317711329915, 2.943386871421371787 ) ) ;
#61405=CARTESIAN_POINT ( 'NONE',  ( -183.0586401562165975, 6.645247303096274649, -6.780310176063176542 ) ) ;
#61407=ORIENTED_EDGE ( 'NONE', *, *, #24665, .F. ) ;
#61411=CARTESIAN_POINT ( 'NONE',  ( -162.8050000000000068, -8.437984349512085203, 5.166775262442717831E-16 ) ) ;
#61413=CARTESIAN_POINT ( 'NONE',  ( -183.4829137129417234, -3.065004353576823881, -8.530224930386903992 ) ) ;
#61414=CARTESIAN_POINT ( 'NONE',  ( -161.8449999999999989, -7.632228543268599452, 2.479861379858951054 ) ) ;
#61415=CARTESIAN_POINT ( 'NONE',  ( -157.4950000000000045, 6.826472737025113702, -4.959722759717902107 ) ) ;
#61421=CARTESIAN_POINT ( 'NONE',  ( -73.55499999999997840, 0.000000000000000000, 8.024999999999991473 ) ) ;
#61424=CARTESIAN_POINT ( 'NONE',  ( -73.94499999999997897, -9.827790563157499189E-16, -8.024999999999991473 ) ) ;
#61440=ORIENTED_EDGE ( 'NONE', *, *, #50914, .F. ) ;
#61441=CARTESIAN_POINT ( 'NONE',  ( -60.20707362346617231, 3.094860106618433360, 9.524999999999991473 ) ) ;
#61445=( BOUNDED_CURVE ( )  B_SPLINE_CURVE ( 2, ( #65718, #1285, #7333, #43962, #28397, #6277, #5922, #65377, #23166, #17559, #33367 ),
 .UNSPECIFIED., .F., .F. ) 
 B_SPLINE_CURVE_WITH_KNOTS ( ( 3, 2, 2, 2, 2, 3 ),
 ( 0.8260869565217391353, 0.8282608695652173836, 0.8304347826086956319, 0.8326086956521738802, 0.8347826086956521285, 0.8369565217391304879 ),
 .UNSPECIFIED. ) 
 CURVE ( )  GEOMETRIC_REPRESENTATION_ITEM ( )  RATIONAL_B_SPLINE_CURVE ( ( 1.000000000000000000, 0.9510565162951535312, 1.000000000000000000, 0.9510565162951535312, 1.000000000000000000, 0.9510565162951535312, 1.000000000000000000, 0.9510565162951535312, 1.000000000000000000, 0.9510565162951535312, 1.000000000000000000 ) ) 
 REPRESENTATION_ITEM ( '' )  );
#61451=DIRECTION ( 'NONE',  ( -1.000000000000000000, -0.000000000000000000, -0.000000000000000000 ) ) ;
#61458=CARTESIAN_POINT ( 'NONE',  ( -113.3949999999999818, -6.826472737025115478, -4.959722759717899443 ) ) ;
#61462=CARTESIAN_POINT ( 'NONE',  ( -54.29292637653379217, 3.094860106618428031, -9.524999999999993250 ) ) ;
#61474=CARTESIAN_POINT ( 'NONE',  ( -137.7549999999999955, 4.716976649647091513, -6.492361379858946790 ) ) ;
#61480=CARTESIAN_POINT ( 'NONE',  ( -107.1570736234661751, -9.058813317711329915, -2.943386871421370898 ) ) ;
#61493=CARTESIAN_POINT ( 'NONE',  ( -51.20707362346615099, 3.094860106618433360, 9.524999999999991473 ) ) ;
#61496=ORIENTED_EDGE ( 'NONE', *, *, #2746, .T. ) ;
#61499=CARTESIAN_POINT ( 'NONE',  ( -97.85499999999998977, 4.716976649647094177, 6.492361379858945902 ) ) ;
#61504=CARTESIAN_POINT ( 'NONE',  ( -99.74499999999999034, 4.716976649647094177, 6.492361379858945902 ) ) ;
#61506=CARTESIAN_POINT ( 'NONE',  ( -79.79500000000000171, 2.607480562269068880, -8.024999999999993250 ) ) ;
#61507=EDGE_CURVE ( 'NONE', #60435, #55574, #64879, .T. ) ;
#61515=CARTESIAN_POINT ( 'NONE',  ( -114.2929263765338135, 3.094860106618428031, -9.524999999999993250 ) ) ;
#61516=CARTESIAN_POINT ( 'NONE',  ( -138.7450000000000045, 4.716976649647094177, 6.492361379858945902 ) ) ;
#61533=ORIENTED_EDGE ( 'NONE', *, *, #20260, .T. ) ;
#61534=CARTESIAN_POINT ( 'NONE',  ( -130.7049999999999841, 2.607480562269072433, 8.024999999999991473 ) ) ;
#61563=CARTESIAN_POINT ( 'NONE',  ( -165.0550000000000068, -9.827790563157499189E-16, -8.024999999999991473 ) ) ;
#61575=CARTESIAN_POINT ( 'NONE',  ( -75.50499999999998124, -6.826472737025115478, -4.959722759717899443 ) ) ;
#61578=CARTESIAN_POINT ( 'NONE',  ( -63.35707362346617089, 5.598654528085804216, 7.705886871421366635 ) ) ;
#61584=CARTESIAN_POINT ( 'NONE',  ( -53.30707362346617373, -10.01517768586948698, 6.132527647946031529E-16 ) ) ;
#61588=CARTESIAN_POINT ( 'NONE',  ( -111.2949999999999733, -2.607480562269069768, 8.024999999999991473 ) ) ;
#61596=CARTESIAN_POINT ( 'NONE',  ( -16.62603730713679795, 11.02523255763448873, 4.739503200942572825 ) ) ;
#61597=CARTESIAN_POINT ( 'NONE',  ( -143.9929263765337737, 8.102448949553171076, -5.886773742842744461 ) ) ;
#61598=CARTESIAN_POINT ( 'NONE',  ( -162.2949999999999875, -2.607480562269069768, 8.024999999999991473 ) ) ;
#61617=CARTESIAN_POINT ( 'NONE',  ( -158.6049999999999898, 6.826472737025113702, -4.959722759717902107 ) ) ;
#61631=CARTESIAN_POINT ( 'NONE',  ( -72.95499999999999829, -7.632228543268599452, 2.479861379858951054 ) ) ;
#61639=CARTESIAN_POINT ( 'NONE',  ( -52.34499999999997755, 7.632228543268599452, -2.479861379858951942 ) ) ;
#61647=CARTESIAN_POINT ( 'NONE',  ( -56.54499999999998749, -7.632228543268600340, -2.479861379858950166 ) ) ;
#61651=CARTESIAN_POINT ( 'NONE',  ( -102.8049999999999784, -8.437984349512085203, 5.166775262442717831E-16 ) ) ;
#61654=CARTESIAN_POINT ( 'NONE',  ( -142.1070736234661638, 8.102448949553171076, -5.886773742842744461 ) ) ;
#61657=CARTESIAN_POINT ( 'NONE',  ( -85.10707362346614957, 8.102448949553171076, -5.886773742842744461 ) ) ;
#61661=DIRECTION ( 'NONE',  ( -0.000000000000000000, 1.000000000000000000, -0.000000000000000000 ) ) ;
#61663=CARTESIAN_POINT ( 'NONE',  ( -118.7049999999999699, 2.607480562269073321, 8.024999999999991473 ) ) ;
#61666=CARTESIAN_POINT ( 'NONE',  ( -133.3449999999999989, 7.632228543268599452, -2.479861379858951942 ) ) ;
#61670=CARTESIAN_POINT ( 'NONE',  ( -116.2449999999999903, -4.716976649647093289, -6.492361379858945902 ) ) ;
#61680=CARTESIAN_POINT ( 'NONE',  ( -169.3429263765337964, -9.058813317711329915, 2.943386871421371787 ) ) ;
#61690=ORIENTED_EDGE ( 'NONE', *, *, #62958, .T. ) ;
#61691=CARTESIAN_POINT ( 'NONE',  ( -88.79292637653379927, -3.094860106618429807, 9.524999999999991473 ) ) ;
#61703=CARTESIAN_POINT ( 'NONE',  ( -64.34292637653379643, -9.058813317711329915, 2.943386871421371787 ) ) ;
#61718=CARTESIAN_POINT ( 'NONE',  ( -70.70707362346615810, -3.094860106618431139, -9.524999999999991473 ) ) ;
#61719=CARTESIAN_POINT ( 'NONE',  ( -78.89499999999999602, 6.826472737025116366, 4.959722759717898555 ) ) ;
#61722=EDGE_CURVE ( 'NONE', #69443, #42429, #48287, .T. ) ;
#61731=ORIENTED_EDGE ( 'NONE', *, *, #54702, .T. ) ;
#61738=CARTESIAN_POINT ( 'NONE',  ( -165.0570736234661524, 0.000000000000000000, 9.524999999999991473 ) ) ;
#61742=CARTESIAN_POINT ( 'NONE',  ( -116.3070736234661666, -10.01517768586948698, 6.132527647946031529E-16 ) ) ;
#61751=CARTESIAN_POINT ( 'NONE',  ( -149.4550000000000125, 7.632228543268599452, -2.479861379858951942 ) ) ;
#61753=CARTESIAN_POINT ( 'NONE',  ( -148.9429263765338192, 0.000000000000000000, 9.524999999999991473 ) ) ;
#61754=CARTESIAN_POINT ( 'NONE',  ( -160.3449999999999989, 7.632228543268599452, -2.479861379858951942 ) ) ;
#61755=CARTESIAN_POINT ( 'NONE',  ( -145.9449999999999932, -9.827790563157499189E-16, -8.024999999999991473 ) ) ;
#61761=CARTESIAN_POINT ( 'NONE',  ( -122.0929263765346064, 3.094860106631541985, 9.524999999990470201 ) ) ;
#61762=CARTESIAN_POINT ( 'NONE',  ( -66.80499999999999261, -8.437984349512085203, 5.166775262442717831E-16 ) ) ;
#61765=CARTESIAN_POINT ( 'NONE',  ( -69.74499999999999034, 4.716976649647094177, 6.492361379858945902 ) ) ;
#61769=EDGE_CURVE ( 'NONE', #52329, #23235, #20661, .T. ) ;
#61778=LINE ( 'NONE', #2670, #58443 ) ;
#61794=ORIENTED_EDGE ( 'NONE', *, *, #52033, .T. ) ;
#61799=CARTESIAN_POINT ( 'NONE',  ( -82.70707362346617231, -3.094860106618431139, -9.524999999999991473 ) ) ;
#61801=CARTESIAN_POINT ( 'NONE',  ( -114.8949999999999818, 6.826472737025116366, 4.959722759717898555 ) ) ;
#61805=CARTESIAN_POINT ( 'NONE',  ( -53.99292637653379501, 8.102448949553172852, -5.886773742842744461 ) ) ;
#61806=CARTESIAN_POINT ( 'NONE',  ( -13.37774330277911794, -11.02468314135572491, -4.740767624907036293 ) ) ;
#61822=CARTESIAN_POINT ( 'NONE',  ( -132.2049999999999841, -2.607480562269071545, -8.024999999999991473 ) ) ;
#61838=CARTESIAN_POINT ( 'NONE',  ( -195.0000000000000000, 1.166476076187852838E-15, -9.524999999999991473 ) ) ;
#61841=CARTESIAN_POINT ( 'NONE',  ( -48.65499999999997272, -7.632228543268600340, -2.479861379858950166 ) ) ;
#61843=CARTESIAN_POINT ( 'NONE',  ( -177.5049999999999670, -6.826472737025115478, -4.959722759717899443 ) ) ;
#61847=CARTESIAN_POINT ( 'NONE',  ( -57.65707362346616804, 9.058813317711329915, 2.943386871421369566 ) ) ;
#61848=CARTESIAN_POINT ( 'NONE',  ( -175.7950000000000159, 2.607480562269069324, -8.024999999999993250 ) ) ;
#61854=CARTESIAN_POINT ( 'NONE',  ( -161.1570736234661751, -9.058813317711329915, -2.943386871421370898 ) ) ;
#61855=EDGE_CURVE ( 'NONE', #64066, #8408, #66750, .T. ) ;
#61858=CARTESIAN_POINT ( 'NONE',  ( -102.0549999999999926, -9.827790563157499189E-16, -8.024999999999991473 ) ) ;
#61863=EDGE_CURVE ( 'NONE', #29745, #12752, #19479, .T. ) ;
#61864=CARTESIAN_POINT ( 'NONE',  ( -102.1449999999999818, -4.716976649647092401, 6.492361379858946790 ) ) ;
#61866=CARTESIAN_POINT ( 'NONE',  ( -66.74499999999999034, 4.716976649647094177, 6.492361379858945902 ) ) ;
#61875=CARTESIAN_POINT ( 'NONE',  ( -118.0429263765338135, -9.058813317711329915, -2.943386871421370898 ) ) ;
#61879=CARTESIAN_POINT ( 'NONE',  ( -141.2949999999999875, -2.607480562269069768, 8.024999999999991473 ) ) ;
#61886=CARTESIAN_POINT ( 'NONE',  ( -174.2929263765339272, 3.094860106616311057, -9.525000000001533351 ) ) ;
#61897=CARTESIAN_POINT ( 'NONE',  ( -127.7049999999999557, 2.607480562269072433, 8.024999999999991473 ) ) ;
#61900=CARTESIAN_POINT ( 'NONE',  ( -122.3070736234661950, -10.01517768586948698, 6.132527647946031529E-16 ) ) ;
#61906=CARTESIAN_POINT ( 'NONE',  ( -102.1429263765337936, 5.598654528085800663, -7.705886871421367523 ) ) ;
#61923=LINE ( 'NONE', #13749, #68900 ) ;
#61925=CARTESIAN_POINT ( 'NONE',  ( -162.3549999999999898, -4.716976649647093289, -6.492361379858945902 ) ) ;
#61926=EDGE_LOOP ( 'NONE', ( #10548, #15820, #33157, #696 ) ) ;
#61931=ORIENTED_EDGE ( 'NONE', *, *, #2755, .T. ) ;
#61935=CIRCLE ( 'NONE', #31605, 5.499999999999985789 ) ;
#61938=CARTESIAN_POINT ( 'NONE',  ( -73.25499999999998124, -4.716976649647092401, 6.492361379858946790 ) ) ;
#61954=CARTESIAN_POINT ( 'NONE',  ( -99.59499999999999886, 2.607480562269073321, 8.024999999999991473 ) ) ;
#61960=CARTESIAN_POINT ( 'NONE',  ( -143.3929263765338078, 8.102448949553176405, 5.886773742842740909 ) ) ;
#61962=CARTESIAN_POINT ( 'NONE',  ( -163.6449999999999818, 4.716976649647091513, -6.492361379858946790 ) ) ;
#61977=CARTESIAN_POINT ( 'NONE',  ( -173.7570736234661695, -5.598654528085801552, 7.705886871421367523 ) ) ;
#61982=CARTESIAN_POINT ( 'NONE',  ( -162.5049999999999670, -6.826472737025113702, -4.959722759717900331 ) ) ;
#61984=VECTOR ( 'NONE', #7577, 1000.000000000000000 ) ;
#61991=CARTESIAN_POINT ( 'NONE',  ( -73.85499999999998977, 4.716976649647094177, 6.492361379858945902 ) ) ;
#61999=CARTESIAN_POINT ( 'NONE',  ( -114.2929263765346803, 3.094860106603773531, -9.525000000010640733 ) ) ;
#62004=CARTESIAN_POINT ( 'NONE',  ( -48.74499999999998323, 4.716976649647094177, 6.492361379858945902 ) ) ;
#62005=ORIENTED_EDGE ( 'NONE', *, *, #5529, .F. ) ;
#62006=( BOUNDED_CURVE ( )  B_SPLINE_CURVE ( 2, ( #45077, #2771, #13710, #18966, #40135, #57312, #56971, #13018, #56266, #8093, #14393 ),
 .UNSPECIFIED., .F., .F. ) 
 B_SPLINE_CURVE_WITH_KNOTS ( ( 3, 2, 2, 2, 2, 3 ),
 ( 0.8804347826086956763, 0.8826086956521739246, 0.8847826086956521729, 0.8869565217391304213, 0.8891304347826086696, 0.8913043478260869179 ),
 .UNSPECIFIED. ) 
 CURVE ( )  GEOMETRIC_REPRESENTATION_ITEM ( )  RATIONAL_B_SPLINE_CURVE ( ( 1.000000000000000000, 0.9510565162951535312, 1.000000000000000000, 0.9510565162951535312, 1.000000000000000000, 0.9510565162951535312, 1.000000000000000000, 0.9510565162951535312, 1.000000000000000000, 0.9510565162951535312, 1.000000000000000000 ) ) 
 REPRESENTATION_ITEM ( '' )  );
#62010=CARTESIAN_POINT ( 'NONE',  ( -53.39499999999998892, -6.826472737025113702, -4.959722759717900331 ) ) ;
#62015=CARTESIAN_POINT ( 'NONE',  ( -101.1550000000000011, 7.632228543268600340, 2.479861379858949277 ) ) ;
#62019=CARTESIAN_POINT ( 'NONE',  ( -136.7070736234661297, -3.094860106618431139, -9.524999999999991473 ) ) ;
#62021=CARTESIAN_POINT ( 'NONE',  ( -59.15707362346617515, -9.058813317711329915, -2.943386871421370898 ) ) ;
#62023=CARTESIAN_POINT ( 'NONE',  ( -73.10707362346614957, 8.102448949553171076, -5.886773742842744461 ) ) ;
#62025=DIRECTION ( 'NONE',  ( 0.7071067811865426878, 8.659560562354994488E-17, 0.7071067811865524577 ) ) ;
#62029=CARTESIAN_POINT ( 'NONE',  ( -99.59292637653487645, -3.094860106636313279, -9.524999999987000976 ) ) ;
#62031=CARTESIAN_POINT ( 'NONE',  ( -121.8549999999999898, 4.716976649647094177, 6.492361379858945902 ) ) ;
#62034=CARTESIAN_POINT ( 'NONE',  ( -138.8949999999999534, 6.826472737025116366, 4.959722759717898555 ) ) ;
#62035=CARTESIAN_POINT ( 'NONE',  ( -121.0449999999999875, 7.632228543268600340, 2.479861379858949277 ) ) ;
#62041=CARTESIAN_POINT ( 'NONE',  ( -174.8929263765337794, -8.102448949553172852, -5.886773742842741797 ) ) ;
#62042=CARTESIAN_POINT ( 'NONE',  ( -53.09499999999997755, -2.607480562269071545, -8.024999999999991473 ) ) ;
#62048=CARTESIAN_POINT ( 'NONE',  ( -88.34292637653381064, -9.058813317711329915, 2.943386871421371787 ) ) ;
#62053=CARTESIAN_POINT ( 'NONE',  ( -180.4429263765338192, -1.166476076187852838E-15, -9.524999999999991473 ) ) ;
#62057=CARTESIAN_POINT ( 'NONE',  ( -157.4070736234665446, 3.094860106613151807, -9.525000000003830181 ) ) ;
#62059=CARTESIAN_POINT ( 'NONE',  ( -136.0429263765338135, -9.058813317711329915, -2.943386871421370898 ) ) ;
#62062=ORIENTED_EDGE ( 'NONE', *, *, #46446, .F. ) ;
#62063=CYLINDRICAL_SURFACE ( 'NONE', #51046, 9.524999999999991473 ) ;
#62064=VECTOR ( 'NONE', #64270, 1000.000000000000000 ) ;
#62069=ORIENTED_EDGE ( 'NONE', *, *, #29859, .T. ) ;
#62070=CARTESIAN_POINT ( 'NONE',  ( -98.15499999999998693, 7.632228543268600340, 2.479861379858949277 ) ) ;
#62072=ORIENTED_EDGE ( 'NONE', *, *, #11446, .F. ) ;
#62079=CARTESIAN_POINT ( 'NONE',  ( -85.94499999999999318, -9.827790563157499189E-16, -8.024999999999991473 ) ) ;
#62089=EDGE_CURVE ( 'NONE', #24627, #53864, #66679, .T. ) ;
#62097=PLANE ( 'NONE',  #38104 ) ;
#62100=CARTESIAN_POINT ( 'NONE',  ( -168.8070736234661808, 10.01517768586948698, -1.839758294383808571E-15 ) ) ;
#62104=CARTESIAN_POINT ( 'NONE',  ( -112.2570736234661837, 5.598654528085800663, -7.705886871421367523 ) ) ;
#62110=LINE ( 'NONE', #18170, #44139 ) ;
#62111=CARTESIAN_POINT ( 'NONE',  ( -81.89292637653380780, -8.102448949553174629, -5.886773742842741797 ) ) ;
#62115=CARTESIAN_POINT ( 'NONE',  ( -150.0550000000000068, -9.827790563157499189E-16, -8.024999999999991473 ) ) ;
#62117=CARTESIAN_POINT ( 'NONE',  ( -162.8949999999999534, 6.826472737025116366, 4.959722759717898555 ) ) ;
#62120=CARTESIAN_POINT ( 'NONE',  ( -149.5449999999999875, -7.632228543268600340, -2.479861379858950166 ) ) ;
#62122=CARTESIAN_POINT ( 'NONE',  ( -67.19292637653377653, -10.01517768586948698, 6.132527647946031529E-16 ) ) ;
#62126=CARTESIAN_POINT ( 'NONE',  ( -63.05499999999998550, -9.827790563157499189E-16, -8.024999999999991473 ) ) ;
#62129=CARTESIAN_POINT ( 'NONE',  ( -63.59499999999997044, 2.607480562269072433, 8.024999999999991473 ) ) ;
#62132=CARTESIAN_POINT ( 'NONE',  ( -142.7070736234666981, -3.094860106626767138, -9.524999999993935873 ) ) ;
#62135=CARTESIAN_POINT ( 'NONE',  ( -159.3570736234661922, 5.598654528085804216, 7.705886871421366635 ) ) ;
#62160=CARTESIAN_POINT ( 'NONE',  ( -157.5570736234661808, -1.166476076187852838E-15, -9.524999999999991473 ) ) ;
#62162=CARTESIAN_POINT ( 'NONE',  ( -113.6949999999999790, -8.437984349512085203, 5.166775262442717831E-16 ) ) ;
#62168=CARTESIAN_POINT ( 'NONE',  ( -164.3070736234661808, -10.01517768586948698, 6.132527647946031529E-16 ) ) ;
#62169=AXIS2_PLACEMENT_3D ( 'NONE', #22281, #44487, #6786 ) ;
#62184=CYLINDRICAL_SURFACE ( 'NONE', #20904, 9.524999999999991473 ) ;
#62185=CARTESIAN_POINT ( 'NONE',  ( -126.6549999999999869, -7.632228543268600340, -2.479861379858950166 ) ) ;
#62202=CARTESIAN_POINT ( 'NONE',  ( -51.20499999999996277, -2.607480562269071545, -8.024999999999991473 ) ) ;
#62205=CARTESIAN_POINT ( 'NONE',  ( -179.1550000000000011, 7.632228543268600340, 2.479861379858949277 ) ) ;
#62207=CARTESIAN_POINT ( 'NONE',  ( -56.30707362346618794, -10.01517768586948698, 6.132527647946031529E-16 ) ) ;
#62209=CARTESIAN_POINT ( 'NONE',  ( -177.4449999999999932, 0.000000000000000000, 8.024999999999991473 ) ) ;
#62211=ORIENTED_EDGE ( 'NONE', *, *, #735, .T. ) ;
#62213=CARTESIAN_POINT ( 'NONE',  ( -161.6070736234661354, -8.102448949553174629, 5.886773742842742685 ) ) ;
#62215=CARTESIAN_POINT ( 'NONE',  ( -163.5570736234661524, -1.166476076187852838E-15, -9.524999999999991473 ) ) ;
#62216=CARTESIAN_POINT ( 'NONE',  ( -88.40499999999997272, -2.607480562269069768, 8.024999999999991473 ) ) ;
#62220=CARTESIAN_POINT ( 'NONE',  ( -88.34499999999999886, 7.632228543268599452, -2.479861379858951942 ) ) ;
#62222=CARTESIAN_POINT ( 'NONE',  ( -67.34499999999998465, 7.632228543268599452, -2.479861379858951942 ) ) ;
#62232=CARTESIAN_POINT ( 'NONE',  ( -112.3429263765337964, -9.058813317711329915, 2.943386871421371787 ) ) ;
#62233=CARTESIAN_POINT ( 'NONE',  ( -127.6450000000000102, 4.716976649647091513, -6.492361379858946790 ) ) ;
#62237=CARTESIAN_POINT ( 'NONE',  ( -131.0929263765344785, 3.094860106629860663, 9.524999999991687005 ) ) ;
#62249=CARTESIAN_POINT ( 'NONE',  ( -133.5549999999999784, 0.000000000000000000, 8.024999999999991473 ) ) ;
#62253=CARTESIAN_POINT ( 'NONE',  ( -125.1570736234661751, -9.058813317711329915, -2.943386871421370898 ) ) ;
#62255=EDGE_LOOP ( 'NONE', ( #17210, #6888 ) ) ;
#62258=VERTEX_POINT ( 'NONE', #68411 ) ;
#62286=CARTESIAN_POINT ( 'NONE',  ( -153.6549999999999727, -7.632228543268600340, -2.479861379858950166 ) ) ;
#62295=ORIENTED_EDGE ( 'NONE', *, *, #60425, .F. ) ;
#62300=CARTESIAN_POINT ( 'NONE',  ( -71.15499999999998693, 7.632228543268600340, 2.479861379858949277 ) ) ;
#62314=CARTESIAN_POINT ( 'NONE',  ( -99.89499999999998181, 6.826472737025116366, 4.959722759717898555 ) ) ;
#62321=CARTESIAN_POINT ( 'NONE',  ( -141.4429263765337907, -1.166476076187852838E-15, -9.524999999999991473 ) ) ;
#62323=CARTESIAN_POINT ( 'NONE',  ( -155.6949999999999932, -8.437984349512085203, 5.166775262442717831E-16 ) ) ;
#62331=( BOUNDED_CURVE ( )  B_SPLINE_CURVE ( 2, ( #22588, #44090, #17342, #65844, #38804, #60217, #43411, #49678, #6054, #27823, #21900 ),
 .UNSPECIFIED., .F., .F. ) 
 B_SPLINE_CURVE_WITH_KNOTS ( ( 3, 2, 2, 2, 2, 3 ),
 ( 0.7717391304347825942, 0.7739130434782608425, 0.7760869565217390909, 0.7782608695652173392, 0.7804347826086956985, 0.7826086956521739468 ),
 .UNSPECIFIED. ) 
 CURVE ( )  GEOMETRIC_REPRESENTATION_ITEM ( )  RATIONAL_B_SPLINE_CURVE ( ( 1.000000000000000000, 0.9510565162951535312, 1.000000000000000000, 0.9510565162951535312, 1.000000000000000000, 0.9510565162951535312, 1.000000000000000000, 0.9510565162951535312, 1.000000000000000000, 0.9510565162951535312, 1.000000000000000000 ) ) 
 REPRESENTATION_ITEM ( '' )  );
#62335=CARTESIAN_POINT ( 'NONE',  ( -173.9070736234663173, -3.094860106616648121, 9.525000000001288214 ) ) ;
#62338=CARTESIAN_POINT ( 'NONE',  ( -159.5049999999999955, -6.826472737025113702, -4.959722759717900331 ) ) ;
#62346=DIRECTION ( 'NONE',  ( -1.000000000000000000, -0.000000000000000000, -0.000000000000000000 ) ) ;
#62354=CARTESIAN_POINT ( 'NONE',  ( -70.70499999999996987, 2.607480562269072433, 8.024999999999991473 ) ) ;
#62366=CARTESIAN_POINT ( 'NONE',  ( -55.49499999999999034, 6.826472737025113702, -4.959722759717902107 ) ) ;
#62377=CARTESIAN_POINT ( 'NONE',  ( -101.9049999999999869, 2.607480562269068880, -8.024999999999993250 ) ) ;
#62383=CARTESIAN_POINT ( 'NONE',  ( -140.0070736234661979, -8.102448949553172852, -5.886773742842741797 ) ) ;
#62388=CARTESIAN_POINT ( 'NONE',  ( -78.20707362346615810, 3.094860106618433360, 9.524999999999991473 ) ) ;
#62392=CARTESIAN_POINT ( 'NONE',  ( -18.05714352263349909, -11.32599168300350279, -3.969768029961437072 ) ) ;
#62394=CARTESIAN_POINT ( 'NONE',  ( -99.74292637653380211, -5.598654528085803328, -7.705886871421366635 ) ) ;
#62395=CARTESIAN_POINT ( 'NONE',  ( -122.4549999999999983, 7.632228543268599452, -2.479861379858951942 ) ) ;
#62396=CARTESIAN_POINT ( 'NONE',  ( -158.5429263765338135, 9.058813317711329915, 2.943386871421369566 ) ) ;
#62398=CARTESIAN_POINT ( 'NONE',  ( -129.4449999999999648, 0.000000000000000000, 8.024999999999991473 ) ) ;
#62399=CARTESIAN_POINT ( 'NONE',  ( -120.1449999999999818, -4.716976649647092401, 6.492361379858946790 ) ) ;
#62405=CARTESIAN_POINT ( 'NONE',  ( -176.9929263765337737, 8.102448949553171076, -5.886773742842744461 ) ) ;
#62414=CARTESIAN_POINT ( 'NONE',  ( -88.49292637653381632, -8.102448949553172852, 5.886773742842742685 ) ) ;
#62418=ADVANCED_FACE ( 'NONE', ( #6797 ), #12767, .T. ) ;
#62420=CARTESIAN_POINT ( 'NONE',  ( -162.5929263765341091, -3.094860106623204210, -9.524999999996525801 ) ) ;
#62429=CARTESIAN_POINT ( 'NONE',  ( -103.6429263765337936, -5.598654528085801552, 7.705886871421367523 ) ) ;
#62431=VERTEX_POINT ( 'NONE', #55693 ) ;
#62433=CARTESIAN_POINT ( 'NONE',  ( -105.8049999999999926, -8.437984349512086979, 5.166775262442717831E-16 ) ) ;
#62435=VERTEX_POINT ( 'NONE', #44152 ) ;
#62444=CARTESIAN_POINT ( 'NONE',  ( -81.44499999999999318, 0.000000000000000000, 8.024999999999991473 ) ) ;
#62456=CARTESIAN_POINT ( 'NONE',  ( -173.6070736234661638, -8.102448949553172852, 5.886773742842742685 ) ) ;
#62460=CARTESIAN_POINT ( 'NONE',  ( -105.2070736234661723, 3.094860106618433360, 9.524999999999991473 ) ) ;
#62464=CARTESIAN_POINT ( 'NONE',  ( -108.2929263765347656, 3.094860106602562944, -9.525000000011520029 ) ) ;
#62466=CARTESIAN_POINT ( 'NONE',  ( -114.2070736234670250, 3.094860106632685071, 9.524999999989637089 ) ) ;
#62469=CARTESIAN_POINT ( 'NONE',  ( -151.2549999999999955, -4.716976649647092401, 6.492361379858946790 ) ) ;
#62471=CARTESIAN_POINT ( 'NONE',  ( -153.4449999999999932, 0.000000000000000000, 8.024999999999991473 ) ) ;
#62472=CARTESIAN_POINT ( 'NONE',  ( -143.8449999999999989, -7.632228543268599452, 2.479861379858951054 ) ) ;
#62473=VERTEX_POINT ( 'NONE', #50088 ) ;
#62477=CARTESIAN_POINT ( 'NONE',  ( -65.00499999999998124, 6.826472737025116366, 4.959722759717898555 ) ) ;
#62479=CARTESIAN_POINT ( 'NONE',  ( -168.4429263765337907, -1.166476076187852838E-15, -9.524999999999991473 ) ) ;
#62481=CARTESIAN_POINT ( 'NONE',  ( -65.99499999999997613, -6.826472737025113702, 4.959722759717902107 ) ) ;
#62490=LINE ( 'NONE', #3358, #68647 ) ;
#62493=DIRECTION ( 'NONE',  ( -1.000000000000000000, -0.000000000000000000, -0.000000000000000000 ) ) ;
#62503=ORIENTED_EDGE ( 'NONE', *, *, #36149, .F. ) ;
#62508=CARTESIAN_POINT ( 'NONE',  ( -65.09292637653379643, 3.094860106618433360, 9.524999999999991473 ) ) ;
#62514=CARTESIAN_POINT ( 'NONE',  ( -111.2949999999999733, -2.607480562269069768, 8.024999999999991473 ) ) ;
#62517=CARTESIAN_POINT ( 'NONE',  ( -178.5570736234661808, -1.166476076187852838E-15, -9.524999999999991473 ) ) ;
#62531=CARTESIAN_POINT ( 'NONE',  ( -120.8049999999999784, -8.437984349512085203, 5.166775262442717831E-16 ) ) ;
#62532=CARTESIAN_POINT ( 'NONE',  ( -183.9999999999999432, -6.383969465318038772, 4.878217756231068236 ) ) ;
#62536=CARTESIAN_POINT ( 'NONE',  ( -195.0000000000000000, 0.000000000000000000, 9.524999999999991473 ) ) ;
#62544=CARTESIAN_POINT ( 'NONE',  ( -183.5049999999999955, -6.826472737025115478, -4.959722759717899443 ) ) ;
#62546=CARTESIAN_POINT ( 'NONE',  ( -54.50707362346614104, 8.102448949553176405, 5.886773742842740909 ) ) ;
#62547=CARTESIAN_POINT ( 'NONE',  ( -179.3950000000000102, -6.826472737025113702, -4.959722759717900331 ) ) ;
#62552=CARTESIAN_POINT ( 'NONE',  ( -93.35499999999998977, -4.716976649647093289, -6.492361379858945902 ) ) ;
#62557=CARTESIAN_POINT ( 'NONE',  ( -93.14499999999999602, -4.716976649647092401, 6.492361379858946790 ) ) ;
#62560=CARTESIAN_POINT ( 'NONE',  ( -73.04499999999998749, 7.632228543268600340, 2.479861379858949277 ) ) ;
#62569=CARTESIAN_POINT ( 'NONE',  ( -113.9929263765338021, 8.102448949553171076, -5.886773742842744461 ) ) ;
#62570=CARTESIAN_POINT ( 'NONE',  ( -128.2450000000000045, -4.716976649647093289, -6.492361379858945902 ) ) ;
#62575=ADVANCED_FACE ( 'NONE', ( #60480 ), #12650, .T. ) ;
#62579=ORIENTED_EDGE ( 'NONE', *, *, #20766, .T. ) ;
#62587=CARTESIAN_POINT ( 'NONE',  ( -127.1049999999999898, -6.826472737025113702, 4.959722759717902107 ) ) ;
#62590=CARTESIAN_POINT ( 'NONE',  ( -126.0570736234661808, 0.000000000000000000, 9.524999999999991473 ) ) ;
#62592=CARTESIAN_POINT ( 'NONE',  ( -172.0429263765338135, -9.058813317711329915, -2.943386871421370898 ) ) ;
#62612=CARTESIAN_POINT ( 'NONE',  ( -56.54292637653379927, 9.058813317711329915, 2.943386871421369566 ) ) ;
#62614=CARTESIAN_POINT ( 'NONE',  ( -148.8549999999999898, 4.716976649647094177, 6.492361379858945902 ) ) ;
#62615=ORIENTED_EDGE ( 'NONE', *, *, #14902, .F. ) ;
#62617=( BOUNDED_CURVE ( )  B_SPLINE_CURVE ( 2, ( #5738, #26164, #26831, #63801, #64510, #42068, #25820, #16356, #69439, #31433, #37830 ),
 .UNSPECIFIED., .F., .F. ) 
 B_SPLINE_CURVE_WITH_KNOTS ( ( 3, 2, 2, 2, 2, 3 ),
 ( 0.7826086956521739468, 0.7847826086956521952, 0.7869565217391304435, 0.7891304347826086918, 0.7913043478260869401, 0.7934782608695651884 ),
 .UNSPECIFIED. ) 
 CURVE ( )  GEOMETRIC_REPRESENTATION_ITEM ( )  RATIONAL_B_SPLINE_CURVE ( ( 1.000000000000000000, 0.9510565162951535312, 1.000000000000000000, 0.9510565162951535312, 1.000000000000000000, 0.9510565162951535312, 1.000000000000000000, 0.9510565162951535312, 1.000000000000000000, 0.9510565162951535312, 1.000000000000000000 ) ) 
 REPRESENTATION_ITEM ( '' )  );
#62627=CARTESIAN_POINT ( 'NONE',  ( -66.65499999999998693, -7.632228543268600340, -2.479861379858950166 ) ) ;
#62640=CARTESIAN_POINT ( 'NONE',  ( -98.24499999999999034, -4.716976649647093289, -6.492361379858945902 ) ) ;
#62645=CARTESIAN_POINT ( 'NONE',  ( -142.3429263765338249, -9.058813317711329915, 2.943386871421371787 ) ) ;
#62646=CARTESIAN_POINT ( 'NONE',  ( -159.7450000000000045, 4.716976649647094177, 6.492361379858945902 ) ) ;
#62653=ORIENTED_EDGE ( 'NONE', *, *, #34773, .F. ) ;
#62660=CARTESIAN_POINT ( 'NONE',  ( -195.0000000000000000, 0.000000000000000000, 0.000000000000000000 ) ) ;
#62666=CARTESIAN_POINT ( 'NONE',  ( -157.4050000000000011, -2.607480562269069768, 8.024999999999991473 ) ) ;
#62672=CARTESIAN_POINT ( 'NONE',  ( -48.05707362346617373, 0.000000000000000000, 9.524999999999991473 ) ) ;
#62677=CARTESIAN_POINT ( 'NONE',  ( -73.70499999999998408, 2.607480562269072433, 8.024999999999991473 ) ) ;
#62678=CARTESIAN_POINT ( 'NONE',  ( -80.15707362346617515, -9.058813317711329915, -2.943386871421370898 ) ) ;
#62681=CYLINDRICAL_SURFACE ( 'NONE', #47936, 9.524999999999991473 ) ;
#62687=CARTESIAN_POINT ( 'NONE',  ( -184.5550000000000068, 0.000000000000000000, 8.024999999999991473 ) ) ;
#62698=VECTOR ( 'NONE', #61661, 1000.000000000000000 ) ;
#62701=CARTESIAN_POINT ( 'NONE',  ( -94.85499999999998977, 4.716976649647094177, 6.492361379858945902 ) ) ;
#62705=CARTESIAN_POINT ( 'NONE',  ( -144.5070736234661695, 8.102448949553176405, 5.886773742842740909 ) ) ;
#62707=CARTESIAN_POINT ( 'NONE',  ( -77.30707362346615241, -10.01517768586948698, 6.132527647946031529E-16 ) ) ;
#62718=CARTESIAN_POINT ( 'NONE',  ( -122.3050000000000068, 8.437984349512085203, -1.550032578732815448E-15 ) ) ;
#62722=CARTESIAN_POINT ( 'NONE',  ( -125.6950000000000074, -8.437984349512085203, 5.166775262442717831E-16 ) ) ;
#62728=CARTESIAN_POINT ( 'NONE',  ( -195.0000000000000000, 0.000000000000000000, 0.000000000000000000 ) ) ;
#62730=CARTESIAN_POINT ( 'NONE',  ( -168.5929263765337680, -3.094860106618431139, -9.524999999999991473 ) ) ;
#62732=CARTESIAN_POINT ( 'NONE',  ( -182.8449999999999989, -7.632228543268599452, 2.479861379858951054 ) ) ;
#62736=VECTOR ( 'NONE', #10149, 1000.000000000000000 ) ;
#62741=CARTESIAN_POINT ( 'NONE',  ( -84.59292637653379643, -3.094860106618431139, -9.524999999999991473 ) ) ;
#62745=CARTESIAN_POINT ( 'NONE',  ( -195.0000000000000000, 0.000000000000000000, 9.524999999999991473 ) ) ;
#62753=CARTESIAN_POINT ( 'NONE',  ( -111.1429263765338078, 5.598654528085800663, -7.705886871421367523 ) ) ;
#62760=CARTESIAN_POINT ( 'NONE',  ( -101.1550000000000011, 7.632228543268600340, 2.479861379858949277 ) ) ;
#62770=CARTESIAN_POINT ( 'NONE',  ( -76.19499999999999318, 8.437984349512085203, -1.550032578732815448E-15 ) ) ;
#62777=VERTEX_POINT ( 'NONE', #5861 ) ;
#62790=CARTESIAN_POINT ( 'NONE',  ( -166.2570736234661695, 5.598654528085800663, -7.705886871421367523 ) ) ;
#62793=CARTESIAN_POINT ( 'NONE',  ( -103.1070736234661638, 8.102448949553171076, -5.886773742842744461 ) ) ;
#62798=CARTESIAN_POINT ( 'NONE',  ( -82.19292637653380496, -10.01517768586948698, 6.132527647946031529E-16 ) ) ;
#62800=CARTESIAN_POINT ( 'NONE',  ( -60.89292637653380069, -8.102448949553174629, -5.886773742842741797 ) ) ;
#62803=CARTESIAN_POINT ( 'NONE',  ( -146.0050000000000239, 6.826472737025116366, 4.959722759717898555 ) ) ;
#62806=CARTESIAN_POINT ( 'NONE',  ( -159.2949999999999875, -2.607480562269069768, 8.024999999999991473 ) ) ;
#62807=CARTESIAN_POINT ( 'NONE',  ( -149.3949999999999818, -6.826472737025113702, -4.959722759717900331 ) ) ;
#62812=CARTESIAN_POINT ( 'NONE',  ( -59.90499999999997982, 2.607480562269068880, -8.024999999999993250 ) ) ;
#62817=CARTESIAN_POINT ( 'NONE',  ( -59.99499999999996902, -6.826472737025113702, 4.959722759717902107 ) ) ;
#62824=DIRECTION ( 'NONE',  ( -1.000000000000000000, -0.000000000000000000, -0.000000000000000000 ) ) ;
#62832=CARTESIAN_POINT ( 'NONE',  ( -195.0000000000000000, 0.000000000000000000, 9.524999999999991473 ) ) ;
#62846=CARTESIAN_POINT ( 'NONE',  ( -108.8070736234661666, 10.01517768586948698, -1.839758294383808966E-15 ) ) ;
#62853=CARTESIAN_POINT ( 'NONE',  ( -108.5949999999999847, 2.607480562269073321, 8.024999999999991473 ) ) ;
#62867=DIRECTION ( 'NONE',  ( 0.000000000000000000, 0.000000000000000000, 1.000000000000000000 ) ) ;
#62868=CARTESIAN_POINT ( 'NONE',  ( -122.6049999999999898, 6.826472737025113702, -4.959722759717902107 ) ) ;
#62885=CARTESIAN_POINT ( 'NONE',  ( -174.9550000000000125, -7.632228543268599452, 2.479861379858951054 ) ) ;
#62886=CARTESIAN_POINT ( 'NONE',  ( -195.0000000000000000, 1.166476076187852838E-15, -9.524999999999991473 ) ) ;
#62889=CARTESIAN_POINT ( 'NONE',  ( -48.35707362346617089, 5.598654528085804216, 7.705886871421366635 ) ) ;
#62892=CARTESIAN_POINT ( 'NONE',  ( -175.6449999999999818, 4.716976649647091513, -6.492361379858946790 ) ) ;
#62894=ORIENTED_EDGE ( 'NONE', *, *, #45228, .F. ) ;
#62897=CARTESIAN_POINT ( 'NONE',  ( -13.69084439013661303, 10.98233027600763023, 4.836677785638663352 ) ) ;
#62898=CARTESIAN_POINT ( 'NONE',  ( -91.40500000000000114, -2.607480562269069768, 8.024999999999991473 ) ) ;
#62903=CARTESIAN_POINT ( 'NONE',  ( -89.99499999999999034, -6.826472737025113702, 4.959722759717902107 ) ) ;
#62905=CARTESIAN_POINT ( 'NONE',  ( -68.69500000000000739, -8.437984349512085203, 5.166775262442717831E-16 ) ) ;
#62912=VERTEX_POINT ( 'NONE', #54404 ) ;
#62913=CARTESIAN_POINT ( 'NONE',  ( -103.4929263765337879, -8.102448949553172852, 5.886773742842742685 ) ) ;
#62914=CARTESIAN_POINT ( 'NONE',  ( -132.5949999999999989, 2.607480562269073321, 8.024999999999991473 ) ) ;
#62915=VECTOR ( 'NONE', #26307, 1000.000000000000000 ) ;
#62931=CARTESIAN_POINT ( 'NONE',  ( -126.8050000000000068, -8.437984349512086979, 5.166775262442717831E-16 ) ) ;
#62933=CARTESIAN_POINT ( 'NONE',  ( -126.5070736234661979, 8.102448949553176405, 5.886773742842740909 ) ) ;
#62936=CARTESIAN_POINT ( 'NONE',  ( -84.44292637653380496, -1.166476076187852838E-15, -9.524999999999991473 ) ) ;
#62940=DIRECTION ( 'NONE',  ( -1.000000000000000000, -0.000000000000000000, -0.000000000000000000 ) ) ;
#62954=CARTESIAN_POINT ( 'NONE',  ( -98.99292637653378790, 8.102448949553172852, -5.886773742842744461 ) ) ;
#62958=EDGE_CURVE ( 'NONE', #62777, #60435, #50190, .T. ) ;
#62961=CARTESIAN_POINT ( 'NONE',  ( -62.39292637653379359, 8.102448949553176405, 5.886773742842740909 ) ) ;
#62963=CARTESIAN_POINT ( 'NONE',  ( -153.2049999999999272, -2.607480562269071545, -8.024999999999991473 ) ) ;
#62980=CARTESIAN_POINT ( 'NONE',  ( -69.80499999999996419, -8.437984349512085203, 5.166775262442717831E-16 ) ) ;
#62998=CARTESIAN_POINT ( 'NONE',  ( -97.34499999999998465, 7.632228543268599452, -2.479861379858951942 ) ) ;
#63005=CARTESIAN_POINT ( 'NONE',  ( -132.1429263765338078, 5.598654528085800663, -7.705886871421367523 ) ) ;
#63008=CARTESIAN_POINT ( 'NONE',  ( -154.4949999999999477, 6.826472737025113702, -4.959722759717902107 ) ) ;
#63012=CARTESIAN_POINT ( 'NONE',  ( -81.05707362346618083, 0.000000000000000000, 9.524999999999991473 ) ) ;
#63015=ORIENTED_EDGE ( 'NONE', *, *, #44992, .T. ) ;
#63023=CARTESIAN_POINT ( 'NONE',  ( -153.6549999999999727, -7.632228543268600340, -2.479861379858950166 ) ) ;
#63032=( BOUNDED_CURVE ( )  B_SPLINE_CURVE ( 2, ( #15318, #47330, #42062, #32145, #53598, #16353, #64144, #5384, #16000, #20905, #37483, #32466, #68757, #48364, #69435, #10361, #5733, #53, #37123, #25817, #20548, #58529, #15644, #36777, #58886, #27180, #53931, #10694, #21586, #5060, #11022, #64506, #48716, #48031, #31791, #42411, #37825, #63466, #57857, #43098, #21225, #53273, #69103, #26507, #59198, #58187, #42750, #418, #4712, #21951, #43458, #63797, #64840, #16687, #9679, #31090, #52585, #4334, #26160, #10008, #31428, #52923, #47697, #11726, #50076, #66582, #12751, #44813, #38151, #22986, #50402, #60259, #44483, #55321, #33193, #27865, #17384, #17032, #45161, #65182, #54627, #65887, #49373, #38850, #6439, #22277, #1093, #6783, #38516, #34222, #23318, #39528, #60582, #55676, #17715, #18043, #1804, #66216, #22633, #54281, #33528, #60933, #39185, #7490, #12399, #6098, #28917, #49716, #27536, #2126, #12061, #54957, #7143, #44136, #59553, #28572, #11376, #23657, #28211, #49061, #1455, #33858, #65538, #43778, #32839, #747, #59908, #66939, #67265, #30296, #8190, #46910, #29975, #8545, #57058, #7825, #51800, #18398, #67621, #24344, #35966, #51441, #34558, #3550, #19058, #61982, #8874, #45840, #39886, #25052, #25394, #52164, #3186, #56010, #24678, #29271, #61291, #45520, #40565, #18731, #50752, #46563, #2501, #67986, #24011, #62338, #35621, #14163, #19771, #30659, #40213, #61617, #13444, #34910, #13097, #41267, #13804, #35264, #56355, #62666, #56727, #9236, #46202, #29639, #19422, #51108, #2853, #40919, #14489, #57411, #3921, #20099, #53852, #15566, #5649, #9930, #15914, #58450, #53189, #4977, #42333, #41606, #64062, #58119, #63023, #57771, #14865, #47958, #10274, #63716, #36702, #27100, #53523, #9597, #31347, #52848, #10948, #37038, #31709, #32385, #36346, #26426, #32064, #4625, #47251, #5306, #26080, #47613, #42658, #69360, #69017, #31014, #68322, #21151, #52508, #37394, #20826, #58799, #68671, #4251, #10614, #26754, #48273, #69692, #21501, #43017, #63381, #25730, #64422, #16271, #37745, #59126, #20469, #41973, #15234, #44404, #60176, #1001, #66132, #60499, #27788, #65088, #65806, #49291, #6358, #27450, #28128, #17964, #23244, #49635, #22909, #65458, #1730, #55233, #44739, #38766, #22547, #33109, #7057, #59463, #48633, #33445, #54876, #44049, #59829, #17307, #28486, #48979, #11985, #49994, #16943, #17641, #39452, #54546, #6697, #1375, #39108, #60855, #12311, #33781, #38432, #12669, #34135, #64767, #55592, #22201, #7418, #331, #21865, #43376, #16607, #38069, #11294, #32748, #54200, #6015, #43699, #11642, #673, #7741, #35872, #29180, #2047, #13718, #40141, #29547, #2409, #13024, #23923, #67183, #50666, #3462, #14075, #30218, #51358, #46469, #8463, #8791, #62249, #40832, #45437, #18972, #67532, #18318, #35538, #28842, #29899, #34819, #67896, #51016, #57318, #56636, #19332, #41185, #51711, #66857, #18661, #61534, #23572, #34481, #50327, #45086, #40478, #39800, #66499, #55935, #56274, #13360, #61214, #8100, #3101, #24595, #56977, #2777, #24267, #35175, #45765, #61897, #46111, #24959, #19687, #62587, #14402, #62931, #36948, #68583, #16180, #57679, #58038, #21072, #20379, #37656, #20741, #68935, #47879, #68238, #42572, #9154, #58356, #15146, #26670, #30571, #10182, #69277, #21411, #31970, #25643, #9508, #47163, #52072, #14776, #3826, #36255, #42929, #63973, #31622, #4169, #69602, #15821, #53443, #41880, #53102, #4890, #37303, #15482, #26338, #58711, #63298, #10532, #5225, #20020, #48196, #42252, #31258, #64327, #25311, #9845, #46832, #41518, #30928, #36620, #52424, #52757, #4532, #25992, #47520, #63640, #6272, #12225, #65713, #55138, #49205, #11548, #43610, #17553, #239, #59051, #33360, #909, #49549, #10868, #38335, #39019, #59370, #22459, #60417, #5917, #6599, #49902, #65003, #17219, #38683, #43956, #1645, #59739, #1279, #27360, #27008, #22115, #33695, #591, #32651, #22815, #17876, #6968, #28391, #32310, #65372, #23160, #33019, #60086, #28041, #54108, #48893, #54458, #37990, #66045, #16525, #11207, #48544, #43287, #5561, #44651, #21772, #54788, #44313, #53766, #64685, #16861, #27704, #11899, #35368, #55501, #39360, #9332, #14249, #67720, #56822, #36064, #41014, #19514, #25146, #13901, #62433, #3291, #66398, #60759, #30062, #46997, #35713, #12576, #25829, #57143, #47342, #51528, #57507, #30393, #46660, #68079, #8975, #24780, #30755, #46297, #34045, #28754, #7328, #19862, #51897, #3651, #8632, #68770, #25483, #50239, #41354, #62760, #52599, #14597, #52258, #4346, #1960, #4015, #68409, #20204, #18217, #41706, #63127, #14968, #36450, #57870, #9692, #23482, #44988, #31101, #39700, #62070, #5069, #26521, #69114, #63481, #5397, #31801, #32155, #43111, #430, #53282, #15653, #32852, #4724, #48375, #10375, #27546, #20921, #69445, #32480, #48043, #49070, #53610, #10705, #59208, #10023, #53941, #38164, #21598, #36788, #11386, #26836, #58199, #5745, #21235, #64157, #11032, #42763, #42078, #27189, #20563, #54293, #65, #31443, #64518, #52935, #15329, #6113, #21962, #37133, #37837, #26174, #16013, #16362, #48730, #43467, #47711, #37493, #64851, #58542, #42419, #58898, #16697, #59567, #63807, #34235, #38860, #45174, #7498, #29285, #55333, #13115, #22999, #7158, #18056, #65550, #60272, #49730, #49382, #7837, #27877, #17396, #61303, #28586, #28927, #12409, #23328, #12071, #39196, #1105, #66593, #55690, #2139, #44826, #18412, #50085, #50414, #23670, #12764, #33536, #17047, #65897, #60591, #39896, #1813, #34567, #66230, #56020, #1472, #755, #39541, #60945, #22289, #43790, #54968, #22644, #6795, #65196, #54641, #38527, #6448, #59920, #11736, #33204, #28221, #44150, #44494, #17727, #33869, #66949, #57425, #18745, #25066, #68000, #46575, #30671, #63038, #13456, #24356, #45851, #40226, #50766, #19786, #24695, #8555, #67282, #41279, #56741, #41621, #35634, #19071, #29988, #13818, #8207, #2515, #40577, #9254, #51452, #24024, #36364, #67634, #57784, #61991, #62677, #40933, #57070, #8885, #45531, #61631, #14504, #35280, #34924, #56371, #68332, #35980, #3202, #29653, #51120, #3564, #46214, #14881, #30311, #19435, #62354, #14176, #2867, #51814, #3935, #52178, #46923, #25407, #20113, #9609, #37761, #41990, #31026, #5322, #21163, #21515, #52520, #4265, #26764, #20843, #25745, #20483, #47263, #10628, #21880, #37050, #58813, #32078, #42675, #43390, #10288, #43033, #69033, #68683, #63728, #59138, #42343, #37410, #64437, #15575, #9940, #10963, #58465, #31721, #64781, #53205, #53536, #48291, #26094, #4990, #26443, #31363, #38084, #58130, #47626, #16619, #33794, #32400, #64077, #16285, #53866, #47974, #69373, #59482, #5665, #27113, #48647, #346, #63400, #15246, #36714, #52861, #15930, #4639, #6713, #49650, #60870, #39123, #28855, #12325, #27468, #2062, #22922, #48993, #1746, #23589, #34153, #27799, #59847, #49304, #54215, #65106, #11309, #16960, #45100, #50008, #33798, #6370, #66513, #17977, #55611, #1015, #44753, #684, #39466, #17655, #7075, #60511, #44066, #55249, #7434, #22216, #28506, #44421, #33461, #1394, #23256, #43711, #66147, #32765, #12682, #17321, #50338, #12001, #38447, #18335, #60193, #54887, #39815, #38782, #6031, #11656, #33126, #54562, #65822, #22563, #65470, #28141, #13041, #18676, #18987, #40154, #50684, #45452, #7752, #67912, #29195, #35554, #8804, #56992, #41200, #3842, #23937, #34835 ),
 .UNSPECIFIED., .F., .F. ) 
 B_SPLINE_CURVE_WITH_KNOTS ( ( 3, 2, 2, 2, 2, 2, 2, 2, 2, 2, 2, 2, 2, 2, 2, 2, 2, 2, 2, 2, 2, 2, 2, 2, 2, 2, 2, 2, 2, 2, 2, 2, 2, 2, 2, 2, 2, 2, 2, 2, 2, 2, 2, 2, 2, 2, 2, 2, 2, 2, 2, 2, 2, 2, 2, 2, 2, 2, 2, 2, 2, 2, 2, 2, 2, 2, 2, 2, 2, 2, 2, 2, 2, 2, 2, 2, 2, 2, 2, 2, 2, 2, 2, 2, 2, 2, 2, 2, 2, 2, 2, 2, 2, 2, 2, 2, 2, 2, 2, 2, 2, 2, 2, 2, 2, 2, 2, 2, 2, 2, 2, 2, 2, 2, 2, 2, 2, 2, 2, 2, 2, 2, 2, 2, 2, 2, 2, 2, 2, 2, 2, 2, 2, 2, 2, 2, 2, 2, 2, 2, 2, 2, 2, 2, 2, 2, 2, 2, 2, 2, 2, 2, 2, 2, 2, 2, 2, 2, 2, 2, 2, 2, 2, 2, 2, 2, 2, 2, 2, 2, 2, 2, 2, 2, 2, 2, 2, 2, 2, 2, 2, 2, 2, 2, 2, 2, 2, 2, 2, 2, 2, 2, 2, 2, 2, 2, 2, 2, 2, 2, 2, 2, 2, 2, 2, 2, 2, 2, 2, 2, 2, 2, 2, 2, 2, 2, 2, 2, 2, 2, 2, 2, 2, 2, 2, 2, 2, 2, 2, 2, 2, 2, 2, 2, 2, 2, 2, 2, 2, 2, 2, 2, 2, 2, 2, 2, 2, 2, 2, 2, 2, 2, 2, 2, 2, 2, 2, 2, 2, 2, 2, 2, 2, 2, 2, 2, 2, 2, 2, 2, 2, 2, 2, 2, 2, 2, 2, 2, 2, 2, 2, 2, 2, 2, 2, 2, 2, 2, 2, 2, 2, 2, 2, 2, 2, 2, 2, 2, 2, 2, 2, 2, 2, 2, 2, 2, 2, 2, 2, 2, 2, 2, 2, 2, 2, 2, 2, 2, 2, 2, 2, 2, 2, 2, 2, 2, 2, 2, 2, 2, 2, 2, 2, 2, 2, 2, 2, 2, 2, 2, 2, 2, 2, 2, 2, 2, 2, 2, 2, 2, 2, 2, 2, 2, 2, 2, 2, 2, 2, 2, 2, 2, 2, 2, 2, 2, 2, 2, 2, 2, 2, 2, 2, 2, 2, 2, 2, 2, 2, 2, 2, 2, 2, 2, 2, 2, 2, 2, 2, 2, 2, 2, 2, 2, 2, 2, 2, 2, 2, 2, 2, 2, 2, 2, 2, 2, 2, 2, 2, 2, 2, 2, 2, 2, 2, 2, 2, 2, 2, 2, 2, 2, 2, 2, 2, 2, 2, 2, 2, 2, 2, 2, 2, 2, 2, 2, 2, 2, 2, 2, 2, 2, 2, 2, 2, 2, 2, 2, 2, 2, 2, 2, 2, 2, 2, 3 ),
 ( 0.004012011224361215593, 0.004347826086956521792, 0.006521739130434782254, 0.008695652173913043584, 0.01086956521739130405, 0.01304347826086956624, 0.01521739130434782844, 0.01739130434782608717, 0.01956521739130434936, 0.02173913043478260809, 0.02391304347826087029, 0.02608695652173912902, 0.02826086956521739121, 0.03043478260869565341, 0.03260869565217391214, 0.03478260869565217434, 0.03695652173913043653, 0.03913043478260869873, 0.04130434782608695399, 0.04347826086956521618, 0.04565217391304347838, 0.04782608695652174058, 0.05000000000000000278, 0.05217391304347825803, 0.05434782608695652023, 0.05652173913043478243, 0.05869565217391304462, 0.06086956521739130682, 0.06304347826086956208, 0.06521739130434782428, 0.06739130434782608647, 0.06956521739130434867, 0.07173913043478261087, 0.07391304347826087306, 0.07608695652173913526, 0.07826086956521739746, 0.08043478260869564578, 0.08260869565217390798, 0.08478260869565217017, 0.08695652173913043237, 0.08913043478260869457, 0.09130434782608695676, 0.09347826086956521896, 0.09565217391304348116, 0.09782608695652174335, 0.1000000000000000056, 0.1021739130434782677, 0.1043478260869565161, 0.1065217391304347783, 0.1086956521739130405, 0.1108695652173913027, 0.1130434782608695649, 0.1152173913043478271, 0.1173913043478260892, 0.1195652173913043514, 0.1217391304347826136, 0.1239130434782608758, 0.1260869565217391242, 0.1282608695652174002, 0.1304347826086956486, 0.1326086956521739246, 0.1347826086956521729, 0.1369565217391304213, 0.1391304347826086973, 0.1413043478260869457, 0.1434782608695652217, 0.1456521739130434701, 0.1478260869565217461, 0.1499999999999999944, 0.1521739130434782705, 0.1543478260869565188, 0.1565217391304347949, 0.1586956521739130432, 0.1608695652173912916, 0.1630434782608695676, 0.1652173913043478160, 0.1673913043478260920, 0.1695652173913043403, 0.1717391304347826164, 0.1739130434782608647, 0.1760869565217391408, 0.1782608695652173891, 0.1804347826086956652, 0.1826086956521739135, 0.1847826086956521618, 0.1869565217391304379, 0.1891304347826086862, 0.1913043478260869623, 0.1934782608695652106, 0.1956521739130434867, 0.1978260869565217350, 0.2000000000000000111, 0.2021739130434782594, 0.2043478260869565355, 0.2065217391304347838, 0.2086956521739130321, 0.2108695652173913082, 0.2130434782608695565, 0.2152173913043478326, 0.2173913043478260809, 0.2195652173913043570, 0.2217391304347826053, 0.2239130434782608814, 0.2260869565217391297, 0.2282608695652173780, 0.2304347826086956541, 0.2326086956521739024, 0.2347826086956521785, 0.2369565217391304268, 0.2391304347826087029, 0.2413043478260869512, 0.2434782608695652273, 0.2456521739130434756, 0.2478260869565217517, 0.2500000000000000000, 0.2521739130434782483, 0.2543478260869564966, 0.2565217391304348005, 0.2586956521739130488, 0.2608695652173912971, 0.2630434782608695454, 0.2652173913043478493, 0.2673913043478260976, 0.2695652173913043459, 0.2717391304347825942, 0.2739130434782608425, 0.2760869565217391464, 0.2782608695652173947, 0.2804347826086956430, 0.2826086956521738913, 0.2847826086956521952, 0.2869565217391304435, 0.2891304347826086918, 0.2913043478260869401, 0.2934782608695652439, 0.2956521739130434923, 0.2978260869565217406, 0.2999999999999999889, 0.3021739130434782372, 0.3043478260869565410, 0.3065217391304347894, 0.3086956521739130377, 0.3108695652173912860, 0.3130434782608695898, 0.3152173913043478382, 0.3173913043478260865, 0.3195652173913043348, 0.3217391304347825831, 0.3239130434782608869, 0.3260869565217391353, 0.3282608695652173836, 0.3304347826086956319, 0.3326086956521739357, 0.3347826086956521840, 0.3369565217391304324, 0.3391304347826086807, 0.3413043478260869290, 0.3434782608695652328, 0.3456521739130434812, 0.3478260869565217295, 0.3499999999999999778, 0.3521739130434782816, 0.3543478260869565299, 0.3565217391304347783, 0.3586956521739130266, 0.3608695652173913304, 0.3630434782608695787, 0.3652173913043478271, 0.3673913043478260754, 0.3695652173913043237, 0.3717391304347826275, 0.3739130434782608758, 0.3760869565217391242, 0.3782608695652173725, 0.3804347826086956763, 0.3826086956521739246, 0.3847826086956521729, 0.3869565217391304213, 0.3891304347826086696, 0.3913043478260869734, 0.3934782608695652217, 0.3956521739130434701, 0.3978260869565217184, 0.4000000000000000222, 0.4021739130434782705, 0.4043478260869565188, 0.4065217391304347672, 0.4086956521739130710, 0.4108695652173913193, 0.4130434782608695676, 0.4152173913043478160, 0.4173913043478260643, 0.4195652173913043681, 0.4217391304347826164, 0.4239130434782608647, 0.4260869565217391131, 0.4282608695652174169, 0.4304347826086956652, 0.4326086956521739135, 0.4347826086956521618, 0.4369565217391304102, 0.4391304347826087140, 0.4413043478260869623, 0.4434782608695652106, 0.4456521739130434590, 0.4478260869565217628, 0.4500000000000000111, 0.4521739130434782594, 0.4543478260869565077, 0.4565217391304347561, 0.4586956521739130599, 0.4608695652173913082, 0.4630434782608695565, 0.4652173913043478048, 0.4673913043478261087, 0.4695652173913043570, 0.4717391304347826053, 0.4739130434782608536, 0.4760869565217391575, 0.4782608695652174058, 0.4804347826086956541, 0.4826086956521739024, 0.4847826086956521507, 0.4869565217391304546, 0.4891304347826087029, 0.4913043478260869512, 0.4934782608695651995, 0.4956521739130435034, 0.4978260869565217517, 0.5000000000000000000, 0.5021739130434782483, 0.5043478260869564966, 0.5065217391304347450, 0.5086956521739129933, 0.5108695652173913526, 0.5130434782608696009, 0.5152173913043478493, 0.5173913043478260976, 0.5195652173913043459, 0.5217391304347825942, 0.5239130434782608425, 0.5260869565217390909, 0.5282608695652173392, 0.5304347826086956985, 0.5326086956521739468, 0.5347826086956521952, 0.5369565217391304435, 0.5391304347826086918, 0.5413043478260869401, 0.5434782608695651884, 0.5456521739130434367, 0.5478260869565216851, 0.5500000000000000444, 0.5521739130434782927, 0.5543478260869565410, 0.5565217391304347894, 0.5586956521739130377, 0.5608695652173912860, 0.5630434782608695343, 0.5652173913043477826, 0.5673913043478261420, 0.5695652173913043903, 0.5717391304347826386, 0.5739130434782608869, 0.5760869565217391353, 0.5782608695652173836, 0.5804347826086956319, 0.5826086956521738802, 0.5847826086956521285, 0.5869565217391304879, 0.5891304347826087362, 0.5913043478260869845, 0.5934782608695652328, 0.5956521739130434812, 0.5978260869565217295, 0.5999999999999999778, 0.6021739130434782261, 0.6043478260869564744, 0.6065217391304348338, 0.6086956521739130821, 0.6108695652173913304, 0.6130434782608695787, 0.6152173913043478271, 0.6173913043478260754, 0.6195652173913043237, 0.6217391304347825720, 0.6239130434782608203, 0.6260869565217391797, 0.6282608695652174280, 0.6304347826086956763, 0.6326086956521739246, 0.6347826086956521729, 0.6369565217391304213, 0.6391304347826086696, 0.6413043478260869179, 0.6434782608695651662, 0.6456521739130435256, 0.6478260869565217739, 0.6500000000000000222, 0.6521739130434782705, 0.6543478260869565188, 0.6565217391304347672, 0.6586956521739130155, 0.6608695652173912638, 0.6630434782608695121, 0.6652173913043478715, 0.6673913043478261198, 0.6695652173913043681, 0.6717391304347826164, 0.6739130434782608647, 0.6760869565217391131, 0.6782608695652173614, 0.6804347826086956097, 0.6826086956521738580, 0.6847826086956522174, 0.6869565217391304657, 0.6891304347826087140, 0.6913043478260869623, 0.6934782608695652106, 0.6956521739130434590, 0.6978260869565217073, 0.6999999999999999556, 0.7021739130434783149, 0.7043478260869565633, 0.7065217391304348116, 0.7086956521739130599, 0.7108695652173913082, 0.7130434782608695565, 0.7152173913043478048, 0.7173913043478260532, 0.7195652173913043015, 0.7217391304347826608, 0.7239130434782609091, 0.7260869565217391575, 0.7282608695652174058, 0.7304347826086956541, 0.7326086956521739024, 0.7347826086956521507, 0.7369565217391303991, 0.7391304347826086474, 0.7413043478260870067, 0.7434782608695652550, 0.7456521739130435034, 0.7478260869565217517, 0.7500000000000000000, 0.7521739130434782483, 0.7543478260869564966, 0.7565217391304347450, 0.7586956521739129933, 0.7608695652173913526, 0.7630434782608696009, 0.7652173913043478493, 0.7673913043478260976, 0.7695652173913043459, 0.7717391304347825942, 0.7739130434782608425, 0.7760869565217390909, 0.7782608695652173392, 0.7804347826086956985, 0.7826086956521739468, 0.7847826086956521952, 0.7869565217391304435, 0.7891304347826086918, 0.7913043478260869401, 0.7934782608695651884, 0.7956521739130434367, 0.7978260869565216851, 0.8000000000000000444, 0.8021739130434782927, 0.8043478260869565410, 0.8065217391304347894, 0.8086956521739130377, 0.8108695652173912860, 0.8130434782608695343, 0.8152173913043477826, 0.8173913043478261420, 0.8195652173913043903, 0.8217391304347826386, 0.8239130434782608869, 0.8260869565217391353, 0.8282608695652173836, 0.8304347826086956319, 0.8326086956521738802, 0.8347826086956521285, 0.8369565217391304879, 0.8391304347826087362, 0.8413043478260869845, 0.8434782608695652328, 0.8456521739130434812, 0.8478260869565217295, 0.8499999999999999778, 0.8521739130434782261, 0.8543478260869564744, 0.8565217391304348338, 0.8586956521739130821, 0.8608695652173913304, 0.8630434782608695787, 0.8652173913043478271, 0.8673913043478260754, 0.8695652173913043237, 0.8717391304347825720, 0.8739130434782608203, 0.8760869565217391797, 0.8782608695652174280, 0.8804347826086956763, 0.8826086956521739246, 0.8847826086956521729, 0.8869565217391304213, 0.8891304347826086696, 0.8913043478260869179, 0.8934782608695651662, 0.8956521739130435256, 0.8978260869565217739, 0.9000000000000000222, 0.9021739130434782705, 0.9043478260869565188, 0.9065217391304347672, 0.9086956521739130155, 0.9108695652173912638, 0.9130434782608695121, 0.9152173913043478715, 0.9173913043478261198, 0.9195652173913043681, 0.9217391304347826164, 0.9239130434782608647, 0.9260869565217391131, 0.9282608695652173614, 0.9304347826086956097, 0.9326086956521738580, 0.9347826086956522174, 0.9369565217391304657, 0.9391304347826087140, 0.9413043478260869623, 0.9434782608695652106, 0.9456521739130434590, 0.9478260869565217073, 0.9499999999999999556, 0.9521739130434783149, 0.9543478260869565633, 0.9565217391304348116, 0.9586956521739130599, 0.9608695652173913082, 0.9630434782608695565, 0.9652173913043478048, 0.9673913043478260532, 0.9695652173913043015, 0.9717391304347826608, 0.9739130434782609091, 0.9760869565217391575, 0.9782608695652174058, 0.9804347826086956541, 0.9826086956521739024, 0.9847826086956521507, 0.9869565217391303991, 0.9891304347826086474, 0.9913043478260870067 ),
 .UNSPECIFIED. ) 
 CURVE ( )  GEOMETRIC_REPRESENTATION_ITEM ( )  RATIONAL_B_SPLINE_CURVE ( ( 0.9872147520176037805, 0.9924394633425718260, 1.000000000000000000, 0.9510565162951535312, 1.000000000000000000, 0.9510565162951535312, 1.000000000000000000, 0.9510565162951535312, 1.000000000000000000, 0.9510565162951535312, 1.000000000000000000, 0.9510565162951535312, 1.000000000000000000, 0.9510565162951535312, 1.000000000000000000, 0.9510565162951535312, 1.000000000000000000, 0.9510565162951535312, 1.000000000000000000, 0.9510565162951535312, 1.000000000000000000, 0.9510565162951535312, 1.000000000000000000, 0.9510565162951535312, 1.000000000000000000, 0.9510565162951535312, 1.000000000000000000, 0.9510565162951535312, 1.000000000000000000, 0.9510565162951535312, 1.000000000000000000, 0.9510565162951535312, 1.000000000000000000, 0.9510565162951535312, 1.000000000000000000, 0.9510565162951535312, 1.000000000000000000, 0.9510565162951535312, 1.000000000000000000, 0.9510565162951535312, 1.000000000000000000, 0.9510565162951535312, 1.000000000000000000, 0.9510565162951535312, 1.000000000000000000, 0.9510565162951535312, 1.000000000000000000, 0.9510565162951535312, 1.000000000000000000, 0.9510565162951535312, 1.000000000000000000, 0.9510565162951535312, 1.000000000000000000, 0.9510565162951535312, 1.000000000000000000, 0.9510565162951535312, 1.000000000000000000, 0.9510565162951535312, 1.000000000000000000, 0.9510565162951535312, 1.000000000000000000, 0.9510565162951535312, 1.000000000000000000, 0.9510565162951535312, 1.000000000000000000, 0.9510565162951535312, 1.000000000000000000, 0.9510565162951535312, 1.000000000000000000, 0.9510565162951535312, 1.000000000000000000, 0.9510565162951535312, 1.000000000000000000, 0.9510565162951535312, 1.000000000000000000, 0.9510565162951535312, 1.000000000000000000, 0.9510565162951535312, 1.000000000000000000, 0.9510565162951535312, 1.000000000000000000, 0.9510565162951535312, 1.000000000000000000, 0.9510565162951535312, 1.000000000000000000, 0.9510565162951535312, 1.000000000000000000, 0.9510565162951535312, 1.000000000000000000, 0.9510565162951535312, 1.000000000000000000, 0.9510565162951535312, 1.000000000000000000, 0.9510565162951535312, 1.000000000000000000, 0.9510565162951535312, 1.000000000000000000, 0.9510565162951535312, 1.000000000000000000, 0.9510565162951535312, 1.000000000000000000, 0.9510565162951535312, 1.000000000000000000, 0.9510565162951535312, 1.000000000000000000, 0.9510565162951535312, 1.000000000000000000, 0.9510565162951535312, 1.000000000000000000, 0.9510565162951535312, 1.000000000000000000, 0.9510565162951535312, 1.000000000000000000, 0.9510565162951535312, 1.000000000000000000, 0.9510565162951535312, 1.000000000000000000, 0.9510565162951535312, 1.000000000000000000, 0.9510565162951535312, 1.000000000000000000, 0.9510565162951535312, 1.000000000000000000, 0.9510565162951535312, 1.000000000000000000, 0.9510565162951535312, 1.000000000000000000, 0.9510565162951535312, 1.000000000000000000, 0.9510565162951535312, 1.000000000000000000, 0.9510565162951535312, 1.000000000000000000, 0.9510565162951535312, 1.000000000000000000, 0.9510565162951535312, 1.000000000000000000, 0.9510565162951535312, 1.000000000000000000, 0.9510565162951535312, 1.000000000000000000, 0.9510565162951535312, 1.000000000000000000, 0.9510565162951535312, 1.000000000000000000, 0.9510565162951535312, 1.000000000000000000, 0.9510565162951535312, 1.000000000000000000, 0.9510565162951535312, 1.000000000000000000, 0.9510565162951535312, 1.000000000000000000, 0.9510565162951535312, 1.000000000000000000, 0.9510565162951535312, 1.000000000000000000, 0.9510565162951535312, 1.000000000000000000, 0.9510565162951535312, 1.000000000000000000, 0.9510565162951535312, 1.000000000000000000, 0.9510565162951535312, 1.000000000000000000, 0.9510565162951535312, 1.000000000000000000, 0.9510565162951535312, 1.000000000000000000, 0.9510565162951535312, 1.000000000000000000, 0.9510565162951535312, 1.000000000000000000, 0.9510565162951535312, 1.000000000000000000, 0.9510565162951535312, 1.000000000000000000, 0.9510565162951535312, 1.000000000000000000, 0.9510565162951535312, 1.000000000000000000, 0.9510565162951535312, 1.000000000000000000, 0.9510565162951535312, 1.000000000000000000, 0.9510565162951535312, 1.000000000000000000, 0.9510565162951535312, 1.000000000000000000, 0.9510565162951535312, 1.000000000000000000, 0.9510565162951535312, 1.000000000000000000, 0.9510565162951535312, 1.000000000000000000, 0.9510565162951535312, 1.000000000000000000, 0.9510565162951535312, 1.000000000000000000, 0.9510565162951535312, 1.000000000000000000, 0.9510565162951535312, 1.000000000000000000, 0.9510565162951535312, 1.000000000000000000, 0.9510565162951535312, 1.000000000000000000, 0.9510565162951535312, 1.000000000000000000, 0.9510565162951535312, 1.000000000000000000, 0.9510565162951535312, 1.000000000000000000, 0.9510565162951535312, 1.000000000000000000, 0.9510565162951535312, 1.000000000000000000, 0.9510565162951535312, 1.000000000000000000, 0.9510565162951535312, 1.000000000000000000, 0.9510565162951535312, 1.000000000000000000, 0.9510565162951535312, 1.000000000000000000, 0.9510565162951535312, 1.000000000000000000, 0.9510565162951535312, 1.000000000000000000, 0.9510565162951535312, 1.000000000000000000, 0.9510565162951535312, 1.000000000000000000, 0.9510565162951535312, 1.000000000000000000, 0.9510565162951535312, 1.000000000000000000, 0.9510565162951535312, 1.000000000000000000, 0.9510565162951535312, 1.000000000000000000, 0.9510565162951535312, 1.000000000000000000, 0.9510565162951535312, 1.000000000000000000, 0.9510565162951535312, 1.000000000000000000, 0.9510565162951535312, 1.000000000000000000, 0.9510565162951535312, 1.000000000000000000, 0.9510565162951535312, 1.000000000000000000, 0.9510565162951535312, 1.000000000000000000, 0.9510565162951535312, 1.000000000000000000, 0.9510565162951535312, 1.000000000000000000, 0.9510565162951535312, 1.000000000000000000, 0.9510565162951535312, 1.000000000000000000, 0.9510565162951535312, 1.000000000000000000, 0.9510565162951535312, 1.000000000000000000, 0.9510565162951535312, 1.000000000000000000, 0.9510565162951535312, 1.000000000000000000, 0.9510565162951535312, 1.000000000000000000, 0.9510565162951535312, 1.000000000000000000, 0.9510565162951535312, 1.000000000000000000, 0.9510565162951535312, 1.000000000000000000, 0.9510565162951535312, 1.000000000000000000, 0.9510565162951535312, 1.000000000000000000, 0.9510565162951535312, 1.000000000000000000, 0.9510565162951535312, 1.000000000000000000, 0.9510565162951535312, 1.000000000000000000, 0.9510565162951535312, 1.000000000000000000, 0.9510565162951535312, 1.000000000000000000, 0.9510565162951535312, 1.000000000000000000, 0.9510565162951535312, 1.000000000000000000, 0.9510565162951535312, 1.000000000000000000, 0.9510565162951535312, 1.000000000000000000, 0.9510565162951535312, 1.000000000000000000, 0.9510565162951535312, 1.000000000000000000, 0.9510565162951535312, 1.000000000000000000, 0.9510565162951535312, 1.000000000000000000, 0.9510565162951535312, 1.000000000000000000, 0.9510565162951535312, 1.000000000000000000, 0.9510565162951535312, 1.000000000000000000, 0.9510565162951535312, 1.000000000000000000, 0.9510565162951535312, 1.000000000000000000, 0.9510565162951535312, 1.000000000000000000, 0.9510565162951535312, 1.000000000000000000, 0.9510565162951535312, 1.000000000000000000, 0.9510565162951535312, 1.000000000000000000, 0.9510565162951535312, 1.000000000000000000, 0.9510565162951535312, 1.000000000000000000, 0.9510565162951535312, 1.000000000000000000, 0.9510565162951535312, 1.000000000000000000, 0.9510565162951535312, 1.000000000000000000, 0.9510565162951535312, 1.000000000000000000, 0.9510565162951535312, 1.000000000000000000, 0.9510565162951535312, 1.000000000000000000, 0.9510565162951535312, 1.000000000000000000, 0.9510565162951535312, 1.000000000000000000, 0.9510565162951535312, 1.000000000000000000, 0.9510565162951535312, 1.000000000000000000, 0.9510565162951535312, 1.000000000000000000, 0.9510565162951535312, 1.000000000000000000, 0.9510565162951535312, 1.000000000000000000, 0.9510565162951535312, 1.000000000000000000, 0.9510565162951535312, 1.000000000000000000, 0.9510565162951535312, 1.000000000000000000, 0.9510565162951535312, 1.000000000000000000, 0.9510565162951535312, 1.000000000000000000, 0.9510565162951535312, 1.000000000000000000, 0.9510565162951535312, 1.000000000000000000, 0.9510565162951535312, 1.000000000000000000, 0.9510565162951535312, 1.000000000000000000, 0.9510565162951535312, 1.000000000000000000, 0.9510565162951535312, 1.000000000000000000, 0.9510565162951535312, 1.000000000000000000, 0.9510565162951535312, 1.000000000000000000, 0.9510565162951535312, 1.000000000000000000, 0.9510565162951535312, 1.000000000000000000, 0.9510565162951535312, 1.000000000000000000, 0.9510565162951535312, 1.000000000000000000, 0.9510565162951535312, 1.000000000000000000, 0.9510565162951535312, 1.000000000000000000, 0.9510565162951535312, 1.000000000000000000, 0.9510565162951535312, 1.000000000000000000, 0.9510565162951535312, 1.000000000000000000, 0.9510565162951535312, 1.000000000000000000, 0.9510565162951535312, 1.000000000000000000, 0.9510565162951535312, 1.000000000000000000, 0.9510565162951535312, 1.000000000000000000, 0.9510565162951535312, 1.000000000000000000, 0.9510565162951535312, 1.000000000000000000, 0.9510565162951535312, 1.000000000000000000, 0.9510565162951535312, 1.000000000000000000, 0.9510565162951535312, 1.000000000000000000, 0.9510565162951535312, 1.000000000000000000, 0.9510565162951535312, 1.000000000000000000, 0.9510565162951535312, 1.000000000000000000, 0.9510565162951535312, 1.000000000000000000, 0.9510565162951535312, 1.000000000000000000, 0.9510565162951535312, 1.000000000000000000, 0.9510565162951535312, 1.000000000000000000, 0.9510565162951535312, 1.000000000000000000, 0.9510565162951535312, 1.000000000000000000, 0.9510565162951535312, 1.000000000000000000, 0.9510565162951535312, 1.000000000000000000, 0.9510565162951535312, 1.000000000000000000, 0.9510565162951535312, 1.000000000000000000, 0.9510565162951535312, 1.000000000000000000, 0.9510565162951535312, 1.000000000000000000, 0.9510565162951535312, 1.000000000000000000, 0.9510565162951535312, 1.000000000000000000, 0.9510565162951535312, 1.000000000000000000, 0.9510565162951535312, 1.000000000000000000, 0.9510565162951535312, 1.000000000000000000, 0.9510565162951535312, 1.000000000000000000, 0.9510565162951535312, 1.000000000000000000, 0.9510565162951535312, 1.000000000000000000, 0.9510565162951535312, 1.000000000000000000, 0.9510565162951535312, 1.000000000000000000, 0.9510565162951535312, 1.000000000000000000, 0.9510565162951535312, 1.000000000000000000, 0.9510565162951535312, 1.000000000000000000, 0.9510565162951535312, 1.000000000000000000, 0.9510565162951535312, 1.000000000000000000, 0.9510565162951535312, 1.000000000000000000, 0.9510565162951535312, 1.000000000000000000, 0.9510565162951535312, 1.000000000000000000, 0.9510565162951535312, 1.000000000000000000, 0.9510565162951535312, 1.000000000000000000, 0.9510565162951535312, 1.000000000000000000, 0.9510565162951535312, 1.000000000000000000, 0.9510565162951535312, 1.000000000000000000, 0.9510565162951535312, 1.000000000000000000, 0.9510565162951535312, 1.000000000000000000, 0.9510565162951535312, 1.000000000000000000, 0.9510565162951535312, 1.000000000000000000, 0.9510565162951535312, 1.000000000000000000, 0.9510565162951535312, 1.000000000000000000, 0.9510565162951535312, 1.000000000000000000, 0.9510565162951535312, 1.000000000000000000, 0.9510565162951535312, 1.000000000000000000, 0.9510565162951535312, 1.000000000000000000, 0.9510565162951535312, 1.000000000000000000, 0.9510565162951535312, 1.000000000000000000, 0.9510565162951535312, 1.000000000000000000, 0.9510565162951535312, 1.000000000000000000, 0.9510565162951535312, 1.000000000000000000, 0.9510565162951535312, 1.000000000000000000, 0.9510565162951535312, 1.000000000000000000, 0.9510565162951535312, 1.000000000000000000, 0.9510565162951535312, 1.000000000000000000, 0.9510565162951535312, 1.000000000000000000, 0.9510565162951535312, 1.000000000000000000, 0.9510565162951535312, 1.000000000000000000, 0.9510565162951535312, 1.000000000000000000, 0.9510565162951535312, 1.000000000000000000, 0.9510565162951535312, 1.000000000000000000, 0.9510565162951535312, 1.000000000000000000, 0.9510565162951535312, 1.000000000000000000, 0.9510565162951535312, 1.000000000000000000, 0.9510565162951535312, 1.000000000000000000, 0.9510565162951535312, 1.000000000000000000, 0.9510565162951535312, 1.000000000000000000, 0.9510565162951535312, 1.000000000000000000, 0.9510565162951535312, 1.000000000000000000, 0.9510565162951535312, 1.000000000000000000, 0.9510565162951535312, 1.000000000000000000, 0.9510565162951535312, 1.000000000000000000, 0.9510565162951535312, 1.000000000000000000, 0.9510565162951535312, 1.000000000000000000, 0.9510565162951535312, 1.000000000000000000, 0.9510565162951535312, 1.000000000000000000, 0.9510565162951535312, 1.000000000000000000, 0.9510565162951535312, 1.000000000000000000, 0.9510565162951535312, 1.000000000000000000, 0.9510565162951535312, 1.000000000000000000, 0.9510565162951535312, 1.000000000000000000, 0.9510565162951535312, 1.000000000000000000, 0.9510565162951535312, 1.000000000000000000, 0.9510565162951535312, 1.000000000000000000, 0.9510565162951535312, 1.000000000000000000, 0.9510565162951535312, 1.000000000000000000, 0.9510565162951535312, 1.000000000000000000, 0.9510565162951535312, 1.000000000000000000, 0.9510565162951535312, 1.000000000000000000, 0.9510565162951535312, 1.000000000000000000, 0.9510565162951535312, 1.000000000000000000, 0.9510565162951535312, 1.000000000000000000, 0.9510565162951535312, 1.000000000000000000, 0.9510565162951535312, 1.000000000000000000, 0.9510565162951535312, 1.000000000000000000, 0.9510565162951535312, 1.000000000000000000, 0.9510565162951535312, 1.000000000000000000, 0.9510565162951535312, 1.000000000000000000, 0.9510565162951535312, 1.000000000000000000, 0.9510565162951535312, 1.000000000000000000, 0.9510565162951535312, 1.000000000000000000, 0.9510565162951535312, 1.000000000000000000, 0.9510565162951535312, 1.000000000000000000, 0.9510565162951535312, 1.000000000000000000, 0.9510565162951535312, 1.000000000000000000, 0.9510565162951535312, 1.000000000000000000, 0.9510565162951535312, 1.000000000000000000, 0.9510565162951535312, 1.000000000000000000, 0.9510565162951535312, 1.000000000000000000, 0.9510565162951535312, 1.000000000000000000, 0.9510565162951535312, 1.000000000000000000, 0.9510565162951535312, 1.000000000000000000, 0.9510565162951535312, 1.000000000000000000, 0.9510565162951535312, 1.000000000000000000, 0.9510565162951535312, 1.000000000000000000, 0.9510565162951535312, 1.000000000000000000, 0.9510565162951535312, 1.000000000000000000, 0.9510565162951535312, 1.000000000000000000, 0.9510565162951535312, 1.000000000000000000, 0.9510565162951535312, 1.000000000000000000, 0.9510565162951535312, 1.000000000000000000, 0.9510565162951535312, 1.000000000000000000, 0.9510565162951535312, 1.000000000000000000, 0.9510565162951535312, 1.000000000000000000, 0.9510565162951535312, 1.000000000000000000, 0.9510565162951535312, 1.000000000000000000, 0.9510565162951535312, 1.000000000000000000, 0.9510565162951535312, 1.000000000000000000, 0.9510565162951535312, 1.000000000000000000, 0.9510565162951535312, 1.000000000000000000, 0.9510565162951535312, 1.000000000000000000, 0.9510565162951535312, 1.000000000000000000, 0.9510565162951535312, 1.000000000000000000, 0.9510565162951535312, 1.000000000000000000, 0.9510565162951535312, 1.000000000000000000, 0.9510565162951535312, 1.000000000000000000, 0.9510565162951535312, 1.000000000000000000, 0.9510565162951535312, 1.000000000000000000, 0.9510565162951535312, 1.000000000000000000, 0.9510565162951535312, 1.000000000000000000, 0.9510565162951535312, 1.000000000000000000, 0.9510565162951535312, 1.000000000000000000, 0.9510565162951535312, 1.000000000000000000, 0.9510565162951535312, 1.000000000000000000, 0.9510565162951535312, 1.000000000000000000, 0.9510565162951535312, 1.000000000000000000, 0.9510565162951535312, 1.000000000000000000, 0.9510565162951535312, 1.000000000000000000, 0.9510565162951535312, 1.000000000000000000, 0.9510565162951535312, 1.000000000000000000, 0.9510565162951535312, 1.000000000000000000, 0.9510565162951535312, 1.000000000000000000, 0.9510565162951535312, 1.000000000000000000, 0.9510565162951535312, 1.000000000000000000, 0.9510565162951535312, 1.000000000000000000, 0.9510565162951535312, 1.000000000000000000, 0.9510565162951535312, 1.000000000000000000, 0.9510565162951535312, 1.000000000000000000, 0.9510565162951535312, 1.000000000000000000, 0.9510565162951535312, 1.000000000000000000, 0.9510565162951535312, 1.000000000000000000, 0.9510565162951535312, 1.000000000000000000, 0.9510565162951535312, 1.000000000000000000, 0.9510565162951535312, 1.000000000000000000, 0.9510565162951535312, 1.000000000000000000, 0.9510565162951535312, 1.000000000000000000, 0.9510565162951535312, 1.000000000000000000, 0.9510565162951535312, 1.000000000000000000, 0.9510565162951535312, 1.000000000000000000, 0.9510565162951535312, 1.000000000000000000, 0.9510565162951535312, 1.000000000000000000, 0.9510565162951535312, 1.000000000000000000, 0.9510565162951535312, 1.000000000000000000, 0.9510565162951535312, 1.000000000000000000, 0.9510565162951535312, 1.000000000000000000, 0.9510565162951535312, 1.000000000000000000, 0.9510565162951535312, 1.000000000000000000, 0.9510565162951535312, 1.000000000000000000, 0.9510565162951535312, 1.000000000000000000, 0.9510565162951535312, 1.000000000000000000, 0.9510565162951535312, 1.000000000000000000, 0.9510565162951535312, 1.000000000000000000, 0.9510565162951535312, 1.000000000000000000, 0.9510565162951535312, 1.000000000000000000, 0.9510565162951535312, 1.000000000000000000, 0.9510565162951535312, 1.000000000000000000, 0.9510565162951535312, 1.000000000000000000, 0.9510565162951535312, 1.000000000000000000, 0.9510565162951535312, 1.000000000000000000, 0.9510565162951535312, 1.000000000000000000, 0.9510565162951535312, 1.000000000000000000, 0.9510565162951535312, 1.000000000000000000, 0.9510565162951535312, 1.000000000000000000, 0.9510565162951535312, 1.000000000000000000, 0.9510565162951535312, 1.000000000000000000, 0.9510565162951535312, 1.000000000000000000, 0.9510565162951535312, 1.000000000000000000, 0.9510565162951535312, 1.000000000000000000, 0.9510565162951535312, 1.000000000000000000, 0.9510565162951535312, 1.000000000000000000, 0.9510565162951535312, 1.000000000000000000, 0.9510565162951535312, 1.000000000000000000, 0.9510565162951535312, 1.000000000000000000, 0.9510565162951535312, 1.000000000000000000, 0.9510565162951535312, 1.000000000000000000, 0.9510565162951535312, 1.000000000000000000, 0.9510565162951535312, 1.000000000000000000, 0.9510565162951535312, 1.000000000000000000, 0.9510565162951535312, 1.000000000000000000, 0.9510565162951535312, 1.000000000000000000, 0.9510565162951535312, 1.000000000000000000, 0.9510565162951535312, 1.000000000000000000, 0.9510565162951535312, 1.000000000000000000, 0.9510565162951535312, 1.000000000000000000, 0.9510565162951535312, 1.000000000000000000, 0.9510565162951535312, 1.000000000000000000, 0.9510565162951535312, 1.000000000000000000, 0.9510565162951535312, 1.000000000000000000, 0.9510565162951535312, 1.000000000000000000, 0.9510565162951535312, 1.000000000000000000, 0.9510565162951535312, 1.000000000000000000, 0.9510565162951535312, 1.000000000000000000, 0.9510565162951535312, 1.000000000000000000, 0.9510565162951535312, 1.000000000000000000, 0.9510565162951535312, 1.000000000000000000, 0.9510565162951535312, 1.000000000000000000, 0.9510565162951535312, 1.000000000000000000, 0.9510565162951535312, 1.000000000000000000, 0.9510565162951535312, 1.000000000000000000, 0.9510565162951535312, 1.000000000000000000, 0.9510565162951535312, 1.000000000000000000, 0.9510565162951535312, 1.000000000000000000, 0.9510565162951535312, 1.000000000000000000, 0.9510565162951535312, 1.000000000000000000, 0.9510565162951535312, 1.000000000000000000, 0.9510565162951535312, 1.000000000000000000, 0.9510565162951535312, 1.000000000000000000, 0.9510565162951535312, 1.000000000000000000, 0.9510565162951535312, 1.000000000000000000, 0.9510565162951535312, 1.000000000000000000, 0.9510565162951535312, 1.000000000000000000, 0.9510565162951535312, 1.000000000000000000, 0.9510565162951535312, 1.000000000000000000, 0.9510565162951535312, 1.000000000000000000 ) ) 
 REPRESENTATION_ITEM ( '' )  );
#63038=CARTESIAN_POINT ( 'NONE',  ( -77.75499999999999545, 4.716976649647091513, -6.492361379858946790 ) ) ;
#63054=CARTESIAN_POINT ( 'NONE',  ( -177.2050000000000125, -2.607480562269071545, -8.024999999999991473 ) ) ;
#63063=CARTESIAN_POINT ( 'NONE',  ( -195.0000000000000000, 1.166476076187852838E-15, -9.524999999999991473 ) ) ;
#63067=CARTESIAN_POINT ( 'NONE',  ( -98.15499999999998693, 7.632228543268600340, 2.479861379858949277 ) ) ;
#63072=CARTESIAN_POINT ( 'NONE',  ( -135.3570736234661638, 5.598654528085804216, 7.705886871421366635 ) ) ;
#63076=CARTESIAN_POINT ( 'NONE',  ( -75.95707362346617231, 9.058813317711329915, -2.943386871421373119 ) ) ;
#63084=CARTESIAN_POINT ( 'NONE',  ( -109.5549999999999926, 0.000000000000000000, 8.024999999999991473 ) ) ;
#63087=CARTESIAN_POINT ( 'NONE',  ( -124.7949999999999733, 2.607480562269068880, -8.024999999999993250 ) ) ;
#63094=CARTESIAN_POINT ( 'NONE',  ( -176.0929263765338249, 3.094860106618433360, 9.524999999999991473 ) ) ;
#63096=CARTESIAN_POINT ( 'NONE',  ( -195.0000000000000000, 1.166476076187852838E-15, -9.524999999999991473 ) ) ;
#63105=CARTESIAN_POINT ( 'NONE',  ( -87.59292637653381064, -3.094860106618431139, -9.524999999999991473 ) ) ;
#63121=CARTESIAN_POINT ( 'NONE',  ( -102.7429263765338021, -5.598654528085803328, -7.705886871421366635 ) ) ;
#63127=CARTESIAN_POINT ( 'NONE',  ( -99.50499999999996703, -6.826472737025113702, -4.959722759717900331 ) ) ;
#63131=ORIENTED_EDGE ( 'NONE', *, *, #6039, .T. ) ;
#63140=CARTESIAN_POINT ( 'NONE',  ( -76.04499999999998749, 7.632228543268600340, 2.479861379858949277 ) ) ;
#63144=CARTESIAN_POINT ( 'NONE',  ( -121.5570736234661808, -1.166476076187852838E-15, -9.524999999999991473 ) ) ;
#63160=CARTESIAN_POINT ( 'NONE',  ( -149.2429263765338021, 5.598654528085804216, 7.705886871421366635 ) ) ;
#63162=CARTESIAN_POINT ( 'NONE',  ( -171.2070736234661865, 3.094860106618433360, 9.524999999999991473 ) ) ;
#63165=CARTESIAN_POINT ( 'NONE',  ( -103.5570736234661808, -1.166476076187852838E-15, -9.524999999999991473 ) ) ;
#63171=CARTESIAN_POINT ( 'NONE',  ( -55.55707362346618083, -1.166476076187852838E-15, -9.524999999999991473 ) ) ;
#63174=CARTESIAN_POINT ( 'NONE',  ( -143.9050000000000011, 2.607480562269068880, -8.024999999999993250 ) ) ;
#63177=CARTESIAN_POINT ( 'NONE',  ( -157.4950000000000045, 6.826472737025113702, -4.959722759717902107 ) ) ;
#63178=CARTESIAN_POINT ( 'NONE',  ( -152.0949999999999420, -2.607480562269071545, -8.024999999999991473 ) ) ;
#63184=CARTESIAN_POINT ( 'NONE',  ( -63.35499999999998266, -4.716976649647093289, -6.492361379858945902 ) ) ;
#63187=CARTESIAN_POINT ( 'NONE',  ( -65.24499999999999034, -4.716976649647093289, -6.492361379858945902 ) ) ;
#63193=CARTESIAN_POINT ( 'NONE',  ( -152.0929263765342512, 3.094860106625323404, 9.524999999994985700 ) ) ;
#63207=EDGE_CURVE ( 'NONE', #34526, #9180, #2367, .T. ) ;
#63215=FACE_OUTER_BOUND ( 'NONE', #55982, .T. ) ;
#63221=CARTESIAN_POINT ( 'NONE',  ( -84.59292637653378222, -3.094860106618431139, -9.524999999999991473 ) ) ;
#63224=CARTESIAN_POINT ( 'NONE',  ( -105.7449999999999903, 4.716976649647094177, 6.492361379858945902 ) ) ;
#63227=CARTESIAN_POINT ( 'NONE',  ( -163.7070736234664139, -3.094860106622296936, -9.524999999997184830 ) ) ;
#63234=VERTEX_POINT ( 'NONE', #7460 ) ;
#63239=CARTESIAN_POINT ( 'NONE',  ( -119.4549999999999983, 7.632228543268599452, -2.479861379858951942 ) ) ;
#63250=CARTESIAN_POINT ( 'NONE',  ( -182.9194972100727625, 8.570615872132687940, -4.445904112569770916 ) ) ;
#63254=CARTESIAN_POINT ( 'NONE',  ( -178.4050000000000011, -2.607480562269069768, 8.024999999999991473 ) ) ;
#63258=CARTESIAN_POINT ( 'NONE',  ( -181.0449999999999875, 7.632228543268600340, 2.479861379858949277 ) ) ;
#63260=CARTESIAN_POINT ( 'NONE',  ( -173.3949999999999818, -6.826472737025113702, -4.959722759717900331 ) ) ;
#63266=CARTESIAN_POINT ( 'NONE',  ( -11.03071027638185697, 11.60717996540982888, 3.057800190812369312 ) ) ;
#63267=CARTESIAN_POINT ( 'NONE',  ( -87.80500000000000682, -8.437984349512085203, 5.166775262442717831E-16 ) ) ;
#63272=CARTESIAN_POINT ( 'NONE',  ( -93.44499999999999318, 0.000000000000000000, 8.024999999999991473 ) ) ;
#63274=CARTESIAN_POINT ( 'NONE',  ( -68.39499999999999602, -6.826472737025115478, -4.959722759717899443 ) ) ;
#63275=DIRECTION ( 'NONE',  ( -1.000000000000000000, -0.000000000000000000, -0.000000000000000000 ) ) ;
#63280=CARTESIAN_POINT ( 'NONE',  ( -105.5929263765338106, -3.094860106618431139, -9.524999999999991473 ) ) ;
#63281=CARTESIAN_POINT ( 'NONE',  ( -132.8950000000000102, 6.826472737025116366, 4.959722759717898555 ) ) ;
#63285=CARTESIAN_POINT ( 'NONE',  ( -130.9429263765338192, 0.000000000000000000, 9.524999999999991473 ) ) ;
#63291=CARTESIAN_POINT ( 'NONE',  ( -174.9570736234661865, 9.058813317711329915, -2.943386871421373119 ) ) ;
#63298=CARTESIAN_POINT ( 'NONE',  ( -120.2049999999999983, -2.607480562269071545, -8.024999999999991473 ) ) ;
#63300=CARTESIAN_POINT ( 'NONE',  ( -137.0070736234661410, -8.102448949553174629, -5.886773742842741797 ) ) ;
#63306=ORIENTED_EDGE ( 'NONE', *, *, #63207, .F. ) ;
#63324=CARTESIAN_POINT ( 'NONE',  ( -62.99292637653378080, 8.102448949553171076, -5.886773742842744461 ) ) ;
#63327=CARTESIAN_POINT ( 'NONE',  ( -156.2050000000000125, -2.607480562269071545, -8.024999999999991473 ) ) ;
#63332=CARTESIAN_POINT ( 'NONE',  ( -69.74292637653380211, -5.598654528085803328, -7.705886871421366635 ) ) ;
#63339=CARTESIAN_POINT ( 'NONE',  ( -63.80499999999998550, -8.437984349512085203, 5.166775262442717831E-16 ) ) ;
#63349=LINE ( 'NONE', #297, #26032 ) ;
#63353=CARTESIAN_POINT ( 'NONE',  ( -100.7950000000000017, 2.607480562269068880, -8.024999999999993250 ) ) ;
#63357=( BOUNDED_CURVE ( )  B_SPLINE_CURVE ( 2, ( #62479, #7982, #40718, #55819, #12906, #66368, #34699, #51589, #9031, #13593, #50558 ),
 .UNSPECIFIED., .F., .F. ) 
 B_SPLINE_CURVE_WITH_KNOTS ( ( 3, 2, 2, 2, 2, 3 ),
 ( 0.1195652173913016036, 0.1217391304347798103, 0.1239130434782580309, 0.1260869565217362376, 0.1282608695652144581, 0.1304347826086926510 ),
 .UNSPECIFIED. ) 
 CURVE ( )  GEOMETRIC_REPRESENTATION_ITEM ( )  RATIONAL_B_SPLINE_CURVE ( ( 1.000000000000061728, 0.9510565162950915807, 1.000000000000000000, 0.9510565162951535312, 1.000000000000000000, 0.9510565162951535312, 1.000000000000000000, 0.9510565162951535312, 1.000000000000000000, 0.9510565162952210327, 0.9999999999999324984 ) ) 
 REPRESENTATION_ITEM ( '' )  );
#63360=VERTEX_POINT ( 'NONE', #41230 ) ;
#63361=CARTESIAN_POINT ( 'NONE',  ( -134.8429263765337964, 9.058813317711329915, -2.943386871421373119 ) ) ;
#63364=CARTESIAN_POINT ( 'NONE',  ( -156.7450000000000045, 4.716976649647094177, 6.492361379858945902 ) ) ;
#63381=CARTESIAN_POINT ( 'NONE',  ( -147.3549999999999898, -4.716976649647093289, -6.492361379858945902 ) ) ;
#63386=CARTESIAN_POINT ( 'NONE',  ( -141.8070736234661808, 10.01517768586948698, -1.839758294383808966E-15 ) ) ;
#63400=CARTESIAN_POINT ( 'NONE',  ( -60.50499999999998124, -6.826472737025113702, -4.959722759717900331 ) ) ;
#63413=CARTESIAN_POINT ( 'NONE',  ( -177.0549999999999784, -9.827790563157499189E-16, -8.024999999999991473 ) ) ;
#63419=EDGE_LOOP ( 'NONE', ( #2952, #47084, #31543, #20098 ) ) ;
#63426=CARTESIAN_POINT ( 'NONE',  ( -99.20499999999999829, -2.607480562269071545, -8.024999999999991473 ) ) ;
#63430=CARTESIAN_POINT ( 'NONE',  ( -134.1570736234661751, -9.058813317711329915, -2.943386871421370898 ) ) ;
#63432=CARTESIAN_POINT ( 'NONE',  ( -71.15707362346617515, -9.058813317711329915, -2.943386871421370898 ) ) ;
#63435=LINE ( 'NONE', #51485, #51597 ) ;
#63440=CARTESIAN_POINT ( 'NONE',  ( -115.5549999999999926, 0.000000000000000000, 8.024999999999991473 ) ) ;
#63443=CARTESIAN_POINT ( 'NONE',  ( -127.3449999999999847, 7.632228543268599452, -2.479861379858951942 ) ) ;
#63445=CARTESIAN_POINT ( 'NONE',  ( -112.1070736234661354, 8.102448949553172852, -5.886773742842744461 ) ) ;
#63447=CARTESIAN_POINT ( 'NONE',  ( -158.8429263765337964, 9.058813317711329915, -2.943386871421373119 ) ) ;
#63449=CARTESIAN_POINT ( 'NONE',  ( -182.6949999999999648, -8.437984349512085203, 5.166775262442717831E-16 ) ) ;
#63458=CARTESIAN_POINT ( 'NONE',  ( -78.44292637653380496, -1.166476076187852838E-15, -9.524999999999991473 ) ) ;
#63463=( BOUNDED_CURVE ( )  B_SPLINE_CURVE ( 2, ( #19152, #7918, #24100, #45607, #61703, #34314, #67356, #55768, #40653, #35002, #29361 ),
 .UNSPECIFIED., .F., .F. ) 
 B_SPLINE_CURVE_WITH_KNOTS ( ( 3, 2, 2, 2, 2, 3 ),
 ( 0.8695652173913043237, 0.8717391304347825720, 0.8739130434782608203, 0.8760869565217391797, 0.8782608695652174280, 0.8804347826086956763 ),
 .UNSPECIFIED. ) 
 CURVE ( )  GEOMETRIC_REPRESENTATION_ITEM ( )  RATIONAL_B_SPLINE_CURVE ( ( 1.000000000000000000, 0.9510565162951535312, 1.000000000000000000, 0.9510565162951535312, 1.000000000000000000, 0.9510565162951535312, 1.000000000000000000, 0.9510565162951535312, 1.000000000000000000, 0.9510565162951535312, 1.000000000000000000 ) ) 
 REPRESENTATION_ITEM ( '' )  );
#63466=CARTESIAN_POINT ( 'NONE',  ( -178.7050000000000125, 2.607480562269072433, 8.024999999999991473 ) ) ;
#63473=DIRECTION ( 'NONE',  ( 0.000000000000000000, 0.000000000000000000, -1.000000000000000000 ) ) ;
#63481=CARTESIAN_POINT ( 'NONE',  ( -97.55499999999999261, 0.000000000000000000, 8.024999999999991473 ) ) ;
#63490=CARTESIAN_POINT ( 'NONE',  ( -73.79499999999997328, 2.607480562269068880, -8.024999999999993250 ) ) ;
#63494=CARTESIAN_POINT ( 'NONE',  ( -124.7070736234668829, -3.094860106630464180, -9.524999999991248245 ) ) ;
#63497=CYLINDRICAL_SURFACE ( 'NONE', #15710, 11.99999999999999645 ) ;
#63505=CARTESIAN_POINT ( 'NONE',  ( -163.2570736234661695, 5.598654528085800663, -7.705886871421367523 ) ) ;
#63508=CARTESIAN_POINT ( 'NONE',  ( -105.0570736234661666, 0.000000000000000000, 9.524999999999991473 ) ) ;
#63511=ORIENTED_EDGE ( 'NONE', *, *, #48508, .F. ) ;
#63513=CARTESIAN_POINT ( 'NONE',  ( -145.1049999999999898, -6.826472737025115478, 4.959722759717900331 ) ) ;
#63514=CARTESIAN_POINT ( 'NONE',  ( -154.6450000000000102, 4.716976649647091513, -6.492361379858946790 ) ) ;
#63515=CARTESIAN_POINT ( 'NONE',  ( -142.9449999999999932, -9.827790563157499189E-16, -8.024999999999991473 ) ) ;
#63518=CARTESIAN_POINT ( 'NONE',  ( -180.5070736234661979, 8.102448949553176405, 5.886773742842740909 ) ) ;
#63523=CARTESIAN_POINT ( 'NONE',  ( -50.75499999999999545, 4.716976649647091513, -6.492361379858946790 ) ) ;
#63526=EDGE_CURVE ( 'NONE', #12224, #30865, #9658, .T. ) ;
#63536=EDGE_CURVE ( 'NONE', #39475, #37240, #26253, .T. ) ;
#63540=CARTESIAN_POINT ( 'NONE',  ( -178.0429263765338135, -9.058813317711329915, -2.943386871421370898 ) ) ;
#63556=VERTEX_POINT ( 'NONE', #42980 ) ;
#63559=CARTESIAN_POINT ( 'NONE',  ( -101.6929263765337765, 10.01517768586948698, -1.839758294383808966E-15 ) ) ;
#63560=ORIENTED_EDGE ( 'NONE', *, *, #42617, .T. ) ;
#63565=CARTESIAN_POINT ( 'NONE',  ( -97.64499999999999602, 4.716976649647091513, -6.492361379858946790 ) ) ;
#63566=ORIENTED_EDGE ( 'NONE', *, *, #68859, .T. ) ;
#63576=VERTEX_POINT ( 'NONE', #28093 ) ;
#63581=DIRECTION ( 'NONE',  ( -1.000000000000000000, -0.000000000000000000, -0.000000000000000000 ) ) ;
#63595=ORIENTED_EDGE ( 'NONE', *, *, #9243, .F. ) ;
#63596=CARTESIAN_POINT ( 'NONE',  ( -154.6429263765338078, -5.598654528085801552, 7.705886871421367523 ) ) ;
#63597=CARTESIAN_POINT ( 'NONE',  ( -171.3550000000000182, -4.716976649647093289, -6.492361379858945902 ) ) ;
#63600=CARTESIAN_POINT ( 'NONE',  ( -48.80707362346616662, 10.01517768586948698, -1.839758294383808571E-15 ) ) ;
#63601=CARTESIAN_POINT ( 'NONE',  ( -168.8949999999999818, 6.826472737025115478, 4.959722759717899443 ) ) ;
#63607=CARTESIAN_POINT ( 'NONE',  ( -14.34071883355357535, 10.92737318490738474, -4.959116828949759359 ) ) ;
#63608=CARTESIAN_POINT ( 'NONE',  ( -90.20499999999999829, -2.607480562269071545, -8.024999999999991473 ) ) ;
#63613=CARTESIAN_POINT ( 'NONE',  ( -92.09499999999998465, -2.607480562269071545, -8.024999999999991473 ) ) ;
#63628=CARTESIAN_POINT ( 'NONE',  ( -132.1429263765338078, 5.598654528085800663, -7.705886871421367523 ) ) ;
#63634=CARTESIAN_POINT ( 'NONE',  ( -134.6929263765337907, 10.01517768586948698, -1.839758294383808966E-15 ) ) ;
#63640=CARTESIAN_POINT ( 'NONE',  ( -117.3549999999999898, -4.716976649647093289, -6.492361379858945902 ) ) ;
#63643=FACE_BOUND ( 'NONE', #5176, .T. ) ;
#63653=CARTESIAN_POINT ( 'NONE',  ( -54.95707362346616520, 9.058813317711329915, -2.943386871421373119 ) ) ;
#63656=EDGE_LOOP ( 'NONE', ( #15651, #5766, #63015, #62653 ) ) ;
#63665=CARTESIAN_POINT ( 'NONE',  ( -62.84292637653379643, 9.058813317711329915, -2.943386871421373119 ) ) ;
#63668=CARTESIAN_POINT ( 'NONE',  ( -151.2549999999999955, -4.716976649647092401, 6.492361379858946790 ) ) ;
#63680=CARTESIAN_POINT ( 'NONE',  ( -68.75499999999998124, 4.716976649647091513, -6.492361379858946790 ) ) ;
#63692=B_SPLINE_CURVE_WITH_KNOTS ( 'NONE', 3,
 ( #32279, #58326, #48509, #63607, #53731, #10152, #68547, #4858, #47848, #5196, #15450, #30894, #64292, #9468, #19981, #52393, #68905, #5523, #26976, #41848, #15113, #31583, #42540, #69245, #53066, #20706, #41481, #63266, #42217, #21375, #15787, #4139, #63939, #25607, #62897, #47121, #4490, #37269 ),
 .UNSPECIFIED., .F., .F.,
 ( 4, 2, 2, 2, 2, 2, 2, 2, 2, 2, 2, 2, 2, 2, 2, 2, 2, 2, 4 ),
 ( 0.01581385303085219851, 0.01630764152937332415, 0.01680143002789444631, 0.01778900702493669064, 0.01828279552345780934, 0.01877658402197893150, 0.01976416101902116890, 0.02075173801606340629, 0.02173931501310564368, 0.02272689201014788107, 0.02371446900719011500, 0.02470204600423234892, 0.02568962300127458631, 0.02667719999831682370, 0.02766477699535906110, 0.02865235399240129849, 0.02963993098944353588, 0.03062750798648576980, 0.03161508498352800373 ),
 .UNSPECIFIED. ) ;
#63695=CARTESIAN_POINT ( 'NONE',  ( -114.7449999999999903, 4.716976649647094177, 6.492361379858945902 ) ) ;
#63697=CARTESIAN_POINT ( 'NONE',  ( -86.24499999999999034, -4.716976649647093289, -6.492361379858945902 ) ) ;
#63699=FACE_OUTER_BOUND ( 'NONE', #69349, .T. ) ;
#63703=CARTESIAN_POINT ( 'NONE',  ( -133.0429263765338135, -9.058813317711329915, -2.943386871421370898 ) ) ;
#63704=CARTESIAN_POINT ( 'NONE',  ( -161.6950000000000216, -8.437984349512085203, 5.166775262442717831E-16 ) ) ;
#63706=EDGE_CURVE ( 'NONE', #51098, #19619, #35723, .T. ) ;
#63716=CARTESIAN_POINT ( 'NONE',  ( -152.9049999999999727, 2.607480562269069324, -8.024999999999993250 ) ) ;
#63728=CARTESIAN_POINT ( 'NONE',  ( -65.60499999999998977, 6.826472737025113702, -4.959722759717902107 ) ) ;
#63734=DIRECTION ( 'NONE',  ( 0.000000000000000000, 0.000000000000000000, 1.000000000000000000 ) ) ;
#63740=CARTESIAN_POINT ( 'NONE',  ( -46.55707362346617373, -1.166476076187852838E-15, -9.524999999999991473 ) ) ;
#63741=CARTESIAN_POINT ( 'NONE',  ( -115.5570736234661808, -1.166476076187852838E-15, -9.524999999999991473 ) ) ;
#63742=CARTESIAN_POINT ( 'NONE',  ( -184.4049999999999727, -2.607480562269069768, 8.024999999999991473 ) ) ;
#63745=DIRECTION ( 'NONE',  ( 0.000000000000000000, 0.000000000000000000, -1.000000000000000000 ) ) ;
#63749=CARTESIAN_POINT ( 'NONE',  ( -48.44292637653380496, -1.166476076187852838E-15, -9.524999999999991473 ) ) ;
#63750=ORIENTED_EDGE ( 'NONE', *, *, #11771, .T. ) ;
#63751=CARTESIAN_POINT ( 'NONE',  ( -127.8570736234661780, -5.598654528085803328, -7.705886871421366635 ) ) ;
#63752=CARTESIAN_POINT ( 'NONE',  ( -97.85499999999998977, 4.716976649647094177, 6.492361379858945902 ) ) ;
#63757=CARTESIAN_POINT ( 'NONE',  ( -134.0070736234661695, -8.102448949553172852, -5.886773742842741797 ) ) ;
#63761=CARTESIAN_POINT ( 'NONE',  ( -63.95707362346617231, 9.058813317711329915, -2.943386871421373119 ) ) ;
#63763=CARTESIAN_POINT ( 'NONE',  ( -80.84292637653379643, 9.058813317711329915, -2.943386871421373119 ) ) ;
#63771=CARTESIAN_POINT ( 'NONE',  ( -110.1549999999999869, 7.632228543268600340, 2.479861379858949277 ) ) ;
#63774=CARTESIAN_POINT ( 'NONE',  ( -124.6449999999999960, 4.716976649647091513, -6.492361379858946790 ) ) ;
#63778=CARTESIAN_POINT ( 'NONE',  ( -118.1929263765337907, -10.01517768586948698, 6.132527647946031529E-16 ) ) ;
#63782=CARTESIAN_POINT ( 'NONE',  ( -163.7929263765337851, -3.094860106618429807, 9.524999999999991473 ) ) ;
#63783=( NAMED_UNIT ( * ) PLANE_ANGLE_UNIT ( ) SI_UNIT ( $, .RADIAN. ) );
#63791=CARTESIAN_POINT ( 'NONE',  ( -77.54292637653379927, 9.058813317711329915, 2.943386871421369566 ) ) ;
#63794=CARTESIAN_POINT ( 'NONE',  ( -165.5929263765340238, -3.094860106622363993, -9.524999999997135092 ) ) ;
#63797=CARTESIAN_POINT ( 'NONE',  ( -176.6049999999999898, 6.826472737025113702, -4.959722759717902107 ) ) ;
#63801=CARTESIAN_POINT ( 'NONE',  ( -74.60707362346617799, -8.102448949553174629, 5.886773742842742685 ) ) ;
#63807=CARTESIAN_POINT ( 'NONE',  ( -88.55499999999999261, 0.000000000000000000, 8.024999999999991473 ) ) ;
#63812=AXIS2_PLACEMENT_3D ( 'NONE', #20603, #57544, #31835 ) ;
#63819=CARTESIAN_POINT ( 'NONE',  ( -70.79499999999998749, 2.607480562269068880, -8.024999999999993250 ) ) ;
#63834=CARTESIAN_POINT ( 'NONE',  ( -159.8070736234662093, 10.01517768586948698, -1.839758294383808571E-15 ) ) ;
#63837=CARTESIAN_POINT ( 'NONE',  ( -103.4070736234661751, 3.094860106618428031, -9.524999999999993250 ) ) ;
#63841=ORIENTED_EDGE ( 'NONE', *, *, #48281, .F. ) ;
#63846=CARTESIAN_POINT ( 'NONE',  ( -142.8550000000000182, 4.716976649647094177, 6.492361379858945902 ) ) ;
#63850=CARTESIAN_POINT ( 'NONE',  ( -153.5949999999999989, 2.607480562269073321, 8.024999999999991473 ) ) ;
#63853=CARTESIAN_POINT ( 'NONE',  ( -133.7949999999999875, 2.607480562269069324, -8.024999999999993250 ) ) ;
#63861=CARTESIAN_POINT ( 'NONE',  ( -51.20499999999996277, -2.607480562269071545, -8.024999999999991473 ) ) ;
#63865=CARTESIAN_POINT ( 'NONE',  ( -138.7429263765338021, -5.598654528085803328, -7.705886871421366635 ) ) ;
#63893=CARTESIAN_POINT ( 'NONE',  ( -103.1950000000000074, 8.437984349512085203, -1.550032578732815448E-15 ) ) ;
#63906=CARTESIAN_POINT ( 'NONE',  ( -62.45707362346617231, -9.058813317711329915, 2.943386871421371787 ) ) ;
#63916=CARTESIAN_POINT ( 'NONE',  ( -125.9929263765338021, 8.102448949553172852, -5.886773742842744461 ) ) ;
#63927=VERTEX_POINT ( 'NONE', #5789 ) ;
#63928=CARTESIAN_POINT ( 'NONE',  ( -169.7050000000000125, 2.607480562269073321, 8.024999999999991473 ) ) ;
#63931=CARTESIAN_POINT ( 'NONE',  ( -49.85707362346617089, -5.598654528085803328, -7.705886871421366635 ) ) ;
#63932=EDGE_CURVE ( 'NONE', #62258, #25953, #33850, .T. ) ;
#63933=CARTESIAN_POINT ( 'NONE',  ( -166.4950000000000045, 6.826472737025113702, -4.959722759717902107 ) ) ;
#63939=CARTESIAN_POINT ( 'NONE',  ( -12.76923511868948502, 11.13042849027246817, 4.486927442365898244 ) ) ;
#63940=CARTESIAN_POINT ( 'NONE',  ( -85.40499999999998693, -2.607480562269069768, 8.024999999999991473 ) ) ;
#63941=CYLINDRICAL_SURFACE ( 'NONE', #9575, 9.524999999999991473 ) ;
#63945=CARTESIAN_POINT ( 'NONE',  ( -83.99499999999999034, -6.826472737025113702, 4.959722759717902107 ) ) ;
#63950=CARTESIAN_POINT ( 'NONE',  ( -171.5070736234661695, 8.102448949553176405, 5.886773742842740909 ) ) ;
#63958=AXIS2_PLACEMENT_3D ( 'NONE', #26737, #6341, #33094 ) ;
#63961=DIRECTION ( 'NONE',  ( -1.000000000000000000, -0.000000000000000000, -0.000000000000000000 ) ) ;
#63973=CARTESIAN_POINT ( 'NONE',  ( -122.1549999999999869, 7.632228543268600340, 2.479861379858949277 ) ) ;
#63991=CARTESIAN_POINT ( 'NONE',  ( -130.4929263765338021, -8.102448949553174629, 5.886773742842742685 ) ) ;
#64004=CARTESIAN_POINT ( 'NONE',  ( -62.09292637653379643, 3.094860106618433360, 9.524999999999991473 ) ) ;
#64007=CARTESIAN_POINT ( 'NONE',  ( -146.0050000000000239, 6.826472737025116366, 4.959722759717898555 ) ) ;
#64019=CARTESIAN_POINT ( 'NONE',  ( -67.55499999999999261, 0.000000000000000000, 8.024999999999991473 ) ) ;
#64020=VERTEX_POINT ( 'NONE', #11090 ) ;
#64031=EDGE_CURVE ( 'NONE', #50251, #4472, #36602, .T. ) ;
#64036=CARTESIAN_POINT ( 'NONE',  ( -113.0949999999999847, -2.607480562269071545, -8.024999999999991473 ) ) ;
#64038=CARTESIAN_POINT ( 'NONE',  ( -92.09499999999998465, -2.607480562269071545, -8.024999999999991473 ) ) ;
#64045=CARTESIAN_POINT ( 'NONE',  ( -130.7929263765338135, -3.094860106618429807, 9.524999999999991473 ) ) ;
#64046=CYLINDRICAL_SURFACE ( 'NONE', #30987, 9.524999999999991473 ) ;
#64047=CARTESIAN_POINT ( 'NONE',  ( -146.9950000000000045, -6.826472737025115478, 4.959722759717900331 ) ) ;
#64049=CARTESIAN_POINT ( 'NONE',  ( -46.64499999999998892, 4.716976649647091513, -6.492361379858946790 ) ) ;
#64062=CARTESIAN_POINT ( 'NONE',  ( -153.9550000000000125, -7.632228543268599452, 2.479861379858951054 ) ) ;
#64066=VERTEX_POINT ( 'NONE', #59979 ) ;
#64077=CARTESIAN_POINT ( 'NONE',  ( -62.00499999999998835, 6.826472737025115478, 4.959722759717899443 ) ) ;
#64078=CARTESIAN_POINT ( 'NONE',  ( -123.8949999999999676, 6.826472737025116366, 4.959722759717898555 ) ) ;
#64092=CARTESIAN_POINT ( 'NONE',  ( -181.5550000000000068, 0.000000000000000000, 8.024999999999991473 ) ) ;
#64104=CARTESIAN_POINT ( 'NONE',  ( -95.75499999999999545, 4.716976649647091513, -6.492361379858946790 ) ) ;
#64108=CARTESIAN_POINT ( 'NONE',  ( -134.9070736234661183, -3.094860106618429807, 9.524999999999991473 ) ) ;
#64112=CARTESIAN_POINT ( 'NONE',  ( -68.90707362346616094, -3.094860106618429807, 9.524999999999991473 ) ) ;
#64114=CARTESIAN_POINT ( 'NONE',  ( -80.39292637653379359, 8.102448949553176405, 5.886773742842740909 ) ) ;
#64116=CARTESIAN_POINT ( 'NONE',  ( -195.0000000000000000, 0.000000000000000000, 9.524999999999991473 ) ) ;
#64120=CARTESIAN_POINT ( 'NONE',  ( -114.6549999999999869, -7.632228543268600340, -2.479861379858950166 ) ) ;
#64123=CARTESIAN_POINT ( 'NONE',  ( -120.8949999999999960, 6.826472737025116366, 4.959722759717898555 ) ) ;
#64127=VECTOR ( 'NONE', #62824, 1000.000000000000000 ) ;
#64132=CARTESIAN_POINT ( 'NONE',  ( -161.8429263765337964, 9.058813317711329915, -2.943386871421373119 ) ) ;
#64133=CARTESIAN_POINT ( 'NONE',  ( -173.6949999999999648, -8.437984349512085203, 5.166775262442717831E-16 ) ) ;
#64137=ORIENTED_EDGE ( 'NONE', *, *, #49981, .T. ) ;
#64138=CARTESIAN_POINT ( 'NONE',  ( -75.74292637653380211, -5.598654528085803328, -7.705886871421366635 ) ) ;
#64144=CARTESIAN_POINT ( 'NONE',  ( -183.3549999999999898, -4.716976649647093289, -6.492361379858945902 ) ) ;
#64157=CARTESIAN_POINT ( 'NONE',  ( -92.90499999999997272, 2.607480562269069324, -8.024999999999993250 ) ) ;
#64168=CARTESIAN_POINT ( 'NONE',  ( -70.19499999999995055, 8.437984349512085203, -1.550032578732815448E-15 ) ) ;
#64169=ORIENTED_EDGE ( 'NONE', *, *, #39903, .T. ) ;
#64180=LINE ( 'NONE', #26542, #49195 ) ;
#64186=CARTESIAN_POINT ( 'NONE',  ( -156.9570736234661581, 9.058813317711329915, -2.943386871421373119 ) ) ;
#64189=CARTESIAN_POINT ( 'NONE',  ( -89.75707362346616947, -5.598654528085801552, 7.705886871421367523 ) ) ;
#64193=CARTESIAN_POINT ( 'NONE',  ( -195.0000000000000000, 0.000000000000000000, 0.000000000000000000 ) ) ;
#64197=CARTESIAN_POINT ( 'NONE',  ( -142.1049999999999613, -6.826472737025115478, 4.959722759717900331 ) ) ;
#64202=CARTESIAN_POINT ( 'NONE',  ( -148.6450000000000102, 4.716976649647091513, -6.492361379858946790 ) ) ;
#64203=CARTESIAN_POINT ( 'NONE',  ( -137.0949999999999989, -2.607480562269071545, -8.024999999999991473 ) ) ;
#64209=CARTESIAN_POINT ( 'NONE',  ( -55.10499999999998266, -6.826472737025115478, 4.959722759717900331 ) ) ;
#64216=PRODUCT_DEFINITION_CONTEXT ( 'detailed design', #39716, 'design' ) ;
#64218=CARTESIAN_POINT ( 'NONE',  ( -152.8429263765337964, 9.058813317711329915, -2.943386871421373119 ) ) ;
#64220=CARTESIAN_POINT ( 'NONE',  ( -75.05707362346616662, 0.000000000000000000, 9.524999999999991473 ) ) ;
#64221=CARTESIAN_POINT ( 'NONE',  ( -100.4070736234672125, 3.094860106601488248, -9.525000000012305179 ) ) ;
#64238=CARTESIAN_POINT ( 'NONE',  ( -195.0000000000000000, 0.000000000000000000, 0.000000000000000000 ) ) ;
#64248=CARTESIAN_POINT ( 'NONE',  ( -105.4449999999999790, 0.000000000000000000, 8.024999999999991473 ) ) ;
#64252=EDGE_CURVE ( 'NONE', #49213, #52470, #20811, .T. ) ;
#64268=( BOUNDED_CURVE ( )  B_SPLINE_CURVE ( 2, ( #11039, #32485, #16705, #49733, #60952, #23331, #1820, #438, #34241, #60597, #54972 ),
 .UNSPECIFIED., .F., .F. ) 
 B_SPLINE_CURVE_WITH_KNOTS ( ( 3, 2, 2, 2, 2, 3 ),
 ( 0.4130434782608596311, 0.4152173913043378239, 0.4173913043478160723, 0.4195652173912943206, 0.4217391304347725689, 0.4239130434782507617 ),
 .UNSPECIFIED. ) 
 CURVE ( )  GEOMETRIC_REPRESENTATION_ITEM ( )  RATIONAL_B_SPLINE_CURVE ( ( 1.000000000000223821, 0.9510565162949298212, 1.000000000000000000, 0.9510565162951535312, 1.000000000000000000, 0.9510565162951535312, 1.000000000000000000, 0.9510565162951535312, 1.000000000000000000, 0.9510565162953810159, 0.9999999999997725153 ) ) 
 REPRESENTATION_ITEM ( '' )  );
#64269=AXIS2_PLACEMENT_3D ( 'NONE', #30695, #35657, #68026 ) ;
#64270=DIRECTION ( 'NONE',  ( -1.000000000000000000, -0.000000000000000000, -0.000000000000000000 ) ) ;
#64275=AXIS2_PLACEMENT_3D ( 'NONE', #27892, #60962, #1481 ) ;
#64279=CARTESIAN_POINT ( 'NONE',  ( -170.7570736234661695, -5.598654528085801552, 7.705886871421367523 ) ) ;
#64281=ORIENTED_EDGE ( 'NONE', *, *, #62958, .F. ) ;
#64283=CARTESIAN_POINT ( 'NONE',  ( -171.9549999999999841, -7.632228543268599452, 2.479861379858951054 ) ) ;
#64286=CARTESIAN_POINT ( 'NONE',  ( -48.50707362346617657, 8.102448949553176405, 5.886773742842740909 ) ) ;
#64287=CARTESIAN_POINT ( 'NONE',  ( -169.9449999999999932, -9.827790563157499189E-16, -8.024999999999991473 ) ) ;
#64292=CARTESIAN_POINT ( 'NONE',  ( -11.69351122144522215, 11.39671261894639187, -3.764684334147166300 ) ) ;
#64293=CARTESIAN_POINT ( 'NONE',  ( -79.10499999999998977, -6.826472737025115478, 4.959722759717900331 ) ) ;
#64297=CARTESIAN_POINT ( 'NONE',  ( -83.09499999999998465, -2.607480562269071545, -8.024999999999991473 ) ) ;
#64301=CARTESIAN_POINT ( 'NONE',  ( -171.9570736234661865, 9.058813317711329915, -2.943386871421373119 ) ) ;
#64315=ORIENTED_EDGE ( 'NONE', *, *, #37480, .T. ) ;
#64327=CARTESIAN_POINT ( 'NONE',  ( -119.1550000000000011, 7.632228543268600340, 2.479861379858949277 ) ) ;
#64335=ADVANCED_FACE ( 'NONE', ( #9914 ), #64046, .T. ) ;
#64336=AXIS2_PLACEMENT_3D ( 'NONE', #34427, #67130, #35479 ) ;
#64342=AXIS2_PLACEMENT_3D ( 'NONE', #15755, #53033, #20673 ) ;
#64347=CARTESIAN_POINT ( 'NONE',  ( -130.6429263765338078, -5.598654528085801552, 7.705886871421367523 ) ) ;
#64348=VERTEX_POINT ( 'NONE', #69004 ) ;
#64361=CARTESIAN_POINT ( 'NONE',  ( -141.9549999999999841, -7.632228543268599452, 2.479861379858951054 ) ) ;
#64366=DIRECTION ( 'NONE',  ( -1.000000000000000000, -0.000000000000000000, -0.000000000000000000 ) ) ;
#64376=CARTESIAN_POINT ( 'NONE',  ( -60.20499999999998408, -2.607480562269071545, -8.024999999999991473 ) ) ;
#64390=CARTESIAN_POINT ( 'NONE',  ( -107.2449999999999903, -4.716976649647093289, -6.492361379858945902 ) ) ;
#64392=CARTESIAN_POINT ( 'NONE',  ( -90.29499999999997328, -2.607480562269069768, 8.024999999999991473 ) ) ;
#64402=CARTESIAN_POINT ( 'NONE',  ( -135.7429263765338021, -5.598654528085803328, -7.705886871421366635 ) ) ;
#64403=CARTESIAN_POINT ( 'NONE',  ( -148.6450000000000102, 4.716976649647091513, -6.492361379858946790 ) ) ;
#64412=AXIS2_PLACEMENT_3D ( 'NONE', #11235, #937, #6999 ) ;
#64417=CARTESIAN_POINT ( 'NONE',  ( -59.69292637653380496, 10.01517768586948698, -1.839758294383808966E-15 ) ) ;
#64420=DIRECTION ( 'NONE',  ( -1.000000000000000000, -0.000000000000000000, -0.000000000000000000 ) ) ;
#64422=CARTESIAN_POINT ( 'NONE',  ( -147.0549999999999784, -9.827790563157499189E-16, -8.024999999999991473 ) ) ;
#64427=ADVANCED_FACE ( 'NONE', ( #45375 ), #54588, .F. ) ;
#64437=CARTESIAN_POINT ( 'NONE',  ( -65.00499999999998124, 6.826472737025115478, 4.959722759717899443 ) ) ;
#64438=CARTESIAN_POINT ( 'NONE',  ( -121.0449999999999875, 7.632228543268600340, 2.479861379858949277 ) ) ;
#64448=ORIENTED_EDGE ( 'NONE', *, *, #9563, .T. ) ;
#64453=CARTESIAN_POINT ( 'NONE',  ( -168.6550000000000011, -7.632228543268600340, -2.479861379858950166 ) ) ;
#64462=CARTESIAN_POINT ( 'NONE',  ( -86.00499999999999545, 6.826472737025116366, 4.959722759717898555 ) ) ;
#64470=CARTESIAN_POINT ( 'NONE',  ( -66.80707362346618083, 10.01517768586948698, -1.839758294383808571E-15 ) ) ;
#64480=CARTESIAN_POINT ( 'NONE',  ( -114.3549999999999898, -4.716976649647093289, -6.492361379858945902 ) ) ;
#64482=CARTESIAN_POINT ( 'NONE',  ( -117.4449999999999932, 0.000000000000000000, 8.024999999999991473 ) ) ;
#64485=AXIS2_PLACEMENT_3D ( 'NONE', #39660, #12539, #2268 ) ;
#64490=CARTESIAN_POINT ( 'NONE',  ( -157.9429263765338192, 0.000000000000000000, 9.524999999999991473 ) ) ;
#64491=CARTESIAN_POINT ( 'NONE',  ( -173.8449999999999989, -7.632228543268599452, 2.479861379858951054 ) ) ;
#64494=ADVANCED_FACE ( 'NONE', ( #54136 ), #59401, .T. ) ;
#64499=CARTESIAN_POINT ( 'NONE',  ( -78.89292637653380780, -8.102448949553172852, -5.886773742842741797 ) ) ;
#64502=ADVANCED_FACE ( 'NONE', ( #28069 ), #22845, .T. ) ;
#64506=CARTESIAN_POINT ( 'NONE',  ( -179.6049999999999898, 6.826472737025113702, -4.959722759717902107 ) ) ;
#64510=CARTESIAN_POINT ( 'NONE',  ( -74.45707362346617231, -9.058813317711329915, 2.943386871421371787 ) ) ;
#64518=CARTESIAN_POINT ( 'NONE',  ( -91.55499999999997840, 0.000000000000000000, 8.024999999999991473 ) ) ;
#64524=VECTOR ( 'NONE', #62493, 1000.000000000000000 ) ;
#64533=CARTESIAN_POINT ( 'NONE',  ( -66.44499999999999318, 0.000000000000000000, 8.024999999999991473 ) ) ;
#64545=CARTESIAN_POINT ( 'NONE',  ( -126.8050000000000068, -8.437984349512085203, 5.166775262442717831E-16 ) ) ;
#64547=CARTESIAN_POINT ( 'NONE',  ( -73.49292637653380211, -8.102448949553174629, 5.886773742842742685 ) ) ;
#64551=VECTOR ( 'NONE', #12495, 1000.000000000000000 ) ;
#64552=CARTESIAN_POINT ( 'NONE',  ( -162.3570736234661922, 5.598654528085804216, 7.705886871421366635 ) ) ;
#64554=CARTESIAN_POINT ( 'NONE',  ( -93.95707362346617231, 9.058813317711329915, -2.943386871421373119 ) ) ;
#64562=CARTESIAN_POINT ( 'NONE',  ( -136.1049999999999898, -6.826472737025115478, 4.959722759717900331 ) ) ;
#64565=CARTESIAN_POINT ( 'NONE',  ( -146.3950000000000102, -6.826472737025115478, -4.959722759717899443 ) ) ;
#64567=CARTESIAN_POINT ( 'NONE',  ( -141.2949999999999875, -2.607480562269069768, 8.024999999999991473 ) ) ;
#64576=CARTESIAN_POINT ( 'NONE',  ( -58.25499999999997414, -4.716976649647092401, 6.492361379858946790 ) ) ;
#64579=CARTESIAN_POINT ( 'NONE',  ( -62.99499999999996902, -6.826472737025115478, 4.959722759717900331 ) ) ;
#64582=DIRECTION ( 'NONE',  ( -1.000000000000000000, -0.000000000000000000, -0.000000000000000000 ) ) ;
#64585=CARTESIAN_POINT ( 'NONE',  ( -107.3929263765338078, 8.102448949553176405, 5.886773742842740909 ) ) ;
#64599=( BOUNDED_CURVE ( )  B_SPLINE_CURVE ( 2, ( #32885, #5419, #59235, #5097, #27575, #69470, #32184, #43815, #11060, #21258, #21623 ),
 .UNSPECIFIED., .F., .F. ) 
 B_SPLINE_CURVE_WITH_KNOTS ( ( 3, 2, 2, 2, 2, 3 ),
 ( 0.1739130434782566736, 0.1760869565217348942, 0.1782608695652131148, 0.1804347826086913353, 0.1826086956521695559, 0.1847826086956477487 ),
 .UNSPECIFIED. ) 
 CURVE ( )  GEOMETRIC_REPRESENTATION_ITEM ( )  RATIONAL_B_SPLINE_CURVE ( ( 1.000000000000094147, 0.9510565162950590512, 1.000000000000000000, 0.9510565162951535312, 1.000000000000000000, 0.9510565162951535312, 1.000000000000000000, 0.9510565162951535312, 1.000000000000000000, 0.9510565162952528961, 0.9999999999999006350 ) ) 
 REPRESENTATION_ITEM ( '' )  );
#64602=ORIENTED_EDGE ( 'NONE', *, *, #45796, .F. ) ;
#64605=DIRECTION ( 'NONE',  ( -1.000000000000000000, -0.000000000000000000, -0.000000000000000000 ) ) ;
#64614=CARTESIAN_POINT ( 'NONE',  ( -100.1949999999999790, 8.437984349512085203, -1.550032578732815448E-15 ) ) ;
#64616=AXIS2_PLACEMENT_3D ( 'NONE', #16952, #48282, #38439 ) ;
#64619=VERTEX_POINT ( 'NONE', #27730 ) ;
#64625=CARTESIAN_POINT ( 'NONE',  ( -165.0570736234661524, 0.000000000000000000, 9.524999999999991473 ) ) ;
#64631=CARTESIAN_POINT ( 'NONE',  ( -60.05707362346616662, 0.000000000000000000, 9.524999999999991473 ) ) ;
#64636=CARTESIAN_POINT ( 'NONE',  ( -48.35707362346617089, 5.598654528085804216, 7.705886871421366635 ) ) ;
#64638=FACE_OUTER_BOUND ( 'NONE', #64690, .T. ) ;
#64642=CARTESIAN_POINT ( 'NONE',  ( -171.2049999999999841, -2.607480562269071545, -8.024999999999991473 ) ) ;
#64646=CARTESIAN_POINT ( 'NONE',  ( -174.2949999999999591, -2.607480562269069768, 8.024999999999991473 ) ) ;
#64649=CARTESIAN_POINT ( 'NONE',  ( -162.7450000000000045, 4.716976649647094177, 6.492361379858945902 ) ) ;
#64653=CARTESIAN_POINT ( 'NONE',  ( -79.40500000000000114, -2.607480562269069768, 8.024999999999991473 ) ) ;
#64658=EDGE_CURVE ( 'NONE', #59896, #57410, #67150, .T. ) ;
#64659=CARTESIAN_POINT ( 'NONE',  ( -76.49499999999999034, 6.826472737025113702, -4.959722759717902107 ) ) ;
#64663=CARTESIAN_POINT ( 'NONE',  ( -170.3929263765337794, 8.102448949553176405, 5.886773742842740909 ) ) ;
#64664=ADVANCED_FACE ( 'NONE', ( #46404 ), #62184, .T. ) ;
#64667=CARTESIAN_POINT ( 'NONE',  ( -73.94292637653379074, 0.000000000000000000, 9.524999999999991473 ) ) ;
#64672=CARTESIAN_POINT ( 'NONE',  ( -50.09292637653378222, 3.094860106618433360, 9.524999999999991473 ) ) ;
#64675=CARTESIAN_POINT ( 'NONE',  ( -78.05707362346616662, 0.000000000000000000, 9.524999999999991473 ) ) ;
#64678=VERTEX_POINT ( 'NONE', #13295 ) ;
#64685=CARTESIAN_POINT ( 'NONE',  ( -108.2049999999999983, -2.607480562269071545, -8.024999999999991473 ) ) ;
#64689=CYLINDRICAL_SURFACE ( 'NONE', #61311, 11.99999999999999645 ) ;
#64690=EDGE_LOOP ( 'NONE', ( #14689, #37857, #56731, #28767 ) ) ;
#64702=CARTESIAN_POINT ( 'NONE',  ( -15.00000000000000000, -10.90871211463571200, 5.000000000000000000 ) ) ;
#64713=CARTESIAN_POINT ( 'NONE',  ( -53.09292637653378932, 3.094860106618433360, 9.524999999999991473 ) ) ;
#64714=CARTESIAN_POINT ( 'NONE',  ( -147.2050000000000125, -2.607480562269071545, -8.024999999999991473 ) ) ;
#64723=CARTESIAN_POINT ( 'NONE',  ( -54.35499999999998977, -4.716976649647093289, -6.492361379858945902 ) ) ;
#64730=CARTESIAN_POINT ( 'NONE',  ( -97.49292637653380211, -8.102448949553174629, 5.886773742842742685 ) ) ;
#64741=CARTESIAN_POINT ( 'NONE',  ( -109.1949999999999790, 8.437984349512086979, -1.550032578732815448E-15 ) ) ;
#64744=CARTESIAN_POINT ( 'NONE',  ( -87.44499999999999318, 0.000000000000000000, 8.024999999999991473 ) ) ;
#64752=CARTESIAN_POINT ( 'NONE',  ( -123.1429263765338078, 5.598654528085800663, -7.705886871421367523 ) ) ;
#64753=CARTESIAN_POINT ( 'NONE',  ( -145.3449999999999989, 7.632228543268599452, -2.479861379858951942 ) ) ;
#64765=CARTESIAN_POINT ( 'NONE',  ( -116.3929263765338078, 8.102448949553176405, 5.886773742842740909 ) ) ;
#64767=CARTESIAN_POINT ( 'NONE',  ( -138.8050000000000068, -8.437984349512086979, 5.166775262442717831E-16 ) ) ;
#64781=CARTESIAN_POINT ( 'NONE',  ( -64.10499999999997556, -6.826472737025113702, 4.959722759717902107 ) ) ;
#64782=CARTESIAN_POINT ( 'NONE',  ( -120.7449999999999903, 4.716976649647094177, 6.492361379858945902 ) ) ;
#64794=CARTESIAN_POINT ( 'NONE',  ( -170.1550000000000011, 7.632228543268600340, 2.479861379858949277 ) ) ;
#64802=CARTESIAN_POINT ( 'NONE',  ( -86.30499999999997840, 8.437984349512085203, -1.550032578732815448E-15 ) ) ;
#64808=CARTESIAN_POINT ( 'NONE',  ( -61.40707362346618226, 3.094860106618428031, -9.524999999999993250 ) ) ;
#64816=CARTESIAN_POINT ( 'NONE',  ( -105.5049999999999812, -6.826472737025115478, -4.959722759717899443 ) ) ;
#64818=CARTESIAN_POINT ( 'NONE',  ( -114.5949999999999704, 2.607480562269073321, 8.024999999999991473 ) ) ;
#64823=CARTESIAN_POINT ( 'NONE',  ( -161.0929263765338249, 3.094860106618433360, 9.524999999999991473 ) ) ;
#64824=( NAMED_UNIT ( * ) SI_UNIT ( $, .STERADIAN. ) SOLID_ANGLE_UNIT ( ) );
#64825=CARTESIAN_POINT ( 'NONE',  ( -176.5450000000000159, -7.632228543268600340, -2.479861379858950166 ) ) ;
#64833=CARTESIAN_POINT ( 'NONE',  ( -78.14292637653380780, 5.598654528085800663, -7.705886871421367523 ) ) ;
#64840=CARTESIAN_POINT ( 'NONE',  ( -176.4550000000000125, 7.632228543268599452, -2.479861379858951942 ) ) ;
#64845=CARTESIAN_POINT ( 'NONE',  ( -183.0000000000000284, -1.154738647139537111, 9.454745033939424559 ) ) ;
#64847=ADVANCED_FACE ( 'NONE', ( #53705 ), #5493, .T. ) ;
#64851=CARTESIAN_POINT ( 'NONE',  ( -89.45499999999999829, 7.632228543268599452, -2.479861379858951942 ) ) ;
#64853=ORIENTED_EDGE ( 'NONE', *, *, #16037, .F. ) ;
#64858=CARTESIAN_POINT ( 'NONE',  ( -64.19499999999999318, 8.437984349512085203, -1.550032578732815448E-15 ) ) ;
#64861=ADVANCED_FACE ( 'NONE', ( #36190 ), #53388, .T. ) ;
#64863=CARTESIAN_POINT ( 'NONE',  ( -138.3570736234661638, 5.598654528085804216, 7.705886871421366635 ) ) ;
#64866=ORIENTED_EDGE ( 'NONE', *, *, #55680, .F. ) ;
#64870=CARTESIAN_POINT ( 'NONE',  ( -111.9549999999999841, -7.632228543268599452, 2.479861379858951054 ) ) ;
#64876=CARTESIAN_POINT ( 'NONE',  ( -15.00000000000000000, 10.90871211463577239, 5.000000000000000888 ) ) ;
#64877=CARTESIAN_POINT ( 'NONE',  ( -162.9570736234661865, 9.058813317711329915, -2.943386871421373119 ) ) ;
#64879=( BOUNDED_CURVE ( )  B_SPLINE_CURVE ( 2, ( #35173, #55933, #45763, #17038, #56634, #7739, #8461, #35536, #27540, #51356, #12667 ),
 .UNSPECIFIED., .F., .F. ) 
 B_SPLINE_CURVE_WITH_KNOTS ( ( 3, 2, 2, 2, 2, 3 ),
 ( 0.4021739130434687226, 0.4043478260869469154, 0.4065217391304251082, 0.4086956521739034121, 0.4108695652173816049, 0.4130434782608597977 ),
 .UNSPECIFIED. ) 
 CURVE ( )  GEOMETRIC_REPRESENTATION_ITEM ( )  RATIONAL_B_SPLINE_CURVE ( ( 1.000000000000214939, 0.9510565162949385920, 1.000000000000000000, 0.9510565162951535312, 1.000000000000000000, 0.9510565162951535312, 1.000000000000000000, 0.9510565162951535312, 1.000000000000000000, 0.9510565162953734664, 0.9999999999997800648 ) ) 
 REPRESENTATION_ITEM ( '' )  );
#64880=CARTESIAN_POINT ( 'NONE',  ( -91.55707362346616662, -1.166476076187852838E-15, -9.524999999999991473 ) ) ;
#64890=CARTESIAN_POINT ( 'NONE',  ( -134.7549999999999955, 4.716976649647091513, -6.492361379858946790 ) ) ;
#64892=CARTESIAN_POINT ( 'NONE',  ( -55.94292637653380496, 0.000000000000000000, 9.524999999999991473 ) ) ;
#64893=CARTESIAN_POINT ( 'NONE',  ( -145.9449999999999932, -9.827790563157499189E-16, -8.024999999999991473 ) ) ;
#64895=CARTESIAN_POINT ( 'NONE',  ( -136.0449999999999875, 7.632228543268600340, 2.479861379858949277 ) ) ;
#64902=CARTESIAN_POINT ( 'NONE',  ( -50.30499999999999261, 8.437984349512085203, -1.550032578732815448E-15 ) ) ;
#64903=CARTESIAN_POINT ( 'NONE',  ( -59.24499999999999034, -4.716976649647093289, -6.492361379858945902 ) ) ;
#64907=CARTESIAN_POINT ( 'NONE',  ( -103.9429263765338050, 0.000000000000000000, 9.524999999999991473 ) ) ;
#64929=CARTESIAN_POINT ( 'NONE',  ( -101.0929263765348622, 3.094860106636045938, 9.524999999987192822 ) ) ;
#64934=CARTESIAN_POINT ( 'NONE',  ( -93.59499999999997044, 2.607480562269073321, 8.024999999999991473 ) ) ;
#64945=B_SPLINE_CURVE_WITH_KNOTS ( 'NONE', 3,
 ( #46774, #14013, #3762, #56921, #4462, #9092, #24537, #14715, #30870, #62532, #25932, #25581, #47098, #67833 ),
 .UNSPECIFIED., .F., .F.,
 ( 4, 2, 2, 2, 2, 2, 4 ),
 ( 0.000000000000000000, 0.002322248283345770738, 0.003483372425018657192, 0.004644496566691544079, 0.006966744850037316986, 0.008127868991710203439, 0.009288993133383091627 ),
 .UNSPECIFIED. ) ;
#64951=CARTESIAN_POINT ( 'NONE',  ( -184.0000000000000000, 0.000000000000000000, 5.499999999999985789 ) ) ;
#64953=CARTESIAN_POINT ( 'NONE',  ( -195.0000000000000000, 0.000000000000000000, 9.524999999999991473 ) ) ;
#64956=CARTESIAN_POINT ( 'NONE',  ( -68.69292637653380496, 10.01517768586948698, -1.839758294383808966E-15 ) ) ;
#64960=CARTESIAN_POINT ( 'NONE',  ( -161.3929263765338078, 8.102448949553176405, 5.886773742842740909 ) ) ;
#64964=CARTESIAN_POINT ( 'NONE',  ( -149.6070736234661638, -8.102448949553174629, 5.886773742842742685 ) ) ;
#64967=CARTESIAN_POINT ( 'NONE',  ( -172.8550000000000182, 4.716976649647094177, 6.492361379858945902 ) ) ;
#64969=CARTESIAN_POINT ( 'NONE',  ( -171.5949999999999704, 2.607480562269073321, 8.024999999999991473 ) ) ;
#64971=CARTESIAN_POINT ( 'NONE',  ( -167.0949999999999704, -2.607480562269071545, -8.024999999999991473 ) ) ;
#64976=CARTESIAN_POINT ( 'NONE',  ( -78.35499999999997556, -4.716976649647093289, -6.492361379858945902 ) ) ;
#64979=CARTESIAN_POINT ( 'NONE',  ( -78.89499999999999602, 6.826472737025115478, 4.959722759717899443 ) ) ;
#65003=CARTESIAN_POINT ( 'NONE',  ( -113.9049999999999727, 2.607480562269069324, -8.024999999999993250 ) ) ;
#65019=CARTESIAN_POINT ( 'NONE',  ( -118.2570736234661695, 5.598654528085800663, -7.705886871421367523 ) ) ;
#65021=CARTESIAN_POINT ( 'NONE',  ( -181.0429263765338135, -9.058813317711329915, -2.943386871421370898 ) ) ;
#65031=CARTESIAN_POINT ( 'NONE',  ( -139.4050000000000296, -2.607480562269069768, 8.024999999999991473 ) ) ;
#65046=CARTESIAN_POINT ( 'NONE',  ( -57.80499999999998550, -8.437984349512085203, 5.166775262442717831E-16 ) ) ;
#65063=CARTESIAN_POINT ( 'NONE',  ( -106.0449999999999875, 7.632228543268600340, 2.479861379858949277 ) ) ;
#65065=CARTESIAN_POINT ( 'NONE',  ( -86.39499999999999602, -6.826472737025115478, -4.959722759717899443 ) ) ;
#65072=CARTESIAN_POINT ( 'NONE',  ( -120.4429263765338050, -1.166476076187852838E-15, -9.524999999999991473 ) ) ;
#65073=CARTESIAN_POINT ( 'NONE',  ( -143.2449999999999761, -4.716976649647093289, -6.492361379858945902 ) ) ;
#65088=CARTESIAN_POINT ( 'NONE',  ( -145.1049999999999898, -6.826472737025113702, 4.959722759717902107 ) ) ;
#65104=CARTESIAN_POINT ( 'NONE',  ( -95.60707362346614957, -8.102448949553174629, 5.886773742842742685 ) ) ;
#65106=CARTESIAN_POINT ( 'NONE',  ( -57.05499999999999261, -9.827790563157499189E-16, -8.024999999999991473 ) ) ;
#65107=CARTESIAN_POINT ( 'NONE',  ( -119.2449999999999903, -4.716976649647093289, -6.492361379858945902 ) ) ;
#65116=FACE_OUTER_BOUND ( 'NONE', #30612, .T. ) ;
#65123=CARTESIAN_POINT ( 'NONE',  ( -174.9550000000000125, -7.632228543268599452, 2.479861379858951054 ) ) ;
#65124=EDGE_CURVE ( 'NONE', #36781, #23235, #40115, .T. ) ;
#65134=ORIENTED_EDGE ( 'NONE', *, *, #50273, .F. ) ;
#65137=CARTESIAN_POINT ( 'NONE',  ( -195.0000000000000000, 0.000000000000000000, 0.000000000000000000 ) ) ;
#65138=CARTESIAN_POINT ( 'NONE',  ( -89.75499999999998124, 4.716976649647091513, -6.492361379858946790 ) ) ;
#65145=CARTESIAN_POINT ( 'NONE',  ( -66.50707362346615525, 8.102448949553176405, 5.886773742842740909 ) ) ;
#65148=ORIENTED_EDGE ( 'NONE', *, *, #7402, .F. ) ;
#65151=CARTESIAN_POINT ( 'NONE',  ( -99.65499999999998693, -7.632228543268600340, -2.479861379858950166 ) ) ;
#65153=CARTESIAN_POINT ( 'NONE',  ( -118.9449999999999932, -9.827790563157499189E-16, -8.024999999999991473 ) ) ;
#65161=CARTESIAN_POINT ( 'NONE',  ( -151.7929263765338135, -3.094860106618429807, 9.524999999999991473 ) ) ;
#65162=CARTESIAN_POINT ( 'NONE',  ( -177.5950000000000273, 2.607480562269073321, 8.024999999999991473 ) ) ;
#65171=CARTESIAN_POINT ( 'NONE',  ( -71.24292637653380211, 5.598654528085804216, 7.705886871421366635 ) ) ;
#65173=CARTESIAN_POINT ( 'NONE',  ( -195.0000000000000000, 1.166476076187852838E-15, -9.524999999999991473 ) ) ;
#65177=CARTESIAN_POINT ( 'NONE',  ( -142.7929263765343251, -3.094860106609758077, 9.525000000006292211 ) ) ;
#65182=CARTESIAN_POINT ( 'NONE',  ( -172.4050000000000011, -2.607480562269069768, 8.024999999999991473 ) ) ;
#65189=CARTESIAN_POINT ( 'NONE',  ( -182.7570736234661979, -5.598654528085801552, 7.705886871421367523 ) ) ;
#65196=CARTESIAN_POINT ( 'NONE',  ( -80.60499999999996135, 6.826472737025113702, -4.959722759717902107 ) ) ;
#65206=CARTESIAN_POINT ( 'NONE',  ( -64.04499999999998749, 7.632228543268600340, 2.479861379858949277 ) ) ;
#65220=CARTESIAN_POINT ( 'NONE',  ( -118.2549999999999812, -4.716976649647092401, 6.492361379858946790 ) ) ;
#65228=CARTESIAN_POINT ( 'NONE',  ( -150.2070736234661581, 3.094860106618433360, 9.524999999999991473 ) ) ;
#65230=CARTESIAN_POINT ( 'NONE',  ( -94.40707362346618936, 3.094860106618428031, -9.524999999999993250 ) ) ;
#65237=CARTESIAN_POINT ( 'NONE',  ( -126.6549999999999869, -7.632228543268600340, -2.479861379858950166 ) ) ;
#65239=CARTESIAN_POINT ( 'NONE',  ( -146.8429263765338249, 9.058813317711329915, -2.943386871421373119 ) ) ;
#65240=CARTESIAN_POINT ( 'NONE',  ( -55.64292637653381490, -5.598654528085801552, 7.705886871421367523 ) ) ;
#65241=CARTESIAN_POINT ( 'NONE',  ( -146.5449999999999875, -7.632228543268600340, -2.479861379858950166 ) ) ;
#65242=CARTESIAN_POINT ( 'NONE',  ( -129.5949999999999989, 2.607480562269072433, 8.024999999999991473 ) ) ;
#65251=CARTESIAN_POINT ( 'NONE',  ( -184.4929263765337737, -8.102448949553172852, 5.886773742842742685 ) ) ;
#65252=CARTESIAN_POINT ( 'NONE',  ( -56.99499999999999034, -6.826472737025115478, 4.959722759717900331 ) ) ;
#65259=CARTESIAN_POINT ( 'NONE',  ( -107.2429263765338021, 5.598654528085804216, 7.705886871421366635 ) ) ;
#65292=CARTESIAN_POINT ( 'NONE',  ( -89.99499999999999034, -6.826472737025115478, 4.959722759717900331 ) ) ;
#65294=( BOUNDED_CURVE ( )  B_SPLINE_CURVE ( 2, ( #59331, #59017, #15444, #32982, #53057, #48502, #54417, #201, #54070, #25948, #42209 ),
 .UNSPECIFIED., .F., .F. ) 
 B_SPLINE_CURVE_WITH_KNOTS ( ( 3, 2, 2, 2, 2, 3 ),
 ( 0.2499999999999941158, 0.2521739130434723086, 0.2543478260869505014, 0.2565217391304288053, 0.2586956521739069981, 0.2608695652173851909 ),
 .UNSPECIFIED. ) 
 CURVE ( )  GEOMETRIC_REPRESENTATION_ITEM ( )  RATIONAL_B_SPLINE_CURVE ( ( 1.000000000000132561, 0.9510565162950210816, 1.000000000000000000, 0.9510565162951535312, 1.000000000000000000, 0.9510565162951535312, 1.000000000000000000, 0.9510565162951535312, 1.000000000000000000, 0.9510565162952909768, 0.9999999999998625544 ) ) 
 REPRESENTATION_ITEM ( '' )  );
#65300=ADVANCED_FACE ( 'NONE', ( #48758 ), #59595, .T. ) ;
#65313=CARTESIAN_POINT ( 'NONE',  ( -176.3070736234661808, -10.01517768586948698, 6.132527647946031529E-16 ) ) ;
#65320=CARTESIAN_POINT ( 'NONE',  ( -162.1429263765338362, 5.598654528085800663, -7.705886871421367523 ) ) ;
#65326=CARTESIAN_POINT ( 'NONE',  ( -158.1550000000000011, 7.632228543268600340, 2.479861379858949277 ) ) ;
#65327=CARTESIAN_POINT ( 'NONE',  ( -183.4034255575450914, -1.261462791345238532, -9.055628821941482443 ) ) ;
#65329=CARTESIAN_POINT ( 'NONE',  ( -172.0450000000000159, 7.632228543268600340, 2.479861379858949277 ) ) ;
#65330=CARTESIAN_POINT ( 'NONE',  ( -161.2450000000000045, -4.716976649647093289, -6.492361379858945902 ) ) ;
#65334=CARTESIAN_POINT ( 'NONE',  ( -89.84292637653381064, 9.058813317711329915, -2.943386871421373119 ) ) ;
#65337=CARTESIAN_POINT ( 'NONE',  ( -69.35499999999998977, -4.716976649647093289, -6.492361379858945902 ) ) ;
#65339=CARTESIAN_POINT ( 'NONE',  ( -85.64499999999998181, 4.716976649647091513, -6.492361379858946790 ) ) ;
#65351=CARTESIAN_POINT ( 'NONE',  ( -50.84292637653378932, 9.058813317711329915, -2.943386871421373119 ) ) ;
#65368=CIRCLE ( 'NONE', #40545, 10.99999999999995381 ) ;
#65369=CARTESIAN_POINT ( 'NONE',  ( -69.65707362346616094, 9.058813317711329915, 2.943386871421369566 ) ) ;
#65372=CARTESIAN_POINT ( 'NONE',  ( -111.2049999999999841, -2.607480562269071545, -8.024999999999991473 ) ) ;
#65377=CARTESIAN_POINT ( 'NONE',  ( -68.00707362346616947, -8.102448949553174629, -5.886773742842741797 ) ) ;
#65385=DIRECTION ( 'NONE',  ( 0.000000000000000000, 0.000000000000000000, 1.000000000000000000 ) ) ;
#65393=CARTESIAN_POINT ( 'NONE',  ( -57.05707362346618083, 0.000000000000000000, 9.524999999999991473 ) ) ;
#65398=CARTESIAN_POINT ( 'NONE',  ( -51.14292637653380780, 5.598654528085800663, -7.705886871421367523 ) ) ;
#65402=CARTESIAN_POINT ( 'NONE',  ( -144.5049999999999670, -6.826472737025115478, -4.959722759717899443 ) ) ;
#65408=CARTESIAN_POINT ( 'NONE',  ( -106.3429263765338106, -9.058813317711329915, 2.943386871421371787 ) ) ;
#65409=CARTESIAN_POINT ( 'NONE',  ( -107.0070736234661695, -8.102448949553174629, -5.886773742842741797 ) ) ;
#65415=CARTESIAN_POINT ( 'NONE',  ( -109.6429263765338078, -5.598654528085801552, 7.705886871421367523 ) ) ;
#65416=CARTESIAN_POINT ( 'NONE',  ( -52.25499999999999545, -4.716976649647092401, 6.492361379858946790 ) ) ;
#65430=CARTESIAN_POINT ( 'NONE',  ( -105.1449999999999818, -4.716976649647092401, 6.492361379858946790 ) ) ;
#65432=CARTESIAN_POINT ( 'NONE',  ( -80.69499999999999318, -8.437984349512085203, 5.166775262442717831E-16 ) ) ;
#65440=CARTESIAN_POINT ( 'NONE',  ( -125.0929263765337964, 3.094860106618433360, 9.524999999999991473 ) ) ;
#65442=CARTESIAN_POINT ( 'NONE',  ( -144.5950000000000273, 2.607480562269073321, 8.024999999999991473 ) ) ;
#65446=CARTESIAN_POINT ( 'NONE',  ( -47.39499999999998892, -6.826472737025113702, -4.959722759717900331 ) ) ;
#65455=CARTESIAN_POINT ( 'NONE',  ( -49.55707362346617373, -1.166476076187852838E-15, -9.524999999999991473 ) ) ;
#65458=CARTESIAN_POINT ( 'NONE',  ( -143.6049999999999613, 6.826472737025113702, -4.959722759717902107 ) ) ;
#65470=CARTESIAN_POINT ( 'NONE',  ( -50.30499999999998550, 8.437984349512086979, -1.550032578732815448E-15 ) ) ;
#65472=ORIENTED_EDGE ( 'NONE', *, *, #50537, .T. ) ;
#65479=ORIENTED_EDGE ( 'NONE', *, *, #7402, .T. ) ;
#65480=CARTESIAN_POINT ( 'NONE',  ( -15.00000000000000000, -12.00000000000000000, 0.000000000000000000 ) ) ;
#65483=CARTESIAN_POINT ( 'NONE',  ( -167.4549999999999841, 7.632228543268599452, -2.479861379858951942 ) ) ;
#65490=VERTEX_POINT ( 'NONE', #53484 ) ;
#65493=CARTESIAN_POINT ( 'NONE',  ( -83.75499999999998124, 4.716976649647091513, -6.492361379858946790 ) ) ;
#65500=CARTESIAN_POINT ( 'NONE',  ( -53.00707362346619078, -8.102448949553172852, -5.886773742842741797 ) ) ;
#65508=CARTESIAN_POINT ( 'NONE',  ( -119.2449999999999903, -4.716976649647093289, -6.492361379858945902 ) ) ;
#65514=CARTESIAN_POINT ( 'NONE',  ( -17.22054250019079902, 11.13153480011775365, -4.482835375932292976 ) ) ;
#65515=CARTESIAN_POINT ( 'NONE',  ( -150.8929263765337794, -8.102448949553172852, -5.886773742842741797 ) ) ;
#65518=CARTESIAN_POINT ( 'NONE',  ( -176.0949999999999704, -2.607480562269071545, -8.024999999999991473 ) ) ;
#65525=VERTEX_POINT ( 'NONE', #36992 ) ;
#65527=VERTEX_POINT ( 'NONE', #20785 ) ;
#65529=CARTESIAN_POINT ( 'NONE',  ( -69.44292637653380496, -1.166476076187852838E-15, -9.524999999999991473 ) ) ;
#65536=EDGE_CURVE ( 'NONE', #19085, #59074, #55432, .T. ) ;
#65538=CARTESIAN_POINT ( 'NONE',  ( -165.9549999999999841, -7.632228543268599452, 2.479861379858951054 ) ) ;
#65539=ORIENTED_EDGE ( 'NONE', *, *, #57703, .F. ) ;
#65540=CARTESIAN_POINT ( 'NONE',  ( -112.4929263765338021, -8.102448949553174629, 5.886773742842742685 ) ) ;
#65550=CARTESIAN_POINT ( 'NONE',  ( -86.90499999999998693, 2.607480562269069324, -8.024999999999993250 ) ) ;
#65558=CARTESIAN_POINT ( 'NONE',  ( -64.34499999999998465, 7.632228543268599452, -2.479861379858951942 ) ) ;
#65569=CARTESIAN_POINT ( 'NONE',  ( -117.5049999999999670, -6.826472737025115478, -4.959722759717899443 ) ) ;
#65570=ORIENTED_EDGE ( 'NONE', *, *, #23989, .T. ) ;
#65576=CARTESIAN_POINT ( 'NONE',  ( -154.8570736234661922, -5.598654528085803328, -7.705886871421366635 ) ) ;
#65579=CARTESIAN_POINT ( 'NONE',  ( -95.30707362346615241, -10.01517768586948698, 6.132527647946031529E-16 ) ) ;
#65587=CARTESIAN_POINT ( 'NONE',  ( -133.8549999999999898, 4.716976649647094177, 6.492361379858945902 ) ) ;
#65590=CARTESIAN_POINT ( 'NONE',  ( -145.6450000000000102, 4.716976649647091513, -6.492361379858946790 ) ) ;
#65593=CARTESIAN_POINT ( 'NONE',  ( -132.4449999999999932, 0.000000000000000000, 8.024999999999991473 ) ) ;
#65601=CARTESIAN_POINT ( 'NONE',  ( -184.1929263765337623, -10.01517768586948698, 6.132527647946031529E-16 ) ) ;
#65602=CARTESIAN_POINT ( 'NONE',  ( -60.89499999999999602, 6.826472737025116366, 4.959722759717898555 ) ) ;
#65612=CARTESIAN_POINT ( 'NONE',  ( -94.79292637653378506, -3.094860106618429807, 9.524999999999991473 ) ) ;
#65616=LINE ( 'NONE', #38590, #43933 ) ;
#65617=EDGE_CURVE ( 'NONE', #40833, #25339, #50514, .T. ) ;
#65637=CARTESIAN_POINT ( 'NONE',  ( -94.25707362346618368, 5.598654528085800663, -7.705886871421367523 ) ) ;
#65641=CARTESIAN_POINT ( 'NONE',  ( -95.54499999999998749, -7.632228543268600340, -2.479861379858950166 ) ) ;
#65651=ORIENTED_EDGE ( 'NONE', *, *, #18753, .F. ) ;
#65658=CARTESIAN_POINT ( 'NONE',  ( -180.8070736234661524, 10.01517768586948698, -1.839758294383808571E-15 ) ) ;
#65667=CARTESIAN_POINT ( 'NONE',  ( -161.7549999999999955, 4.716976649647091513, -6.492361379858946790 ) ) ;
#65671=CARTESIAN_POINT ( 'NONE',  ( -173.5450000000000159, -7.632228543268600340, -2.479861379858950166 ) ) ;
#65672=CARTESIAN_POINT ( 'NONE',  ( -155.2450000000000045, -4.716976649647093289, -6.492361379858945902 ) ) ;
#65675=AXIS2_PLACEMENT_3D ( 'NONE', #28449, #45739, #24565 ) ;
#65679=CARTESIAN_POINT ( 'NONE',  ( -74.30499999999996419, 8.437984349512085203, -1.550032578732815448E-15 ) ) ;
#65683=CARTESIAN_POINT ( 'NONE',  ( -75.29499999999998749, -2.607480562269069768, 8.024999999999991473 ) ) ;
#65693=ORIENTED_EDGE ( 'NONE', *, *, #5795, .T. ) ;
#65704=VERTEX_POINT ( 'NONE', #24906 ) ;
#65706=( BOUNDED_CURVE ( )  B_SPLINE_CURVE ( 2, ( #11917, #39372, #49918, #33377, #6612, #23176, #39036, #60432, #43624, #12240, #11219 ),
 .UNSPECIFIED., .F., .F. ) 
 B_SPLINE_CURVE_WITH_KNOTS ( ( 3, 2, 2, 2, 2, 3 ),
 ( 0.2173913043478209739, 0.2195652173912991945, 0.2217391304347773873, 0.2239130434782556356, 0.2260869565217338284, 0.2282608695652120212 ),
 .UNSPECIFIED. ) 
 CURVE ( )  GEOMETRIC_REPRESENTATION_ITEM ( )  RATIONAL_B_SPLINE_CURVE ( ( 1.000000000000115019, 0.9510565162950385121, 1.000000000000000000, 0.9510565162951535312, 1.000000000000000000, 0.9510565162951535312, 1.000000000000000000, 0.9510565162951535312, 1.000000000000000000, 0.9510565162952741014, 0.9999999999998794298 ) ) 
 REPRESENTATION_ITEM ( '' )  );
#65710=CYLINDRICAL_SURFACE ( 'NONE', #17300, 9.524999999999991473 ) ;
#65713=CARTESIAN_POINT ( 'NONE',  ( -116.9050000000000011, 2.607480562269069324, -8.024999999999993250 ) ) ;
#65718=CARTESIAN_POINT ( 'NONE',  ( -69.05707362346618083, 0.000000000000000000, 9.524999999999991473 ) ) ;
#65744=CARTESIAN_POINT ( 'NONE',  ( -131.9050000000000011, 2.607480562269068880, -8.024999999999993250 ) ) ;
#65747=ORIENTED_EDGE ( 'NONE', *, *, #35521, .F. ) ;
#65752=CARTESIAN_POINT ( 'NONE',  ( -157.0429263765338135, -9.058813317711329915, -2.943386871421370898 ) ) ;
#65754=VERTEX_POINT ( 'NONE', #56223 ) ;
#65759=CARTESIAN_POINT ( 'NONE',  ( -54.50499999999998835, -6.826472737025115478, -4.959722759717899443 ) ) ;
#65768=CARTESIAN_POINT ( 'NONE',  ( -195.0000000000000000, 0.000000000000000000, 0.000000000000000000 ) ) ;
#65778=CARTESIAN_POINT ( 'NONE',  ( -104.0949999999999989, -2.607480562269071545, -8.024999999999991473 ) ) ;
#65780=CARTESIAN_POINT ( 'NONE',  ( -78.59499999999999886, 2.607480562269073321, 8.024999999999991473 ) ) ;
#65790=CARTESIAN_POINT ( 'NONE',  ( -123.7429263765338021, -5.598654528085803328, -7.705886871421366635 ) ) ;
#65791=CARTESIAN_POINT ( 'NONE',  ( -134.9950000000000045, -6.826472737025115478, 4.959722759717900331 ) ) ;
#65796=ORIENTED_EDGE ( 'NONE', *, *, #177, .F. ) ;
#65803=CARTESIAN_POINT ( 'NONE',  ( -131.4570736234661865, -9.058813317711329915, 2.943386871421371787 ) ) ;
#65805=VERTEX_POINT ( 'NONE', #10486 ) ;
#65806=CARTESIAN_POINT ( 'NONE',  ( -144.9550000000000125, -7.632228543268599452, 2.479861379858951054 ) ) ;
#65809=VERTEX_POINT ( 'NONE', #21719 ) ;
#65820=CARTESIAN_POINT ( 'NONE',  ( -195.0000000000000000, 0.000000000000000000, 0.000000000000000000 ) ) ;
#65822=CARTESIAN_POINT ( 'NONE',  ( -50.60499999999996845, 6.826472737025113702, -4.959722759717902107 ) ) ;
#65837=CARTESIAN_POINT ( 'NONE',  ( -173.3049999999999500, 8.437984349512085203, -1.550032578732815448E-15 ) ) ;
#65838=ORIENTED_EDGE ( 'NONE', *, *, #34615, .T. ) ;
#65841=ADVANCED_FACE ( 'NONE', ( #64638 ), #32268, .T. ) ;
#65844=CARTESIAN_POINT ( 'NONE',  ( -77.99292637653378790, 8.102448949553172852, -5.886773742842744461 ) ) ;
#65851=CARTESIAN_POINT ( 'NONE',  ( -87.20499999999999829, -2.607480562269071545, -8.024999999999991473 ) ) ;
#65861=EDGE_CURVE ( 'NONE', #63927, #66633, #11881, .T. ) ;
#65864=CARTESIAN_POINT ( 'NONE',  ( -106.7949999999999733, 2.607480562269068880, -8.024999999999993250 ) ) ;
#65868=CARTESIAN_POINT ( 'NONE',  ( -148.4929263765337737, -8.102448949553172852, 5.886773742842742685 ) ) ;
#65870=CARTESIAN_POINT ( 'NONE',  ( -166.7950000000000159, 2.607480562269068880, -8.024999999999993250 ) ) ;
#65877=CARTESIAN_POINT ( 'NONE',  ( -68.54292637653379927, 9.058813317711329915, 2.943386871421369566 ) ) ;
#65883=CARTESIAN_POINT ( 'NONE',  ( -141.8929263765337794, -8.102448949553174629, -5.886773742842741797 ) ) ;
#65885=CARTESIAN_POINT ( 'NONE',  ( -79.19292637653379074, -10.01517768586948698, 6.132527647946031529E-16 ) ) ;
#65887=CARTESIAN_POINT ( 'NONE',  ( -172.1050000000000182, -6.826472737025113702, 4.959722759717902107 ) ) ;
#65897=CARTESIAN_POINT ( 'NONE',  ( -83.00499999999998124, 6.826472737025115478, 4.959722759717899443 ) ) ;
#65902=CARTESIAN_POINT ( 'NONE',  ( -113.6929263765337907, 10.01517768586948698, -1.839758294383808966E-15 ) ) ;
#65903=CARTESIAN_POINT ( 'NONE',  ( -195.0000000000000000, 0.000000000000000000, 7.499999999999984901 ) ) ;
#65909=CARTESIAN_POINT ( 'NONE',  ( -63.44499999999998607, 0.000000000000000000, 8.024999999999991473 ) ) ;
#65912=CARTESIAN_POINT ( 'NONE',  ( -48.74292637653379501, -5.598654528085803328, -7.705886871421366635 ) ) ;
#65916=CARTESIAN_POINT ( 'NONE',  ( -51.59499999999997755, 2.607480562269072433, 8.024999999999991473 ) ) ;
#65918=ORIENTED_EDGE ( 'NONE', *, *, #20545, .F. ) ;
#65921=CARTESIAN_POINT ( 'NONE',  ( -109.8549999999999898, 4.716976649647094177, 6.492361379858945902 ) ) ;
#65926=CARTESIAN_POINT ( 'NONE',  ( -145.8570736234661638, -5.598654528085803328, -7.705886871421366635 ) ) ;
#65927=EDGE_CURVE ( 'NONE', #62912, #68888, #98, .T. ) ;
#65930=CARTESIAN_POINT ( 'NONE',  ( -88.40707362346614673, 3.094860106618428031, -9.524999999999993250 ) ) ;
#65936=EDGE_CURVE ( 'NONE', #9180, #33812, #24003, .T. ) ;
#65937=CARTESIAN_POINT ( 'NONE',  ( -130.5549999999999784, 0.000000000000000000, 8.024999999999991473 ) ) ;
#65942=CARTESIAN_POINT ( 'NONE',  ( -139.9449999999999932, -9.827790563157499189E-16, -8.024999999999991473 ) ) ;
#65944=CARTESIAN_POINT ( 'NONE',  ( -129.1449999999999818, -4.716976649647092401, 6.492361379858946790 ) ) ;
#65949=CARTESIAN_POINT ( 'NONE',  ( -178.1929263765338192, -10.01517768586948698, 6.132527647946031529E-16 ) ) ;
#65950=CARTESIAN_POINT ( 'NONE',  ( -58.19500000000000028, 8.437984349512085203, -1.550032578732815448E-15 ) ) ;
#65953=DIRECTION ( 'NONE',  ( -1.000000000000000000, -0.000000000000000000, -0.000000000000000000 ) ) ;
#65955=CARTESIAN_POINT ( 'NONE',  ( -99.29292637653378506, 3.094860106618428031, -9.524999999999993250 ) ) ;
#65959=CARTESIAN_POINT ( 'NONE',  ( -163.6429263765338078, -5.598654528085801552, 7.705886871421367523 ) ) ;
#65972=AXIS2_PLACEMENT_3D ( 'NONE', #47470, #31570, #5180 ) ;
#65980=CARTESIAN_POINT ( 'NONE',  ( -92.84499999999998465, -7.632228543268599452, 2.479861379858951054 ) ) ;
#65999=CARTESIAN_POINT ( 'NONE',  ( -176.4570736234661865, -9.058813317711329915, 2.943386871421371787 ) ) ;
#66003=CARTESIAN_POINT ( 'NONE',  ( -110.6070736234661780, -8.102448949553172852, 5.886773742842742685 ) ) ;
#66012=CARTESIAN_POINT ( 'NONE',  ( -156.2050000000000125, -2.607480562269071545, -8.024999999999991473 ) ) ;
#66014=CARTESIAN_POINT ( 'NONE',  ( -171.8949999999999534, 6.826472737025116366, 4.959722759717898555 ) ) ;
#66015=CARTESIAN_POINT ( 'NONE',  ( -154.3449999999999704, 7.632228543268599452, -2.479861379858951942 ) ) ;
#66016=( BOUNDED_CURVE ( )  B_SPLINE_CURVE ( 2, ( #51661, #51314, #28800, #7695, #19643, #45037, #3416, #18263, #67483, #34771, #18930 ),
 .UNSPECIFIED., .F., .F. ) 
 B_SPLINE_CURVE_WITH_KNOTS ( ( 3, 2, 2, 2, 2, 3 ),
 ( 0.4239130434782509282, 0.4260869565217291211, 0.4282608695652073694, 0.4304347826086855622, 0.4326086956521637550, 0.4347826086956419478 ),
 .UNSPECIFIED. ) 
 CURVE ( )  GEOMETRIC_REPRESENTATION_ITEM ( )  RATIONAL_B_SPLINE_CURVE ( ( 1.000000000000223821, 0.9510565162949298212, 1.000000000000000000, 0.9510565162951535312, 1.000000000000000000, 0.9510565162951535312, 1.000000000000000000, 0.9510565162951535312, 1.000000000000000000, 0.9510565162953834584, 0.9999999999997700728 ) ) 
 REPRESENTATION_ITEM ( '' )  );
#66018=CARTESIAN_POINT ( 'NONE',  ( -89.69292637653379074, 10.01517768586948698, -1.839758294383808966E-15 ) ) ;
#66021=CARTESIAN_POINT ( 'NONE',  ( -75.95499999999998408, -7.632228543268599452, 2.479861379858951054 ) ) ;
#66025=CARTESIAN_POINT ( 'NONE',  ( -71.09499999999998465, -2.607480562269071545, -8.024999999999991473 ) ) ;
#66045=CARTESIAN_POINT ( 'NONE',  ( -109.8549999999999898, 4.716976649647094177, 6.492361379858945902 ) ) ;
#66058=CARTESIAN_POINT ( 'NONE',  ( -51.44292637653380496, -1.166476076187852838E-15, -9.524999999999991473 ) ) ;
#66077=CARTESIAN_POINT ( 'NONE',  ( -129.2049999999999841, -2.607480562269071545, -8.024999999999991473 ) ) ;
#66094=CARTESIAN_POINT ( 'NONE',  ( -182.8449999999999989, -7.632228543268599452, 2.479861379858951054 ) ) ;
#66097=CARTESIAN_POINT ( 'NONE',  ( -144.9570736234661865, 9.058813317711329915, -2.943386871421373119 ) ) ;
#66102=CARTESIAN_POINT ( 'NONE',  ( -95.39499999999999602, -6.826472737025113702, -4.959722759717900331 ) ) ;
#66104=CARTESIAN_POINT ( 'NONE',  ( -82.49499999999997613, 6.826472737025113702, -4.959722759717902107 ) ) ;
#66106=VECTOR ( 'NONE', #13808, 1000.000000000000000 ) ;
#66115=CARTESIAN_POINT ( 'NONE',  ( -125.6929263765338192, 10.01517768586948698, -1.839758294383808571E-15 ) ) ;
#66116=CARTESIAN_POINT ( 'NONE',  ( -137.3950000000000102, -6.826472737025115478, -4.959722759717899443 ) ) ;
#66132=CARTESIAN_POINT ( 'NONE',  ( -145.5549999999999784, 0.000000000000000000, 8.024999999999991473 ) ) ;
#66147=CARTESIAN_POINT ( 'NONE',  ( -53.00499999999999545, 6.826472737025115478, 4.959722759717899443 ) ) ;
#66162=VECTOR ( 'NONE', #69282, 1000.000000000000000 ) ;
#66165=CARTESIAN_POINT ( 'NONE',  ( -163.7049999999999841, 2.607480562269073321, 8.024999999999991473 ) ) ;
#66177=CARTESIAN_POINT ( 'NONE',  ( -74.30499999999996419, 8.437984349512085203, -1.550032578732815448E-15 ) ) ;
#66190=CARTESIAN_POINT ( 'NONE',  ( -111.4449999999999932, 0.000000000000000000, 8.024999999999991473 ) ) ;
#66193=CARTESIAN_POINT ( 'NONE',  ( -96.35707362346616378, 5.598654528085804216, 7.705886871421366635 ) ) ;
#66195=CARTESIAN_POINT ( 'NONE',  ( -149.3929263765338078, 8.102448949553176405, 5.886773742842740909 ) ) ;
#66196=CARTESIAN_POINT ( 'NONE',  ( -170.2450000000000045, -4.716976649647093289, -6.492361379858945902 ) ) ;
#66204=CARTESIAN_POINT ( 'NONE',  ( -71.09292637653381064, 3.094860106618433360, 9.524999999999991473 ) ) ;
#66208=ADVANCED_FACE ( 'NONE', ( #37171 ), #57905, .T. ) ;
#66210=CARTESIAN_POINT ( 'NONE',  ( -141.7429263765338021, -5.598654528085803328, -7.705886871421366635 ) ) ;
#66216=CARTESIAN_POINT ( 'NONE',  ( -169.7049999999999841, 2.607480562269072433, 8.024999999999991473 ) ) ;
#66221=CARTESIAN_POINT ( 'NONE',  ( -112.9429263765338050, 0.000000000000000000, 9.524999999999991473 ) ) ;
#66230=CARTESIAN_POINT ( 'NONE',  ( -82.25499999999998124, -4.716976649647092401, 6.492361379858946790 ) ) ;
#66236=CARTESIAN_POINT ( 'NONE',  ( -73.40707362346617515, 3.094860106618428031, -9.524999999999993250 ) ) ;
#66244=CARTESIAN_POINT ( 'NONE',  ( -54.59499999999997044, 2.607480562269073321, 8.024999999999991473 ) ) ;
#66249=ORIENTED_EDGE ( 'NONE', *, *, #33064, .T. ) ;
#66251=CARTESIAN_POINT ( 'NONE',  ( -53.99499999999998323, -6.826472737025113702, 4.959722759717902107 ) ) ;
#66254=CARTESIAN_POINT ( 'NONE',  ( -116.6049999999999756, 6.826472737025113702, -4.959722759717902107 ) ) ;
#66256=ADVANCED_FACE ( 'NONE', ( #42807 ), #41749, .T. ) ;
#66261=CARTESIAN_POINT ( 'NONE',  ( -151.5570736234661808, -1.166476076187852838E-15, -9.524999999999991473 ) ) ;
#66263=VECTOR ( 'NONE', #16601, 1000.000000000000000 ) ;
#66264=CARTESIAN_POINT ( 'NONE',  ( -58.70707362346615810, -3.094860106618431139, -9.524999999999991473 ) ) ;
#66266=CARTESIAN_POINT ( 'NONE',  ( -85.85707362346617799, -5.598654528085803328, -7.705886871421366635 ) ) ;
#66269=VECTOR ( 'NONE', #8276, 1000.000000000000000 ) ;
#66274=CARTESIAN_POINT ( 'NONE',  ( -134.9050000000000011, 2.607480562269068880, -8.024999999999993250 ) ) ;
#66278=CARTESIAN_POINT ( 'NONE',  ( -136.6449999999999818, 4.716976649647091513, -6.492361379858946790 ) ) ;
#66279=CARTESIAN_POINT ( 'NONE',  ( -130.0449999999999875, 7.632228543268600340, 2.479861379858949277 ) ) ;
#66286=CARTESIAN_POINT ( 'NONE',  ( -181.9429263765338192, 0.000000000000000000, 9.524999999999991473 ) ) ;
#66296=CARTESIAN_POINT ( 'NONE',  ( -96.89292637653379359, -8.102448949553172852, -5.886773742842741797 ) ) ;
#66309=VERTEX_POINT ( 'NONE', #63171 ) ;
#66310=DIRECTION ( 'NONE',  ( 0.000000000000000000, 0.000000000000000000, 1.000000000000000000 ) ) ;
#66323=VECTOR ( 'NONE', #63961, 1000.000000000000000 ) ;
#66325=CARTESIAN_POINT ( 'NONE',  ( -71.15707362346617515, -9.058813317711329915, -2.943386871421370898 ) ) ;
#66326=CARTESIAN_POINT ( 'NONE',  ( -89.69499999999999318, -8.437984349512085203, 5.166775262442717831E-16 ) ) ;
#66336=DIRECTION ( 'NONE',  ( 0.000000000000000000, 0.000000000000000000, -1.000000000000000000 ) ) ;
#66338=CYLINDRICAL_SURFACE ( 'NONE', #57454, 9.524999999999991473 ) ;
#66342=CARTESIAN_POINT ( 'NONE',  ( -179.9070736234661751, -3.094860106618429807, 9.524999999999991473 ) ) ;
#66343=DIRECTION ( 'NONE',  ( 0.000000000000000000, 0.000000000000000000, 1.000000000000000000 ) ) ;
#66344=CARTESIAN_POINT ( 'NONE',  ( -195.0000000000000000, 1.166476076187852838E-15, -9.524999999999991473 ) ) ;
#66345=CARTESIAN_POINT ( 'NONE',  ( -115.4070736234661609, 3.094860106618428031, -9.524999999999993250 ) ) ;
#66349=ORIENTED_EDGE ( 'NONE', *, *, #37871, .F. ) ;
#66354=CARTESIAN_POINT ( 'NONE',  ( -157.4050000000000011, -2.607480562269069768, 8.024999999999991473 ) ) ;
#66358=CARTESIAN_POINT ( 'NONE',  ( -159.8950000000000102, 6.826472737025116366, 4.959722759717898555 ) ) ;
#66359=CARTESIAN_POINT ( 'NONE',  ( -158.9950000000000045, -6.826472737025113702, 4.959722759717902107 ) ) ;
#66365=CARTESIAN_POINT ( 'NONE',  ( -72.65499999999998693, -7.632228543268600340, -2.479861379858950166 ) ) ;
#66368=CARTESIAN_POINT ( 'NONE',  ( -167.6929263765338192, 10.01517768586948698, -1.839758294383808966E-15 ) ) ;
#66369=CARTESIAN_POINT ( 'NONE',  ( -73.49499999999999034, 6.826472737025113702, -4.959722759717902107 ) ) ;
#66398=CARTESIAN_POINT ( 'NONE',  ( -105.5049999999999670, -6.826472737025113702, -4.959722759717900331 ) ) ;
#66410=CARTESIAN_POINT ( 'NONE',  ( -120.1449999999999818, -4.716976649647092401, 6.492361379858946790 ) ) ;
#66430=CARTESIAN_POINT ( 'NONE',  ( -135.6550000000000011, -7.632228543268600340, -2.479861379858950166 ) ) ;
#66440=COLOUR_RGB ( '', 0.40784314, 0.44705882, 0.49803922) ;
#66443=CARTESIAN_POINT ( 'NONE',  ( -52.10707362346616378, 8.102448949553172852, -5.886773742842744461 ) ) ;
#66444=CARTESIAN_POINT ( 'NONE',  ( -50.90499999999997982, 2.607480562269068880, -8.024999999999993250 ) ) ;
#66448=CARTESIAN_POINT ( 'NONE',  ( -163.9429263765338192, 0.000000000000000000, 9.524999999999991473 ) ) ;
#66450=CARTESIAN_POINT ( 'NONE',  ( -178.4070736234662604, 3.094860106617537188, -9.525000000000639844 ) ) ;
#66457=CARTESIAN_POINT ( 'NONE',  ( -99.95499999999998408, -7.632228543268599452, 2.479861379858951054 ) ) ;
#66462=CARTESIAN_POINT ( 'NONE',  ( -98.09499999999997044, -2.607480562269071545, -8.024999999999991473 ) ) ;
#66464=CARTESIAN_POINT ( 'NONE',  ( -80.09499999999998465, -2.607480562269071545, -8.024999999999991473 ) ) ;
#66476=ORIENTED_EDGE ( 'NONE', *, *, #51160, .F. ) ;
#66477=CARTESIAN_POINT ( 'NONE',  ( -115.9429263765338050, 0.000000000000000000, 9.524999999999991473 ) ) ;
#66479=CARTESIAN_POINT ( 'NONE',  ( -140.8449999999999989, -7.632228543268599452, 2.479861379858951054 ) ) ;
#66495=CARTESIAN_POINT ( 'NONE',  ( -98.75707362346616947, -5.598654528085801552, 7.705886871421367523 ) ) ;
#66496=VECTOR ( 'NONE', #52186, 1000.000000000000000 ) ;
#66499=CARTESIAN_POINT ( 'NONE',  ( -129.6550000000000011, -7.632228543268600340, -2.479861379858950166 ) ) ;
#66513=CARTESIAN_POINT ( 'NONE',  ( -56.00499999999996703, 6.826472737025115478, 4.959722759717899443 ) ) ;
#66528=CARTESIAN_POINT ( 'NONE',  ( -162.0550000000000068, -9.827790563157499189E-16, -8.024999999999991473 ) ) ;
#66531=EDGE_CURVE ( 'NONE', #51470, #11299, #40259, .T. ) ;
#66538=VERTEX_POINT ( 'NONE', #13146 ) ;
#66539=DIRECTION ( 'NONE',  ( -1.000000000000000000, -0.000000000000000000, -0.000000000000000000 ) ) ;
#66541=CARTESIAN_POINT ( 'NONE',  ( -78.20499999999996987, -2.607480562269071545, -8.024999999999991473 ) ) ;
#66546=( BOUNDED_CURVE ( )  B_SPLINE_CURVE ( 2, ( #3297, #29371, #30763, #52263, #8980, #4021, #24786, #24111, #19866, #30396, #10381 ),
 .UNSPECIFIED., .F., .F. ) 
 B_SPLINE_CURVE_WITH_KNOTS ( ( 3, 2, 2, 2, 2, 3 ),
 ( 0.5652173913043346820, 0.5673913043478129303, 0.5695652173912910676, 0.5717391304347693159, 0.5739130434782474532, 0.5760869565217255905 ),
 .UNSPECIFIED. ) 
 CURVE ( )  GEOMETRIC_REPRESENTATION_ITEM ( )  RATIONAL_B_SPLINE_CURVE ( ( 1.000000000000294875, 0.9510565162948585449, 1.000000000000000000, 0.9510565162951535312, 1.000000000000000000, 0.9510565162951535312, 1.000000000000000000, 0.9510565162951535312, 1.000000000000000000, 0.9510565162954585094, 0.9999999999996950217 ) ) 
 REPRESENTATION_ITEM ( '' )  );
#66555=CARTESIAN_POINT ( 'NONE',  ( -105.5949999999999989, 2.607480562269073321, 8.024999999999991473 ) ) ;
#66559=CARTESIAN_POINT ( 'NONE',  ( -15.66262743815122604, 10.92411111548398139, 4.966771479319564087 ) ) ;
#66562=CARTESIAN_POINT ( 'NONE',  ( -143.5429263765338135, 9.058813317711329915, 2.943386871421369566 ) ) ;
#66563=CARTESIAN_POINT ( 'NONE',  ( -168.2950000000000159, -2.607480562269069768, 8.024999999999991473 ) ) ;
#66582=CARTESIAN_POINT ( 'NONE',  ( -174.5049999999999955, -6.826472737025113702, -4.959722759717900331 ) ) ;
#66593=CARTESIAN_POINT ( 'NONE',  ( -84.65500000000000114, -7.632228543268600340, -2.479861379858950166 ) ) ;
#66601=CARTESIAN_POINT ( 'NONE',  ( -113.3070736234661666, -10.01517768586948698, 6.132527647946031529E-16 ) ) ;
#66607=CARTESIAN_POINT ( 'NONE',  ( -51.14499999999999602, -4.716976649647092401, 6.492361379858946790 ) ) ;
#66617=CARTESIAN_POINT ( 'NONE',  ( -52.34499999999997755, 7.632228543268599452, -2.479861379858951942 ) ) ;
#66620=CARTESIAN_POINT ( 'NONE',  ( -100.2549999999999812, -4.716976649647092401, 6.492361379858946790 ) ) ;
#66624=DIRECTION ( 'NONE',  ( -1.000000000000000000, -0.000000000000000000, -0.000000000000000000 ) ) ;
#66625=CARTESIAN_POINT ( 'NONE',  ( -149.7570736234661979, -5.598654528085801552, 7.705886871421367523 ) ) ;
#66626=B_SPLINE_CURVE_WITH_KNOTS ( 'NONE', 3,
 ( #60890, #54907, #11325, #1414, #33816, #32789 ),
 .UNSPECIFIED., .F., .F.,
 ( 4, 2, 4 ),
 ( 2.727025168375190138E-16, 0.001158410220312347267, 0.002316820440624422616 ),
 .UNSPECIFIED. ) ;
#66629=CARTESIAN_POINT ( 'NONE',  ( -88.10707362346616378, 8.102448949553171076, -5.886773742842744461 ) ) ;
#66633=VERTEX_POINT ( 'NONE', #24734 ) ;
#66635=CIRCLE ( 'NONE', #328, 11.99999999999999645 ) ;
#66638=CARTESIAN_POINT ( 'NONE',  ( -119.7549999999999812, 4.716976649647091513, -6.492361379858946790 ) ) ;
#66643=CARTESIAN_POINT ( 'NONE',  ( -136.7949999999999875, 2.607480562269068880, -8.024999999999993250 ) ) ;
#66644=CARTESIAN_POINT ( 'NONE',  ( -125.5449999999999875, -7.632228543268600340, -2.479861379858950166 ) ) ;
#66652=CARTESIAN_POINT ( 'NONE',  ( -181.6429263765338078, -5.598654528085801552, 7.705886871421367523 ) ) ;
#66653=CARTESIAN_POINT ( 'NONE',  ( -53.99499999999998323, -6.826472737025115478, 4.959722759717900331 ) ) ;
#66654=EDGE_CURVE ( 'NONE', #45514, #68810, #9646, .T. ) ;
#66660=CARTESIAN_POINT ( 'NONE',  ( -92.09292637653381064, 3.094860106618433360, 9.524999999999991473 ) ) ;
#66679=LINE ( 'NONE', #55418, #64551 ) ;
#66686=CARTESIAN_POINT ( 'NONE',  ( -71.60707362346617799, -8.102448949553174629, 5.886773742842742685 ) ) ;
#66687=CARTESIAN_POINT ( 'NONE',  ( -84.29499999999998749, -2.607480562269069768, 8.024999999999991473 ) ) ;
#66704=CARTESIAN_POINT ( 'NONE',  ( -174.8070736234661240, 10.01517768586948698, -1.839758294383808571E-15 ) ) ;
#66706=CARTESIAN_POINT ( 'NONE',  ( -109.4070736234661609, 3.094860106618428031, -9.524999999999993250 ) ) ;
#66719=CARTESIAN_POINT ( 'NONE',  ( -164.4549999999999841, 7.632228543268599452, -2.479861379858951942 ) ) ;
#66721=CARTESIAN_POINT ( 'NONE',  ( -183.6962785619511749, -6.980536562595337280, -5.441974211641010584 ) ) ;
#66722=CARTESIAN_POINT ( 'NONE',  ( -164.2450000000000045, -4.716976649647093289, -6.492361379858945902 ) ) ;
#66724=CARTESIAN_POINT ( 'NONE',  ( -160.1949999999999932, 8.437984349512086979, -1.550032578732815448E-15 ) ) ;
#66728=CARTESIAN_POINT ( 'NONE',  ( -122.9929263765338021, 8.102448949553172852, -5.886773742842744461 ) ) ;
#66730=CARTESIAN_POINT ( 'NONE',  ( -70.85499999999998977, 4.716976649647094177, 6.492361379858945902 ) ) ;
#66735=CARTESIAN_POINT ( 'NONE',  ( -71.84499999999999886, -7.632228543268599452, 2.479861379858951054 ) ) ;
#66738=CARTESIAN_POINT ( 'NONE',  ( -155.9070736234665162, -3.094860106612816519, 9.525000000004069989 ) ) ;
#66750=CIRCLE ( 'NONE', #16229, 11.99999999999999467 ) ;
#66757=ORIENTED_EDGE ( 'NONE', *, *, #19452, .T. ) ;
#66762=CARTESIAN_POINT ( 'NONE',  ( -65.24292637653380211, 5.598654528085804216, 7.705886871421366635 ) ) ;
#66768=CARTESIAN_POINT ( 'NONE',  ( -109.4949999999999761, 6.826472737025113702, -4.959722759717902107 ) ) ;
#66774=CARTESIAN_POINT ( 'NONE',  ( -12.77502540130583952, -11.12935009515152807, -4.489552594659124374 ) ) ;
#66775=CARTESIAN_POINT ( 'NONE',  ( -180.4429263765338192, -1.166476076187852838E-15, -9.524999999999991473 ) ) ;
#66780=DIRECTION ( 'NONE',  ( 0.000000000000000000, 0.000000000000000000, 1.000000000000000000 ) ) ;
#66787=ORIENTED_EDGE ( 'NONE', *, *, #44181, .T. ) ;
#66792=CARTESIAN_POINT ( 'NONE',  ( -137.9049999999999727, 2.607480562269068880, -8.024999999999993250 ) ) ;
#66798=VECTOR ( 'NONE', #183, 1000.000000000000000 ) ;
#66800=CARTESIAN_POINT ( 'NONE',  ( -107.9070736234670989, -3.094860106603102512, 9.525000000011129231 ) ) ;
#66809=CARTESIAN_POINT ( 'NONE',  ( -50.15499999999997982, 7.632228543268600340, 2.479861379858949277 ) ) ;
#66812=CARTESIAN_POINT ( 'NONE',  ( -184.4049999999999727, -2.607480562269069768, 8.024999999999991473 ) ) ;
#66815=CARTESIAN_POINT ( 'NONE',  ( -59.30707362346615952, -10.01517768586948698, 6.132527647946031529E-16 ) ) ;
#66817=EDGE_CURVE ( 'NONE', #53684, #40833, #50922, .T. ) ;
#66819=CARTESIAN_POINT ( 'NONE',  ( -161.4570736234661865, -9.058813317711329915, 2.943386871421371787 ) ) ;
#66823=CARTESIAN_POINT ( 'NONE',  ( -98.00500000000000966, 6.826472737025116366, 4.959722759717898555 ) ) ;
#66828=CARTESIAN_POINT ( 'NONE',  ( -100.4949999999999761, 6.826472737025113702, -4.959722759717902107 ) ) ;
#66830=CARTESIAN_POINT ( 'NONE',  ( -77.39499999999999602, -6.826472737025115478, -4.959722759717899443 ) ) ;
#66840=CARTESIAN_POINT ( 'NONE',  ( -117.5929263765338106, -3.094860106618431139, -9.524999999999991473 ) ) ;
#66842=( BOUNDED_CURVE ( )  B_SPLINE_CURVE ( 2, ( #3153, #14829, #19735, #26040, #68630, #36307, #47578, #57731, #41229, #30977, #68985 ),
 .UNSPECIFIED., .F., .F. ) 
 B_SPLINE_CURVE_WITH_KNOTS ( ( 3, 2, 2, 2, 2, 3 ),
 ( 0.6630434782608540800, 0.6652173913043323283, 0.6673913043478105767, 0.6695652173912887140, 0.6717391304347669623, 0.6739130434782450996 ),
 .UNSPECIFIED. ) 
 CURVE ( )  GEOMETRIC_REPRESENTATION_ITEM ( )  RATIONAL_B_SPLINE_CURVE ( ( 1.000000000000347500, 0.9510565162948061424, 1.000000000000000000, 0.9510565162951535312, 1.000000000000000000, 0.9510565162951535312, 1.000000000000000000, 0.9510565162951535312, 1.000000000000000000, 0.9510565162955084695, 0.9999999999996450617 ) ) 
 REPRESENTATION_ITEM ( '' )  );
#66843=CARTESIAN_POINT ( 'NONE',  ( -136.3449999999999989, 7.632228543268599452, -2.479861379858951942 ) ) ;
#66857=CARTESIAN_POINT ( 'NONE',  ( -131.0049999999999670, 6.826472737025115478, 4.959722759717899443 ) ) ;
#66862=CARTESIAN_POINT ( 'NONE',  ( -83.54292637653381348, 9.058813317711329915, 2.943386871421369566 ) ) ;
#66863=ORIENTED_EDGE ( 'NONE', *, *, #33369, .T. ) ;
#66876=CARTESIAN_POINT ( 'NONE',  ( -87.44292637653380496, -1.166476076187852838E-15, -9.524999999999991473 ) ) ;
#66885=CARTESIAN_POINT ( 'NONE',  ( -123.0570736234661808, 0.000000000000000000, 9.524999999999991473 ) ) ;
#66887=CARTESIAN_POINT ( 'NONE',  ( -161.1550000000000011, 7.632228543268600340, 2.479861379858949277 ) ) ;
#66899=CARTESIAN_POINT ( 'NONE',  ( -72.80499999999997840, -8.437984349512085203, 5.166775262442717831E-16 ) ) ;
#66912=CARTESIAN_POINT ( 'NONE',  ( -106.0449999999999875, 7.632228543268600340, 2.479861379858949277 ) ) ;
#66919=CARTESIAN_POINT ( 'NONE',  ( -144.7429263765338021, -5.598654528085803328, -7.705886871421366635 ) ) ;
#66921=CARTESIAN_POINT ( 'NONE',  ( -164.9949999999999761, -6.826472737025115478, 4.959722759717900331 ) ) ;
#66939=CARTESIAN_POINT ( 'NONE',  ( -165.2049999999999841, -2.607480562269071545, -8.024999999999991473 ) ) ;
#66941=CARTESIAN_POINT ( 'NONE',  ( -190.0000000000000000, 9.184850993605132167E-16, -7.499999999999985789 ) ) ;
#66943=EDGE_LOOP ( 'NONE', ( #23267, #37998, #14279, #49134 ) ) ;
#66949=CARTESIAN_POINT ( 'NONE',  ( -78.80500000000000682, -8.437984349512086979, 5.166775262442717831E-16 ) ) ;
#66954=CARTESIAN_POINT ( 'NONE',  ( -113.1570736234661751, -9.058813317711329915, -2.943386871421370898 ) ) ;
#66961=CARTESIAN_POINT ( 'NONE',  ( -49.94499999999998607, -9.827790563157499189E-16, -8.024999999999991473 ) ) ;
#66971=CARTESIAN_POINT ( 'NONE',  ( -57.59499999999997755, 2.607480562269072433, 8.024999999999991473 ) ) ;
#66975=CARTESIAN_POINT ( 'NONE',  ( -105.0549999999999926, -9.827790563157499189E-16, -8.024999999999991473 ) ) ;
#66977=DIRECTION ( 'NONE',  ( -1.000000000000000000, -0.000000000000000000, -0.000000000000000000 ) ) ;
#66981=CARTESIAN_POINT ( 'NONE',  ( -137.3070736234661808, -10.01517768586948698, 6.132527647946031529E-16 ) ) ;
#66985=CARTESIAN_POINT ( 'NONE',  ( -86.30707362346615241, -10.01517768586948698, 6.132527647946031529E-16 ) ) ;
#66990=CARTESIAN_POINT ( 'NONE',  ( -119.1550000000000011, 7.632228543268600340, 2.479861379858949277 ) ) ;
#66993=CARTESIAN_POINT ( 'NONE',  ( -131.3949999999999818, -6.826472737025115478, -4.959722759717899443 ) ) ;
#66994=CARTESIAN_POINT ( 'NONE',  ( -123.5949999999999704, 2.607480562269072433, 8.024999999999991473 ) ) ;
#67000=CARTESIAN_POINT ( 'NONE',  ( -170.9929263765337737, 8.102448949553171076, -5.886773742842744461 ) ) ;
#67002=CARTESIAN_POINT ( 'NONE',  ( -49.64499999999999602, 4.716976649647091513, -6.492361379858946790 ) ) ;
#67004=CARTESIAN_POINT ( 'NONE',  ( -66.44292637653380496, -1.166476076187852838E-15, -9.524999999999991473 ) ) ;
#67006=DIRECTION ( 'NONE',  ( -1.000000000000000000, -0.000000000000000000, -0.000000000000000000 ) ) ;
#67010=CARTESIAN_POINT ( 'NONE',  ( -96.29292637653381348, 3.094860106618428031, -9.524999999999993250 ) ) ;
#67014=EDGE_CURVE ( 'NONE', #18409, #17310, #68288, .T. ) ;
#67015=CARTESIAN_POINT ( 'NONE',  ( -179.0929263765338817, 3.094860106619634177, 9.524999999999119282 ) ) ;
#67017=CARTESIAN_POINT ( 'NONE',  ( -78.35707362346616378, 5.598654528085804216, 7.705886871421366635 ) ) ;
#67037=CARTESIAN_POINT ( 'NONE',  ( -85.34499999999998465, 7.632228543268599452, -2.479861379858951942 ) ) ;
#67050=CYLINDRICAL_SURFACE ( 'NONE', #20683, 9.524999999999991473 ) ;
#67054=FACE_OUTER_BOUND ( 'NONE', #20588, .T. ) ;
#67056=CARTESIAN_POINT ( 'NONE',  ( -165.5070736234661126, 8.102448949553176405, 5.886773742842740909 ) ) ;
#67059=CARTESIAN_POINT ( 'NONE',  ( -114.3570736234661780, 5.598654528085804216, 7.705886871421366635 ) ) ;
#67060=CARTESIAN_POINT ( 'NONE',  ( -183.1155613406150167, 5.490944093040150520, -7.649849691780579164 ) ) ;
#67064=DIRECTION ( 'NONE',  ( -1.000000000000000000, -0.000000000000000000, -0.000000000000000000 ) ) ;
#67068=CARTESIAN_POINT ( 'NONE',  ( -150.3549999999999898, -4.716976649647093289, -6.492361379858945902 ) ) ;
#67071=CARTESIAN_POINT ( 'NONE',  ( -167.8449999999999989, -7.632228543268599452, 2.479861379858951054 ) ) ;
#67072=CARTESIAN_POINT ( 'NONE',  ( -148.4949999999999761, 6.826472737025113702, -4.959722759717902107 ) ) ;
#67075=CARTESIAN_POINT ( 'NONE',  ( -66.95499999999998408, -7.632228543268599452, 2.479861379858951054 ) ) ;
#67077=CARTESIAN_POINT ( 'NONE',  ( -67.19499999999999318, 8.437984349512086979, -1.550032578732815448E-15 ) ) ;
#67104=CARTESIAN_POINT ( 'NONE',  ( -66.29292637653379927, 3.094860106618428031, -9.524999999999993250 ) ) ;
#67109=CARTESIAN_POINT ( 'NONE',  ( -113.9949999999999903, -6.826472737025115478, 4.959722759717900331 ) ) ;
#67113=CARTESIAN_POINT ( 'NONE',  ( -10.03253578442417115, -11.98633051154418183, 0.6595741458992528949 ) ) ;
#67126=CARTESIAN_POINT ( 'NONE',  ( -133.7049999999999557, 2.607480562269073321, 8.024999999999991473 ) ) ;
#67130=DIRECTION ( 'NONE',  ( -1.000000000000000000, -0.000000000000000000, -0.000000000000000000 ) ) ;
#67141=CARTESIAN_POINT ( 'NONE',  ( -179.7549999999999955, 4.716976649647091513, -6.492361379858946790 ) ) ;
#67145=CARTESIAN_POINT ( 'NONE',  ( -54.95707362346616520, 9.058813317711329915, -2.943386871421373119 ) ) ;
#67150=( BOUNDED_CURVE ( )  B_SPLINE_CURVE ( 2, ( #54487, #938, #22491, #56919, #9090, #39733, #51301, #56564, #14345, #61154, #50604 ),
 .UNSPECIFIED., .F., .F. ) 
 B_SPLINE_CURVE_WITH_KNOTS ( ( 3, 2, 2, 2, 2, 3 ),
 ( 0.1739130434782567292, 0.1760869565217349497, 0.1782608695652131703, 0.1804347826086913908, 0.1826086956521696114, 0.1847826086956478042 ),
 .UNSPECIFIED. ) 
 CURVE ( )  GEOMETRIC_REPRESENTATION_ITEM ( )  RATIONAL_B_SPLINE_CURVE ( ( 1.000000000000093037, 0.9510565162950602724, 1.000000000000000000, 0.9510565162951535312, 1.000000000000000000, 0.9510565162951535312, 1.000000000000000000, 0.9510565162951535312, 1.000000000000000000, 0.9510565162952516749, 0.9999999999999018563 ) ) 
 REPRESENTATION_ITEM ( '' )  );
#67153=CARTESIAN_POINT ( 'NONE',  ( -105.6549999999999869, -7.632228543268600340, -2.479861379858950166 ) ) ;
#67159=CARTESIAN_POINT ( 'NONE',  ( -100.0450000000000017, 7.632228543268600340, 2.479861379858949277 ) ) ;
#67161=CARTESIAN_POINT ( 'NONE',  ( -65.24499999999999034, -4.716976649647093289, -6.492361379858945902 ) ) ;
#67168=CARTESIAN_POINT ( 'NONE',  ( -112.0429263765337993, -9.058813317711329915, -2.943386871421370898 ) ) ;
#67169=CARTESIAN_POINT ( 'NONE',  ( -142.4949999999999761, 6.826472737025113702, -4.959722759717902107 ) ) ;
#67174=EDGE_LOOP ( 'NONE', ( #23774, #69488, #17911, #44339 ) ) ;
#67178=DIRECTION ( 'NONE',  ( -1.000000000000000000, -0.000000000000000000, -0.000000000000000000 ) ) ;
#67182=ORIENTED_EDGE ( 'NONE', *, *, #53310, .F. ) ;
#67183=CARTESIAN_POINT ( 'NONE',  ( -134.9050000000000011, 2.607480562269069324, -8.024999999999993250 ) ) ;
#67185=CARTESIAN_POINT ( 'NONE',  ( -125.4570736234661723, -9.058813317711329915, 2.943386871421371787 ) ) ;
#67186=ADVANCED_FACE ( 'NONE', ( #18544 ), #56867, .T. ) ;
#67205=CARTESIAN_POINT ( 'NONE',  ( -195.0000000000000000, 0.000000000000000000, 0.000000000000000000 ) ) ;
#67211=ORIENTED_EDGE ( 'NONE', *, *, #37480, .F. ) ;
#67215=CARTESIAN_POINT ( 'NONE',  ( -162.9549999999999841, -7.632228543268599452, 2.479861379858951054 ) ) ;
#67227=CARTESIAN_POINT ( 'NONE',  ( -72.20499999999998408, -2.607480562269071545, -8.024999999999991473 ) ) ;
#67231=CARTESIAN_POINT ( 'NONE',  ( -63.05707362346617373, 0.000000000000000000, 9.524999999999991473 ) ) ;
#67233=AXIS2_PLACEMENT_3D ( 'NONE', #59674, #47818, #48481 ) ;
#67242=CARTESIAN_POINT ( 'NONE',  ( -109.0449999999999875, 7.632228543268600340, 2.479861379858949277 ) ) ;
#67249=CARTESIAN_POINT ( 'NONE',  ( -139.9429263765337907, 0.000000000000000000, 9.524999999999991473 ) ) ;
#67250=CARTESIAN_POINT ( 'NONE',  ( -165.5949999999999704, 2.607480562269073321, 8.024999999999991473 ) ) ;
#67257=ORIENTED_EDGE ( 'NONE', *, *, #27614, .F. ) ;
#67265=CARTESIAN_POINT ( 'NONE',  ( -165.0550000000000068, -9.827790563157499189E-16, -8.024999999999991473 ) ) ;
#67282=CARTESIAN_POINT ( 'NONE',  ( -76.40499999999997272, -2.607480562269069768, 8.024999999999991473 ) ) ;
#67297=CARTESIAN_POINT ( 'NONE',  ( -49.04499999999998039, 7.632228543268600340, 2.479861379858949277 ) ) ;
#67304=CARTESIAN_POINT ( 'NONE',  ( -55.64499999999997470, 4.716976649647091513, -6.492361379858946790 ) ) ;
#67306=ORIENTED_EDGE ( 'NONE', *, *, #33550, .T. ) ;
#67308=CARTESIAN_POINT ( 'NONE',  ( -102.5049999999999955, -6.826472737025115478, -4.959722759717899443 ) ) ;
#67311=CARTESIAN_POINT ( 'NONE',  ( -138.0570736234661808, 0.000000000000000000, 9.524999999999991473 ) ) ;
#67314=CARTESIAN_POINT ( 'NONE',  ( -79.25707362346618368, 5.598654528085800663, -7.705886871421367523 ) ) ;
#67317=CARTESIAN_POINT ( 'NONE',  ( -16.31094249435444254, -10.98238678365111021, -4.836562941872261767 ) ) ;
#67319=CARTESIAN_POINT ( 'NONE',  ( -100.4929263765337879, -8.102448949553174629, 5.886773742842742685 ) ) ;
#67321=CARTESIAN_POINT ( 'NONE',  ( -117.5049999999999670, -6.826472737025115478, -4.959722759717899443 ) ) ;
#67323=CARTESIAN_POINT ( 'NONE',  ( -136.1949999999999363, 8.437984349512085203, -1.550032578732815448E-15 ) ) ;
#67325=CARTESIAN_POINT ( 'NONE',  ( -123.2949999999999875, -2.607480562269069768, 8.024999999999991473 ) ) ;
#67334=CARTESIAN_POINT ( 'NONE',  ( -174.7429263765338305, -5.598654528085803328, -7.705886871421366635 ) ) ;
#67336=CARTESIAN_POINT ( 'NONE',  ( -50.09499999999996334, -2.607480562269071545, -8.024999999999991473 ) ) ;
#67342=CARTESIAN_POINT ( 'NONE',  ( -84.14292637653379359, 5.598654528085800663, -7.705886871421367523 ) ) ;
#67347=CARTESIAN_POINT ( 'NONE',  ( -179.6929263765337907, 10.01517768586948698, -1.839758294383808966E-15 ) ) ;
#67348=CARTESIAN_POINT ( 'NONE',  ( -78.50707362346616947, 8.102448949553176405, 5.886773742842740909 ) ) ;
#67351=CARTESIAN_POINT ( 'NONE',  ( -136.7929263765344103, -3.094860106608278816, 9.525000000007368683 ) ) ;
#67356=CARTESIAN_POINT ( 'NONE',  ( -64.04292637653379927, -9.058813317711329915, -2.943386871421370898 ) ) ;
#67365=CARTESIAN_POINT ( 'NONE',  ( -94.34292637653379643, -9.058813317711329915, 2.943386871421371787 ) ) ;
#67372=CARTESIAN_POINT ( 'NONE',  ( -77.69499999999999318, -8.437984349512085203, 5.166775262442717831E-16 ) ) ;
#67389=CARTESIAN_POINT ( 'NONE',  ( -173.7570736234661695, -5.598654528085801552, 7.705886871421367523 ) ) ;
#67392=CARTESIAN_POINT ( 'NONE',  ( -117.5070736234661553, 8.102448949553176405, 5.886773742842740909 ) ) ;
#67400=CARTESIAN_POINT ( 'NONE',  ( -114.0570736234661808, 0.000000000000000000, 9.524999999999991473 ) ) ;
#67401=CARTESIAN_POINT ( 'NONE',  ( -150.6549999999999727, -7.632228543268600340, -2.479861379858950166 ) ) ;
#67403=CARTESIAN_POINT ( 'NONE',  ( -166.0449999999999875, 7.632228543268600340, 2.479861379858949277 ) ) ;
#67404=CARTESIAN_POINT ( 'NONE',  ( -150.7449999999999761, 4.716976649647094177, 6.492361379858945902 ) ) ;
#67409=CARTESIAN_POINT ( 'NONE',  ( -65.45499999999998408, 7.632228543268599452, -2.479861379858951942 ) ) ;
#67413=CARTESIAN_POINT ( 'NONE',  ( -64.94499999999999318, -9.827790563157499189E-16, -8.024999999999991473 ) ) ;
#67418=CARTESIAN_POINT ( 'NONE',  ( -160.2570736234661979, 5.598654528085800663, -7.705886871421367523 ) ) ;
#67441=CARTESIAN_POINT ( 'NONE',  ( -144.4429263765337907, -1.166476076187852838E-15, -9.524999999999991473 ) ) ;
#67446=CARTESIAN_POINT ( 'NONE',  ( -111.8949999999999960, 6.826472737025116366, 4.959722759717898555 ) ) ;
#67452=CARTESIAN_POINT ( 'NONE',  ( -179.1570736234662036, -9.058813317711329915, -2.943386871421370898 ) ) ;
#67456=FACE_OUTER_BOUND ( 'NONE', #5846, .T. ) ;
#67467=CARTESIAN_POINT ( 'NONE',  ( -128.4549999999999841, 7.632228543268599452, -2.479861379858951942 ) ) ;
#67481=CARTESIAN_POINT ( 'NONE',  ( -48.95499999999996987, -7.632228543268599452, 2.479861379858951054 ) ) ;
#67483=CARTESIAN_POINT ( 'NONE',  ( -123.3570736234661780, 5.598654528085804216, 7.705886871421366635 ) ) ;
#67484=CARTESIAN_POINT ( 'NONE',  ( -182.6049999999999613, 6.826472737025113702, -4.959722759717902107 ) ) ;
#67486=CARTESIAN_POINT ( 'NONE',  ( -58.10707362346618510, 8.102448949553171076, -5.886773742842744461 ) ) ;
#67487=CARTESIAN_POINT ( 'NONE',  ( -179.5450000000000159, -7.632228543268600340, -2.479861379858950166 ) ) ;
#67494=CARTESIAN_POINT ( 'NONE',  ( -91.85499999999998977, 4.716976649647094177, 6.492361379858945902 ) ) ;
#67499=CARTESIAN_POINT ( 'NONE',  ( -92.54499999999998749, -7.632228543268600340, -2.479861379858950166 ) ) ;
#67502=CARTESIAN_POINT ( 'NONE',  ( -71.99500000000000455, -6.826472737025115478, 4.959722759717900331 ) ) ;
#67511=CARTESIAN_POINT ( 'NONE',  ( -113.3929263765337936, 8.102448949553176405, 5.886773742842740909 ) ) ;
#67513=CARTESIAN_POINT ( 'NONE',  ( -130.4950000000000045, 6.826472737025113702, -4.959722759717902107 ) ) ;
#67519=CARTESIAN_POINT ( 'NONE',  ( -131.9929263765338021, 8.102448949553172852, -5.886773742842744461 ) ) ;
#67532=CARTESIAN_POINT ( 'NONE',  ( -132.9549999999999841, -7.632228543268599452, 2.479861379858951054 ) ) ;
#67534=CARTESIAN_POINT ( 'NONE',  ( -124.8570736234661780, -5.598654528085803328, -7.705886871421366635 ) ) ;
#67545=CARTESIAN_POINT ( 'NONE',  ( -141.3570736234661638, 5.598654528085804216, 7.705886871421366635 ) ) ;
#67547=CARTESIAN_POINT ( 'NONE',  ( -54.35707362346617089, 5.598654528085804216, 7.705886871421366635 ) ) ;
#67551=ORIENTED_EDGE ( 'NONE', *, *, #42864, .F. ) ;
#67555=CARTESIAN_POINT ( 'NONE',  ( -99.29292637653485087, 3.094860106600546334, -9.525000000012985524 ) ) ;
#67562=CARTESIAN_POINT ( 'NONE',  ( -120.4429263765338050, -1.166476076187852838E-15, -9.524999999999991473 ) ) ;
#67565=CARTESIAN_POINT ( 'NONE',  ( -159.8049999999999784, -8.437984349512085203, 5.166775262442717831E-16 ) ) ;
#67581=CARTESIAN_POINT ( 'NONE',  ( -71.45499999999998408, 7.632228543268599452, -2.479861379858951942 ) ) ;
#67597=CARTESIAN_POINT ( 'NONE',  ( -92.99500000000000455, -6.826472737025115478, 4.959722759717900331 ) ) ;
#67601=CARTESIAN_POINT ( 'NONE',  ( -144.1429263765338078, 5.598654528085800663, -7.705886871421367523 ) ) ;
#67603=CARTESIAN_POINT ( 'NONE',  ( -156.8950000000000102, 6.826472737025116366, 4.959722759717898555 ) ) ;
#67607=DIRECTION ( 'NONE',  ( -1.000000000000000000, -0.000000000000000000, -0.000000000000000000 ) ) ;
#67614=AXIS2_PLACEMENT_3D ( 'NONE', #62728, #48954, #51865 ) ;
#67616=CARTESIAN_POINT ( 'NONE',  ( -173.3070736234661808, -10.01517768586948698, 6.132527647946031529E-16 ) ) ;
#67621=CARTESIAN_POINT ( 'NONE',  ( -163.5550000000000068, 0.000000000000000000, 8.024999999999991473 ) ) ;
#67626=VERTEX_POINT ( 'NONE', #69083 ) ;
#67628=EDGE_CURVE ( 'NONE', #62473, #20781, #42962, .T. ) ;
#67629=CARTESIAN_POINT ( 'NONE',  ( -57.95707362346616520, 9.058813317711329915, -2.943386871421373119 ) ) ;
#67634=CARTESIAN_POINT ( 'NONE',  ( -74.15499999999998693, 7.632228543268600340, 2.479861379858949277 ) ) ;
#67647=CARTESIAN_POINT ( 'NONE',  ( -56.54499999999998749, -7.632228543268600340, -2.479861379858950166 ) ) ;
#67658=CARTESIAN_POINT ( 'NONE',  ( -108.5049999999999812, -6.826472737025115478, -4.959722759717899443 ) ) ;
#67663=CARTESIAN_POINT ( 'NONE',  ( -140.7570736234661695, -5.598654528085801552, 7.705886871421367523 ) ) ;
#67664=CARTESIAN_POINT ( 'NONE',  ( -58.85707362346617799, -5.598654528085803328, -7.705886871421366635 ) ) ;
#67666=CARTESIAN_POINT ( 'NONE',  ( -70.40707362346616094, 3.094860106618428031, -9.524999999999993250 ) ) ;
#67670=CARTESIAN_POINT ( 'NONE',  ( -19.96607921494393167, -11.98575909856985611, 0.6678542743433295570 ) ) ;
#67673=CARTESIAN_POINT ( 'NONE',  ( -125.3049999999999926, 8.437984349512085203, -1.550032578732815448E-15 ) ) ;
#67678=CARTESIAN_POINT ( 'NONE',  ( -122.8449999999999847, -7.632228543268599452, 2.479861379858951054 ) ) ;
#67680=CARTESIAN_POINT ( 'NONE',  ( -121.1949999999999790, 8.437984349512086979, -1.550032578732815448E-15 ) ) ;
#67689=CARTESIAN_POINT ( 'NONE',  ( -169.7929263765338135, -3.094860106618429807, 9.524999999999991473 ) ) ;
#67690=CARTESIAN_POINT ( 'NONE',  ( -49.34499999999997044, 7.632228543268599452, -2.479861379858951942 ) ) ;
#67698=CARTESIAN_POINT ( 'NONE',  ( -87.89292637653379359, -8.102448949553172852, -5.886773742842741797 ) ) ;
#67712=CARTESIAN_POINT ( 'NONE',  ( -142.9429263765337907, 0.000000000000000000, 9.524999999999991473 ) ) ;
#67720=CARTESIAN_POINT ( 'NONE',  ( -106.8549999999999898, 4.716976649647094177, 6.492361379858945902 ) ) ;
#67727=CARTESIAN_POINT ( 'NONE',  ( -71.30707362346616662, -10.01517768586948698, 6.132527647946031529E-16 ) ) ;
#67728=CARTESIAN_POINT ( 'NONE',  ( -77.09499999999997044, -2.607480562269071545, -8.024999999999991473 ) ) ;
#67742=ORIENTED_EDGE ( 'NONE', *, *, #3621, .F. ) ;
#67745=CARTESIAN_POINT ( 'NONE',  ( -172.4070736234661467, 3.094860106618428031, -9.524999999999993250 ) ) ;
#67749=CARTESIAN_POINT ( 'NONE',  ( -108.2070736234661723, 3.094860106618433360, 9.524999999999991473 ) ) ;
#67757=CARTESIAN_POINT ( 'NONE',  ( -60.44292637653379785, -1.166476076187852838E-15, -9.524999999999991473 ) ) ;
#67758=CARTESIAN_POINT ( 'NONE',  ( -154.1049999999999898, -6.826472737025115478, 4.959722759717900331 ) ) ;
#67761=CARTESIAN_POINT ( 'NONE',  ( -168.5949999999999989, 2.607480562269073321, 8.024999999999991473 ) ) ;
#67764=CARTESIAN_POINT ( 'NONE',  ( -147.1450000000000102, -4.716976649647092401, 6.492361379858946790 ) ) ;
#67772=CARTESIAN_POINT ( 'NONE',  ( -60.95499999999998408, -7.632228543268599452, 2.479861379858951054 ) ) ;
#67774=CARTESIAN_POINT ( 'NONE',  ( -64.64499999999998181, 4.716976649647091513, -6.492361379858946790 ) ) ;
#67787=DIRECTION ( 'NONE',  ( -1.000000000000000000, -0.000000000000000000, -0.000000000000000000 ) ) ;
#67788=LINE ( 'NONE', #62832, #64524 ) ;
#67799=CARTESIAN_POINT ( 'NONE',  ( -77.15707362346617515, -9.058813317711329915, -2.943386871421370898 ) ) ;
#67810=CARTESIAN_POINT ( 'NONE',  ( -114.5949999999999704, 2.607480562269073321, 8.024999999999991473 ) ) ;
#67811=EDGE_LOOP ( 'NONE', ( #21800, #63511, #53113, #39441 ) ) ;
#67824=EDGE_CURVE ( 'NONE', #55900, #18673, #57714, .T. ) ;
#67831=CARTESIAN_POINT ( 'NONE',  ( -121.7049999999999841, 2.607480562269073321, 8.024999999999991473 ) ) ;
#67833=CARTESIAN_POINT ( 'NONE',  ( -184.0000000000000000, -7.358988424933670558, 3.200923985616050071 ) ) ;
#67842=ORIENTED_EDGE ( 'NONE', *, *, #48594, .F. ) ;
#67844=AXIS2_PLACEMENT_3D ( 'NONE', #26356, #608, #69617 ) ;
#67849=CARTESIAN_POINT ( 'NONE',  ( -182.7549999999999955, 4.716976649647091513, -6.492361379858946790 ) ) ;
#67852=CARTESIAN_POINT ( 'NONE',  ( -56.00707362346614815, -8.102448949553172852, -5.886773742842741797 ) ) ;
#67855=CARTESIAN_POINT ( 'NONE',  ( -181.0449999999999875, 7.632228543268600340, 2.479861379858949277 ) ) ;
#67863=CARTESIAN_POINT ( 'NONE',  ( -92.30499999999999261, 8.437984349512085203, -1.550032578732815448E-15 ) ) ;
#67867=CARTESIAN_POINT ( 'NONE',  ( -87.59499999999999886, 2.607480562269072433, 8.024999999999991473 ) ) ;
#67869=CARTESIAN_POINT ( 'NONE',  ( -72.14499999999998181, -4.716976649647092401, 6.492361379858946790 ) ) ;
#67870=CARTESIAN_POINT ( 'NONE',  ( -195.0000000000000000, 1.166476076187852838E-15, -9.524999999999991473 ) ) ;
#67878=CARTESIAN_POINT ( 'NONE',  ( -116.8429263765338106, 9.058813317711329915, -2.943386871421373119 ) ) ;
#67879=CARTESIAN_POINT ( 'NONE',  ( -130.6449999999999818, 4.716976649647091513, -6.492361379858946790 ) ) ;
#67884=CARTESIAN_POINT ( 'NONE',  ( -195.0000000000000000, 0.000000000000000000, 0.000000000000000000 ) ) ;
#67886=ORIENTED_EDGE ( 'NONE', *, *, #68560, .T. ) ;
#67892=CARTESIAN_POINT ( 'NONE',  ( -43.99999999999998579, 0.000000000000000000, 0.000000000000000000 ) ) ;
#67896=CARTESIAN_POINT ( 'NONE',  ( -132.0549999999999784, -9.827790563157499189E-16, -8.024999999999991473 ) ) ;
#67899=CARTESIAN_POINT ( 'NONE',  ( -122.0070736234661553, -8.102448949553172852, -5.886773742842741797 ) ) ;
#67907=ORIENTED_EDGE ( 'NONE', *, *, #2893, .F. ) ;
#67912=CARTESIAN_POINT ( 'NONE',  ( -48.95499999999996987, -7.632228543268599452, 2.479861379858951054 ) ) ;
#67927=CARTESIAN_POINT ( 'NONE',  ( -63.14292637653380780, 5.598654528085800663, -7.705886871421367523 ) ) ;
#67931=LINE ( 'NONE', #13054, #26139 ) ;
#67932=CARTESIAN_POINT ( 'NONE',  ( -152.1549999999999727, 7.632228543268600340, 2.479861379858949277 ) ) ;
#67933=ORIENTED_EDGE ( 'NONE', *, *, #17591, .F. ) ;
#67944=EDGE_CURVE ( 'NONE', #61162, #65527, #24544, .T. ) ;
#67947=CARTESIAN_POINT ( 'NONE',  ( -67.85499999999998977, 4.716976649647094177, 6.492361379858945902 ) ) ;
#67948=AXIS2_PLACEMENT_3D ( 'NONE', #48366, #423, #21589 ) ;
#67960=CARTESIAN_POINT ( 'NONE',  ( -95.24499999999997613, -4.716976649647093289, -6.492361379858945902 ) ) ;
#67969=CARTESIAN_POINT ( 'NONE',  ( -147.8929263765338362, -8.102448949553172852, -5.886773742842741797 ) ) ;
#67971=CARTESIAN_POINT ( 'NONE',  ( -161.3950000000000102, -6.826472737025115478, -4.959722759717899443 ) ) ;
#67977=VERTEX_POINT ( 'NONE', #43335 ) ;
#67986=CARTESIAN_POINT ( 'NONE',  ( -159.8049999999999784, -8.437984349512086979, 5.166775262442717831E-16 ) ) ;
#67989=CARTESIAN_POINT ( 'NONE',  ( -48.14292637653380780, 5.598654528085800663, -7.705886871421367523 ) ) ;
#67995=( BOUNDED_CURVE ( )  B_SPLINE_CURVE ( 2, ( #25384, #25716, #52837, #20457, #46899, #4613, #25041, #57400, #20090, #9224, #52498 ),
 .UNSPECIFIED., .F., .F. ) 
 B_SPLINE_CURVE_WITH_KNOTS ( ( 3, 2, 2, 2, 2, 3 ),
 ( 0.3695652173912954974, 0.3717391304347737457, 0.3739130434782519385, 0.3760869565217300758, 0.3782608695652082687, 0.3804347826086865170 ),
 .UNSPECIFIED. ) 
 CURVE ( )  GEOMETRIC_REPRESENTATION_ITEM ( )  RATIONAL_B_SPLINE_CURVE ( ( 1.000000000000198730, 0.9510565162949548013, 1.000000000000000000, 0.9510565162951535312, 1.000000000000000000, 0.9510565162951535312, 1.000000000000000000, 0.9510565162951535312, 1.000000000000000000, 0.9510565162953596996, 0.9999999999997938316 ) ) 
 REPRESENTATION_ITEM ( '' )  );
#68000=CARTESIAN_POINT ( 'NONE',  ( -78.20499999999996987, -2.607480562269071545, -8.024999999999991473 ) ) ;
#68005=DIRECTION ( 'NONE',  ( -1.000000000000000000, -0.000000000000000000, -0.000000000000000000 ) ) ;
#68012=CARTESIAN_POINT ( 'NONE',  ( -181.2549999999999955, -4.716976649647092401, 6.492361379858946790 ) ) ;
#68024=CARTESIAN_POINT ( 'NONE',  ( -106.4049999999999727, -2.607480562269069768, 8.024999999999991473 ) ) ;
#68026=DIRECTION ( 'NONE',  ( 0.000000000000000000, 0.000000000000000000, 1.000000000000000000 ) ) ;
#68029=CARTESIAN_POINT ( 'NONE',  ( -138.8070736234661524, 10.01517768586948698, -1.839758294383808571E-15 ) ) ;
#68030=VECTOR ( 'NONE', #3055, 1000.000000000000000 ) ;
#68033=CARTESIAN_POINT ( 'NONE',  ( -73.85707362346617799, -5.598654528085803328, -7.705886871421366635 ) ) ;
#68040=CARTESIAN_POINT ( 'NONE',  ( -123.8049999999999926, -8.437984349512085203, 5.166775262442717831E-16 ) ) ;
#68043=CARTESIAN_POINT ( 'NONE',  ( -126.8949999999999818, 6.826472737025116366, 4.959722759717898555 ) ) ;
#68045=CARTESIAN_POINT ( 'NONE',  ( -111.3570736234661780, 5.598654528085804216, 7.705886871421366635 ) ) ;
#68050=CARTESIAN_POINT ( 'NONE',  ( -166.5570736234661808, -1.166476076187852838E-15, -9.524999999999991473 ) ) ;
#68051=VECTOR ( 'NONE', #67006, 1000.000000000000000 ) ;
#68052=CARTESIAN_POINT ( 'NONE',  ( -175.1929263765337623, -10.01517768586948698, 6.132527647946031529E-16 ) ) ;
#68058=CARTESIAN_POINT ( 'NONE',  ( -82.34292637653379643, -9.058813317711329915, 2.943386871421371787 ) ) ;
#68062=CARTESIAN_POINT ( 'NONE',  ( -180.2929263765338987, 3.094860106617521200, -9.525000000000654055 ) ) ;
#68067=CARTESIAN_POINT ( 'NONE',  ( -136.4929263765338305, -8.102448949553174629, 5.886773742842742685 ) ) ;
#68079=CARTESIAN_POINT ( 'NONE',  ( -103.5549999999999926, 0.000000000000000000, 8.024999999999991473 ) ) ;
#68091=CARTESIAN_POINT ( 'NONE',  ( -86.24499999999999034, -4.716976649647093289, -6.492361379858945902 ) ) ;
#68096=ADVANCED_FACE ( 'NONE', ( #45039 ), #29133, .T. ) ;
#68105=VERTEX_POINT ( 'NONE', #66448 ) ;
#68108=CARTESIAN_POINT ( 'NONE',  ( -167.1570736234661751, -9.058813317711329915, -2.943386871421370898 ) ) ;
#68110=CARTESIAN_POINT ( 'NONE',  ( -102.3570736234661780, 5.598654528085804216, 7.705886871421366635 ) ) ;
#68114=CARTESIAN_POINT ( 'NONE',  ( -82.64292637653379359, -5.598654528085801552, 7.705886871421367523 ) ) ;
#68117=CARTESIAN_POINT ( 'NONE',  ( -148.7049999999999841, 2.607480562269073321, 8.024999999999991473 ) ) ;
#68120=CARTESIAN_POINT ( 'NONE',  ( -156.8950000000000102, 6.826472737025116366, 4.959722759717898555 ) ) ;
#68122=CARTESIAN_POINT ( 'NONE',  ( -150.1450000000000102, -4.716976649647092401, 6.492361379858946790 ) ) ;
#68123=B_SPLINE_CURVE_WITH_KNOTS ( 'NONE', 3,
 ( #42683, #41996, #4644, #21169 ),
 .UNSPECIFIED., .F., .F.,
 ( 4, 4 ),
 ( 0.000000000000000000, 0.001157321451656189446 ),
 .UNSPECIFIED. ) ;
#68128=CARTESIAN_POINT ( 'NONE',  ( -66.05499999999999261, -9.827790563157499189E-16, -8.024999999999991473 ) ) ;
#68132=CARTESIAN_POINT ( 'NONE',  ( -60.74499999999997613, 4.716976649647094177, 6.492361379858945902 ) ) ;
#68136=CARTESIAN_POINT ( 'NONE',  ( -195.0000000000000000, 0.000000000000000000, 9.524999999999991473 ) ) ;
#68139=CARTESIAN_POINT ( 'NONE',  ( -145.5570736234661808, -1.166476076187852838E-15, -9.524999999999991473 ) ) ;
#68142=ORIENTED_EDGE ( 'NONE', *, *, #48644, .F. ) ;
#68146=ADVANCED_FACE ( 'NONE', ( #18267 ), #2362, .T. ) ;
#68165=CARTESIAN_POINT ( 'NONE',  ( -106.1949999999999932, 8.437984349512085203, -1.550032578732815448E-15 ) ) ;
#68168=CARTESIAN_POINT ( 'NONE',  ( -164.9070736234663741, -3.094860106614866879, 9.525000000002579625 ) ) ;
#68180=CARTESIAN_POINT ( 'NONE',  ( -195.0000000000000000, 0.000000000000000000, 0.000000000000000000 ) ) ;
#68183=CARTESIAN_POINT ( 'NONE',  ( -120.9549999999999983, -7.632228543268599452, 2.479861379858951054 ) ) ;
#68195=CARTESIAN_POINT ( 'NONE',  ( -176.4550000000000125, 7.632228543268599452, -2.479861379858951942 ) ) ;
#68196=CARTESIAN_POINT ( 'NONE',  ( -91.04292637653379927, -9.058813317711329915, -2.943386871421370898 ) ) ;
#68197=CARTESIAN_POINT ( 'NONE',  ( -48.05707362346617373, 0.000000000000000000, 9.524999999999991473 ) ) ;
#68198=CARTESIAN_POINT ( 'NONE',  ( -177.1450000000000102, -4.716976649647092401, 6.492361379858946790 ) ) ;
#68205=CARTESIAN_POINT ( 'NONE',  ( -89.00499999999999545, 6.826472737025116366, 4.959722759717898555 ) ) ;
#68210=CARTESIAN_POINT ( 'NONE',  ( -92.69499999999996476, -8.437984349512086979, 5.166775262442717831E-16 ) ) ;
#68213=CARTESIAN_POINT ( 'NONE',  ( -64.49499999999997613, 6.826472737025113702, -4.959722759717902107 ) ) ;
#68214=LINE ( 'NONE', #67870, #57800 ) ;
#68220=CARTESIAN_POINT ( 'NONE',  ( -104.2429263765338021, 5.598654528085804216, 7.705886871421366635 ) ) ;
#68221=CARTESIAN_POINT ( 'NONE',  ( -128.5449999999999875, -7.632228543268600340, -2.479861379858950166 ) ) ;
#68238=CARTESIAN_POINT ( 'NONE',  ( -125.0049999999999812, 6.826472737025115478, 4.959722759717899443 ) ) ;
#68241=CARTESIAN_POINT ( 'NONE',  ( -126.3570736234661780, 5.598654528085804216, 7.705886871421366635 ) ) ;
#68265=CARTESIAN_POINT ( 'NONE',  ( -58.49292637653379501, -8.102448949553172852, 5.886773742842742685 ) ) ;
#68268=CARTESIAN_POINT ( 'NONE',  ( -155.6049999999999329, 6.826472737025113702, -4.959722759717902107 ) ) ;
#68273=CARTESIAN_POINT ( 'NONE',  ( -70.94292637653380496, 0.000000000000000000, 9.524999999999991473 ) ) ;
#68276=ORIENTED_EDGE ( 'NONE', *, *, #28177, .T. ) ;
#68279=CARTESIAN_POINT ( 'NONE',  ( -62.00499999999999545, 6.826472737025116366, 4.959722759717898555 ) ) ;
#68288=LINE ( 'NONE', #35590, #9912 ) ;
#68291=CARTESIAN_POINT ( 'NONE',  ( -93.74499999999999034, 4.716976649647094177, 6.492361379858945902 ) ) ;
#68292=B_SPLINE_CURVE_WITH_KNOTS ( 'NONE', 3,
 ( #50547, #12896, #65327, #34004, #61413, #55101, #28715, #55810, #38991, #44271, #6237, #34361, #2269, #66721, #40024, #7288, #13230, #49173, #60382, #43916, #33658, #54747, #1598, #874, #55464, #23126 ),
 .UNSPECIFIED., .F., .F.,
 ( 4, 2, 2, 2, 2, 2, 2, 2, 2, 2, 2, 2, 4 ),
 ( 0.008651501742289673114, 0.01053121843691355759, 0.01241093513153744381, 0.01335079347884938865, 0.01429065182616133696, 0.01523051017347328354, 0.01617036852078523185, 0.01805008521540912153, 0.01898994356272106984, 0.01992980191003301815, 0.02086966025734496299, 0.02180951860465690784, 0.02368923529928080099 ),
 .UNSPECIFIED. ) ;
#68295=( BOUNDED_CURVE ( )  B_SPLINE_CURVE ( 2, ( #15464, #11182, #48175, #26649, #15126, #31240, #5539, #36926, #10850, #42230, #64667 ),
 .UNSPECIFIED., .F., .F. ) 
 B_SPLINE_CURVE_WITH_KNOTS ( ( 3, 2, 2, 2, 2, 3 ),
 ( 0.7934782608695651884, 0.7956521739130434367, 0.7978260869565216851, 0.8000000000000000444, 0.8021739130434782927, 0.8043478260869565410 ),
 .UNSPECIFIED. ) 
 CURVE ( )  GEOMETRIC_REPRESENTATION_ITEM ( )  RATIONAL_B_SPLINE_CURVE ( ( 1.000000000000000000, 0.9510565162951535312, 1.000000000000000000, 0.9510565162951535312, 1.000000000000000000, 0.9510565162951535312, 1.000000000000000000, 0.9510565162951535312, 1.000000000000000000, 0.9510565162951535312, 1.000000000000000000 ) ) 
 REPRESENTATION_ITEM ( '' )  );
#68299=CARTESIAN_POINT ( 'NONE',  ( -137.8429263765337964, 9.058813317711329915, -2.943386871421373119 ) ) ;
#68301=CARTESIAN_POINT ( 'NONE',  ( -154.6450000000000102, 4.716976649647091513, -6.492361379858946790 ) ) ;
#68304=AXIS2_PLACEMENT_3D ( 'NONE', #64193, #68812, #30795 ) ;
#68322=CARTESIAN_POINT ( 'NONE',  ( -149.4550000000000125, 7.632228543268599452, -2.479861379858951942 ) ) ;
#68330=CARTESIAN_POINT ( 'NONE',  ( -58.79292637653379927, -3.094860106618429807, 9.524999999999991473 ) ) ;
#68332=CARTESIAN_POINT ( 'NONE',  ( -72.20499999999998408, -2.607480562269071545, -8.024999999999991473 ) ) ;
#68345=CARTESIAN_POINT ( 'NONE',  ( -177.5049999999999670, -6.826472737025115478, -4.959722759717899443 ) ) ;
#68357=CARTESIAN_POINT ( 'NONE',  ( -93.50499999999999545, -6.826472737025115478, -4.959722759717899443 ) ) ;
#68361=CARTESIAN_POINT ( 'NONE',  ( -138.9570736234661865, 9.058813317711329915, -2.943386871421373119 ) ) ;
#68363=CARTESIAN_POINT ( 'NONE',  ( -78.65707362346617515, 9.058813317711329915, 2.943386871421369566 ) ) ;
#68364=EDGE_CURVE ( 'NONE', #33812, #63576, #65294, .T. ) ;
#68369=CARTESIAN_POINT ( 'NONE',  ( -110.9049999999999727, 2.607480562269068880, -8.024999999999993250 ) ) ;
#68372=CARTESIAN_POINT ( 'NONE',  ( -126.4450000000000074, 0.000000000000000000, 8.024999999999991473 ) ) ;
#68373=CARTESIAN_POINT ( 'NONE',  ( -111.2070736234670534, 3.094860106633222863, 9.524999999989246291 ) ) ;
#68379=CARTESIAN_POINT ( 'NONE',  ( -174.4429263765337907, -1.166476076187852838E-15, -9.524999999999991473 ) ) ;
#68389=CARTESIAN_POINT ( 'NONE',  ( -81.29292637653379927, 3.094860106618428031, -9.524999999999993250 ) ) ;
#68391=( BOUNDED_CURVE ( )  B_SPLINE_CURVE ( 2, ( #62053, #68062, #51878, #41341, #35352, #67347, #51182, #3635, #56093, #67015, #14235 ),
 .UNSPECIFIED., .F., .F. ) 
 B_SPLINE_CURVE_WITH_KNOTS ( ( 3, 2, 2, 2, 2, 3 ),
 ( 0.03260869565217316274, 0.03478260869565137636, 0.03695652173912958999, 0.03913043478260780361, 0.04130434782608601030, 0.04347826086956422392 ),
 .UNSPECIFIED. ) 
 CURVE ( )  GEOMETRIC_REPRESENTATION_ITEM ( )  RATIONAL_B_SPLINE_CURVE ( ( 1.000000000000016653, 0.9510565162951365448, 1.000000000000000000, 0.9510565162951535312, 1.000000000000000000, 0.9510565162951535312, 1.000000000000000000, 0.9510565162951535312, 1.000000000000000000, 0.9510565162951758467, 0.9999999999999776845 ) ) 
 REPRESENTATION_ITEM ( '' )  );
#68398=CARTESIAN_POINT ( 'NONE',  ( -135.8929263765338078, -8.102448949553174629, -5.886773742842741797 ) ) ;
#68409=CARTESIAN_POINT ( 'NONE',  ( -100.1049999999999898, -6.826472737025113702, 4.959722759717902107 ) ) ;
#68411=CARTESIAN_POINT ( 'NONE',  ( -55.94292637653380496, 0.000000000000000000, 9.524999999999991473 ) ) ;
#68417=ORIENTED_EDGE ( 'NONE', *, *, #47750, .T. ) ;
#68420=CARTESIAN_POINT ( 'NONE',  ( -76.79499999999998749, 2.607480562269068880, -8.024999999999993250 ) ) ;
#68427=FACE_OUTER_BOUND ( 'NONE', #15507, .T. ) ;
#68434=AXIS2_PLACEMENT_3D ( 'NONE', #2987, #18182, #34009 ) ;
#68436=CARTESIAN_POINT ( 'NONE',  ( -150.4429263765338192, -1.166476076187852838E-15, -9.524999999999991473 ) ) ;
#68439=CARTESIAN_POINT ( 'NONE',  ( -165.6570736234661751, 9.058813317711329915, 2.943386871421369566 ) ) ;
#68442=CARTESIAN_POINT ( 'NONE',  ( -104.1570736234661751, -9.058813317711329915, -2.943386871421370898 ) ) ;
#68450=CARTESIAN_POINT ( 'NONE',  ( -145.8549999999999898, 4.716976649647094177, 6.492361379858945902 ) ) ;
#68453=CARTESIAN_POINT ( 'NONE',  ( -159.1449999999999818, -4.716976649647092401, 6.492361379858946790 ) ) ;
#68455=CARTESIAN_POINT ( 'NONE',  ( -146.5449999999999875, -7.632228543268600340, -2.479861379858950166 ) ) ;
#68462=CARTESIAN_POINT ( 'NONE',  ( -66.50499999999996703, -6.826472737025115478, -4.959722759717899443 ) ) ;
#68465=CARTESIAN_POINT ( 'NONE',  ( -62.54499999999998749, -7.632228543268600340, -2.479861379858950166 ) ) ;
#68468=CARTESIAN_POINT ( 'NONE',  ( -143.0070736234661695, -8.102448949553174629, -5.886773742842741797 ) ) ;
#68473=CARTESIAN_POINT ( 'NONE',  ( -152.9929263765337737, 8.102448949553172852, -5.886773742842744461 ) ) ;
#68478=EDGE_CURVE ( 'NONE', #50010, #24888, #68292, .T. ) ;
#68495=CARTESIAN_POINT ( 'NONE',  ( -76.70707362346617231, -3.094860106618431139, -9.524999999999991473 ) ) ;
#68505=CARTESIAN_POINT ( 'NONE',  ( -104.0949999999999989, -2.607480562269071545, -8.024999999999991473 ) ) ;
#68509=CARTESIAN_POINT ( 'NONE',  ( -164.7570736234661695, -5.598654528085801552, 7.705886871421367523 ) ) ;
#68515=CARTESIAN_POINT ( 'NONE',  ( -61.70707362346615810, -3.094860106618431139, -9.524999999999991473 ) ) ;
#68520=CARTESIAN_POINT ( 'NONE',  ( -119.7549999999999812, 4.716976649647091513, -6.492361379858946790 ) ) ;
#68533=CARTESIAN_POINT ( 'NONE',  ( -183.0000000000000000, 7.623482428031956637, -5.710353812986356026 ) ) ;
#68536=CARTESIAN_POINT ( 'NONE',  ( -183.6549999999999727, -7.632228543268600340, -2.479861379858950166 ) ) ;
#68540=CARTESIAN_POINT ( 'NONE',  ( -182.8449999999999989, -7.632228543268599452, 2.479861379858951054 ) ) ;
#68542=CARTESIAN_POINT ( 'NONE',  ( -173.6949999999999648, -8.437984349512086979, 5.166775262442717831E-16 ) ) ;
#68544=ORIENTED_EDGE ( 'NONE', *, *, #16734, .F. ) ;
#68547=CARTESIAN_POINT ( 'NONE',  ( -13.37648924254744642, 11.02484219126050391, -4.740415575798497372 ) ) ;
#68548=CARTESIAN_POINT ( 'NONE',  ( -97.10499999999998977, -6.826472737025115478, 4.959722759717900331 ) ) ;
#68552=CARTESIAN_POINT ( 'NONE',  ( -95.24499999999997613, -4.716976649647093289, -6.492361379858945902 ) ) ;
#68554=CARTESIAN_POINT ( 'NONE',  ( -71.54499999999998749, -7.632228543268600340, -2.479861379858950166 ) ) ;
#68560=EDGE_CURVE ( 'NONE', #65490, #24108, #36147, .T. ) ;
#68565=VERTEX_POINT ( 'NONE', #36111 ) ;
#68567=CARTESIAN_POINT ( 'NONE',  ( -100.3429263765337964, -9.058813317711329915, 2.943386871421371787 ) ) ;
#68568=CARTESIAN_POINT ( 'NONE',  ( -128.8449999999999989, -7.632228543268599452, 2.479861379858951054 ) ) ;
#68569=CARTESIAN_POINT ( 'NONE',  ( -132.2929263765344672, 3.094860106607336903, -9.525000000008052581 ) ) ;
#68576=CARTESIAN_POINT ( 'NONE',  ( -134.3929263765338078, 8.102448949553176405, 5.886773742842740909 ) ) ;
#68579=CARTESIAN_POINT ( 'NONE',  ( -97.85707362346616378, -5.598654528085803328, -7.705886871421366635 ) ) ;
#68583=CARTESIAN_POINT ( 'NONE',  ( -126.5049999999999528, -6.826472737025113702, -4.959722759717900331 ) ) ;
#68584=ORIENTED_EDGE ( 'NONE', *, *, #67824, .T. ) ;
#68585=CARTESIAN_POINT ( 'NONE',  ( -126.6570736234661751, 9.058813317711329915, 2.943386871421369566 ) ) ;
#68604=CARTESIAN_POINT ( 'NONE',  ( -47.15707362346616094, -9.058813317711329915, -2.943386871421370898 ) ) ;
#68611=CARTESIAN_POINT ( 'NONE',  ( -58.94292637653381206, 0.000000000000000000, 9.524999999999991473 ) ) ;
#68613=CARTESIAN_POINT ( 'NONE',  ( -148.2549999999999955, -4.716976649647092401, 6.492361379858946790 ) ) ;
#68624=CARTESIAN_POINT ( 'NONE',  ( -195.0000000000000000, 0.000000000000000000, 0.000000000000000000 ) ) ;
#68626=CARTESIAN_POINT ( 'NONE',  ( -70.10499999999998977, -6.826472737025115478, 4.959722759717900331 ) ) ;
#68630=CARTESIAN_POINT ( 'NONE',  ( -90.95707362346617231, 9.058813317711329915, -2.943386871421373119 ) ) ;
#68640=CARTESIAN_POINT ( 'NONE',  ( -92.54499999999998749, -7.632228543268600340, -2.479861379858950166 ) ) ;
#68647=VECTOR ( 'NONE', #52651, 1000.000000000000000 ) ;
#68651=CARTESIAN_POINT ( 'NONE',  ( -133.4929263765338021, -8.102448949553172852, 5.886773742842742685 ) ) ;
#68654=CARTESIAN_POINT ( 'NONE',  ( -160.1950000000000216, 8.437984349512085203, -1.550032578732815448E-15 ) ) ;
#68664=ORIENTED_EDGE ( 'NONE', *, *, #56059, .T. ) ;
#68667=CARTESIAN_POINT ( 'NONE',  ( -110.9070736234670846, -3.094860106603640304, 9.525000000010738432 ) ) ;
#68671=CARTESIAN_POINT ( 'NONE',  ( -148.5550000000000068, 0.000000000000000000, 8.024999999999991473 ) ) ;
#68683=CARTESIAN_POINT ( 'NONE',  ( -65.75499999999998124, 4.716976649647091513, -6.492361379858946790 ) ) ;
#68686=( BOUNDED_CURVE ( )  B_SPLINE_CURVE ( 2, ( #22248, #69070, #20874, #32116, #63763, #42716, #37088, #64114, #5027, #15968, #58848 ),
 .UNSPECIFIED., .F., .F. ) 
 B_SPLINE_CURVE_WITH_KNOTS ( ( 3, 2, 2, 2, 2, 3 ),
 ( 0.7500000000000000000, 0.7521739130434782483, 0.7543478260869564966, 0.7565217391304347450, 0.7586956521739129933, 0.7608695652173913526 ),
 .UNSPECIFIED. ) 
 CURVE ( )  GEOMETRIC_REPRESENTATION_ITEM ( )  RATIONAL_B_SPLINE_CURVE ( ( 1.000000000000000000, 0.9510565162951535312, 1.000000000000000000, 0.9510565162951535312, 1.000000000000000000, 0.9510565162951535312, 1.000000000000000000, 0.9510565162951535312, 1.000000000000000000, 0.9510565162951535312, 1.000000000000000000 ) ) 
 REPRESENTATION_ITEM ( '' )  );
#68694=ORIENTED_EDGE ( 'NONE', *, *, #5531, .T. ) ;
#68698=CARTESIAN_POINT ( 'NONE',  ( -178.2549999999999955, -4.716976649647092401, 6.492361379858946790 ) ) ;
#68712=CARTESIAN_POINT ( 'NONE',  ( -99.35499999999998977, -4.716976649647093289, -6.492361379858945902 ) ) ;
#68718=CARTESIAN_POINT ( 'NONE',  ( -135.2070736234661865, 3.094860106618433360, 9.524999999999991473 ) ) ;
#68721=CARTESIAN_POINT ( 'NONE',  ( -72.20707362346617231, 3.094860106618433360, 9.524999999999991473 ) ) ;
#68724=CARTESIAN_POINT ( 'NONE',  ( -91.94292637653380496, 0.000000000000000000, 9.524999999999991473 ) ) ;
#68727=CARTESIAN_POINT ( 'NONE',  ( -15.65791276157354694, -10.92369435878044293, -4.967701894473437463 ) ) ;
#68730=CARTESIAN_POINT ( 'NONE',  ( -112.4050000000000011, -2.607480562269069768, 8.024999999999991473 ) ) ;
#68733=CARTESIAN_POINT ( 'NONE',  ( -130.6449999999999818, 4.716976649647091513, -6.492361379858946790 ) ) ;
#68736=CARTESIAN_POINT ( 'NONE',  ( -111.9570736234661723, 9.058813317711329915, -2.943386871421373119 ) ) ;
#68737=CARTESIAN_POINT ( 'NONE',  ( -118.6429263765337936, -5.598654528085801552, 7.705886871421367523 ) ) ;
#68742=CARTESIAN_POINT ( 'NONE',  ( -162.2929263765337851, 3.094860106618428031, -9.524999999999993250 ) ) ;
#68743=CARTESIAN_POINT ( 'NONE',  ( -183.4449999999999932, 0.000000000000000000, 8.024999999999991473 ) ) ;
#68747=CARTESIAN_POINT ( 'NONE',  ( -195.0000000000000000, 1.166476076187852838E-15, -9.524999999999991473 ) ) ;
#68751=CARTESIAN_POINT ( 'NONE',  ( -79.34292637653379643, -9.058813317711329915, 2.943386871421371787 ) ) ;
#68752=DIRECTION ( 'NONE',  ( -1.000000000000000000, -0.000000000000000000, -0.000000000000000000 ) ) ;
#68754=VECTOR ( 'NONE', #55948, 1000.000000000000000 ) ;
#68757=CARTESIAN_POINT ( 'NONE',  ( -182.4550000000000125, 7.632228543268599452, -2.479861379858951942 ) ) ;
#68770=CARTESIAN_POINT ( 'NONE',  ( -101.7549999999999812, 4.716976649647091513, -6.492361379858946790 ) ) ;
#68781=CARTESIAN_POINT ( 'NONE',  ( -73.19499999999999318, 8.437984349512085203, -1.550032578732815448E-15 ) ) ;
#68786=CARTESIAN_POINT ( 'NONE',  ( -120.0570736234661808, 0.000000000000000000, 9.524999999999991473 ) ) ;
#68803=CARTESIAN_POINT ( 'NONE',  ( -157.5570736234661808, -1.166476076187852838E-15, -9.524999999999991473 ) ) ;
#68805=CARTESIAN_POINT ( 'NONE',  ( -99.65707362346617515, 9.058813317711329915, 2.943386871421369566 ) ) ;
#68810=VERTEX_POINT ( 'NONE', #44537 ) ;
#68812=DIRECTION ( 'NONE',  ( -1.000000000000000000, -0.000000000000000000, -0.000000000000000000 ) ) ;
#68816=CARTESIAN_POINT ( 'NONE',  ( -143.1549999999999727, 7.632228543268600340, 2.479861379858949277 ) ) ;
#68817=CARTESIAN_POINT ( 'NONE',  ( -158.9950000000000045, -6.826472737025115478, 4.959722759717900331 ) ) ;
#68818=CARTESIAN_POINT ( 'NONE',  ( -142.3449999999999989, 7.632228543268599452, -2.479861379858951942 ) ) ;
#68820=( BOUNDED_CURVE ( )  B_SPLINE_CURVE ( 2, ( #36412, #4685, #14929, #63445, #68736, #57829, #20165, #36756, #68045, #68373, #19830 ),
 .UNSPECIFIED., .F., .F. ) 
 B_SPLINE_CURVE_WITH_KNOTS ( ( 3, 2, 2, 2, 2, 3 ),
 ( 0.5108695652173793622, 0.5130434782608576105, 0.5152173913043357478, 0.5173913043478139961, 0.5195652173912921334, 0.5217391304347703818 ),
 .UNSPECIFIED. ) 
 CURVE ( )  GEOMETRIC_REPRESENTATION_ITEM ( )  RATIONAL_B_SPLINE_CURVE ( ( 1.000000000000270006, 0.9510565162948835249, 1.000000000000000000, 0.9510565162951535312, 1.000000000000000000, 0.9510565162951535312, 1.000000000000000000, 0.9510565162951535312, 1.000000000000000000, 0.9510565162954285334, 0.9999999999997249978 ) ) 
 REPRESENTATION_ITEM ( '' )  );
#68824=CARTESIAN_POINT ( 'NONE',  ( -50.00499999999998835, 6.826472737025116366, 4.959722759717898555 ) ) ;
#68829=CARTESIAN_POINT ( 'NONE',  ( -143.1570736234662036, -9.058813317711329915, -2.943386871421370898 ) ) ;
#68859=EDGE_CURVE ( 'NONE', #24108, #55259, #19049, .T. ) ;
#68861=CARTESIAN_POINT ( 'NONE',  ( -101.2449999999999903, -4.716976649647093289, -6.492361379858945902 ) ) ;
#68878=CARTESIAN_POINT ( 'NONE',  ( -195.0000000000000000, 0.000000000000000000, 0.000000000000000000 ) ) ;
#68888=VERTEX_POINT ( 'NONE', #57108 ) ;
#68896=CARTESIAN_POINT ( 'NONE',  ( -167.4549999999999841, 7.632228543268599452, -2.479861379858951942 ) ) ;
#68899=CARTESIAN_POINT ( 'NONE',  ( -49.25707362346617657, 5.598654528085800663, -7.705886871421367523 ) ) ;
#68900=VECTOR ( 'NONE', #34509, 1000.000000000000000 ) ;
#68901=CARTESIAN_POINT ( 'NONE',  ( -178.7949999999999875, 2.607480562269069324, -8.024999999999993250 ) ) ;
#68905=CARTESIAN_POINT ( 'NONE',  ( -10.51142403643257239, 11.79550216340572000, -2.227010390538998408 ) ) ;
#68907=CARTESIAN_POINT ( 'NONE',  ( -92.45499999999998408, 7.632228543268599452, -2.479861379858951942 ) ) ;
#68912=CARTESIAN_POINT ( 'NONE',  ( -91.79499999999998749, 2.607480562269069324, -8.024999999999993250 ) ) ;
#68915=CARTESIAN_POINT ( 'NONE',  ( -169.9429263765337907, 0.000000000000000000, 9.524999999999991473 ) ) ;
#68917=EDGE_CURVE ( 'NONE', #23846, #6192, #2812, .T. ) ;
#68935=CARTESIAN_POINT ( 'NONE',  ( -125.3050000000000068, 8.437984349512086979, -1.550032578732815448E-15 ) ) ;
#68949=CARTESIAN_POINT ( 'NONE',  ( -129.5929263765345070, -3.094860106630128449, -9.524999999991493382 ) ) ;
#68964=CARTESIAN_POINT ( 'NONE',  ( -61.34292637653379643, -9.058813317711329915, 2.943386871421371787 ) ) ;
#68967=CARTESIAN_POINT ( 'NONE',  ( -153.3549999999999898, -4.716976649647093289, -6.492361379858945902 ) ) ;
#68981=CARTESIAN_POINT ( 'NONE',  ( -63.05499999999998550, -9.827790563157499189E-16, -8.024999999999991473 ) ) ;
#68985=CARTESIAN_POINT ( 'NONE',  ( -90.05707362346616662, 0.000000000000000000, 9.524999999999991473 ) ) ;
#68994=CARTESIAN_POINT ( 'NONE',  ( -115.4949999999999903, 6.826472737025113702, -4.959722759717902107 ) ) ;
#68996=CARTESIAN_POINT ( 'NONE',  ( -95.84499999999998465, -7.632228543268599452, 2.479861379858951054 ) ) ;
#69002=CARTESIAN_POINT ( 'NONE',  ( -130.1929263765337907, -10.01517768586948698, 6.132527647946031529E-16 ) ) ;
#69004=CARTESIAN_POINT ( 'NONE',  ( -48.14292637653380780, 5.598654528085800663, -7.705886871421367523 ) ) ;
#69005=CARTESIAN_POINT ( 'NONE',  ( -160.4949999999999761, 6.826472737025113702, -4.959722759717902107 ) ) ;
#69010=EDGE_LOOP ( 'NONE', ( #66349, #12249, #48264, #43331 ) ) ;
#69012=AXIS2_PLACEMENT_3D ( 'NONE', #38645, #33657, #55100 ) ;
#69015=CARTESIAN_POINT ( 'NONE',  ( -195.0000000000000000, 1.166476076187852838E-15, -9.524999999999991473 ) ) ;
#69017=CARTESIAN_POINT ( 'NONE',  ( -149.7549999999999955, 4.716976649647091513, -6.492361379858946790 ) ) ;
#69020=DIRECTION ( 'NONE',  ( -1.000000000000000000, -0.000000000000000000, -0.000000000000000000 ) ) ;
#69033=CARTESIAN_POINT ( 'NONE',  ( -65.90499999999998693, 2.607480562269069324, -8.024999999999993250 ) ) ;
#69034=CARTESIAN_POINT ( 'NONE',  ( -80.60707362346614957, -8.102448949553174629, 5.886773742842742685 ) ) ;
#69046=CARTESIAN_POINT ( 'NONE',  ( -46.94499999999998607, -9.827790563157499189E-16, -8.024999999999991473 ) ) ;
#69047=ORIENTED_EDGE ( 'NONE', *, *, #56359, .T. ) ;
#69051=EDGE_CURVE ( 'NONE', #56670, #68565, #43668, .T. ) ;
#69056=DIRECTION ( 'NONE',  ( 0.000000000000000000, 0.000000000000000000, 1.000000000000000000 ) ) ;
#69060=CARTESIAN_POINT ( 'NONE',  ( -94.55499999999999261, 0.000000000000000000, 8.024999999999991473 ) ) ;
#69064=CARTESIAN_POINT ( 'NONE',  ( -130.7070736234661581, -3.094860106618431139, -9.524999999999991473 ) ) ;
#69067=CARTESIAN_POINT ( 'NONE',  ( -66.95707362346617231, 9.058813317711329915, -2.943386871421373119 ) ) ;
#69070=CARTESIAN_POINT ( 'NONE',  ( -81.29292637653378506, 3.094860106618428031, -9.524999999999993250 ) ) ;
#69076=CARTESIAN_POINT ( 'NONE',  ( -113.0049999999999812, 6.826472737025116366, 4.959722759717898555 ) ) ;
#69078=CARTESIAN_POINT ( 'NONE',  ( -124.4949999999999761, 6.826472737025113702, -4.959722759717902107 ) ) ;
#69083=CARTESIAN_POINT ( 'NONE',  ( -130.9429263765338192, 0.000000000000000000, 9.524999999999991473 ) ) ;
#69085=CARTESIAN_POINT ( 'NONE',  ( -162.7429263765338021, -5.598654528085803328, -7.705886871421366635 ) ) ;
#69094=CARTESIAN_POINT ( 'NONE',  ( -75.14292637653380780, 5.598654528085800663, -7.705886871421367523 ) ) ;
#69103=CARTESIAN_POINT ( 'NONE',  ( -177.9550000000000125, -7.632228543268599452, 2.479861379858951054 ) ) ;
#69107=VERTEX_POINT ( 'NONE', #968 ) ;
#69113=CARTESIAN_POINT ( 'NONE',  ( -101.7570736234661695, -5.598654528085801552, 7.705886871421367523 ) ) ;
#69114=CARTESIAN_POINT ( 'NONE',  ( -97.70499999999996987, 2.607480562269072433, 8.024999999999991473 ) ) ;
#69125=CARTESIAN_POINT ( 'NONE',  ( -70.34499999999998465, 7.632228543268599452, -2.479861379858951942 ) ) ;
#69141=CARTESIAN_POINT ( 'NONE',  ( -161.7570736234661695, -5.598654528085801552, 7.705886871421367523 ) ) ;
#69144=CARTESIAN_POINT ( 'NONE',  ( -108.3570736234661780, 5.598654528085804216, 7.705886871421366635 ) ) ;
#69147=ORIENTED_EDGE ( 'NONE', *, *, #64252, .T. ) ;
#69152=CARTESIAN_POINT ( 'NONE',  ( -138.9549999999999841, -7.632228543268599452, 2.479861379858951054 ) ) ;
#69153=CARTESIAN_POINT ( 'NONE',  ( -85.70707362346617231, -3.094860106618431139, -9.524999999999991473 ) ) ;
#69155=CARTESIAN_POINT ( 'NONE',  ( -154.7950000000000159, 2.607480562269068880, -8.024999999999993250 ) ) ;
#69156=CARTESIAN_POINT ( 'NONE',  ( -139.4949999999999761, 6.826472737025113702, -4.959722759717902107 ) ) ;
#69163=CARTESIAN_POINT ( 'NONE',  ( -54.35499999999998977, -4.716976649647093289, -6.492361379858945902 ) ) ;
#69165=AXIS2_PLACEMENT_3D ( 'NONE', #49232, #44342, #43986 ) ;
#69175=CARTESIAN_POINT ( 'NONE',  ( -178.3429263765338249, -9.058813317711329915, 2.943386871421371787 ) ) ;
#69198=CARTESIAN_POINT ( 'NONE',  ( -115.9429263765338050, 0.000000000000000000, 9.524999999999991473 ) ) ;
#69202=CARTESIAN_POINT ( 'NONE',  ( -102.2949999999999733, -2.607480562269069768, 8.024999999999991473 ) ) ;
#69209=CARTESIAN_POINT ( 'NONE',  ( -195.0000000000000000, 0.000000000000000000, 11.99999999999999645 ) ) ;
#69211=FACE_OUTER_BOUND ( 'NONE', #7492, .T. ) ;
#69214=EDGE_LOOP ( 'NONE', ( #62062, #18042, #68694, #58045 ) ) ;
#69231=CARTESIAN_POINT ( 'NONE',  ( -170.4570736234661865, -9.058813317711329915, 2.943386871421371787 ) ) ;
#69235=CARTESIAN_POINT ( 'NONE',  ( -170.1550000000000011, 7.632228543268600340, 2.479861379858949277 ) ) ;
#69236=CYLINDRICAL_SURFACE ( 'NONE', #21748, 9.524999999999991473 ) ;
#69238=CARTESIAN_POINT ( 'NONE',  ( -181.7949999999999875, 2.607480562269068880, -8.024999999999993250 ) ) ;
#69240=CARTESIAN_POINT ( 'NONE',  ( -170.8449999999999989, -7.632228543268599452, 2.479861379858951054 ) ) ;
#69245=CARTESIAN_POINT ( 'NONE',  ( -10.16325816446478569, 11.93274896293544884, 1.310308443953213997 ) ) ;
#69246=CARTESIAN_POINT ( 'NONE',  ( -80.45499999999998408, 7.632228543268599452, -2.479861379858951942 ) ) ;
#69249=CARTESIAN_POINT ( 'NONE',  ( -81.59499999999997044, 2.607480562269072433, 8.024999999999991473 ) ) ;
#69252=CARTESIAN_POINT ( 'NONE',  ( -171.2929263765339556, 3.094860106615688888, -9.525000000001982770 ) ) ;
#69277=CARTESIAN_POINT ( 'NONE',  ( -123.8049999999999784, -8.437984349512086979, 5.166775262442717831E-16 ) ) ;
#69282=DIRECTION ( 'NONE',  ( -1.000000000000000000, -0.000000000000000000, -0.000000000000000000 ) ) ;
#69300=EDGE_CURVE ( 'NONE', #66633, #16901, #33457, .T. ) ;
#69304=CARTESIAN_POINT ( 'NONE',  ( -61.64292637653380780, -5.598654528085801552, 7.705886871421367523 ) ) ;
#69306=CARTESIAN_POINT ( 'NONE',  ( -156.5050000000000239, -6.826472737025115478, -4.959722759717899443 ) ) ;
#69308=EDGE_CURVE ( 'NONE', #1270, #19619, #59028, .T. ) ;
#69319=CARTESIAN_POINT ( 'NONE',  ( -66.35499999999998977, -4.716976649647093289, -6.492361379858945902 ) ) ;
#69333=CARTESIAN_POINT ( 'NONE',  ( -121.3449999999999989, 7.632228543268599452, -2.479861379858951942 ) ) ;
#69335=CARTESIAN_POINT ( 'NONE',  ( -89.69499999999999318, -8.437984349512085203, 5.166775262442717831E-16 ) ) ;
#69342=CARTESIAN_POINT ( 'NONE',  ( -129.5929263765338249, -3.094860106618431139, -9.524999999999991473 ) ) ;
#69344=CARTESIAN_POINT ( 'NONE',  ( -147.1450000000000102, -4.716976649647092401, 6.492361379858946790 ) ) ;
#69349=EDGE_LOOP ( 'NONE', ( #11293, #36860, #36703, #41368 ) ) ;
#69354=CARTESIAN_POINT ( 'NONE',  ( -129.8070736234661240, 10.01517768586948698, -1.839758294383808966E-15 ) ) ;
#69360=CARTESIAN_POINT ( 'NONE',  ( -149.9050000000000011, 2.607480562269069324, -8.024999999999993250 ) ) ;
#69370=ORIENTED_EDGE ( 'NONE', *, *, #19140, .F. ) ;
#69373=CARTESIAN_POINT ( 'NONE',  ( -61.40499999999998693, -2.607480562269069768, 8.024999999999991473 ) ) ;
#69374=CARTESIAN_POINT ( 'NONE',  ( -123.1449999999999960, -4.716976649647092401, 6.492361379858946790 ) ) ;
#69383=DIRECTION ( 'NONE',  ( -0.000000000000000000, 0.000000000000000000, 1.000000000000000000 ) ) ;
#69386=CARTESIAN_POINT ( 'NONE',  ( -180.0550000000000068, -9.827790563157499189E-16, -8.024999999999991473 ) ) ;
#69395=CARTESIAN_POINT ( 'NONE',  ( -128.9070736234668857, -3.094860106607204120, 9.525000000008148504 ) ) ;
#69396=CARTESIAN_POINT ( 'NONE',  ( -90.50499999999999545, -6.826472737025115478, -4.959722759717899443 ) ) ;
#69400=CARTESIAN_POINT ( 'NONE',  ( -131.9070736234661751, -3.094860106618429807, 9.524999999999991473 ) ) ;
#69403=CARTESIAN_POINT ( 'NONE',  ( -68.00707362346616947, -8.102448949553172852, -5.886773742842741797 ) ) ;
#69411=CARTESIAN_POINT ( 'NONE',  ( -116.1550000000000011, 7.632228543268600340, 2.479861379858949277 ) ) ;
#69413=CARTESIAN_POINT ( 'NONE',  ( -120.5949999999999704, 2.607480562269073321, 8.024999999999991473 ) ) ;
#69419=ORIENTED_EDGE ( 'NONE', *, *, #47656, .F. ) ;
#69420=CARTESIAN_POINT ( 'NONE',  ( -159.7429263765338021, -5.598654528085803328, -7.705886871421366635 ) ) ;
#69421=( NAMED_UNIT ( * ) PLANE_ANGLE_UNIT ( ) SI_UNIT ( $, .RADIAN. ) );
#69429=CARTESIAN_POINT ( 'NONE',  ( -79.79292637653381348, -3.094860106618429807, 9.524999999999991473 ) ) ;
#69435=CARTESIAN_POINT ( 'NONE',  ( -182.1549999999999727, 7.632228543268600340, 2.479861379858949277 ) ) ;
#69439=CARTESIAN_POINT ( 'NONE',  ( -73.85707362346617799, -5.598654528085803328, -7.705886871421366635 ) ) ;
#69443=VERTEX_POINT ( 'NONE', #39672 ) ;
#69445=CARTESIAN_POINT ( 'NONE',  ( -95.45499999999998408, 7.632228543268599452, -2.479861379858951942 ) ) ;
#69456=EDGE_LOOP ( 'NONE', ( #43897, #7569, #5960, #36002 ) ) ;
#69458=CARTESIAN_POINT ( 'NONE',  ( -72.89499999999999602, 6.826472737025116366, 4.959722759717898555 ) ) ;
#69470=CARTESIAN_POINT ( 'NONE',  ( -160.1929263765337907, -10.01517768586948698, 6.132527647946031529E-16 ) ) ;
#69472=CARTESIAN_POINT ( 'NONE',  ( -157.4070736234661751, 3.094860106618428031, -9.524999999999993250 ) ) ;
#69474=CARTESIAN_POINT ( 'NONE',  ( -96.20707362346614389, 3.094860106618433360, 9.524999999999991473 ) ) ;
#69482=CARTESIAN_POINT ( 'NONE',  ( -138.2049999999999272, -2.607480562269071545, -8.024999999999991473 ) ) ;
#69484=CARTESIAN_POINT ( 'NONE',  ( -147.7449999999999761, 4.716976649647094177, 6.492361379858945902 ) ) ;
#69487=CARTESIAN_POINT ( 'NONE',  ( -141.7450000000000045, 4.716976649647094177, 6.492361379858945902 ) ) ;
#69488=ORIENTED_EDGE ( 'NONE', *, *, #56861, .T. ) ;
#69494=CARTESIAN_POINT ( 'NONE',  ( -55.55499999999999261, 0.000000000000000000, 8.024999999999991473 ) ) ;
#69495=( BOUNDED_CURVE ( )  B_SPLINE_CURVE ( 2, ( #10076, #9034, #40721, #35426, #15384, #45991, #68829, #68468, #30452, #62132, #36839 ),
 .UNSPECIFIED., .F., .F. ) 
 B_SPLINE_CURVE_WITH_KNOTS ( ( 3, 2, 2, 2, 2, 3 ),
 ( 0.2826086956521673410, 0.2847826086956455893, 0.2869565217391237821, 0.2891304347826019194, 0.2913043478260801122, 0.2934782608695583606 ),
 .UNSPECIFIED. ) 
 CURVE ( )  GEOMETRIC_REPRESENTATION_ITEM ( )  RATIONAL_B_SPLINE_CURVE ( ( 1.000000000000147438, 0.9510565162950060936, 1.000000000000000000, 0.9510565162951535312, 1.000000000000000000, 0.9510565162951535312, 1.000000000000000000, 0.9510565162951535312, 1.000000000000000000, 0.9510565162953085183, 0.9999999999998450129 ) ) 
 REPRESENTATION_ITEM ( '' )  );
#69510=( BOUNDED_CURVE ( )  B_SPLINE_CURVE ( 2, ( #15926, #53534, #38082, #65104, #27110, #22214, #54213, #38444, #11654, #682, #6711 ),
 .UNSPECIFIED., .F., .F. ) 
 B_SPLINE_CURVE_WITH_KNOTS ( ( 3, 2, 2, 2, 2, 3 ),
 ( 0.6304347826086809103, 0.6326086956521591587, 0.6347826086956372960, 0.6369565217391155443, 0.6391304347825936816, 0.6413043478260719299 ),
 .UNSPECIFIED. ) 
 CURVE ( )  GEOMETRIC_REPRESENTATION_ITEM ( )  RATIONAL_B_SPLINE_CURVE ( ( 1.000000000000332401, 0.9510565162948211304, 1.000000000000000000, 0.9510565162951535312, 1.000000000000000000, 0.9510565162951535312, 1.000000000000000000, 0.9510565162951535312, 1.000000000000000000, 0.9510565162954909280, 0.9999999999996626032 ) ) 
 REPRESENTATION_ITEM ( '' )  );
#69528=CARTESIAN_POINT ( 'NONE',  ( -99.59499999999999886, 2.607480562269073321, 8.024999999999991473 ) ) ;
#69541=ORIENTED_EDGE ( 'NONE', *, *, #23485, .T. ) ;
#69551=EDGE_LOOP ( 'NONE', ( #26677, #64137, #47567 ) ) ;
#69554=CARTESIAN_POINT ( 'NONE',  ( -161.8429263765337964, 9.058813317711329915, -2.943386871421373119 ) ) ;
#69560=CARTESIAN_POINT ( 'NONE',  ( -168.3550000000000182, -4.716976649647093289, -6.492361379858945902 ) ) ;
#69564=CARTESIAN_POINT ( 'NONE',  ( -179.2449999999999761, -4.716976649647093289, -6.492361379858945902 ) ) ;
#69565=CARTESIAN_POINT ( 'NONE',  ( -164.3949999999999818, -6.826472737025113702, -4.959722759717900331 ) ) ;
#69571=CARTESIAN_POINT ( 'NONE',  ( -85.85499999999998977, 4.716976649647094177, 6.492361379858945902 ) ) ;
#69576=CARTESIAN_POINT ( 'NONE',  ( -77.99499999999996191, -6.826472737025113702, 4.959722759717902107 ) ) ;
#69582=CARTESIAN_POINT ( 'NONE',  ( -171.6570736234661751, 9.058813317711329915, 2.943386871421369566 ) ) ;
#69597=CARTESIAN_POINT ( 'NONE',  ( -174.3570736234661638, 5.598654528085804216, 7.705886871421366635 ) ) ;
#69602=CARTESIAN_POINT ( 'NONE',  ( -121.7049999999999841, 2.607480562269072433, 8.024999999999991473 ) ) ;
#69617=DIRECTION ( 'NONE',  ( 0.000000000000000000, 0.000000000000000000, 1.000000000000000000 ) ) ;
#69630=CARTESIAN_POINT ( 'NONE',  ( -146.1549999999999727, 7.632228543268600340, 2.479861379858949277 ) ) ;
#69632=AXIS2_PLACEMENT_3D ( 'NONE', #67892, #46830, #52421 ) ;
#69638=CYLINDRICAL_SURFACE ( 'NONE', #58973, 5.499999999999985789 ) ;
#69645=CARTESIAN_POINT ( 'NONE',  ( -59.60499999999998977, 6.826472737025113702, -4.959722759717902107 ) ) ;
#69654=CARTESIAN_POINT ( 'NONE',  ( -97.04292637653379927, -9.058813317711329915, -2.943386871421370898 ) ) ;
#69658=LINE ( 'NONE', #21829, #4695 ) ;
#69662=CARTESIAN_POINT ( 'NONE',  ( -110.6949999999999932, -8.437984349512086979, 5.166775262442717831E-16 ) ) ;
#69664=CARTESIAN_POINT ( 'NONE',  ( -91.94499999999997897, -9.827790563157499189E-16, -8.024999999999991473 ) ) ;
#69672=CARTESIAN_POINT ( 'NONE',  ( -137.2429263765338021, 5.598654528085804216, 7.705886871421366635 ) ) ;
#69674=CARTESIAN_POINT ( 'NONE',  ( -151.1950000000000216, 8.437984349512085203, -1.550032578732815448E-15 ) ) ;
#69680=LINE ( 'NONE', #43365, #34972 ) ;
#69692=CARTESIAN_POINT ( 'NONE',  ( -147.8049999999999500, -8.437984349512086979, 5.166775262442717831E-16 ) ) ;
ENDSEC;
END-ISO-10303-21;
